ISO-10303-21;
HEADER;
FILE_DESCRIPTION (('STEP AP214'),
    '1' );
FILE_NAME ('internal spur gear_iso_ISO - Internal spur gear 2M 118T 20PA 18FW ---S118S260OD 1.0AF.step',
    '2026-10-08T11:45:07',
    ( '' ),
    ( '' ),
    'SwSTEP 2.0',
    'SolidWorks 2026',
    '' );
FILE_SCHEMA (( 'AUTOMOTIVE_DESIGN' ));
ENDSEC;

DATA;
#2=EDGE_CURVE ( 'NONE', #17487, #8430, #16356, .T. ) ;
#5=ORIENTED_EDGE ( 'NONE', *, *, #3352, .T. ) ;
#10=ORIENTED_EDGE ( 'NONE', *, *, #28549, .F. ) ;
#11=ORIENTED_EDGE ( 'NONE', *, *, #25156, .T. ) ;
#13=DIRECTION ( 'NONE',  ( -1.000000000000000000, -0.000000000000000000, 0.000000000000000000 ) ) ;
#18=VERTEX_POINT ( 'NONE', #18483 ) ;
#22=AXIS2_PLACEMENT_3D ( 'NONE', #1481, #10457, #24659 ) ;
#23=ORIENTED_EDGE ( 'NONE', *, *, #27542, .T. ) ;
#24=CARTESIAN_POINT ( 'NONE',  ( 17.99999999999999645, 110.3490479609632615, -20.28201389785435182 ) ) ;
#25=CARTESIAN_POINT ( 'NONE',  ( 0.000000000000000000, 87.74575819880270444, -75.87280091124384285 ) ) ;
#28=EDGE_LOOP ( 'NONE', ( #968, #9890, #25897, #21708 ) ) ;
#29=AXIS2_PLACEMENT_3D ( 'NONE', #16710, #27155, #33463 ) ;
#30=DIRECTION ( 'NONE',  ( -1.000000000000000000, 0.000000000000000000, 0.000000000000000000 ) ) ;
#31=AXIS2_PLACEMENT_3D ( 'NONE', #21762, #8191, #21965 ) ;
#33=DIRECTION ( 'NONE',  ( -1.000000000000000000, -0.000000000000000000, -0.000000000000000000 ) ) ;
#37=ORIENTED_EDGE ( 'NONE', *, *, #41403, .T. ) ;
#38=DIRECTION ( 'NONE',  ( 0.000000000000000000, 0.6382441836448160544, 0.7698339834299096074 ) ) ;
#39=AXIS2_PLACEMENT_3D ( 'NONE', #35001, #14966, #41543 ) ;
#41=EDGE_LOOP ( 'NONE', ( #1865, #17158, #11037, #34239 ) ) ;
#42=CARTESIAN_POINT ( 'NONE',  ( 17.99999999999999645, 101.1249659627849269, 48.60055280209592610 ) ) ;
#45=CIRCLE ( 'NONE', #32135, 59.00000000000000000 ) ;
#47=DIRECTION ( 'NONE',  ( 0.000000000000000000, 0.8183027759081663577, 0.5747874102144109321 ) ) ;
#50=DIRECTION ( 'NONE',  ( 0.000000000000000000, -0.4610925014493325591, 0.8873520750565681015 ) ) ;
#54=VECTOR ( 'NONE', #12478, 1000.000000000000000 ) ;
#57=CARTESIAN_POINT ( 'NONE',  ( -10.00000000000000000, 0.000000000000000000, 0.000000000000000000 ) ) ;
#60=DIRECTION ( 'NONE',  ( 1.000000000000000000, 0.000000000000000000, 0.000000000000000000 ) ) ;
#62=AXIS2_PLACEMENT_3D ( 'NONE', #40135, #23391, #36432 ) ;
#64=CARTESIAN_POINT ( 'NONE',  ( 17.99999999999999645, 52.88069566989454273, 103.2454939717370905 ) ) ;
#67=AXIS2_PLACEMENT_3D ( 'NONE', #34351, #28055, #11038 ) ;
#69=VERTEX_POINT ( 'NONE', #8400 ) ;
#72=EDGE_CURVE ( 'NONE', #28961, #19587, #1411, .T. ) ;
#77=CARTESIAN_POINT ( 'NONE',  ( 17.99999999999999645, -107.2703412112692689, -32.88383143828572486 ) ) ;
#78=ORIENTED_EDGE ( 'NONE', *, *, #40490, .F. ) ;
#83=DIRECTION ( 'NONE',  ( -1.000000000000000000, 0.000000000000000000, 0.000000000000000000 ) ) ;
#86=FACE_OUTER_BOUND ( 'NONE', #37742, .T. ) ;
#88=DIRECTION ( 'NONE',  ( 0.000000000000000000, -0.3641605752528294659, 0.9313361774523355452 ) ) ;
#96=DIRECTION ( 'NONE',  ( -1.000000000000000000, -0.000000000000000000, -0.000000000000000000 ) ) ;
#98=CARTESIAN_POINT ( 'NONE',  ( 17.99999999999999645, -63.24564713401724703, -102.5693868539701299 ) ) ;
#99=AXIS2_PLACEMENT_3D ( 'NONE', #5218, #41425, #18366 ) ;
#100=CARTESIAN_POINT ( 'NONE',  ( 17.99999999999999645, 103.1672962317651496, 44.09967643725903486 ) ) ;
#102=CARTESIAN_POINT ( 'NONE',  ( 17.99999999999999645, 83.49789599728782719, 86.88263557826796557 ) ) ;
#104=EDGE_CURVE ( 'NONE', #19737, #29429, #22699, .T. ) ;
#105=AXIS2_PLACEMENT_3D ( 'NONE', #12289, #32756, #5713 ) ;
#107=DIRECTION ( 'NONE',  ( 0.000000000000000000, 0.000000000000000000, 1.000000000000000000 ) ) ;
#110=FACE_OUTER_BOUND ( 'NONE', #19769, .T. ) ;
#111=EDGE_LOOP ( 'NONE', ( #9631, #34860, #21695, #15312 ) ) ;
#114=CARTESIAN_POINT ( 'NONE',  ( 0.000000000000000000, 0.000000000000000000, 0.000000000000000000 ) ) ;
#115=ORIENTED_EDGE ( 'NONE', *, *, #13945, .F. ) ;
#117=EDGE_LOOP ( 'NONE', ( #1029, #31405, #36009, #13275 ) ) ;
#122=ORIENTED_EDGE ( 'NONE', *, *, #28926, .T. ) ;
#123=EDGE_LOOP ( 'NONE', ( #24537, #25112, #5248, #36147 ) ) ;
#125=AXIS2_PLACEMENT_3D ( 'NONE', #20168, #39735, #23218 ) ;
#127=CARTESIAN_POINT ( 'NONE',  ( 17.99999999999999645, -69.90696807222417419, -98.15042952503588936 ) ) ;
#129=EDGE_CURVE ( 'NONE', #6394, #7217, #14300, .T. ) ;
#135=ORIENTED_EDGE ( 'NONE', *, *, #35134, .T. ) ;
#136=CARTESIAN_POINT ( 'NONE',  ( 17.99999999999999645, 41.60679253225764285, 108.2814610871947423 ) ) ;
#138=CARTESIAN_POINT ( 'NONE',  ( 17.99999999999999645, 107.2885202478266251, 54.86040852957351888 ) ) ;
#141=ORIENTED_EDGE ( 'NONE', *, *, #25701, .T. ) ;
#142=DIRECTION ( 'NONE',  ( 1.000000000000000000, 0.000000000000000000, -0.000000000000000000 ) ) ;
#143=CARTESIAN_POINT ( 'NONE',  ( 0.000000000000000000, 101.1249659627849269, 48.60055280209592610 ) ) ;
#145=ORIENTED_EDGE ( 'NONE', *, *, #19754, .F. ) ;
#146=FACE_OUTER_BOUND ( 'NONE', #5091, .T. ) ;
#147=ORIENTED_EDGE ( 'NONE', *, *, #18446, .T. ) ;
#149=DIRECTION ( 'NONE',  ( 0.000000000000000000, 0.000000000000000000, 1.000000000000000000 ) ) ;
#150=CARTESIAN_POINT ( 'NONE',  ( 17.99999999999999645, 69.90696807222620635, -98.15042952503443985 ) ) ;
#152=CARTESIAN_POINT ( 'NONE',  ( 17.99999999999999645, -53.40478689619660457, -108.0204598100370816 ) ) ;
#154=CARTESIAN_POINT ( 'NONE',  ( 17.99999999999999645, 120.2856157092986678, 7.201503623197233139 ) ) ;
#155=DIRECTION ( 'NONE',  ( 1.000000000000000000, 0.000000000000000000, 0.000000000000000000 ) ) ;
#156=EDGE_LOOP ( 'NONE', ( #41702, #6494, #6185, #41274 ) ) ;
#158=AXIS2_PLACEMENT_3D ( 'NONE', #4980, #24654, #21174 ) ;
#160=CARTESIAN_POINT ( 'NONE',  ( 9.000000000000001776, -13.00789606333550097, 115.2683592318614672 ) ) ;
#162=DIRECTION ( 'NONE',  ( 0.000000000000000000, 0.1062934856473588541, 0.9943348002101377592 ) ) ;
#163=ORIENTED_EDGE ( 'NONE', *, *, #20925, .F. ) ;
#164=CARTESIAN_POINT ( 'NONE',  ( 17.99999999999999645, -97.89532456239533076, 54.81585448086167389 ) ) ;
#165=CIRCLE ( 'NONE', #25315, 58.99999999999999289 ) ;
#169=AXIS2_PLACEMENT_3D ( 'NONE', #24006, #33787, #20520 ) ;
#173=DIRECTION ( 'NONE',  ( 1.000000000000000000, 0.000000000000000000, 0.000000000000000000 ) ) ;
#174=EDGE_CURVE ( 'NONE', #31622, #37862, #2414, .T. ) ;
#176=ADVANCED_FACE ( 'NONE', ( #26221 ), #23396, .F. ) ;
#177=ORIENTED_EDGE ( 'NONE', *, *, #6345, .F. ) ;
#179=DIRECTION ( 'NONE',  ( -1.000000000000000000, 0.000000000000000000, 0.000000000000000000 ) ) ;
#180=ADVANCED_FACE ( 'NONE', ( #36225 ), #26652, .F. ) ;
#182=ORIENTED_EDGE ( 'NONE', *, *, #35349, .F. ) ;
#186=ORIENTED_EDGE ( 'NONE', *, *, #2030, .F. ) ;
#187=CARTESIAN_POINT ( 'NONE',  ( 0.000000000000000000, 82.63181128086846172, -81.41243003646886223 ) ) ;
#189=VERTEX_POINT ( 'NONE', #6781 ) ;
#193=COLOUR_RGB ( '', 0.72549020, 0.75294118, 0.79215686) ;
#194=AXIS2_PLACEMENT_3D ( 'NONE', #18783, #32450, #2540 ) ;
#198=ORIENTED_EDGE ( 'NONE', *, *, #13590, .F. ) ;
#201=DIRECTION ( 'NONE',  ( 1.000000000000000000, -0.000000000000000000, 0.000000000000000000 ) ) ;
#203=CARTESIAN_POINT ( 'NONE',  ( 0.000000000000000000, -112.8457601792517124, 26.86697618949339272 ) ) ;
#205=AXIS2_PLACEMENT_3D ( 'NONE', #38248, #21520, #38029 ) ;
#206=DIRECTION ( 'NONE',  ( 0.000000000000000000, -0.9407002666710364558, 0.3392388661180213427 ) ) ;
#208=AXIS2_PLACEMENT_3D ( 'NONE', #11929, #8841, #8617 ) ;
#209=CARTESIAN_POINT ( 'NONE',  ( 17.99999999999999645, -110.0562500189201955, 49.07252625220073838 ) ) ;
#210=ORIENTED_EDGE ( 'NONE', *, *, #16995, .T. ) ;
#214=VERTEX_POINT ( 'NONE', #29493 ) ;
#222=AXIS2_PLACEMENT_3D ( 'NONE', #57, #6628, #19990 ) ;
#223=ORIENTED_EDGE ( 'NONE', *, *, #13346, .T. ) ;
#227=AXIS2_PLACEMENT_3D ( 'NONE', #26910, #27140, #24089 ) ;
#231=ORIENTED_EDGE ( 'NONE', *, *, #17154, .T. ) ;
#232=LINE ( 'NONE', #33434, #6211 ) ;
#236=DIRECTION ( 'NONE',  ( 0.000000000000000000, 0.3140767120219495334, -0.9493976084683810601 ) ) ;
#241=EDGE_LOOP ( 'NONE', ( #31770, #30351, #32768, #20385 ) ) ;
#242=DIRECTION ( 'NONE',  ( -1.000000000000000000, -0.000000000000000000, -0.000000000000000000 ) ) ;
#244=CIRCLE ( 'NONE', #9337, 59.00000000000001421 ) ;
#250=EDGE_LOOP ( 'NONE', ( #8958, #20095, #42612, #31165 ) ) ;
#251=DIRECTION ( 'NONE',  ( -1.000000000000000000, -0.000000000000000000, 0.000000000000000000 ) ) ;
#252=VERTEX_POINT ( 'NONE', #20289 ) ;
#260=FACE_OUTER_BOUND ( 'NONE', #10790, .T. ) ;
#263=AXIS2_PLACEMENT_3D ( 'NONE', #41212, #8072, #27508 ) ;
#264=ORIENTED_EDGE ( 'NONE', *, *, #41206, .T. ) ;
#267=VERTEX_POINT ( 'NONE', #42555 ) ;
#272=EDGE_LOOP ( 'NONE', ( #37199, #32601, #38048, #42708 ) ) ;
#274=CARTESIAN_POINT ( 'NONE',  ( 0.000000000000000000, -47.58001226230612701, 110.7096808509482031 ) ) ;
#275=AXIS2_PLACEMENT_3D ( 'NONE', #8438, #38320, #31571 ) ;
#276=VERTEX_POINT ( 'NONE', #12704 ) ;
#277=FACE_OUTER_BOUND ( 'NONE', #26968, .T. ) ;
#278=DIRECTION ( 'NONE',  ( 1.000000000000000000, 0.000000000000000000, 0.000000000000000000 ) ) ;
#279=DIRECTION ( 'NONE',  ( 0.000000000000000000, 2.587384167558627638E-15, -1.000000000000000000 ) ) ;
#280=EDGE_CURVE ( 'NONE', #25913, #26598, #17814, .T. ) ;
#282=AXIS2_PLACEMENT_3D ( 'NONE', #26118, #29184, #16298 ) ;
#284=AXIS2_PLACEMENT_3D ( 'NONE', #17141, #30851, #4209 ) ;
#287=VERTEX_POINT ( 'NONE', #19913 ) ;
#288=DIRECTION ( 'NONE',  ( 1.000000000000000000, -0.000000000000000000, 0.000000000000000000 ) ) ;
#289=DIRECTION ( 'NONE',  ( -1.000000000000000000, -0.000000000000000000, -0.000000000000000000 ) ) ;
#290=DIRECTION ( 'NONE',  ( -1.000000000000000000, -0.000000000000000000, 0.000000000000000000 ) ) ;
#293=DIRECTION ( 'NONE',  ( -1.000000000000000000, -0.000000000000000000, -0.000000000000000000 ) ) ;
#295=CARTESIAN_POINT ( 'NONE',  ( 0.000000000000000000, -58.30069736313732420, 100.2847380560565256 ) ) ;
#298=AXIS2_PLACEMENT_3D ( 'NONE', #37715, #19724, #6582 ) ;
#301=EDGE_CURVE ( 'NONE', #6489, #17266, #7326, .T. ) ;
#304=CYLINDRICAL_SURFACE ( 'NONE', #9787, 116.0000000000000000 ) ;
#305=AXIS2_PLACEMENT_3D ( 'NONE', #35239, #21983, #28308 ) ;
#306=ADVANCED_FACE ( 'NONE', ( #37955 ), #862, .F. ) ;
#308=ORIENTED_EDGE ( 'NONE', *, *, #23205, .T. ) ;
#309=UNCERTAINTY_MEASURE_WITH_UNIT (LENGTH_MEASURE( 1.000000000000000082E-05 ), #5379, 'distance_accuracy_value', 'NONE');
#313=CARTESIAN_POINT ( 'NONE',  ( 0.000000000000000000, -69.72480978690109055, 92.70626138605992139 ) ) ;
#315=DIRECTION ( 'NONE',  ( -1.000000000000000000, 0.000000000000000000, -0.000000000000000000 ) ) ;
#317=EDGE_LOOP ( 'NONE', ( #16591, #23774, #39955, #12184 ) ) ;
#328=ORIENTED_EDGE ( 'NONE', *, *, #42015, .T. ) ;
#331=AXIS2_PLACEMENT_3D ( 'NONE', #35354, #42727, #6106 ) ;
#334=ORIENTED_EDGE ( 'NONE', *, *, #29415, .T. ) ;
#336=VECTOR ( 'NONE', #7785, 1000.000000000000000 ) ;
#337=ORIENTED_EDGE ( 'NONE', *, *, #41838, .F. ) ;
#338=AXIS2_PLACEMENT_3D ( 'NONE', #11324, #23403, #24655 ) ;
#339=CARTESIAN_POINT ( 'NONE',  ( 17.99999999999999645, -10.40101730206447961, 120.0512800434970728 ) ) ;
#342=AXIS2_PLACEMENT_3D ( 'NONE', #2271, #15629, #28936 ) ;
#343=FACE_OUTER_BOUND ( 'NONE', #19727, .T. ) ;
#345=AXIS2_PLACEMENT_3D ( 'NONE', #9675, #6388, #43032 ) ;
#348=ORIENTED_EDGE ( 'NONE', *, *, #42438, .F. ) ;
#350=FACE_OUTER_BOUND ( 'NONE', #25908, .T. ) ;
#358=DIRECTION ( 'NONE',  ( -1.000000000000000000, -0.000000000000000000, -0.000000000000000000 ) ) ;
#360=CARTESIAN_POINT ( 'NONE',  ( 17.99999999999999645, -103.5682682299991342, 43.14958040911493242 ) ) ;
#366=AXIS2_PLACEMENT_3D ( 'NONE', #25494, #18321, #32020 ) ;
#368=ORIENTED_EDGE ( 'NONE', *, *, #3508, .T. ) ;
#369=LINE ( 'NONE', #17453, #16327 ) ;
#372=CIRCLE ( 'NONE', #37296, 58.99999999999999289 ) ;
#375=AXIS2_PLACEMENT_3D ( 'NONE', #42673, #13475, #23302 ) ;
#376=AXIS2_PLACEMENT_3D ( 'NONE', #13765, #3889, #24670 ) ;
#379=CARTESIAN_POINT ( 'NONE',  ( 17.99999999999999645, 0.000000000000000000, 0.000000000000000000 ) ) ;
#380=ORIENTED_EDGE ( 'NONE', *, *, #4869, .F. ) ;
#382=DIRECTION ( 'NONE',  ( 1.000000000000000000, -0.000000000000000000, -0.000000000000000000 ) ) ;
#384=VERTEX_POINT ( 'NONE', #3914 ) ;
#385=DIRECTION ( 'NONE',  ( 1.000000000000000000, 0.000000000000000000, 0.000000000000000000 ) ) ;
#389=DIRECTION ( 'NONE',  ( -1.000000000000000000, 0.000000000000000000, 0.000000000000000000 ) ) ;
#394=AXIS2_PLACEMENT_3D ( 'NONE', #20858, #497, #13633 ) ;
#403=AXIS2_PLACEMENT_3D ( 'NONE', #31124, #18726, #31983 ) ;
#404=DIRECTION ( 'NONE',  ( 0.000000000000000000, 0.9911528310040075285, -0.1327255272837188915 ) ) ;
#409=CYLINDRICAL_SURFACE ( 'NONE', #39727, 116.0000000000000000 ) ;
#410=CIRCLE ( 'NONE', #16542, 120.5010000000000474 ) ;
#411=EDGE_CURVE ( 'NONE', #1566, #6181, #12925, .T. ) ;
#412=ORIENTED_EDGE ( 'NONE', *, *, #27431, .T. ) ;
#415=CARTESIAN_POINT ( 'NONE',  ( 17.99999999999999645, 92.25992191227497585, -77.51514567967304004 ) ) ;
#416=VERTEX_POINT ( 'NONE', #20792 ) ;
#417=ADVANCED_FACE ( 'NONE', ( #17508 ), #30784, .F. ) ;
#418=DIRECTION ( 'NONE',  ( 1.000000000000000000, 0.000000000000000000, 0.000000000000000000 ) ) ;
#421=DIRECTION ( 'NONE',  ( -1.000000000000000000, -0.000000000000000000, 0.000000000000000000 ) ) ;
#422=ORIENTED_EDGE ( 'NONE', *, *, #41036, .F. ) ;
#423=CARTESIAN_POINT ( 'NONE',  ( 9.000000000000001776, -112.5220807139882311, -28.19186676675956704 ) ) ;
#424=ORIENTED_EDGE ( 'NONE', *, *, #31392, .T. ) ;
#425=DIRECTION ( 'NONE',  ( 0.000000000000000000, 0.000000000000000000, 1.000000000000000000 ) ) ;
#427=ORIENTED_EDGE ( 'NONE', *, *, #25866, .T. ) ;
#432=CARTESIAN_POINT ( 'NONE',  ( 17.99999999999999645, 104.2166695095712470, 60.49278301857841456 ) ) ;
#433=VERTEX_POINT ( 'NONE', #7858 ) ;
#434=VECTOR ( 'NONE', #34383, 1000.000000000000000 ) ;
#435=CARTESIAN_POINT ( 'NONE',  ( 17.99999999999999645, 105.3681574666269256, -38.54638589714782881 ) ) ;
#436=CIRCLE ( 'NONE', #24900, 59.00000000000000000 ) ;
#438=ADVANCED_FACE ( 'NONE', ( #21215 ), #30995, .F. ) ;
#439=ADVANCED_FACE ( 'NONE', ( #21867 ), #29028, .F. ) ;
#442=STYLED_ITEM ( 'NONE', ( #20930 ), #28802 ) ;
#443=ADVANCED_FACE ( 'NONE', ( #12453 ), #25139, .F. ) ;
#445=CARTESIAN_POINT ( 'NONE',  ( 0.000000000000000000, 69.90696807222620635, -98.15042952503443985 ) ) ;
#454=CARTESIAN_POINT ( 'NONE',  ( 17.99999999999999645, -46.12538073176424547, 111.3235835452210267 ) ) ;
#456=CARTESIAN_POINT ( 'NONE',  ( 17.99999999999999645, 0.000000000000000000, 0.000000000000000000 ) ) ;
#459=EDGE_LOOP ( 'NONE', ( #38424, #13249, #34753, #39465 ) ) ;
#464=CIRCLE ( 'NONE', #39460, 59.00000000000000000 ) ;
#465=ORIENTED_EDGE ( 'NONE', *, *, #10281, .F. ) ;
#472=DIRECTION ( 'NONE',  ( 0.000000000000000000, 0.000000000000000000, 1.000000000000000000 ) ) ;
#473=LINE ( 'NONE', #3521, #19907 ) ;
#477=ORIENTED_EDGE ( 'NONE', *, *, #12046, .F. ) ;
#481=DIRECTION ( 'NONE',  ( 1.000000000000000000, 0.000000000000000000, 0.000000000000000000 ) ) ;
#482=EDGE_LOOP ( 'NONE', ( #35569, #28830, #27446, #17028 ) ) ;
#485=ORIENTED_EDGE ( 'NONE', *, *, #20784, .T. ) ;
#486=DIRECTION ( 'NONE',  ( 1.000000000000000000, 0.000000000000000000, 0.000000000000000000 ) ) ;
#490=ORIENTED_EDGE ( 'NONE', *, *, #30914, .T. ) ;
#492=CIRCLE ( 'NONE', #22825, 59.00000000000000000 ) ;
#493=DIRECTION ( 'NONE',  ( 0.000000000000000000, -0.1062934856473723849, 0.9943348002101364269 ) ) ;
#496=EDGE_CURVE ( 'NONE', #16818, #9730, #22290, .T. ) ;
#497=DIRECTION ( 'NONE',  ( -1.000000000000000000, -0.000000000000000000, -0.000000000000000000 ) ) ;
#499=DIRECTION ( 'NONE',  ( 1.000000000000000000, 0.000000000000000000, 0.000000000000000000 ) ) ;
#500=AXIS2_PLACEMENT_3D ( 'NONE', #1335, #20821, #14680 ) ;
#504=ADVANCED_FACE ( 'NONE', ( #22074 ), #11814, .F. ) ;
#505=VECTOR ( 'NONE', #4362, 1000.000000000000000 ) ;
#506=CARTESIAN_POINT ( 'NONE',  ( 8.999999999999998224, -97.97378550988267421, 62.10585602713726416 ) ) ;
#507=AXIS2_PLACEMENT_3D ( 'NONE', #19360, #40003, #6868 ) ;
#508=VERTEX_POINT ( 'NONE', #34910 ) ;
#509=CARTESIAN_POINT ( 'NONE',  ( 17.99999999999999645, 21.55123232222474172, 118.5581519187672654 ) ) ;
#510=VECTOR ( 'NONE', #27183, 1000.000000000000000 ) ;
#514=CARTESIAN_POINT ( 'NONE',  ( 17.99999999999999645, 51.98489025774451733, -108.7109110710156159 ) ) ;
#519=FACE_OUTER_BOUND ( 'NONE', #1708, .T. ) ;
#524=CARTESIAN_POINT ( 'NONE',  ( 8.999999999999998224, -86.84764344322910290, -76.89919913989835720 ) ) ;
#528=DIRECTION ( 'NONE',  ( 0.000000000000000000, -0.9996456111234528485, 0.02662052143776447166 ) ) ;
#529=DIRECTION ( 'NONE',  ( 1.000000000000000000, 0.000000000000000000, 0.000000000000000000 ) ) ;
#532=EDGE_LOOP ( 'NONE', ( #15360, #37430, #26856, #20407 ) ) ;
#535=VECTOR ( 'NONE', #20780, 1000.000000000000000 ) ;
#537=CIRCLE ( 'NONE', #20124, 58.99999999999999289 ) ;
#540=ORIENTED_EDGE ( 'NONE', *, *, #2625, .F. ) ;
#542=CARTESIAN_POINT ( 'NONE',  ( 0.000000000000000000, -119.7318547011702634, 13.59315897125686057 ) ) ;
#543=AXIS2_PLACEMENT_3D ( 'NONE', #13775, #29697, #16847 ) ;
#546=ORIENTED_EDGE ( 'NONE', *, *, #32103, .F. ) ;
#550=CARTESIAN_POINT ( 'NONE',  ( 9.000000000000001776, 37.07968990261626629, -109.9140418541953750 ) ) ;
#552=CARTESIAN_POINT ( 'NONE',  ( 8.999999999999998224, -91.65951123222531294, 71.09524597798055368 ) ) ;
#553=VERTEX_POINT ( 'NONE', #42298 ) ;
#555=ORIENTED_EDGE ( 'NONE', *, *, #25691, .F. ) ;
#556=DIRECTION ( 'NONE',  ( 0.000000000000000000, 0.000000000000000000, 1.000000000000000000 ) ) ;
#557=CARTESIAN_POINT ( 'NONE',  ( 0.000000000000000000, 104.0201923570382405, -51.34003878070953419 ) ) ;
#559=VECTOR ( 'NONE', #25999, 1000.000000000000000 ) ;
#560=CARTESIAN_POINT ( 'NONE',  ( -10.00000000000000000, 0.000000000000000000, 0.000000000000000000 ) ) ;
#562=ORIENTED_EDGE ( 'NONE', *, *, #6863, .F. ) ;
#565=CARTESIAN_POINT ( 'NONE',  ( 8.999999999999998224, 104.0201923570375300, 51.34003878071097660 ) ) ;
#566=VERTEX_POINT ( 'NONE', #8945 ) ;
#568=CIRCLE ( 'NONE', #31967, 59.00000000000000711 ) ;
#571=LINE ( 'NONE', #20474, #42329 ) ;
#572=DIRECTION ( 'NONE',  ( 1.000000000000000000, 0.000000000000000000, 0.000000000000000000 ) ) ;
#576=ORIENTED_EDGE ( 'NONE', *, *, #13519, .F. ) ;
#579=CYLINDRICAL_SURFACE ( 'NONE', #23483, 58.99999999999999289 ) ;
#580=CARTESIAN_POINT ( 'NONE',  ( 0.000000000000000000, -71.21168426767167148, 86.70160608319299911 ) ) ;
#582=ORIENTED_EDGE ( 'NONE', *, *, #18176, .T. ) ;
#583=CYLINDRICAL_SURFACE ( 'NONE', #5170, 120.5010000000000190 ) ;
#592=ORIENTED_EDGE ( 'NONE', *, *, #38847, .F. ) ;
#596=VERTEX_POINT ( 'NONE', #38814 ) ;
#598=LINE ( 'NONE', #13951, #7008 ) ;
#601=CARTESIAN_POINT ( 'NONE',  ( 0.000000000000000000, 0.000000000000000000, 0.000000000000000000 ) ) ;
#602=ORIENTED_EDGE ( 'NONE', *, *, #42111, .T. ) ;
#603=CARTESIAN_POINT ( 'NONE',  ( -10.00000000000000000, 0.000000000000000000, 0.000000000000000000 ) ) ;
#607=CARTESIAN_POINT ( 'NONE',  ( 17.99999999999999645, 110.3490479609632615, 38.71798610214565173 ) ) ;
#611=CARTESIAN_POINT ( 'NONE',  ( 0.000000000000000000, 62.45178862086345362, -93.20969140437443912 ) ) ;
#612=EDGE_CURVE ( 'NONE', #31034, #38131, #30956, .T. ) ;
#615=ORIENTED_EDGE ( 'NONE', *, *, #5876, .F. ) ;
#616=AXIS2_PLACEMENT_3D ( 'NONE', #33760, #3842, #17229 ) ;
#620=DIRECTION ( 'NONE',  ( -1.000000000000000000, -0.000000000000000000, 0.000000000000000000 ) ) ;
#623=ORIENTED_EDGE ( 'NONE', *, *, #22304, .T. ) ;
#624=DIRECTION ( 'NONE',  ( 1.000000000000000000, 0.000000000000000000, 0.000000000000000000 ) ) ;
#625=CARTESIAN_POINT ( 'NONE',  ( -10.00000000000000000, 0.000000000000000000, 0.000000000000000000 ) ) ;
#626=ORIENTED_EDGE ( 'NONE', *, *, #10787, .F. ) ;
#629=CARTESIAN_POINT ( 'NONE',  ( 17.99999999999999645, 3.996885678774600326, -120.4346956066681713 ) ) ;
#630=EDGE_CURVE ( 'NONE', #32233, #22705, #22711, .T. ) ;
#636=CARTESIAN_POINT ( 'NONE',  ( 0.000000000000000000, -53.40478689619801145, 108.0204598100363711 ) ) ;
#642=LINE ( 'NONE', #17948, #38766 ) ;
#647=CIRCLE ( 'NONE', #38965, 59.00000000000000711 ) ;
#649=DIRECTION ( 'NONE',  ( 0.000000000000000000, 0.000000000000000000, 1.000000000000000000 ) ) ;
#654=DIRECTION ( 'NONE',  ( -1.000000000000000000, 0.000000000000000000, 0.000000000000000000 ) ) ;
#655=ORIENTED_EDGE ( 'NONE', *, *, #12968, .T. ) ;
#657=EDGE_CURVE ( 'NONE', #1834, #41377, #28882, .T. ) ;
#658=DIRECTION ( 'NONE',  ( 1.000000000000000000, -0.000000000000000000, -0.000000000000000000 ) ) ;
#661=CARTESIAN_POINT ( 'NONE',  ( 17.99999999999999645, 110.3490479609632615, -20.28201389785435182 ) ) ;
#664=ORIENTED_EDGE ( 'NONE', *, *, #26225, .F. ) ;
#665=CARTESIAN_POINT ( 'NONE',  ( 0.000000000000000000, 112.5220807139887853, -28.19186676675730752 ) ) ;
#668=AXIS2_PLACEMENT_3D ( 'NONE', #2033, #36049, #15804 ) ;
#669=AXIS2_PLACEMENT_3D ( 'NONE', #24618, #14789, #11734 ) ;
#670=ORIENTED_EDGE ( 'NONE', *, *, #7404, .F. ) ;
#678=ORIENTED_EDGE ( 'NONE', *, *, #20185, .T. ) ;
#681=EDGE_CURVE ( 'NONE', #10180, #38227, #28202, .T. ) ;
#684=DIRECTION ( 'NONE',  ( 0.000000000000000000, -0.8993121301712229121, 0.4373073204588476259 ) ) ;
#685=EDGE_CURVE ( 'NONE', #596, #26693, #23143, .T. ) ;
#690=ORIENTED_EDGE ( 'NONE', *, *, #18292, .T. ) ;
#691=DIRECTION ( 'NONE',  ( 0.000000000000000000, 0.000000000000000000, 1.000000000000000000 ) ) ;
#693=FACE_OUTER_BOUND ( 'NONE', #20264, .T. ) ;
#696=CIRCLE ( 'NONE', #4186, 58.99999999999999289 ) ;
#698=CARTESIAN_POINT ( 'NONE',  ( 17.99999999999999645, 87.92975456462900752, 69.68953103478187927 ) ) ;
#703=CIRCLE ( 'NONE', #5586, 120.5010000000000332 ) ;
#706=DIRECTION ( 'NONE',  ( -1.000000000000000000, -0.000000000000000000, -0.000000000000000000 ) ) ;
#709=CARTESIAN_POINT ( 'NONE',  ( 17.99999999999999645, 0.000000000000000000, 0.000000000000000000 ) ) ;
#710=VERTEX_POINT ( 'NONE', #16148 ) ;
#713=DIRECTION ( 'NONE',  ( 1.000000000000000000, 0.000000000000000000, 0.000000000000000000 ) ) ;
#714=VERTEX_POINT ( 'NONE', #33356 ) ;
#715=CARTESIAN_POINT ( 'NONE',  ( 17.99999999999999645, -98.39501399267994941, 53.91376164787647696 ) ) ;
#717=EDGE_CURVE ( 'NONE', #31117, #17266, #28240, .T. ) ;
#718=CARTESIAN_POINT ( 'NONE',  ( 17.99999999999999645, -96.25468616236712194, 72.49500943364458294 ) ) ;
#719=VERTEX_POINT ( 'NONE', #32704 ) ;
#721=ORIENTED_EDGE ( 'NONE', *, *, #30636, .F. ) ;
#722=CIRCLE ( 'NONE', #25184, 59.00000000000000000 ) ;
#725=CARTESIAN_POINT ( 'NONE',  ( 17.99999999999999645, -111.2721026680459602, -14.38025178762732104 ) ) ;
#727=CARTESIAN_POINT ( 'NONE',  ( 17.99999999999999645, 106.5605152861902951, 56.26142179985861702 ) ) ;
#728=CIRCLE ( 'NONE', #30018, 116.0000000000000000 ) ;
#734=AXIS2_PLACEMENT_3D ( 'NONE', #32595, #16248, #28912 ) ;
#735=CYLINDRICAL_SURFACE ( 'NONE', #36721, 59.00000000000000711 ) ;
#739=ORIENTED_EDGE ( 'NONE', *, *, #1316, .F. ) ;
#740=ORIENTED_EDGE ( 'NONE', *, *, #38677, .F. ) ;
#743=EDGE_CURVE ( 'NONE', #6489, #1587, #4491, .T. ) ;
#746=ORIENTED_EDGE ( 'NONE', *, *, #4004, .T. ) ;
#747=DIRECTION ( 'NONE',  ( 0.000000000000000000, 0.000000000000000000, 1.000000000000000000 ) ) ;
#748=ORIENTED_EDGE ( 'NONE', *, *, #42765, .F. ) ;
#751=EDGE_CURVE ( 'NONE', #27172, #14763, #37265, .T. ) ;
#752=DIRECTION ( 'NONE',  ( 1.000000000000000000, 0.000000000000000000, 0.000000000000000000 ) ) ;
#753=EDGE_LOOP ( 'NONE', ( #6646, #13684, #10, #35379 ) ) ;
#756=DIRECTION ( 'NONE',  ( -1.000000000000000000, -0.000000000000000000, -0.000000000000000000 ) ) ;
#758=EDGE_CURVE ( 'NONE', #33221, #42002, #39448, .T. ) ;
#759=DIRECTION ( 'NONE',  ( 0.000000000000000000, 0.000000000000000000, 1.000000000000000000 ) ) ;
#765=ORIENTED_EDGE ( 'NONE', *, *, #22439, .T. ) ;
#766=AXIS2_PLACEMENT_3D ( 'NONE', #15610, #16042, #9468 ) ;
#768=DIRECTION ( 'NONE',  ( -1.000000000000000000, -0.000000000000000000, -0.000000000000000000 ) ) ;
#769=CARTESIAN_POINT ( 'NONE',  ( 17.99999999999999645, 0.000000000000000000, 0.000000000000000000 ) ) ;
#772=DIRECTION ( 'NONE',  ( 1.000000000000000000, 0.000000000000000000, 0.000000000000000000 ) ) ;
#773=ORIENTED_EDGE ( 'NONE', *, *, #5473, .F. ) ;
#774=DIRECTION ( 'NONE',  ( 0.000000000000000000, 0.6382441836448161654, 0.7698339834299096074 ) ) ;
#777=VECTOR ( 'NONE', #3980, 1000.000000000000000 ) ;
#778=ORIENTED_EDGE ( 'NONE', *, *, #36013, .T. ) ;
#779=CARTESIAN_POINT ( 'NONE',  ( 17.99999999999999645, 17.33727698085324320, -110.8498592715971967 ) ) ;
#780=CARTESIAN_POINT ( 'NONE',  ( 8.999999999999998224, -82.63181128086789329, 81.41243003646944487 ) ) ;
#787=CARTESIAN_POINT ( 'NONE',  ( 17.99999999999999645, 95.31344542257821217, -66.11616384574354299 ) ) ;
#789=DIRECTION ( 'NONE',  ( 0.000000000000000000, 0.9213119778704139673, -0.3888241754733182676 ) ) ;
#790=FACE_OUTER_BOUND ( 'NONE', #38920, .T. ) ;
#791=ORIENTED_EDGE ( 'NONE', *, *, #42785, .T. ) ;
#793=DIRECTION ( 'NONE',  ( 0.000000000000000000, 0.8183027759081702435, -0.5747874102144051589 ) ) ;
#794=ORIENTED_EDGE ( 'NONE', *, *, #5997, .T. ) ;
#795=CARTESIAN_POINT ( 'NONE',  ( 0.000000000000000000, 0.6819280456829140968, 115.9979955608738749 ) ) ;
#797=DIRECTION ( 'NONE',  ( 0.000000000000000000, 0.000000000000000000, -1.000000000000000000 ) ) ;
#798=CIRCLE ( 'NONE', #6381, 58.99999999999998579 ) ;
#800=DIRECTION ( 'NONE',  ( 0.000000000000000000, 0.000000000000000000, 1.000000000000000000 ) ) ;
#801=DIRECTION ( 'NONE',  ( -1.000000000000000000, -0.000000000000000000, -0.000000000000000000 ) ) ;
#802=AXIS2_PLACEMENT_3D ( 'NONE', #24031, #418, #849 ) ;
#803=ORIENTED_EDGE ( 'NONE', *, *, #3371, .T. ) ;
#805=CARTESIAN_POINT ( 'NONE',  ( 0.000000000000000000, -17.77780072541773748, 114.6296200873375284 ) ) ;
#807=CARTESIAN_POINT ( 'NONE',  ( 17.99999999999999645, -100.8494052988166345, -65.95368414179013428 ) ) ;
#810=CARTESIAN_POINT ( 'NONE',  ( 17.99999999999999645, -68.61497464550522807, -99.05794392877676557 ) ) ;
#814=DIRECTION ( 'NONE',  ( 0.000000000000000000, -0.8477344278896755680, 0.5304209081197349684 ) ) ;
#815=VERTEX_POINT ( 'NONE', #10445 ) ;
#816=CARTESIAN_POINT ( 'NONE',  ( 17.99999999999999645, 114.6488492393084613, -37.09625815499892809 ) ) ;
#821=VERTEX_POINT ( 'NONE', #40521 ) ;
#823=DIRECTION ( 'NONE',  ( 0.000000000000000000, -0.4610925014493143514, -0.8873520750565775383 ) ) ;
#825=CARTESIAN_POINT ( 'NONE',  ( 9.000000000000001776, 19.12429268481864142, -114.4126803693777248 ) ) ;
#826=AXIS2_PLACEMENT_3D ( 'NONE', #21872, #28610, #21453 ) ;
#828=AXIS2_PLACEMENT_3D ( 'NONE', #23833, #39922, #37099 ) ;
#829=EDGE_CURVE ( 'NONE', #19014, #17523, #39330, .T. ) ;
#830=AXIS2_PLACEMENT_3D ( 'NONE', #30813, #14241, #7673 ) ;
#835=CIRCLE ( 'NONE', #12740, 59.00000000000000000 ) ;
#836=DIRECTION ( 'NONE',  ( -1.000000000000000000, -0.000000000000000000, -0.000000000000000000 ) ) ;
#838=DIRECTION ( 'NONE',  ( -1.000000000000000000, 0.000000000000000000, -0.000000000000000000 ) ) ;
#839=LINE ( 'NONE', #24020, #21677 ) ;
#840=ORIENTED_EDGE ( 'NONE', *, *, #25056, .F. ) ;
#842=DIRECTION ( 'NONE',  ( -1.000000000000000000, -0.000000000000000000, 0.000000000000000000 ) ) ;
#844=VERTEX_POINT ( 'NONE', #37259 ) ;
#848=VERTEX_POINT ( 'NONE', #27911 ) ;
#849=DIRECTION ( 'NONE',  ( 0.000000000000000000, 0.9996456111234526265, -0.02662052143777148688 ) ) ;
#852=DIRECTION ( 'NONE',  ( -1.000000000000000000, -0.000000000000000000, -0.000000000000000000 ) ) ;
#854=EDGE_CURVE ( 'NONE', #30629, #15430, #13742, .T. ) ;
#855=DIRECTION ( 'NONE',  ( -1.000000000000000000, 0.000000000000000000, -0.000000000000000000 ) ) ;
#856=ORIENTED_EDGE ( 'NONE', *, *, #38823, .F. ) ;
#857=DIRECTION ( 'NONE',  ( 1.000000000000000000, 0.000000000000000000, 0.000000000000000000 ) ) ;
#860=EDGE_LOOP ( 'NONE', ( #15062, #36163, #30682, #9307 ) ) ;
#862=CYLINDRICAL_SURFACE ( 'NONE', #8706, 59.00000000000000000 ) ;
#863=DIRECTION ( 'NONE',  ( 0.000000000000000000, 0.000000000000000000, 1.000000000000000000 ) ) ;
#864=ORIENTED_EDGE ( 'NONE', *, *, #13821, .F. ) ;
#866=AXIS2_PLACEMENT_3D ( 'NONE', #26406, #23791, #17470 ) ;
#867=CARTESIAN_POINT ( 'NONE',  ( 0.000000000000000000, 0.000000000000000000, 0.000000000000000000 ) ) ;
#868=DIRECTION ( 'NONE',  ( 0.000000000000000000, 0.000000000000000000, 1.000000000000000000 ) ) ;
#869=DIRECTION ( 'NONE',  ( 0.000000000000000000, 0.000000000000000000, 1.000000000000000000 ) ) ;
#874=EDGE_CURVE ( 'NONE', #13955, #7568, #32381, .T. ) ;
#877=CARTESIAN_POINT ( 'NONE',  ( 17.99999999999999645, 0.000000000000000000, 0.000000000000000000 ) ) ;
#878=EDGE_CURVE ( 'NONE', #38848, #5227, #1025, .T. ) ;
#887=DIRECTION ( 'NONE',  ( 0.000000000000000000, 0.000000000000000000, 1.000000000000000000 ) ) ;
#889=DIRECTION ( 'NONE',  ( 1.000000000000000000, 0.000000000000000000, 0.000000000000000000 ) ) ;
#890=MECHANICAL_DESIGN_GEOMETRIC_PRESENTATION_REPRESENTATION('',(#26712),#21180);
#894=EDGE_LOOP ( 'NONE', ( #24102, #33769, #35658, #18050 ) ) ;
#897=EDGE_LOOP ( 'NONE', ( #25009, #43120, #20954, #33292 ) ) ;
#899=CARTESIAN_POINT ( 'NONE',  ( 17.99999999999999645, 107.5680526044915410, 31.89649718262280231 ) ) ;
#901=FACE_OUTER_BOUND ( 'NONE', #22484, .T. ) ;
#903=FACE_OUTER_BOUND ( 'NONE', #27461, .T. ) ;
#904=EDGE_CURVE ( 'NONE', #35878, #42716, #20582, .T. ) ;
#910=DIRECTION ( 'NONE',  ( -1.000000000000000000, -0.000000000000000000, -0.000000000000000000 ) ) ;
#913=DIRECTION ( 'NONE',  ( 1.000000000000000000, 0.000000000000000000, 0.000000000000000000 ) ) ;
#917=CYLINDRICAL_SURFACE ( 'NONE', #38439, 116.0000000000000000 ) ;
#922=ORIENTED_EDGE ( 'NONE', *, *, #27475, .T. ) ;
#924=CIRCLE ( 'NONE', #15612, 116.0000000000000000 ) ;
#932=ADVANCED_FACE ( 'NONE', ( #32027 ), #38338, .F. ) ;
#935=ORIENTED_EDGE ( 'NONE', *, *, #8134, .T. ) ;
#936=ORIENTED_EDGE ( 'NONE', *, *, #3217, .T. ) ;
#941=AXIS2_PLACEMENT_3D ( 'NONE', #14396, #33790, #37498 ) ;
#947=CARTESIAN_POINT ( 'NONE',  ( 17.99999999999999645, 112.1427988504408404, -3.502162136922268409 ) ) ;
#949=DIRECTION ( 'NONE',  ( 1.000000000000000000, 0.000000000000000000, 0.000000000000000000 ) ) ;
#950=DIRECTION ( 'NONE',  ( -1.000000000000000000, 0.000000000000000000, 0.000000000000000000 ) ) ;
#951=EDGE_LOOP ( 'NONE', ( #22743, #10963, #794, #31874 ) ) ;
#953=DIRECTION ( 'NONE',  ( -1.000000000000000000, -0.000000000000000000, 0.000000000000000000 ) ) ;
#957=DIRECTION ( 'NONE',  ( -1.000000000000000000, 0.000000000000000000, 0.000000000000000000 ) ) ;
#961=ORIENTED_EDGE ( 'NONE', *, *, #23057, .T. ) ;
#968=ORIENTED_EDGE ( 'NONE', *, *, #16720, .T. ) ;
#979=CARTESIAN_POINT ( 'NONE',  ( 17.99999999999999645, 35.72777019205667415, 106.3569410558018404 ) ) ;
#980=EDGE_CURVE ( 'NONE', #6774, #2440, #28766, .T. ) ;
#986=EDGE_CURVE ( 'NONE', #1564, #14692, #18727, .T. ) ;
#993=DIRECTION ( 'NONE',  ( -1.000000000000000000, -0.000000000000000000, 0.000000000000000000 ) ) ;
#1001=DIRECTION ( 'NONE',  ( -1.000000000000000000, 0.000000000000000000, 0.000000000000000000 ) ) ;
#1002=ORIENTED_EDGE ( 'NONE', *, *, #16383, .T. ) ;
#1004=AXIS2_PLACEMENT_3D ( 'NONE', #40545, #838, #17927 ) ;
#1005=LINE ( 'NONE', #30507, #336 ) ;
#1006=VECTOR ( 'NONE', #32825, 1000.000000000000000 ) ;
#1007=DIRECTION ( 'NONE',  ( 0.000000000000000000, 0.000000000000000000, 1.000000000000000000 ) ) ;
#1011=DIRECTION ( 'NONE',  ( 0.000000000000000000, -0.5963673585385078635, 0.8027116379309588989 ) ) ;
#1018=CIRCLE ( 'NONE', #40724, 116.0000000000000000 ) ;
#1022=ORIENTED_EDGE ( 'NONE', *, *, #9532, .F. ) ;
#1025=LINE ( 'NONE', #34207, #33055 ) ;
#1026=AXIS2_PLACEMENT_3D ( 'NONE', #28287, #21111, #7751 ) ;
#1027=CARTESIAN_POINT ( 'NONE',  ( 17.99999999999999645, -111.1352304691228596, 15.40237066878559524 ) ) ;
#1029=ORIENTED_EDGE ( 'NONE', *, *, #12507, .F. ) ;
#1034=FACE_OUTER_BOUND ( 'NONE', #27525, .T. ) ;
#1035=AXIS2_PLACEMENT_3D ( 'NONE', #1477, #28568, #4981 ) ;
#1037=ORIENTED_EDGE ( 'NONE', *, *, #36924, .F. ) ;
#1038=CARTESIAN_POINT ( 'NONE',  ( 0.000000000000000000, 0.000000000000000000, 0.000000000000000000 ) ) ;
#1039=CIRCLE ( 'NONE', #13632, 120.5010000000000190 ) ;
#1040=ADVANCED_FACE ( 'NONE', ( #31818 ), #1685, .F. ) ;
#1041=EDGE_CURVE ( 'NONE', #35404, #38913, #11022, .T. ) ;
#1045=CARTESIAN_POINT ( 'NONE',  ( 17.99999999999999645, 23.10276247328101817, 118.2656051737070726 ) ) ;
#1051=ADVANCED_FACE ( 'NONE', ( #41826 ), #22022, .F. ) ;
#1056=AXIS2_PLACEMENT_3D ( 'NONE', #38928, #28514, #25246 ) ;
#1058=DIRECTION ( 'NONE',  ( -1.000000000000000000, -0.000000000000000000, -0.000000000000000000 ) ) ;
#1061=AXIS2_PLACEMENT_3D ( 'NONE', #3485, #16649, #12857 ) ;
#1062=LINE ( 'NONE', #10025, #39695 ) ;
#1063=ORIENTED_EDGE ( 'NONE', *, *, #11889, .T. ) ;
#1065=CARTESIAN_POINT ( 'NONE',  ( 17.99999999999999645, -119.7318547011700502, -13.59315897125848238 ) ) ;
#1068=ORIENTED_EDGE ( 'NONE', *, *, #42063, .F. ) ;
#1071=AXIS2_PLACEMENT_3D ( 'NONE', #15177, #27600, #8166 ) ;
#1074=EDGE_LOOP ( 'NONE', ( #11891, #33108, #40829, #19012 ) ) ;
#1075=ADVANCED_FACE ( 'NONE', ( #35492 ), #15037, .F. ) ;
#1076=CARTESIAN_POINT ( 'NONE',  ( 17.99999999999999645, 108.8684555192050425, -27.12806418649509865 ) ) ;
#1080=ORIENTED_EDGE ( 'NONE', *, *, #13414, .F. ) ;
#1082=CARTESIAN_POINT ( 'NONE',  ( 17.99999999999999645, -75.72520367775034345, -82.78868281116056949 ) ) ;
#1083=ORIENTED_EDGE ( 'NONE', *, *, #35669, .F. ) ;
#1086=VECTOR ( 'NONE', #19756, 1000.000000000000000 ) ;
#1090=AXIS2_PLACEMENT_3D ( 'NONE', #18379, #25768, #18816 ) ;
#1093=AXIS2_PLACEMENT_3D ( 'NONE', #27876, #28528, #8219 ) ;
#1098=VECTOR ( 'NONE', #1166, 1000.000000000000000 ) ;
#1099=FACE_OUTER_BOUND ( 'NONE', #14245, .T. ) ;
#1101=VECTOR ( 'NONE', #5570, 1000.000000000000000 ) ;
#1102=CARTESIAN_POINT ( 'NONE',  ( 0.000000000000000000, 0.000000000000000000, 0.000000000000000000 ) ) ;
#1106=VECTOR ( 'NONE', #4814, 1000.000000000000000 ) ;
#1107=FACE_OUTER_BOUND ( 'NONE', #41830, .T. ) ;
#1110=EDGE_CURVE ( 'NONE', #26358, #42713, #39820, .T. ) ;
#1112=FACE_OUTER_BOUND ( 'NONE', #23319, .T. ) ;
#1113=EDGE_CURVE ( 'NONE', #25476, #1122, #22887, .T. ) ;
#1114=DIRECTION ( 'NONE',  ( -1.000000000000000000, 0.000000000000000000, 0.000000000000000000 ) ) ;
#1120=CYLINDRICAL_SURFACE ( 'NONE', #4108, 120.5010000000000190 ) ;
#1122=VERTEX_POINT ( 'NONE', #9534 ) ;
#1126=ORIENTED_EDGE ( 'NONE', *, *, #36071, .T. ) ;
#1129=ORIENTED_EDGE ( 'NONE', *, *, #17307, .T. ) ;
#1135=CARTESIAN_POINT ( 'NONE',  ( 17.99999999999999645, 66.49630760163600485, 90.36876423296011751 ) ) ;
#1137=EDGE_LOOP ( 'NONE', ( #30207, #1126, #30886, #19679 ) ) ;
#1138=ADVANCED_FACE ( 'NONE', ( #39392 ), #9094, .F. ) ;
#1140=AXIS2_PLACEMENT_3D ( 'NONE', #22224, #25270, #35675 ) ;
#1141=DIRECTION ( 'NONE',  ( 0.000000000000000000, 0.000000000000000000, 1.000000000000000000 ) ) ;
#1143=CARTESIAN_POINT ( 'NONE',  ( 0.000000000000000000, -19.12429268481634281, -114.4126803693781085 ) ) ;
#1147=CARTESIAN_POINT ( 'NONE',  ( 17.99999999999999645, 23.10276247328255650, -118.2656051737067600 ) ) ;
#1149=AXIS2_PLACEMENT_3D ( 'NONE', #42196, #42420, #12567 ) ;
#1152=EDGE_CURVE ( 'NONE', #33231, #25294, #1928, .T. ) ;
#1154=LINE ( 'NONE', #28469, #26160 ) ;
#1156=CARTESIAN_POINT ( 'NONE',  ( 17.99999999999999645, 0.000000000000000000, 0.000000000000000000 ) ) ;
#1157=CIRCLE ( 'NONE', #3913, 116.0000000000000000 ) ;
#1161=ADVANCED_FACE ( 'NONE', ( #39182 ), #28973, .F. ) ;
#1162=AXIS2_PLACEMENT_3D ( 'NONE', #1977, #1334, #17979 ) ;
#1165=ORIENTED_EDGE ( 'NONE', *, *, #22144, .F. ) ;
#1166=DIRECTION ( 'NONE',  ( -1.000000000000000000, 0.000000000000000000, 0.000000000000000000 ) ) ;
#1171=CARTESIAN_POINT ( 'NONE',  ( 17.99999999999999645, 0.000000000000000000, 0.000000000000000000 ) ) ;
#1172=CIRCLE ( 'NONE', #28380, 59.00000000000000000 ) ;
#1178=DIRECTION ( 'NONE',  ( 0.000000000000000000, -0.9996456111234529596, 0.02662052143776450636 ) ) ;
#1180=EDGE_LOOP ( 'NONE', ( #17105, #24847, #19897, #18235 ) ) ;
#1181=EDGE_LOOP ( 'NONE', ( #24173, #32686, #12826, #41645 ) ) ;
#1185=ORIENTED_EDGE ( 'NONE', *, *, #14879, .T. ) ;
#1186=DIRECTION ( 'NONE',  ( 0.000000000000000000, 0.000000000000000000, 1.000000000000000000 ) ) ;
#1187=ORIENTED_EDGE ( 'NONE', *, *, #19283, .F. ) ;
#1192=CIRCLE ( 'NONE', #3258, 58.99999999999998579 ) ;
#1196=ORIENTED_EDGE ( 'NONE', *, *, #1926, .F. ) ;
#1198=AXIS2_PLACEMENT_3D ( 'NONE', #38100, #11288, #30916 ) ;
#1199=VECTOR ( 'NONE', #41315, 1000.000000000000000 ) ;
#1202=DIRECTION ( 'NONE',  ( 1.000000000000000000, 0.000000000000000000, 0.000000000000000000 ) ) ;
#1206=DIRECTION ( 'NONE',  ( -1.000000000000000000, 0.000000000000000000, -0.000000000000000000 ) ) ;
#1207=ADVANCED_FACE ( 'NONE', ( #5817 ), #3387, .F. ) ;
#1208=ORIENTED_EDGE ( 'NONE', *, *, #35087, .T. ) ;
#1210=DIRECTION ( 'NONE',  ( 1.000000000000000000, 0.000000000000000000, -0.000000000000000000 ) ) ;
#1213=DIRECTION ( 'NONE',  ( 0.000000000000000000, -0.9213119778704087492, -0.3888241754733308131 ) ) ;
#1214=ORIENTED_EDGE ( 'NONE', *, *, #36823, .T. ) ;
#1216=DIRECTION ( 'NONE',  ( 1.000000000000000000, 0.000000000000000000, 0.000000000000000000 ) ) ;
#1222=EDGE_CURVE ( 'NONE', #25672, #815, #10160, .T. ) ;
#1227=DIRECTION ( 'NONE',  ( 0.000000000000000000, -0.4132121857683850874, 0.9106347728549100129 ) ) ;
#1228=AXIS2_PLACEMENT_3D ( 'NONE', #13976, #31198, #33796 ) ;
#1232=ORIENTED_EDGE ( 'NONE', *, *, #22577, .T. ) ;
#1233=AXIS2_PLACEMENT_3D ( 'NONE', #17157, #20430, #27832 ) ;
#1234=FACE_OUTER_BOUND ( 'NONE', #15938, .T. ) ;
#1235=FACE_OUTER_BOUND ( 'NONE', #41355, .T. ) ;
#1236=AXIS2_PLACEMENT_3D ( 'NONE', #12534, #4173, #10527 ) ;
#1237=CYLINDRICAL_SURFACE ( 'NONE', #2547, 116.0000000000000000 ) ;
#1240=ORIENTED_EDGE ( 'NONE', *, *, #38847, .T. ) ;
#1245=EDGE_LOOP ( 'NONE', ( #28084, #35112, #6542, #37 ) ) ;
#1246=EDGE_CURVE ( 'NONE', #6594, #34567, #33508, .T. ) ;
#1248=ADVANCED_FACE ( 'NONE', ( #7102 ), #37425, .F. ) ;
#1249=CYLINDRICAL_SURFACE ( 'NONE', #23927, 116.0000000000000000 ) ;
#1250=EDGE_CURVE ( 'NONE', #22146, #27962, #27029, .T. ) ;
#1252=DIRECTION ( 'NONE',  ( -1.000000000000000000, 0.000000000000000000, -0.000000000000000000 ) ) ;
#1254=DIRECTION ( 'NONE',  ( 0.000000000000000000, -0.4132121857683850874, 0.9106347728549100129 ) ) ;
#1263=AXIS2_PLACEMENT_3D ( 'NONE', #33333, #9330, #12840 ) ;
#1264=CARTESIAN_POINT ( 'NONE',  ( 0.000000000000000000, -106.6051926090974007, 45.73109345704783379 ) ) ;
#1267=ORIENTED_EDGE ( 'NONE', *, *, #21003, .T. ) ;
#1268=VECTOR ( 'NONE', #14046, 1000.000000000000000 ) ;
#1269=CARTESIAN_POINT ( 'NONE',  ( 17.99999999999999645, 117.6086855750634470, 26.24286718912143712 ) ) ;
#1273=DIRECTION ( 'NONE',  ( 1.000000000000000000, 0.000000000000000000, 0.000000000000000000 ) ) ;
#1276=DIRECTION ( 'NONE',  ( 0.000000000000000000, 0.000000000000000000, 1.000000000000000000 ) ) ;
#1283=CYLINDRICAL_SURFACE ( 'NONE', #38174, 59.00000000000000000 ) ;
#1287=CARTESIAN_POINT ( 'NONE',  ( 17.99999999999999645, 30.01658535635412406, -108.1077105353194838 ) ) ;
#1288=ORIENTED_EDGE ( 'NONE', *, *, #14682, .T. ) ;
#1294=DIRECTION ( 'NONE',  ( -1.000000000000000000, 0.000000000000000000, 0.000000000000000000 ) ) ;
#1299=EDGE_CURVE ( 'NONE', #13037, #20999, #3593, .T. ) ;
#1303=ORIENTED_EDGE ( 'NONE', *, *, #30038, .T. ) ;
#1304=EDGE_CURVE ( 'NONE', #37428, #15011, #7754, .T. ) ;
#1309=ORIENTED_EDGE ( 'NONE', *, *, #28423, .T. ) ;
#1312=CARTESIAN_POINT ( 'NONE',  ( 0.000000000000000000, -53.40478689619659747, -108.0204598100370816 ) ) ;
#1315=DIRECTION ( 'NONE',  ( 1.000000000000000000, 0.000000000000000000, 0.000000000000000000 ) ) ;
#1316=EDGE_CURVE ( 'NONE', #17266, #6343, #30474, .T. ) ;
#1317=EDGE_LOOP ( 'NONE', ( #30939, #28167, #23527, #23489 ) ) ;
#1318=AXIS2_PLACEMENT_3D ( 'NONE', #17445, #4506, #34191 ) ;
#1319=CYLINDRICAL_SURFACE ( 'NONE', #30831, 59.00000000000000000 ) ;
#1326=VERTEX_POINT ( 'NONE', #40902 ) ;
#1329=CARTESIAN_POINT ( 'NONE',  ( 17.99999999999999645, -104.2166695095708491, -60.49278301857915352 ) ) ;
#1334=DIRECTION ( 'NONE',  ( -1.000000000000000000, -0.000000000000000000, -0.000000000000000000 ) ) ;
#1335=CARTESIAN_POINT ( 'NONE',  ( 17.99999999999999645, 61.59243992711459015, 93.77976230226062171 ) ) ;
#1340=VERTEX_POINT ( 'NONE', #11056 ) ;
#1343=EDGE_LOOP ( 'NONE', ( #41084, #12283, #18643, #25685 ) ) ;
#1344=CIRCLE ( 'NONE', #42448, 58.99999999999999289 ) ;
#1346=DIRECTION ( 'NONE',  ( 0.000000000000000000, 0.6382441836448211614, -0.7698339834299053885 ) ) ;
#1347=EDGE_CURVE ( 'NONE', #36755, #39935, #24383, .T. ) ;
#1348=DIRECTION ( 'NONE',  ( -1.000000000000000000, -0.000000000000000000, -0.000000000000000000 ) ) ;
#1350=DIRECTION ( 'NONE',  ( 0.000000000000000000, 0.8477344278896686847, 0.5304209081197459597 ) ) ;
#1353=ORIENTED_EDGE ( 'NONE', *, *, #34670, .F. ) ;
#1354=DIRECTION ( 'NONE',  ( 0.000000000000000000, 0.9911528310040076395, -0.1327255272837190025 ) ) ;
#1356=EDGE_LOOP ( 'NONE', ( #36830, #1080, #6475, #23716 ) ) ;
#1358=EDGE_CURVE ( 'NONE', #37944, #3752, #39471, .T. ) ;
#1359=DIRECTION ( 'NONE',  ( -1.000000000000000000, 0.000000000000000000, 0.000000000000000000 ) ) ;
#1362=DIRECTION ( 'NONE',  ( -1.000000000000000000, 0.000000000000000000, 0.000000000000000000 ) ) ;
#1370=DIRECTION ( 'NONE',  ( 0.000000000000000000, 0.000000000000000000, 1.000000000000000000 ) ) ;
#1371=ORIENTED_EDGE ( 'NONE', *, *, #9764, .F. ) ;
#1375=ORIENTED_EDGE ( 'NONE', *, *, #11380, .F. ) ;
#1377=AXIS2_PLACEMENT_3D ( 'NONE', #15007, #24843, #38308 ) ;
#1378=FACE_OUTER_BOUND ( 'NONE', #24533, .T. ) ;
#1380=EDGE_LOOP ( 'NONE', ( #24309, #27972, #18983, #30106 ) ) ;
#1382=EDGE_CURVE ( 'NONE', #11528, #32977, #36990, .T. ) ;
#1384=ORIENTED_EDGE ( 'NONE', *, *, #40939, .F. ) ;
#1387=CYLINDRICAL_SURFACE ( 'NONE', #37984, 59.00000000000000000 ) ;
#1388=DIRECTION ( 'NONE',  ( 1.000000000000000000, 0.000000000000000000, 0.000000000000000000 ) ) ;
#1392=DIRECTION ( 'NONE',  ( 0.000000000000000000, 0.000000000000000000, -1.000000000000000000 ) ) ;
#1398=FACE_OUTER_BOUND ( 'NONE', #30424, .T. ) ;
#1400=AXIS2_PLACEMENT_3D ( 'NONE', #34444, #15066, #14847 ) ;
#1406=AXIS2_PLACEMENT_3D ( 'NONE', #30781, #21002, #41434 ) ;
#1407=CARTESIAN_POINT ( 'NONE',  ( 0.000000000000000000, 31.17727234463848163, -111.7317219465816862 ) ) ;
#1408=AXIS2_PLACEMENT_3D ( 'NONE', #15972, #42962, #8970 ) ;
#1410=CARTESIAN_POINT ( 'NONE',  ( 17.99999999999999645, 116.0452958106480708, 32.46506308663498430 ) ) ;
#1411=LINE ( 'NONE', #41324, #24064 ) ;
#1412=ORIENTED_EDGE ( 'NONE', *, *, #33372, .F. ) ;
#1415=DIRECTION ( 'NONE',  ( 1.000000000000000000, 0.000000000000000000, 0.000000000000000000 ) ) ;
#1419=DIRECTION ( 'NONE',  ( -1.000000000000000000, 0.000000000000000000, -0.000000000000000000 ) ) ;
#1420=ORIENTED_EDGE ( 'NONE', *, *, #21705, .F. ) ;
#1421=SURFACE_STYLE_USAGE ( .BOTH. , #38079 ) ;
#1430=AXIS2_PLACEMENT_3D ( 'NONE', #39969, #23881, #37145 ) ;
#1433=ADVANCED_FACE ( 'NONE', ( #34584 ), #41777, .F. ) ;
#1437=VECTOR ( 'NONE', #37464, 1000.000000000000000 ) ;
#1445=VERTEX_POINT ( 'NONE', #25245 ) ;
#1446=DIRECTION ( 'NONE',  ( -1.000000000000000000, -0.000000000000000000, -0.000000000000000000 ) ) ;
#1448=CARTESIAN_POINT ( 'NONE',  ( 17.99999999999999645, -76.48293397876204835, -82.08917884620389316 ) ) ;
#1450=CYLINDRICAL_SURFACE ( 'NONE', #14595, 59.00000000000000000 ) ;
#1453=CARTESIAN_POINT ( 'NONE',  ( 17.99999999999999645, 0.000000000000000000, 0.000000000000000000 ) ) ;
#1455=ADVANCED_FACE ( 'NONE', ( #11264 ), #35019, .F. ) ;
#1456=DIRECTION ( 'NONE',  ( 1.000000000000000000, 0.000000000000000000, 0.000000000000000000 ) ) ;
#1457=CARTESIAN_POINT ( 'NONE',  ( -10.00000000000000000, 0.000000000000000000, 0.000000000000000000 ) ) ;
#1461=ORIENTED_EDGE ( 'NONE', *, *, #17602, .T. ) ;
#1465=AXIS2_PLACEMENT_3D ( 'NONE', #42756, #39917, #17079 ) ;
#1472=LINE ( 'NONE', #24883, #10518 ) ;
#1476=DIRECTION ( 'NONE',  ( 1.000000000000000000, 0.000000000000000000, 0.000000000000000000 ) ) ;
#1477=CARTESIAN_POINT ( 'NONE',  ( 0.000000000000000000, 0.000000000000000000, 0.000000000000000000 ) ) ;
#1481=CARTESIAN_POINT ( 'NONE',  ( 17.99999999999999645, 0.000000000000000000, 0.000000000000000000 ) ) ;
#1482=CARTESIAN_POINT ( 'NONE',  ( 0.000000000000000000, 0.000000000000000000, 0.000000000000000000 ) ) ;
#1485=EDGE_CURVE ( 'NONE', #40340, #3463, #1630, .T. ) ;
#1486=ADVANCED_FACE ( 'NONE', ( #34809 ), #31977, .F. ) ;
#1487=VERTEX_POINT ( 'NONE', #25449 ) ;
#1489=EDGE_CURVE ( 'NONE', #27244, #29070, #11648, .T. ) ;
#1490=EDGE_CURVE ( 'NONE', #40777, #23134, #15822, .T. ) ;
#1492=VERTEX_POINT ( 'NONE', #28714 ) ;
#1499=DIRECTION ( 'NONE',  ( -1.000000000000000000, 0.000000000000000000, -0.000000000000000000 ) ) ;
#1500=ORIENTED_EDGE ( 'NONE', *, *, #16941, .F. ) ;
#1501=DIRECTION ( 'NONE',  ( -1.000000000000000000, 0.000000000000000000, 0.000000000000000000 ) ) ;
#1502=CARTESIAN_POINT ( 'NONE',  ( 17.99999999999999645, -47.58001226230612701, 110.7096808509482031 ) ) ;
#1506=AXIS2_PLACEMENT_3D ( 'NONE', #23245, #29347, #42409 ) ;
#1511=DIRECTION ( 'NONE',  ( -1.000000000000000000, -0.000000000000000000, -0.000000000000000000 ) ) ;
#1512=ORIENTED_EDGE ( 'NONE', *, *, #39526, .T. ) ;
#1515=ORIENTED_EDGE ( 'NONE', *, *, #36276, .F. ) ;
#1516=DIRECTION ( 'NONE',  ( 1.000000000000000000, -0.000000000000000000, -0.000000000000000000 ) ) ;
#1519=EDGE_CURVE ( 'NONE', #13726, #7950, #22815, .T. ) ;
#1520=CARTESIAN_POINT ( 'NONE',  ( 17.99999999999999645, 116.0452958106484971, -32.46506308663343532 ) ) ;
#1522=ORIENTED_EDGE ( 'NONE', *, *, #5733, .T. ) ;
#1524=AXIS2_PLACEMENT_3D ( 'NONE', #27752, #41012, #11160 ) ;
#1525=VECTOR ( 'NONE', #20373, 1000.000000000000000 ) ;
#1526=DIRECTION ( 'NONE',  ( 0.000000000000000000, 0.000000000000000000, 1.000000000000000000 ) ) ;
#1527=ORIENTED_EDGE ( 'NONE', *, *, #23327, .T. ) ;
#1528=CARTESIAN_POINT ( 'NONE',  ( -10.00000000000000000, 0.000000000000000000, 0.000000000000000000 ) ) ;
#1530=CYLINDRICAL_SURFACE ( 'NONE', #23575, 116.0000000000000000 ) ;
#1534=CIRCLE ( 'NONE', #41238, 58.99999999999999289 ) ;
#1540=VERTEX_POINT ( 'NONE', #31542 ) ;
#1541=ADVANCED_FACE ( 'NONE', ( #38072 ), #21560, .F. ) ;
#1542=EDGE_CURVE ( 'NONE', #10322, #22974, #16546, .T. ) ;
#1546=EDGE_CURVE ( 'NONE', #21840, #276, #30548, .T. ) ;
#1548=DIRECTION ( 'NONE',  ( 1.000000000000000000, 0.000000000000000000, 0.000000000000000000 ) ) ;
#1557=FACE_OUTER_BOUND ( 'NONE', #26440, .T. ) ;
#1558=DIRECTION ( 'NONE',  ( 0.000000000000000000, 0.000000000000000000, 1.000000000000000000 ) ) ;
#1561=CARTESIAN_POINT ( 'NONE',  ( 0.000000000000000000, 0.000000000000000000, 0.000000000000000000 ) ) ;
#1564=VERTEX_POINT ( 'NONE', #12986 ) ;
#1566=VERTEX_POINT ( 'NONE', #25670 ) ;
#1568=VERTEX_POINT ( 'NONE', #39563 ) ;
#1569=CYLINDRICAL_SURFACE ( 'NONE', #11124, 58.99999999999999289 ) ;
#1573=EDGE_CURVE ( 'NONE', #20690, #32792, #39134, .T. ) ;
#1575=VERTEX_POINT ( 'NONE', #9693 ) ;
#1580=CARTESIAN_POINT ( 'NONE',  ( 17.99999999999999645, -67.32409792376564894, 89.75376489259340929 ) ) ;
#1582=CARTESIAN_POINT ( 'NONE',  ( 17.99999999999999645, 88.00363688980654331, -82.31555682352568226 ) ) ;
#1583=DIRECTION ( 'NONE',  ( -1.000000000000000000, -0.000000000000000000, -0.000000000000000000 ) ) ;
#1585=CIRCLE ( 'NONE', #25992, 59.00000000000000711 ) ;
#1586=FACE_OUTER_BOUND ( 'NONE', #37622, .T. ) ;
#1587=VERTEX_POINT ( 'NONE', #32607 ) ;
#1588=CARTESIAN_POINT ( 'NONE',  ( 0.000000000000000000, 117.6086855750638165, -26.24286718911982774 ) ) ;
#1589=CYLINDRICAL_SURFACE ( 'NONE', #29710, 59.00000000000000000 ) ;
#1590=DIRECTION ( 'NONE',  ( 1.000000000000000000, 0.000000000000000000, 0.000000000000000000 ) ) ;
#1592=CIRCLE ( 'NONE', #22536, 120.5010000000000190 ) ;
#1593=EDGE_CURVE ( 'NONE', #38742, #16728, #32617, .T. ) ;
#1596=CIRCLE ( 'NONE', #19055, 120.5010000000000332 ) ;
#1598=ORIENTED_EDGE ( 'NONE', *, *, #28032, .T. ) ;
#1601=CARTESIAN_POINT ( 'NONE',  ( 17.99999999999999645, -95.38615066514023511, 59.07414607872794932 ) ) ;
#1603=EDGE_CURVE ( 'NONE', #22368, #7685, #16049, .T. ) ;
#1607=DIRECTION ( 'NONE',  ( 0.000000000000000000, 1.423061292157245201E-14, -1.000000000000000000 ) ) ;
#1613=VERTEX_POINT ( 'NONE', #18921 ) ;
#1615=CARTESIAN_POINT ( 'NONE',  ( 8.999999999999998224, -83.58328028049608349, -80.43528614701409651 ) ) ;
#1616=CIRCLE ( 'NONE', #23243, 120.5010000000000190 ) ;
#1618=CYLINDRICAL_SURFACE ( 'NONE', #16685, 120.5010000000000190 ) ;
#1622=CARTESIAN_POINT ( 'NONE',  ( 8.999999999999998224, -48.55277268144258329, -105.3500273609084843 ) ) ;
#1627=DIRECTION ( 'NONE',  ( -1.000000000000000000, 0.000000000000000000, -0.000000000000000000 ) ) ;
#1628=VECTOR ( 'NONE', #12194, 1000.000000000000000 ) ;
#1630=LINE ( 'NONE', #18719, #34602 ) ;
#1631=CARTESIAN_POINT ( 'NONE',  ( 17.99999999999999645, -97.19627249181141337, 71.22763238166453448 ) ) ;
#1633=DIRECTION ( 'NONE',  ( 0.000000000000000000, 0.000000000000000000, 1.000000000000000000 ) ) ;
#1635=ORIENTED_EDGE ( 'NONE', *, *, #34762, .F. ) ;
#1639=AXIS2_PLACEMENT_3D ( 'NONE', #41736, #34977, #25208 ) ;
#1642=ORIENTED_EDGE ( 'NONE', *, *, #28139, .T. ) ;
#1645=EDGE_CURVE ( 'NONE', #20720, #16577, #30447, .T. ) ;
#1646=DIRECTION ( 'NONE',  ( -1.000000000000000000, -0.000000000000000000, -0.000000000000000000 ) ) ;
#1647=VECTOR ( 'NONE', #26840, 1000.000000000000000 ) ;
#1648=ORIENTED_EDGE ( 'NONE', *, *, #10294, .F. ) ;
#1649=DIRECTION ( 'NONE',  ( -1.000000000000000000, -0.000000000000000000, 0.000000000000000000 ) ) ;
#1656=CARTESIAN_POINT ( 'NONE',  ( 17.99999999999999645, -110.0562500189195561, -49.07252625220223052 ) ) ;
#1659=EDGE_CURVE ( 'NONE', #14903, #38713, #36091, .T. ) ;
#1660=CARTESIAN_POINT ( 'NONE',  ( 17.99999999999999645, -89.07460286905796920, -81.15544420875052367 ) ) ;
#1663=CARTESIAN_POINT ( 'NONE',  ( 0.000000000000000000, -107.2885202478262556, -54.86040852957423652 ) ) ;
#1665=DIRECTION ( 'NONE',  ( 1.000000000000000000, 0.000000000000000000, 0.000000000000000000 ) ) ;
#1670=ORIENTED_EDGE ( 'NONE', *, *, #29679, .T. ) ;
#1675=DIRECTION ( 'NONE',  ( 0.000000000000000000, 0.000000000000000000, 1.000000000000000000 ) ) ;
#1676=CIRCLE ( 'NONE', #21230, 116.0000000000000000 ) ;
#1677=VERTEX_POINT ( 'NONE', #42410 ) ;
#1679=EDGE_CURVE ( 'NONE', #1587, #16211, #9474, .T. ) ;
#1680=VERTEX_POINT ( 'NONE', #36080 ) ;
#1683=CYLINDRICAL_SURFACE ( 'NONE', #42445, 59.00000000000000000 ) ;
#1685=CYLINDRICAL_SURFACE ( 'NONE', #31197, 59.00000000000000000 ) ;
#1686=CARTESIAN_POINT ( 'NONE',  ( 0.000000000000000000, -68.63002662989811142, 93.51962064069482494 ) ) ;
#1687=ORIENTED_EDGE ( 'NONE', *, *, #18227, .T. ) ;
#1689=LINE ( 'NONE', #38134, #22089 ) ;
#1690=VERTEX_POINT ( 'NONE', #39770 ) ;
#1693=CARTESIAN_POINT ( 'NONE',  ( 0.000000000000000000, -63.55543939553702160, -97.03971415477388973 ) ) ;
#1698=AXIS2_PLACEMENT_3D ( 'NONE', #14434, #8719, #5019 ) ;
#1699=DIRECTION ( 'NONE',  ( -1.000000000000000000, -0.000000000000000000, -0.000000000000000000 ) ) ;
#1707=AXIS2_PLACEMENT_3D ( 'NONE', #31150, #34618, #793 ) ;
#1708=EDGE_LOOP ( 'NONE', ( #10398, #37993, #11211, #26932 ) ) ;
#1712=DIRECTION ( 'NONE',  ( 0.000000000000000000, 0.8477344278896721264, -0.5304209081197405196 ) ) ;
#1714=ORIENTED_EDGE ( 'NONE', *, *, #33506, .T. ) ;
#1715=CARTESIAN_POINT ( 'NONE',  ( 9.000000000000001776, 35.78484819117785776, -110.3423972910429143 ) ) ;
#1717=AXIS2_PLACEMENT_3D ( 'NONE', #37382, #7499, #20862 ) ;
#1723=DIRECTION ( 'NONE',  ( -1.000000000000000000, 0.000000000000000000, 0.000000000000000000 ) ) ;
#1725=CYLINDRICAL_SURFACE ( 'NONE', #26329, 116.0000000000000000 ) ;
#1726=ORIENTED_EDGE ( 'NONE', *, *, #15773, .T. ) ;
#1728=ORIENTED_EDGE ( 'NONE', *, *, #8593, .F. ) ;
#1729=LINE ( 'NONE', #38809, #31640 ) ;
#1730=ORIENTED_EDGE ( 'NONE', *, *, #21825, .T. ) ;
#1732=CARTESIAN_POINT ( 'NONE',  ( 17.99999999999999645, -51.27532863109303918, -99.79535634195178773 ) ) ;
#1733=LINE ( 'NONE', #25556, #7441 ) ;
#1734=EDGE_CURVE ( 'NONE', #26760, #12939, #15154, .T. ) ;
#1739=FACE_OUTER_BOUND ( 'NONE', #12587, .T. ) ;
#1742=DIRECTION ( 'NONE',  ( 0.000000000000000000, -5.351180891996252112E-15, -1.000000000000000000 ) ) ;
#1745=DIRECTION ( 'NONE',  ( 0.000000000000000000, 0.000000000000000000, 1.000000000000000000 ) ) ;
#1754=AXIS2_PLACEMENT_3D ( 'NONE', #12987, #22608, #29997 ) ;
#1755=ORIENTED_EDGE ( 'NONE', *, *, #12188, .F. ) ;
#1756=AXIS2_PLACEMENT_3D ( 'NONE', #34470, #27963, #14657 ) ;
#1760=AXIS2_PLACEMENT_3D ( 'NONE', #28995, #11618, #11837 ) ;
#1761=EDGE_CURVE ( 'NONE', #39524, #24229, #29802, .T. ) ;
#1762=AXIS2_PLACEMENT_3D ( 'NONE', #27667, #30279, #789 ) ;
#1763=DIRECTION ( 'NONE',  ( 1.000000000000000000, 0.000000000000000000, 0.000000000000000000 ) ) ;
#1764=VECTOR ( 'NONE', #23522, 1000.000000000000000 ) ;
#1770=AXIS2_PLACEMENT_3D ( 'NONE', #19960, #39540, #42804 ) ;
#1774=CARTESIAN_POINT ( 'NONE',  ( 9.000000000000001776, -115.6826031496112677, 8.575274253897077870 ) ) ;
#1775=CYLINDRICAL_SURFACE ( 'NONE', #29863, 59.00000000000000000 ) ;
#1777=DIRECTION ( 'NONE',  ( 1.000000000000000000, 0.000000000000000000, 0.000000000000000000 ) ) ;
#1779=ORIENTED_EDGE ( 'NONE', *, *, #39181, .T. ) ;
#1782=VERTEX_POINT ( 'NONE', #39977 ) ;
#1783=DIRECTION ( 'NONE',  ( 0.000000000000000000, 0.000000000000000000, 1.000000000000000000 ) ) ;
#1784=EDGE_CURVE ( 'NONE', #3612, #28259, #36711, .T. ) ;
#1786=VERTEX_POINT ( 'NONE', #29995 ) ;
#1787=CARTESIAN_POINT ( 'NONE',  ( 17.99999999999999645, -6.486220790507708500, -112.0098273076987994 ) ) ;
#1788=EDGE_CURVE ( 'NONE', #40221, #1575, #38128, .T. ) ;
#1789=AXIS2_PLACEMENT_3D ( 'NONE', #21509, #5299, #5514 ) ;
#1790=EDGE_CURVE ( 'NONE', #7217, #33553, #19352, .T. ) ;
#1795=DIRECTION ( 'NONE',  ( 0.000000000000000000, 0.3641605752528230266, -0.9313361774523382097 ) ) ;
#1799=DIRECTION ( 'NONE',  ( 0.000000000000000000, 0.000000000000000000, 1.000000000000000000 ) ) ;
#1806=DIRECTION ( 'NONE',  ( 0.000000000000000000, 0.4132121857683790922, -0.9106347728549127885 ) ) ;
#1811=ORIENTED_EDGE ( 'NONE', *, *, #1382, .T. ) ;
#1813=ORIENTED_EDGE ( 'NONE', *, *, #7774, .T. ) ;
#1814=VERTEX_POINT ( 'NONE', #3544 ) ;
#1815=DIRECTION ( 'NONE',  ( 0.000000000000000000, 0.000000000000000000, -1.000000000000000000 ) ) ;
#1817=VECTOR ( 'NONE', #39641, 1000.000000000000000 ) ;
#1819=CARTESIAN_POINT ( 'NONE',  ( 17.99999999999999645, 56.51398178981825993, 96.92493144647468739 ) ) ;
#1822=AXIS2_PLACEMENT_3D ( 'NONE', #3123, #23058, #3356 ) ;
#1823=DIRECTION ( 'NONE',  ( 0.000000000000000000, 0.000000000000000000, 1.000000000000000000 ) ) ;
#1825=DIRECTION ( 'NONE',  ( -1.000000000000000000, 0.000000000000000000, -0.000000000000000000 ) ) ;
#1830=AXIS2_PLACEMENT_3D ( 'NONE', #32331, #15999, #41930 ) ;
#1831=AXIS2_PLACEMENT_3D ( 'NONE', #34391, #17651, #21143 ) ;
#1833=DIRECTION ( 'NONE',  ( -1.000000000000000000, -0.000000000000000000, 0.000000000000000000 ) ) ;
#1834=VERTEX_POINT ( 'NONE', #16918 ) ;
#1836=CARTESIAN_POINT ( 'NONE',  ( -10.00000000000000000, 0.000000000000000000, 0.000000000000000000 ) ) ;
#1841=ORIENTED_EDGE ( 'NONE', *, *, #1734, .F. ) ;
#1844=CARTESIAN_POINT ( 'NONE',  ( 9.000000000000001776, 6.854627147198713466, 115.7972974066013734 ) ) ;
#1850=ORIENTED_EDGE ( 'NONE', *, *, #38700, .F. ) ;
#1852=DIRECTION ( 'NONE',  ( -1.000000000000000000, -0.000000000000000000, 0.000000000000000000 ) ) ;
#1854=CARTESIAN_POINT ( 'NONE',  ( 0.000000000000000000, 0.5156212287294736907, -112.1962860721878315 ) ) ;
#1855=AXIS2_PLACEMENT_3D ( 'NONE', #27043, #40312, #13954 ) ;
#1856=VERTEX_POINT ( 'NONE', #24106 ) ;
#1857=CARTESIAN_POINT ( 'NONE',  ( 0.000000000000000000, -63.24564713401861837, 102.5693868539693341 ) ) ;
#1861=LINE ( 'NONE', #41783, #36631 ) ;
#1862=EDGE_CURVE ( 'NONE', #2165, #22806, #9572, .T. ) ;
#1865=ORIENTED_EDGE ( 'NONE', *, *, #32961, .F. ) ;
#1866=DIRECTION ( 'NONE',  ( 0.000000000000000000, -0.5076658003388467844, 0.8615540813938020737 ) ) ;
#1870=CARTESIAN_POINT ( 'NONE',  ( 0.000000000000000000, -111.2721026680459602, -14.38025178762732104 ) ) ;
#1874=DIRECTION ( 'NONE',  ( -1.000000000000000000, -0.000000000000000000, -0.000000000000000000 ) ) ;
#1875=ADVANCED_FACE ( 'NONE', ( #10771 ), #41062, .F. ) ;
#1877=CYLINDRICAL_SURFACE ( 'NONE', #15876, 59.00000000000000000 ) ;
#1883=DIRECTION ( 'NONE',  ( 0.000000000000000000, 0.5528000653611888637, 0.8333139190825179510 ) ) ;
#1884=ORIENTED_EDGE ( 'NONE', *, *, #31822, .F. ) ;
#1885=DIRECTION ( 'NONE',  ( 1.000000000000000000, 0.000000000000000000, 0.000000000000000000 ) ) ;
#1889=ORIENTED_EDGE ( 'NONE', *, *, #29827, .F. ) ;
#1894=DIRECTION ( 'NONE',  ( 1.000000000000000000, 0.000000000000000000, 0.000000000000000000 ) ) ;
#1899=FACE_OUTER_BOUND ( 'NONE', #32104, .T. ) ;
#1901=CARTESIAN_POINT ( 'NONE',  ( 17.99999999999999645, -111.1352304691226607, -15.40237066878709449 ) ) ;
#1903=CARTESIAN_POINT ( 'NONE',  ( 17.99999999999999645, 112.1702510623870097, 2.471285140324554153 ) ) ;
#1906=CYLINDRICAL_SURFACE ( 'NONE', #39428, 116.0000000000000000 ) ;
#1910=LINE ( 'NONE', #38348, #33814 ) ;
#1913=AXIS2_PLACEMENT_3D ( 'NONE', #19735, #32996, #26904 ) ;
#1915=AXIS2_PLACEMENT_3D ( 'NONE', #6755, #173, #42960 ) ;
#1919=AXIS2_PLACEMENT_3D ( 'NONE', #28460, #29089, #38444 ) ;
#1926=EDGE_CURVE ( 'NONE', #26169, #28773, #7919, .T. ) ;
#1928=CIRCLE ( 'NONE', #26344, 120.5010000000000190 ) ;
#1929=DIRECTION ( 'NONE',  ( -1.000000000000000000, 0.000000000000000000, -0.000000000000000000 ) ) ;
#1932=VERTEX_POINT ( 'NONE', #31699 ) ;
#1935=ORIENTED_EDGE ( 'NONE', *, *, #31361, .T. ) ;
#1938=ORIENTED_EDGE ( 'NONE', *, *, #18657, .T. ) ;
#1941=DIRECTION ( 'NONE',  ( -1.000000000000000000, 0.000000000000000000, 0.000000000000000000 ) ) ;
#1943=ORIENTED_EDGE ( 'NONE', *, *, #4066, .F. ) ;
#1944=AXIS2_PLACEMENT_3D ( 'NONE', #29688, #36411, #36632 ) ;
#1945=ADVANCED_FACE ( 'NONE', ( #18436 ), #5075, .F. ) ;
#1946=CIRCLE ( 'NONE', #31930, 120.5010000000000190 ) ;
#1947=ORIENTED_EDGE ( 'NONE', *, *, #31855, .F. ) ;
#1948=VECTOR ( 'NONE', #35399, 1000.000000000000000 ) ;
#1949=DIRECTION ( 'NONE',  ( 0.000000000000000000, 0.000000000000000000, 1.000000000000000000 ) ) ;
#1955=CARTESIAN_POINT ( 'NONE',  ( 17.99999999999999645, 67.32409792376505209, 89.75376489259387824 ) ) ;
#1956=LINE ( 'NONE', #5865, #17884 ) ;
#1959=UNCERTAINTY_MEASURE_WITH_UNIT (LENGTH_MEASURE( 1.000000000000000082E-05 ), #24390, 'distance_accuracy_value', 'NONE');
#1961=CARTESIAN_POINT ( 'NONE',  ( 17.99999999999999645, 34.74871106919619024, 106.6808302961373158 ) ) ;
#1964=ADVANCED_FACE ( 'NONE', ( #21508 ), #14717, .F. ) ;
#1965=DIRECTION ( 'NONE',  ( 0.000000000000000000, 0.5076658003388409002, -0.8615540813938056264 ) ) ;
#1970=DIRECTION ( 'NONE',  ( -1.000000000000000000, -0.000000000000000000, -0.000000000000000000 ) ) ;
#1974=AXIS2_PLACEMENT_3D ( 'NONE', #16341, #358, #9340 ) ;
#1976=EDGE_CURVE ( 'NONE', #39935, #35045, #2570, .T. ) ;
#1977=CARTESIAN_POINT ( 'NONE',  ( -10.00000000000000000, 0.000000000000000000, 0.000000000000000000 ) ) ;
#1980=DIRECTION ( 'NONE',  ( 1.000000000000000000, 0.000000000000000000, 0.000000000000000000 ) ) ;
#1982=ORIENTED_EDGE ( 'NONE', *, *, #20784, .F. ) ;
#1985=CARTESIAN_POINT ( 'NONE',  ( 17.99999999999999645, 0.000000000000000000, 0.000000000000000000 ) ) ;
#1988=DIRECTION ( 'NONE',  ( 1.000000000000000000, 0.000000000000000000, 0.000000000000000000 ) ) ;
#1989=ORIENTED_EDGE ( 'NONE', *, *, #42017, .T. ) ;
#1991=ORIENTED_EDGE ( 'NONE', *, *, #26679, .F. ) ;
#1992=ADVANCED_FACE ( 'NONE', ( #41280 ), #37589, .F. ) ;
#1994=CARTESIAN_POINT ( 'NONE',  ( 17.99999999999999645, 108.8880088604282008, -39.99251838045848473 ) ) ;
#2010=CARTESIAN_POINT ( 'NONE',  ( 17.99999999999999645, -103.4151313792875158, 61.85306461934377609 ) ) ;
#2012=VERTEX_POINT ( 'NONE', #34317 ) ;
#2014=CARTESIAN_POINT ( 'NONE',  ( 17.99999999999999645, 115.9387338813861419, 3.769613505536437259 ) ) ;
#2016=CARTESIAN_POINT ( 'NONE',  ( 17.99999999999999645, -114.1529630473446986, -38.59523323561551678 ) ) ;
#2017=ORIENTED_EDGE ( 'NONE', *, *, #39289, .T. ) ;
#2020=VERTEX_POINT ( 'NONE', #22991 ) ;
#2023=CARTESIAN_POINT ( 'NONE',  ( 0.000000000000000000, 0.000000000000000000, 0.000000000000000000 ) ) ;
#2025=AXIS2_PLACEMENT_3D ( 'NONE', #33005, #28704, #15604 ) ;
#2026=ADVANCED_FACE ( 'NONE', ( #29500 ), #2211, .F. ) ;
#2029=EDGE_CURVE ( 'NONE', #416, #27001, #9206, .T. ) ;
#2030=EDGE_CURVE ( 'NONE', #18, #17680, #8814, .T. ) ;
#2033=CARTESIAN_POINT ( 'NONE',  ( 0.000000000000000000, -67.32409792376564894, 89.75376489259340929 ) ) ;
#2034=VERTEX_POINT ( 'NONE', #29293 ) ;
#2036=EDGE_LOOP ( 'NONE', ( #23878, #10776, #20193, #33755 ) ) ;
#2041=VERTEX_POINT ( 'NONE', #16419 ) ;
#2049=CARTESIAN_POINT ( 'NONE',  ( 0.000000000000000000, 68.61497464550733127, -99.05794392877533028 ) ) ;
#2050=DIRECTION ( 'NONE',  ( -1.000000000000000000, 0.000000000000000000, 0.000000000000000000 ) ) ;
#2052=VERTEX_POINT ( 'NONE', #29086 ) ;
#2054=AXIS2_PLACEMENT_3D ( 'NONE', #22164, #9018, #1823 ) ;
#2056=CARTESIAN_POINT ( 'NONE',  ( 17.99999999999999645, -61.59243992711397198, -93.77976230226100540 ) ) ;
#2059=ORIENTED_EDGE ( 'NONE', *, *, #29299, .F. ) ;
#2066=CARTESIAN_POINT ( 'NONE',  ( 17.99999999999999645, 0.000000000000000000, 0.000000000000000000 ) ) ;
#2067=EDGE_LOOP ( 'NONE', ( #24561, #31518, #15195, #20919 ) ) ;
#2070=LINE ( 'NONE', #24836, #5448 ) ;
#2071=CARTESIAN_POINT ( 'NONE',  ( 17.99999999999999645, -107.2885202478262698, -54.86040852957422942 ) ) ;
#2072=EDGE_CURVE ( 'NONE', #14692, #36478, #10913, .T. ) ;
#2076=EDGE_CURVE ( 'NONE', #6200, #40762, #29720, .T. ) ;
#2077=DIRECTION ( 'NONE',  ( -1.000000000000000000, 0.000000000000000000, 0.000000000000000000 ) ) ;
#2080=CARTESIAN_POINT ( 'NONE',  ( -10.00000000000000000, 0.000000000000000000, 0.000000000000000000 ) ) ;
#2081=ORIENTED_EDGE ( 'NONE', *, *, #1382, .F. ) ;
#2082=CARTESIAN_POINT ( 'NONE',  ( 0.000000000000000000, -103.5682682299985515, -43.14958040911633219 ) ) ;
#2090=DIRECTION ( 'NONE',  ( 0.000000000000000000, -1.599473849036242511E-14, -1.000000000000000000 ) ) ;
#2094=EDGE_CURVE ( 'NONE', #40855, #13726, #32552, .T. ) ;
#2097=DIRECTION ( 'NONE',  ( -1.000000000000000000, -0.000000000000000000, -0.000000000000000000 ) ) ;
#2099=ORIENTED_EDGE ( 'NONE', *, *, #36276, .T. ) ;
#2100=CARTESIAN_POINT ( 'NONE',  ( 0.000000000000000000, 0.000000000000000000, 0.000000000000000000 ) ) ;
#2103=CARTESIAN_POINT ( 'NONE',  ( 0.000000000000000000, -109.3506818544107659, -38.70953859161124910 ) ) ;
#2104=CIRCLE ( 'NONE', #11204, 120.5010000000000474 ) ;
#2105=EDGE_CURVE ( 'NONE', #18385, #10543, #20686, .T. ) ;
#2106=DIRECTION ( 'NONE',  ( 0.000000000000000000, 0.000000000000000000, 1.000000000000000000 ) ) ;
#2108=DIRECTION ( 'NONE',  ( -1.000000000000000000, -0.000000000000000000, -0.000000000000000000 ) ) ;
#2109=CIRCLE ( 'NONE', #4192, 59.00000000000000711 ) ;
#2111=CYLINDRICAL_SURFACE ( 'NONE', #38367, 59.00000000000000000 ) ;
#2113=VECTOR ( 'NONE', #29831, 1000.000000000000000 ) ;
#2114=DIRECTION ( 'NONE',  ( 0.000000000000000000, -0.9826841245925227453, 0.1852887240871045060 ) ) ;
#2115=CARTESIAN_POINT ( 'NONE',  ( 9.000000000000001776, 63.55543939553896848, -97.03971415477259654 ) ) ;
#2122=AXIS2_PLACEMENT_3D ( 'NONE', #11957, #8440, #18526 ) ;
#2129=EDGE_LOOP ( 'NONE', ( #17727, #37551, #22985, #23177 ) ) ;
#2130=DIRECTION ( 'NONE',  ( -1.000000000000000000, 0.000000000000000000, 0.000000000000000000 ) ) ;
#2134=DIRECTION ( 'NONE',  ( 1.000000000000000000, 0.000000000000000000, 0.000000000000000000 ) ) ;
#2137=CIRCLE ( 'NONE', #26549, 59.00000000000001421 ) ;
#2139=ADVANCED_FACE ( 'NONE', ( #19493 ), #32757, .F. ) ;
#2143=AXIS2_PLACEMENT_3D ( 'NONE', #35011, #31325, #38705 ) ;
#2144=AXIS2_PLACEMENT_3D ( 'NONE', #9889, #251, #10762 ) ;
#2152=ORIENTED_EDGE ( 'NONE', *, *, #33282, .T. ) ;
#2155=AXIS2_PLACEMENT_3D ( 'NONE', #11538, #8833, #41170 ) ;
#2157=LINE ( 'NONE', #15514, #10955 ) ;
#2161=ORIENTED_EDGE ( 'NONE', *, *, #33722, .T. ) ;
#2162=CARTESIAN_POINT ( 'NONE',  ( 17.99999999999999645, 0.000000000000000000, 0.000000000000000000 ) ) ;
#2164=CARTESIAN_POINT ( 'NONE',  ( 17.99999999999999645, -34.03109950475805334, 115.5957406979048727 ) ) ;
#2165=VERTEX_POINT ( 'NONE', #16658 ) ;
#2166=CARTESIAN_POINT ( 'NONE',  ( 17.99999999999999645, -10.40101730206447961, 120.0512800434970728 ) ) ;
#2167=CARTESIAN_POINT ( 'NONE',  ( 0.000000000000000000, 112.1427988504407551, 3.502162136923788083 ) ) ;
#2168=CYLINDRICAL_SURFACE ( 'NONE', #33717, 59.00000000000000000 ) ;
#2179=CYLINDRICAL_SURFACE ( 'NONE', #25628, 120.5010000000000190 ) ;
#2180=DIRECTION ( 'NONE',  ( 0.000000000000000000, 0.000000000000000000, 1.000000000000000000 ) ) ;
#2181=CARTESIAN_POINT ( 'NONE',  ( -10.00000000000000000, 0.000000000000000000, 0.000000000000000000 ) ) ;
#2182=EDGE_CURVE ( 'NONE', #16388, #11355, #29943, .T. ) ;
#2183=ORIENTED_EDGE ( 'NONE', *, *, #4223, .F. ) ;
#2185=VERTEX_POINT ( 'NONE', #37103 ) ;
#2186=CARTESIAN_POINT ( 'NONE',  ( 17.99999999999999645, 0.000000000000000000, 0.000000000000000000 ) ) ;
#2188=ORIENTED_EDGE ( 'NONE', *, *, #16579, .T. ) ;
#2191=EDGE_LOOP ( 'NONE', ( #8546, #16543, #35546, #24311 ) ) ;
#2192=CARTESIAN_POINT ( 'NONE',  ( 0.000000000000000000, -110.3490479609630910, -20.28201389785511211 ) ) ;
#2193=ORIENTED_EDGE ( 'NONE', *, *, #12425, .T. ) ;
#2197=CIRCLE ( 'NONE', #17587, 116.0000000000000000 ) ;
#2199=EDGE_LOOP ( 'NONE', ( #19507, #33307, #37312, #33705 ) ) ;
#2201=AXIS2_PLACEMENT_3D ( 'NONE', #9390, #41760, #42972 ) ;
#2204=DIRECTION ( 'NONE',  ( 0.000000000000000000, 0.000000000000000000, 1.000000000000000000 ) ) ;
#2205=CARTESIAN_POINT ( 'NONE',  ( 17.99999999999999645, -30.01658535635190361, -108.1077105353201233 ) ) ;
#2210=CARTESIAN_POINT ( 'NONE',  ( 17.99999999999999645, -64.58410930313458209, -101.7319213743688664 ) ) ;
#2211=CYLINDRICAL_SURFACE ( 'NONE', #37364, 58.99999999999999289 ) ;
#2212=DIRECTION ( 'NONE',  ( 1.000000000000000000, -0.000000000000000000, -0.000000000000000000 ) ) ;
#2225=ORIENTED_EDGE ( 'NONE', *, *, #27472, .F. ) ;
#2229=DIRECTION ( 'NONE',  ( -1.000000000000000000, -0.000000000000000000, -0.000000000000000000 ) ) ;
#2235=DIRECTION ( 'NONE',  ( 0.000000000000000000, 0.000000000000000000, 1.000000000000000000 ) ) ;
#2236=VECTOR ( 'NONE', #25974, 1000.000000000000000 ) ;
#2238=EDGE_CURVE ( 'NONE', #24063, #30314, #12903, .T. ) ;
#2239=CARTESIAN_POINT ( 'NONE',  ( 0.000000000000000000, -75.72520367775142347, 82.78868281115956052 ) ) ;
#2241=ORIENTED_EDGE ( 'NONE', *, *, #27292, .T. ) ;
#2244=ORIENTED_EDGE ( 'NONE', *, *, #15325, .T. ) ;
#2251=ORIENTED_EDGE ( 'NONE', *, *, #38807, .T. ) ;
#2252=VECTOR ( 'NONE', #35073, 1000.000000000000000 ) ;
#2254=EDGE_CURVE ( 'NONE', #4572, #1856, #41466, .T. ) ;
#2255=DIRECTION ( 'NONE',  ( 1.000000000000000000, 0.000000000000000000, 0.000000000000000000 ) ) ;
#2256=DIRECTION ( 'NONE',  ( 1.000000000000000000, 0.000000000000000000, 0.000000000000000000 ) ) ;
#2258=AXIS2_PLACEMENT_3D ( 'NONE', #25084, #35267, #21377 ) ;
#2264=AXIS2_PLACEMENT_3D ( 'NONE', #5191, #11780, #14393 ) ;
#2265=DIRECTION ( 'NONE',  ( 0.000000000000000000, 0.6783118362696173298, -0.7347741508630660778 ) ) ;
#2266=CARTESIAN_POINT ( 'NONE',  ( 0.000000000000000000, 17.33727698085324320, -110.8498592715971967 ) ) ;
#2269=CARTESIAN_POINT ( 'NONE',  ( 17.99999999999999645, -115.6826031496112677, 8.575274253897077870 ) ) ;
#2271=CARTESIAN_POINT ( 'NONE',  ( 17.99999999999999645, 0.000000000000000000, 0.000000000000000000 ) ) ;
#2274=DIRECTION ( 'NONE',  ( -1.000000000000000000, -0.000000000000000000, 0.000000000000000000 ) ) ;
#2278=CARTESIAN_POINT ( 'NONE',  ( 0.000000000000000000, 0.000000000000000000, 0.000000000000000000 ) ) ;
#2280=AXIS2_PLACEMENT_3D ( 'NONE', #16765, #36785, #29844 ) ;
#2281=ORIENTED_EDGE ( 'NONE', *, *, #19704, .T. ) ;
#2282=CARTESIAN_POINT ( 'NONE',  ( 17.99999999999999645, -62.45178862086154226, -93.20969140437570388 ) ) ;
#2283=ORIENTED_EDGE ( 'NONE', *, *, #829, .T. ) ;
#2284=CARTESIAN_POINT ( 'NONE',  ( 0.000000000000000000, 90.81729652456265001, -72.16798910853526650 ) ) ;
#2285=EDGE_CURVE ( 'NONE', #27962, #5227, #28246, .T. ) ;
#2286=CARTESIAN_POINT ( 'NONE',  ( 17.99999999999999645, -63.55543939553828636, 97.03971415477303708 ) ) ;
#2291=CARTESIAN_POINT ( 'NONE',  ( 17.99999999999999645, 0.000000000000000000, 0.000000000000000000 ) ) ;
#2293=AXIS2_PLACEMENT_3D ( 'NONE', #28778, #5414, #32036 ) ;
#2294=ORIENTED_EDGE ( 'NONE', *, *, #39324, .F. ) ;
#2296=CARTESIAN_POINT ( 'NONE',  ( 17.99999999999999645, 0.000000000000000000, 0.000000000000000000 ) ) ;
#2298=ORIENTED_EDGE ( 'NONE', *, *, #2587, .F. ) ;
#2300=DIRECTION ( 'NONE',  ( 1.000000000000000000, 0.000000000000000000, -0.000000000000000000 ) ) ;
#2306=DIRECTION ( 'NONE',  ( -1.000000000000000000, -0.000000000000000000, -0.000000000000000000 ) ) ;
#2322=DIRECTION ( 'NONE',  ( 1.000000000000000000, -0.000000000000000000, 0.000000000000000000 ) ) ;
#2324=AXIS2_PLACEMENT_3D ( 'NONE', #35656, #8845, #12566 ) ;
#2325=DIRECTION ( 'NONE',  ( 0.000000000000000000, -0.3140767120219362107, -0.9493976084683853900 ) ) ;
#2329=VECTOR ( 'NONE', #26273, 1000.000000000000000 ) ;
#2331=CYLINDRICAL_SURFACE ( 'NONE', #34563, 59.00000000000000000 ) ;
#2332=DIRECTION ( 'NONE',  ( -1.000000000000000000, -0.000000000000000000, -0.000000000000000000 ) ) ;
#2337=CARTESIAN_POINT ( 'NONE',  ( 17.99999999999999645, 23.21237537461889389, -109.7700237000589709 ) ) ;
#2339=AXIS2_PLACEMENT_3D ( 'NONE', #20489, #13498, #26583 ) ;
#2342=DIRECTION ( 'NONE',  ( 0.000000000000000000, 0.000000000000000000, 1.000000000000000000 ) ) ;
#2345=ORIENTED_EDGE ( 'NONE', *, *, #3883, .F. ) ;
#2350=VERTEX_POINT ( 'NONE', #11987 ) ;
#2351=DIRECTION ( 'NONE',  ( 1.000000000000000000, 0.000000000000000000, 0.000000000000000000 ) ) ;
#2352=LINE ( 'NONE', #32492, #24211 ) ;
#2353=DIRECTION ( 'NONE',  ( -1.000000000000000000, -0.000000000000000000, -0.000000000000000000 ) ) ;
#2354=EDGE_CURVE ( 'NONE', #3997, #39762, #19898, .T. ) ;
#2355=ADVANCED_FACE ( 'NONE', ( #32235 ), #25304, .F. ) ;
#2356=DIRECTION ( 'NONE',  ( -1.000000000000000000, 0.000000000000000000, 0.000000000000000000 ) ) ;
#2359=DIRECTION ( 'NONE',  ( -1.000000000000000000, 0.000000000000000000, 0.000000000000000000 ) ) ;
#2361=ADVANCED_FACE ( 'NONE', ( #41393 ), #8900, .F. ) ;
#2366=ORIENTED_EDGE ( 'NONE', *, *, #33916, .F. ) ;
#2370=EDGE_CURVE ( 'NONE', #29797, #28903, #35701, .T. ) ;
#2372=AXIS2_PLACEMENT_3D ( 'NONE', #18751, #25705, #32006 ) ;
#2375=DIRECTION ( 'NONE',  ( 0.000000000000000000, 0.000000000000000000, 1.000000000000000000 ) ) ;
#2376=EDGE_CURVE ( 'NONE', #16211, #42312, #7336, .T. ) ;
#2381=FACE_OUTER_BOUND ( 'NONE', #41664, .T. ) ;
#2382=FACE_OUTER_BOUND ( 'NONE', #35047, .T. ) ;
#2384=CIRCLE ( 'NONE', #12196, 116.0000000000000000 ) ;
#2385=CARTESIAN_POINT ( 'NONE',  ( 17.99999999999999645, -3.996885678773838713, 120.4346956066681713 ) ) ;
#2391=CIRCLE ( 'NONE', #35810, 120.5010000000000190 ) ;
#2394=VERTEX_POINT ( 'NONE', #1693 ) ;
#2395=DIRECTION ( 'NONE',  ( -1.000000000000000000, 0.000000000000000000, -0.000000000000000000 ) ) ;
#2401=VERTEX_POINT ( 'NONE', #14827 ) ;
#2403=EDGE_CURVE ( 'NONE', #28151, #34294, #15047, .T. ) ;
#2407=AXIS2_PLACEMENT_3D ( 'NONE', #8361, #21518, #15163 ) ;
#2410=CYLINDRICAL_SURFACE ( 'NONE', #11679, 116.0000000000000000 ) ;
#2412=DIRECTION ( 'NONE',  ( 0.000000000000000000, -0.5076658003388292428, -0.8615540813938123987 ) ) ;
#2413=EDGE_CURVE ( 'NONE', #6459, #6927, #34865, .T. ) ;
#2414=CIRCLE ( 'NONE', #26838, 59.00000000000001421 ) ;
#2415=CARTESIAN_POINT ( 'NONE',  ( 17.99999999999999645, 0.000000000000000000, 0.000000000000000000 ) ) ;
#2417=CARTESIAN_POINT ( 'NONE',  ( 9.000000000000001776, -41.60679253225837471, 108.2814610871944581 ) ) ;
#2419=ORIENTED_EDGE ( 'NONE', *, *, #37837, .T. ) ;
#2420=EDGE_CURVE ( 'NONE', #35898, #31916, #1910, .T. ) ;
#2422=ORIENTED_EDGE ( 'NONE', *, *, #24709, .F. ) ;
#2424=DIRECTION ( 'NONE',  ( 0.000000000000000000, 0.000000000000000000, 1.000000000000000000 ) ) ;
#2425=EDGE_CURVE ( 'NONE', #32233, #39191, #15048, .T. ) ;
#2431=CIRCLE ( 'NONE', #14318, 59.00000000000000711 ) ;
#2432=VERTEX_POINT ( 'NONE', #5411 ) ;
#2437=CARTESIAN_POINT ( 'NONE',  ( -10.00000000000000000, 0.000000000000000000, 0.000000000000000000 ) ) ;
#2438=CARTESIAN_POINT ( 'NONE',  ( 0.000000000000000000, 34.03109950475887047, -115.5957406979046596 ) ) ;
#2439=DIRECTION ( 'NONE',  ( -1.000000000000000000, -0.000000000000000000, -0.000000000000000000 ) ) ;
#2440=VERTEX_POINT ( 'NONE', #11777 ) ;
#2442=ORIENTED_EDGE ( 'NONE', *, *, #12993, .F. ) ;
#2443=CARTESIAN_POINT ( 'NONE',  ( 0.000000000000000000, -58.30069736313598128, -100.2847380560572930 ) ) ;
#2444=EDGE_CURVE ( 'NONE', #5962, #11572, #18779, .T. ) ;
#2452=ORIENTED_EDGE ( 'NONE', *, *, #8968, .F. ) ;
#2453=CIRCLE ( 'NONE', #15744, 120.5010000000000190 ) ;
#2454=FACE_OUTER_BOUND ( 'NONE', #22799, .T. ) ;
#2456=ORIENTED_EDGE ( 'NONE', *, *, #10369, .F. ) ;
#2457=AXIS2_PLACEMENT_3D ( 'NONE', #27437, #40709, #40935 ) ;
#2458=LINE ( 'NONE', #36273, #2724 ) ;
#2464=AXIS2_PLACEMENT_3D ( 'NONE', #28481, #11026, #17805 ) ;
#2473=ORIENTED_EDGE ( 'NONE', *, *, #35565, .F. ) ;
#2476=ADVANCED_FACE ( 'NONE', ( #33309 ), #6256, .F. ) ;
#2482=CARTESIAN_POINT ( 'NONE',  ( 17.99999999999999645, 58.30069736313667050, 100.2847380560568951 ) ) ;
#2483=AXIS2_PLACEMENT_3D ( 'NONE', #16919, #30201, #24108 ) ;
#2485=CIRCLE ( 'NONE', #31081, 59.00000000000000000 ) ;
#2490=DIRECTION ( 'NONE',  ( 0.000000000000000000, 0.000000000000000000, -1.000000000000000000 ) ) ;
#2496=LINE ( 'NONE', #9066, #24736 ) ;
#2497=AXIS2_PLACEMENT_3D ( 'NONE', #42016, #15457, #9517 ) ;
#2498=ORIENTED_EDGE ( 'NONE', *, *, #30840, .T. ) ;
#2500=ORIENTED_EDGE ( 'NONE', *, *, #39057, .T. ) ;
#2501=EDGE_CURVE ( 'NONE', #21981, #21881, #35917, .T. ) ;
#2502=DIRECTION ( 'NONE',  ( 0.000000000000000000, 0.7525707698561353576, 0.6585113790650422017 ) ) ;
#2503=ADVANCED_FACE ( 'NONE', ( #12612 ), #26556, .F. ) ;
#2506=ORIENTED_EDGE ( 'NONE', *, *, #36381, .T. ) ;
#2508=CARTESIAN_POINT ( 'NONE',  ( 17.99999999999999645, -100.6739960869714139, -49.52796165323368172 ) ) ;
#2509=CARTESIAN_POINT ( 'NONE',  ( 17.99999999999999645, -56.51398178981889941, 96.92493144647428949 ) ) ;
#2510=ORIENTED_EDGE ( 'NONE', *, *, #37505, .F. ) ;
#2512=DIRECTION ( 'NONE',  ( 0.000000000000000000, -0.7164567402983066380, -0.6976315211349933820 ) ) ;
#2513=AXIS2_PLACEMENT_3D ( 'NONE', #9564, #2763, #35520 ) ;
#2514=ADVANCED_FACE ( 'NONE', ( #36555 ), #40036, .F. ) ;
#2516=VECTOR ( 'NONE', #22247, 1000.000000000000000 ) ;
#2521=ORIENTED_EDGE ( 'NONE', *, *, #14490, .F. ) ;
#2526=DIRECTION ( 'NONE',  ( 0.000000000000000000, 0.000000000000000000, 1.000000000000000000 ) ) ;
#2528=CARTESIAN_POINT ( 'NONE',  ( 9.000000000000001776, 25.18647942089742031, 113.2326863338528824 ) ) ;
#2533=ORIENTED_EDGE ( 'NONE', *, *, #36863, .F. ) ;
#2535=DIRECTION ( 'NONE',  ( 0.000000000000000000, 0.8747630845319623871, -0.4845508703326481537 ) ) ;
#2536=FACE_OUTER_BOUND ( 'NONE', #7477, .T. ) ;
#2538=ADVANCED_FACE ( 'NONE', ( #9312 ), #16766, .F. ) ;
#2540=DIRECTION ( 'NONE',  ( 0.000000000000000000, -0.4132121857683668242, -0.9106347728549183396 ) ) ;
#2546=DIRECTION ( 'NONE',  ( 1.000000000000000000, 0.000000000000000000, 0.000000000000000000 ) ) ;
#2547=AXIS2_PLACEMENT_3D ( 'NONE', #18749, #8435, #1007 ) ;
#2548=ORIENTED_EDGE ( 'NONE', *, *, #27711, .F. ) ;
#2551=CARTESIAN_POINT ( 'NONE',  ( 17.99999999999999645, -76.48293397876204835, -82.08917884620389316 ) ) ;
#2554=CIRCLE ( 'NONE', #13041, 59.00000000000000711 ) ;
#2557=DIRECTION ( 'NONE',  ( 1.000000000000000000, 0.000000000000000000, 0.000000000000000000 ) ) ;
#2564=CARTESIAN_POINT ( 'NONE',  ( 17.99999999999999645, 83.58328028049660929, 80.43528614701352808 ) ) ;
#2566=CIRCLE ( 'NONE', #40187, 120.5010000000000332 ) ;
#2567=VERTEX_POINT ( 'NONE', #16107 ) ;
#2569=DIRECTION ( 'NONE',  ( 1.000000000000000000, 0.000000000000000000, 0.000000000000000000 ) ) ;
#2570=CIRCLE ( 'NONE', #24948, 116.0000000000000000 ) ;
#2578=CARTESIAN_POINT ( 'NONE',  ( 0.000000000000000000, -76.48293397876315680, 82.08917884620285577 ) ) ;
#2580=DIRECTION ( 'NONE',  ( 1.000000000000000000, 0.000000000000000000, 0.000000000000000000 ) ) ;
#2581=DIRECTION ( 'NONE',  ( -1.000000000000000000, -0.000000000000000000, 0.000000000000000000 ) ) ;
#2583=AXIS2_PLACEMENT_3D ( 'NONE', #14238, #27543, #34284 ) ;
#2587=EDGE_CURVE ( 'NONE', #27036, #40970, #5967, .T. ) ;
#2590=DIRECTION ( 'NONE',  ( 0.000000000000000000, 0.000000000000000000, 1.000000000000000000 ) ) ;
#2592=DIRECTION ( 'NONE',  ( -1.000000000000000000, -0.000000000000000000, -0.000000000000000000 ) ) ;
#2596=CARTESIAN_POINT ( 'NONE',  ( 9.000000000000001776, -52.88069566989523906, 103.2454939717367211 ) ) ;
#2598=DIRECTION ( 'NONE',  ( 1.000000000000000000, 0.000000000000000000, 0.000000000000000000 ) ) ;
#2602=DIRECTION ( 'NONE',  ( 0.000000000000000000, -0.3140767120219556952, 0.9493976084683790617 ) ) ;
#2603=DIRECTION ( 'NONE',  ( -1.000000000000000000, -0.000000000000000000, 0.000000000000000000 ) ) ;
#2605=ADVANCED_FACE ( 'NONE', ( #2536 ), #22894, .F. ) ;
#2606=ADVANCED_FACE ( 'NONE', ( #23946 ), #40475, .F. ) ;
#2607=CARTESIAN_POINT ( 'NONE',  ( -10.00000000000000000, 0.000000000000000000, 0.000000000000000000 ) ) ;
#2610=EDGE_CURVE ( 'NONE', #12969, #19737, #14345, .T. ) ;
#2618=CIRCLE ( 'NONE', #40972, 116.0000000000000000 ) ;
#2620=ORIENTED_EDGE ( 'NONE', *, *, #30859, .F. ) ;
#2622=VERTEX_POINT ( 'NONE', #24167 ) ;
#2623=VERTEX_POINT ( 'NONE', #36786 ) ;
#2624=DIRECTION ( 'NONE',  ( -1.000000000000000000, -0.000000000000000000, -0.000000000000000000 ) ) ;
#2625=EDGE_CURVE ( 'NONE', #39096, #26320, #10610, .T. ) ;
#2627=EDGE_LOOP ( 'NONE', ( #39846, #23283, #6339, #35435 ) ) ;
#2628=DIRECTION ( 'NONE',  ( 1.000000000000000000, 0.000000000000000000, 0.000000000000000000 ) ) ;
#2630=CARTESIAN_POINT ( 'NONE',  ( 0.000000000000000000, -114.8812324315176312, 16.07179003769107339 ) ) ;
#2635=VECTOR ( 'NONE', #15550, 1000.000000000000000 ) ;
#2639=FACE_OUTER_BOUND ( 'NONE', #15345, .T. ) ;
#2641=VERTEX_POINT ( 'NONE', #26992 ) ;
#2642=CIRCLE ( 'NONE', #36076, 58.99999999999999289 ) ;
#2646=DIRECTION ( 'NONE',  ( -1.000000000000000000, 0.000000000000000000, -0.000000000000000000 ) ) ;
#2647=FACE_OUTER_BOUND ( 'NONE', #897, .T. ) ;
#2648=VERTEX_POINT ( 'NONE', #30896 ) ;
#2656=CARTESIAN_POINT ( 'NONE',  ( 17.99999999999999645, -29.36437154452078246, 116.8684075565134890 ) ) ;
#2659=ORIENTED_EDGE ( 'NONE', *, *, #25976, .F. ) ;
#2662=DIRECTION ( 'NONE',  ( 0.000000000000000000, 0.000000000000000000, 1.000000000000000000 ) ) ;
#2663=CARTESIAN_POINT ( 'NONE',  ( -10.00000000000000000, 0.000000000000000000, 0.000000000000000000 ) ) ;
#2666=CARTESIAN_POINT ( 'NONE',  ( 0.000000000000000000, 98.39501399267960835, 53.91376164787712355 ) ) ;
#2667=VERTEX_POINT ( 'NONE', #557 ) ;
#2668=DIRECTION ( 'NONE',  ( -1.000000000000000000, 0.000000000000000000, 0.000000000000000000 ) ) ;
#2669=ORIENTED_EDGE ( 'NONE', *, *, #12932, .T. ) ;
#2670=LINE ( 'NONE', #6184, #2329 ) ;
#2672=ORIENTED_EDGE ( 'NONE', *, *, #42069, .T. ) ;
#2674=ORIENTED_EDGE ( 'NONE', *, *, #26231, .F. ) ;
#2675=EDGE_CURVE ( 'NONE', #39824, #23529, #13912, .T. ) ;
#2678=CARTESIAN_POINT ( 'NONE',  ( 17.99999999999999645, -94.83915810436441518, 59.94836581341558457 ) ) ;
#2679=ADVANCED_FACE ( 'NONE', ( #33725 ), #21125, .F. ) ;
#2682=ORIENTED_EDGE ( 'NONE', *, *, #23317, .T. ) ;
#2686=LINE ( 'NONE', #3338, #40792 ) ;
#2687=ORIENTED_EDGE ( 'NONE', *, *, #23226, .F. ) ;
#2688=DIRECTION ( 'NONE',  ( -1.000000000000000000, 0.000000000000000000, 0.000000000000000000 ) ) ;
#2691=EDGE_CURVE ( 'NONE', #14749, #35045, #34529, .T. ) ;
#2693=CARTESIAN_POINT ( 'NONE',  ( 17.99999999999999645, 0.000000000000000000, 0.000000000000000000 ) ) ;
#2696=CARTESIAN_POINT ( 'NONE',  ( 17.99999999999999645, 47.58001226230686598, -110.7096808509478763 ) ) ;
#2699=AXIS2_PLACEMENT_3D ( 'NONE', #10312, #23223, #3953 ) ;
#2702=CARTESIAN_POINT ( 'NONE',  ( 9.000000000000001776, 19.12429268481714217, 114.4126803693779948 ) ) ;
#2703=LINE ( 'NONE', #11940, #28336 ) ;
#2706=FACE_OUTER_BOUND ( 'NONE', #26574, .T. ) ;
#2708=ORIENTED_EDGE ( 'NONE', *, *, #33060, .F. ) ;
#2709=DIRECTION ( 'NONE',  ( -1.000000000000000000, 0.000000000000000000, 0.000000000000000000 ) ) ;
#2711=CARTESIAN_POINT ( 'NONE',  ( 17.99999999999999645, 8.827181066045881153, 120.1772519049559662 ) ) ;
#2712=DIRECTION ( 'NONE',  ( 0.000000000000000000, 0.000000000000000000, 1.000000000000000000 ) ) ;
#2715=DIRECTION ( 'NONE',  ( -1.000000000000000000, -0.000000000000000000, -0.000000000000000000 ) ) ;
#2717=EDGE_CURVE ( 'NONE', #34186, #20139, #30371, .T. ) ;
#2720=DIRECTION ( 'NONE',  ( -1.000000000000000000, -0.000000000000000000, -0.000000000000000000 ) ) ;
#2722=EDGE_CURVE ( 'NONE', #5323, #34842, #4473, .T. ) ;
#2724=VECTOR ( 'NONE', #15407, 1000.000000000000000 ) ;
#2725=CARTESIAN_POINT ( 'NONE',  ( 17.99999999999999645, -53.40478689619801145, 108.0204598100363711 ) ) ;
#2726=AXIS2_PLACEMENT_3D ( 'NONE', #36677, #33628, #26456 ) ;
#2727=EDGE_CURVE ( 'NONE', #2740, #5428, #13659, .T. ) ;
#2738=VERTEX_POINT ( 'NONE', #7551 ) ;
#2740=VERTEX_POINT ( 'NONE', #40265 ) ;
#2741=EDGE_CURVE ( 'NONE', #2623, #4572, #34158, .T. ) ;
#2742=DIRECTION ( 'NONE',  ( -1.000000000000000000, -0.000000000000000000, -0.000000000000000000 ) ) ;
#2745=EDGE_CURVE ( 'NONE', #39003, #32420, #28311, .T. ) ;
#2748=CARTESIAN_POINT ( 'NONE',  ( 17.99999999999999645, -11.65176648921111635, 115.4133282497342066 ) ) ;
#2750=CIRCLE ( 'NONE', #37594, 120.5010000000000190 ) ;
#2751=AXIS2_PLACEMENT_3D ( 'NONE', #7124, #33328, #26779 ) ;
#2752=EDGE_CURVE ( 'NONE', #13070, #7249, #7372, .T. ) ;
#2753=AXIS2_PLACEMENT_3D ( 'NONE', #15765, #39265, #32744 ) ;
#2754=DIRECTION ( 'NONE',  ( -1.000000000000000000, -0.000000000000000000, -0.000000000000000000 ) ) ;
#2760=DIRECTION ( 'NONE',  ( 0.000000000000000000, 0.000000000000000000, 1.000000000000000000 ) ) ;
#2763=DIRECTION ( 'NONE',  ( -1.000000000000000000, -0.000000000000000000, -0.000000000000000000 ) ) ;
#2765=DIRECTION ( 'NONE',  ( 0.000000000000000000, 0.000000000000000000, 1.000000000000000000 ) ) ;
#2771=DIRECTION ( 'NONE',  ( 0.000000000000000000, 0.000000000000000000, 1.000000000000000000 ) ) ;
#2775=EDGE_CURVE ( 'NONE', #32990, #28231, #10885, .T. ) ;
#2777=CYLINDRICAL_SURFACE ( 'NONE', #12164, 59.00000000000000000 ) ;
#2778=CIRCLE ( 'NONE', #1400, 59.00000000000000000 ) ;
#2779=ORIENTED_EDGE ( 'NONE', *, *, #6027, .T. ) ;
#2781=AXIS2_PLACEMENT_3D ( 'NONE', #13245, #6661, #20025 ) ;
#2789=ORIENTED_EDGE ( 'NONE', *, *, #10317, .T. ) ;
#2792=ADVANCED_FACE ( 'NONE', ( #41337 ), #21776, .F. ) ;
#2794=DIRECTION ( 'NONE',  ( -1.000000000000000000, -0.000000000000000000, -0.000000000000000000 ) ) ;
#2802=ORIENTED_EDGE ( 'NONE', *, *, #1862, .T. ) ;
#2805=VECTOR ( 'NONE', #22454, 1000.000000000000000 ) ;
#2806=AXIS2_PLACEMENT_3D ( 'NONE', #32221, #2097, #15460 ) ;
#2807=DIRECTION ( 'NONE',  ( 1.000000000000000000, 0.000000000000000000, -0.000000000000000000 ) ) ;
#2809=AXIS2_PLACEMENT_3D ( 'NONE', #26393, #39661, #36387 ) ;
#2810=AXIS2_PLACEMENT_3D ( 'NONE', #21371, #24630, #4285 ) ;
#2812=DIRECTION ( 'NONE',  ( 0.000000000000000000, 0.000000000000000000, 1.000000000000000000 ) ) ;
#2813=EDGE_CURVE ( 'NONE', #2738, #35175, #1861, .T. ) ;
#2814=VERTEX_POINT ( 'NONE', #28725 ) ;
#2818=VECTOR ( 'NONE', #36838, 1000.000000000000000 ) ;
#2820=EDGE_CURVE ( 'NONE', #40482, #23547, #8777, .T. ) ;
#2822=FACE_OUTER_BOUND ( 'NONE', #20800, .T. ) ;
#2826=ORIENTED_EDGE ( 'NONE', *, *, #8648, .T. ) ;
#2827=CARTESIAN_POINT ( 'NONE',  ( 17.99999999999999645, -104.2166695095716591, 60.49278301857773243 ) ) ;
#2829=VERTEX_POINT ( 'NONE', #22200 ) ;
#2832=AXIS2_PLACEMENT_3D ( 'NONE', #35023, #14555, #27862 ) ;
#2833=FACE_OUTER_BOUND ( 'NONE', #41844, .T. ) ;
#2840=EDGE_CURVE ( 'NONE', #38342, #12939, #35452, .T. ) ;
#2841=LINE ( 'NONE', #2210, #7110 ) ;
#2844=EDGE_CURVE ( 'NONE', #5301, #8980, #31341, .T. ) ;
#2845=CIRCLE ( 'NONE', #39, 59.00000000000000711 ) ;
#2851=EDGE_LOOP ( 'NONE', ( #32167, #18591, #2081, #11622 ) ) ;
#2853=DIRECTION ( 'NONE',  ( -1.000000000000000000, -0.000000000000000000, -0.000000000000000000 ) ) ;
#2855=DIRECTION ( 'NONE',  ( -1.000000000000000000, -0.000000000000000000, -0.000000000000000000 ) ) ;
#2858=ORIENTED_EDGE ( 'NONE', *, *, #35961, .F. ) ;
#2859=ORIENTED_EDGE ( 'NONE', *, *, #30376, .F. ) ;
#2860=CARTESIAN_POINT ( 'NONE',  ( 0.000000000000000000, 0.6819280456844267757, -115.9979955608738607 ) ) ;
#2861=DIRECTION ( 'NONE',  ( 0.000000000000000000, 0.000000000000000000, 1.000000000000000000 ) ) ;
#2862=CARTESIAN_POINT ( 'NONE',  ( 17.99999999999999645, 0.000000000000000000, 0.000000000000000000 ) ) ;
#2863=LINE ( 'NONE', #6584, #20262 ) ;
#2864=VERTEX_POINT ( 'NONE', #38298 ) ;
#2865=DIRECTION ( 'NONE',  ( 0.000000000000000000, -0.8183027759081743513, 0.5747874102143993857 ) ) ;
#2866=ORIENTED_EDGE ( 'NONE', *, *, #18599, .T. ) ;
#2869=CARTESIAN_POINT ( 'NONE',  ( 17.99999999999999645, 88.00363688980546328, 82.31555682352686176 ) ) ;
#2870=AXIS2_PLACEMENT_3D ( 'NONE', #12810, #19589, #42458 ) ;
#2873=DIRECTION ( 'NONE',  ( -1.000000000000000000, 0.000000000000000000, 0.000000000000000000 ) ) ;
#2874=ORIENTED_EDGE ( 'NONE', *, *, #39352, .F. ) ;
#2879=VERTEX_POINT ( 'NONE', #21569 ) ;
#2880=DIRECTION ( 'NONE',  ( 0.000000000000000000, 0.000000000000000000, 1.000000000000000000 ) ) ;
#2881=VERTEX_POINT ( 'NONE', #38082 ) ;
#2886=DIRECTION ( 'NONE',  ( 1.000000000000000000, 0.000000000000000000, 0.000000000000000000 ) ) ;
#2889=CARTESIAN_POINT ( 'NONE',  ( 0.000000000000000000, -59.07817985938929439, -105.0250430397515089 ) ) ;
#2892=EDGE_CURVE ( 'NONE', #42055, #36478, #33845, .T. ) ;
#2895=CYLINDRICAL_SURFACE ( 'NONE', #39069, 59.00000000000000000 ) ;
#2901=DIRECTION ( 'NONE',  ( 1.000000000000000000, 0.000000000000000000, 0.000000000000000000 ) ) ;
#2905=DIRECTION ( 'NONE',  ( 1.000000000000000000, 0.000000000000000000, 0.000000000000000000 ) ) ;
#2907=AXIS2_PLACEMENT_3D ( 'NONE', #14203, #27079, #6977 ) ;
#2910=CIRCLE ( 'NONE', #14123, 116.0000000000000000 ) ;
#2911=EDGE_CURVE ( 'NONE', #38131, #41436, #35861, .T. ) ;
#2913=CARTESIAN_POINT ( 'NONE',  ( 17.99999999999999645, 103.5682682299982673, 43.14958040911701431 ) ) ;
#2914=CYLINDRICAL_SURFACE ( 'NONE', #35975, 59.00000000000000000 ) ;
#2920=CARTESIAN_POINT ( 'NONE',  ( 0.000000000000000000, 2.418575551220858877, 120.4767259403369053 ) ) ;
#2922=CARTESIAN_POINT ( 'NONE',  ( 0.000000000000000000, 88.56657216608705596, -68.87840567545838155 ) ) ;
#2923=CARTESIAN_POINT ( 'NONE',  ( 17.99999999999999645, 106.6051926090976991, -45.73109345704713036 ) ) ;
#2929=CARTESIAN_POINT ( 'NONE',  ( 17.99999999999999645, 80.02407177073062883, -78.64108602299866391 ) ) ;
#2935=FACE_OUTER_BOUND ( 'NONE', #3580, .T. ) ;
#2938=ORIENTED_EDGE ( 'NONE', *, *, #3217, .F. ) ;
#2946=ORIENTED_EDGE ( 'NONE', *, *, #21666, .F. ) ;
#2947=DIRECTION ( 'NONE',  ( -1.000000000000000000, 0.000000000000000000, 0.000000000000000000 ) ) ;
#2948=VERTEX_POINT ( 'NONE', #19551 ) ;
#2949=CARTESIAN_POINT ( 'NONE',  ( 0.000000000000000000, 0.000000000000000000, 0.000000000000000000 ) ) ;
#2953=ORIENTED_EDGE ( 'NONE', *, *, #5829, .F. ) ;
#2955=DIRECTION ( 'NONE',  ( 0.000000000000000000, 0.000000000000000000, 1.000000000000000000 ) ) ;
#2958=EDGE_CURVE ( 'NONE', #27071, #39096, #22663, .T. ) ;
#2960=ORIENTED_EDGE ( 'NONE', *, *, #28767, .T. ) ;
#2966=VECTOR ( 'NONE', #36400, 1000.000000000000000 ) ;
#2972=CARTESIAN_POINT ( 'NONE',  ( 17.99999999999999645, 109.1131968883998695, -26.12628443611929896 ) ) ;
#2974=DIRECTION ( 'NONE',  ( -1.000000000000000000, 0.000000000000000000, 0.000000000000000000 ) ) ;
#2978=EDGE_CURVE ( 'NONE', #33352, #41276, #42416, .T. ) ;
#2980=VERTEX_POINT ( 'NONE', #29564 ) ;
#2981=CARTESIAN_POINT ( 'NONE',  ( 17.99999999999999645, 76.48293397876260258, 82.08917884620340999 ) ) ;
#2988=CARTESIAN_POINT ( 'NONE',  ( 0.000000000000000000, 112.1702510623870097, 2.471285140324554153 ) ) ;
#2989=VERTEX_POINT ( 'NONE', #12992 ) ;
#2990=DIRECTION ( 'NONE',  ( 1.000000000000000000, 0.000000000000000000, 0.000000000000000000 ) ) ;
#2992=CARTESIAN_POINT ( 'NONE',  ( 17.99999999999999645, 99.97660604680052643, -67.26937820704789317 ) ) ;
#2997=ADVANCED_FACE ( 'NONE', ( #12356 ), #22615, .F. ) ;
#2998=EDGE_LOOP ( 'NONE', ( #38993, #21878, #4452, #41577 ) ) ;
#3000=ORIENTED_EDGE ( 'NONE', *, *, #12133, .T. ) ;
#3003=CIRCLE ( 'NONE', #21217, 120.5010000000000332 ) ;
#3006=DIRECTION ( 'NONE',  ( 0.000000000000000000, -0.5528000653611835347, -0.8333139190825215037 ) ) ;
#3012=VECTOR ( 'NONE', #5209, 1000.000000000000000 ) ;
#3014=CARTESIAN_POINT ( 'NONE',  ( 0.000000000000000000, 10.40101730206365716, 120.0512800434971581 ) ) ;
#3015=DIRECTION ( 'NONE',  ( 0.000000000000000000, 0.000000000000000000, 1.000000000000000000 ) ) ;
#3022=CARTESIAN_POINT ( 'NONE',  ( 0.000000000000000000, 101.1249659627855806, -48.60055280209454054 ) ) ;
#3023=ORIENTED_EDGE ( 'NONE', *, *, #28442, .F. ) ;
#3025=DIRECTION ( 'NONE',  ( -1.000000000000000000, -0.000000000000000000, 0.000000000000000000 ) ) ;
#3030=EDGE_LOOP ( 'NONE', ( #39867, #18777, #540, #13187 ) ) ;
#3034=CARTESIAN_POINT ( 'NONE',  ( 17.99999999999999645, -99.97660604679919061, -67.26937820704989690 ) ) ;
#3036=ORIENTED_EDGE ( 'NONE', *, *, #35516, .T. ) ;
#3038=CIRCLE ( 'NONE', #25419, 120.5010000000000474 ) ;
#3040=DIRECTION ( 'NONE',  ( 1.000000000000000000, 0.000000000000000000, 0.000000000000000000 ) ) ;
#3041=ORIENTED_EDGE ( 'NONE', *, *, #5596, .F. ) ;
#3042=FACE_OUTER_BOUND ( 'NONE', #8836, .T. ) ;
#3043=EDGE_CURVE ( 'NONE', #3310, #14855, #29615, .T. ) ;
#3044=AXIS2_PLACEMENT_3D ( 'NONE', #14359, #1446, #11296 ) ;
#3048=FACE_OUTER_BOUND ( 'NONE', #2199, .T. ) ;
#3049=ORIENTED_EDGE ( 'NONE', *, *, #26660, .T. ) ;
#3054=AXIS2_PLACEMENT_3D ( 'NONE', #15330, #18184, #28618 ) ;
#3058=LINE ( 'NONE', #36899, #31194 ) ;
#3063=ORIENTED_EDGE ( 'NONE', *, *, #38288, .T. ) ;
#3064=VECTOR ( 'NONE', #10682, 1000.000000000000000 ) ;
#3065=ORIENTED_EDGE ( 'NONE', *, *, #22670, .T. ) ;
#3067=FACE_OUTER_BOUND ( 'NONE', #30229, .T. ) ;
#3070=CARTESIAN_POINT ( 'NONE',  ( 0.000000000000000000, -47.31079789947416003, -105.9135893174955783 ) ) ;
#3076=CARTESIAN_POINT ( 'NONE',  ( 8.999999999999998224, -42.87700105098536341, -107.7847984684009219 ) ) ;
#3077=FACE_OUTER_BOUND ( 'NONE', #3567, .T. ) ;
#3079=ORIENTED_EDGE ( 'NONE', *, *, #22378, .F. ) ;
#3080=EDGE_CURVE ( 'NONE', #18124, #23222, #10064, .T. ) ;
#3083=EDGE_CURVE ( 'NONE', #20671, #14903, #40427, .T. ) ;
#3086=ORIENTED_EDGE ( 'NONE', *, *, #5442, .T. ) ;
#3087=CARTESIAN_POINT ( 'NONE',  ( 17.99999999999999645, 72.00556975657703163, 86.04342158279412445 ) ) ;
#3092=CARTESIAN_POINT ( 'NONE',  ( 0.000000000000000000, -27.83061035787035564, 117.2431154827796576 ) ) ;
#3096=DIRECTION ( 'NONE',  ( 0.000000000000000000, -0.3140767120219362663, -0.9493976084683853900 ) ) ;
#3098=AXIS2_PLACEMENT_3D ( 'NONE', #18010, #26754, #1141 ) ;
#3099=EDGE_LOOP ( 'NONE', ( #10824, #21270, #1500, #32852 ) ) ;
#3101=VERTEX_POINT ( 'NONE', #509 ) ;
#3105=FACE_OUTER_BOUND ( 'NONE', #2067, .T. ) ;
#3106=CARTESIAN_POINT ( 'NONE',  ( 17.99999999999999645, 24.22031524825977300, 109.5520369638038289 ) ) ;
#3107=AXIS2_PLACEMENT_3D ( 'NONE', #7065, #60, #20214 ) ;
#3110=DIRECTION ( 'NONE',  ( 0.000000000000000000, 0.2631025642275218179, -0.9647678688145158166 ) ) ;
#3115=DIRECTION ( 'NONE',  ( -1.000000000000000000, -0.000000000000000000, -0.000000000000000000 ) ) ;
#3117=DIRECTION ( 'NONE',  ( 0.000000000000000000, 0.000000000000000000, 1.000000000000000000 ) ) ;
#3119=EDGE_LOOP ( 'NONE', ( #30945, #2669, #1670, #1288 ) ) ;
#3122=DIRECTION ( 'NONE',  ( -1.000000000000000000, 0.000000000000000000, 0.000000000000000000 ) ) ;
#3123=CARTESIAN_POINT ( 'NONE',  ( 17.99999999999999645, -0.5156212287287311735, 112.1962860721878172 ) ) ;
#3124=AXIS2_PLACEMENT_3D ( 'NONE', #7971, #20904, #31115 ) ;
#3128=AXIS2_PLACEMENT_3D ( 'NONE', #19236, #2598, #39464 ) ;
#3130=VECTOR ( 'NONE', #9319, 1000.000000000000000 ) ;
#3132=VERTEX_POINT ( 'NONE', #16925 ) ;
#3134=ORIENTED_EDGE ( 'NONE', *, *, #22481, .T. ) ;
#3135=CARTESIAN_POINT ( 'NONE',  ( 0.000000000000000000, 115.9750404417044081, 2.406240749597859718 ) ) ;
#3139=EDGE_CURVE ( 'NONE', #33598, #38342, #38650, .T. ) ;
#3140=ADVANCED_FACE ( 'NONE', ( #27588 ), #30208, .F. ) ;
#3143=FACE_OUTER_BOUND ( 'NONE', #34090, .T. ) ;
#3144=LINE ( 'NONE', #32642, #18684 ) ;
#3146=CIRCLE ( 'NONE', #7342, 59.00000000000000000 ) ;
#3147=DIRECTION ( 'NONE',  ( 0.000000000000000000, -0.9574220383620022368, -0.2886919473396314384 ) ) ;
#3148=CARTESIAN_POINT ( 'NONE',  ( 17.99999999999999645, 0.000000000000000000, 0.000000000000000000 ) ) ;
#3152=CARTESIAN_POINT ( 'NONE',  ( 17.99999999999999645, -58.30069736313598128, -100.2847380560572930 ) ) ;
#3158=CARTESIAN_POINT ( 'NONE',  ( 17.99999999999999645, 0.000000000000000000, 0.000000000000000000 ) ) ;
#3160=AXIS2_PLACEMENT_3D ( 'NONE', #23041, #39772, #5766 ) ;
#3165=DIRECTION ( 'NONE',  ( 1.000000000000000000, 0.000000000000000000, -0.000000000000000000 ) ) ;
#3167=ORIENTED_EDGE ( 'NONE', *, *, #18450, .F. ) ;
#3172=DIRECTION ( 'NONE',  ( 0.000000000000000000, 0.000000000000000000, 1.000000000000000000 ) ) ;
#3173=CIRCLE ( 'NONE', #11576, 58.99999999999999289 ) ;
#3174=ORIENTED_EDGE ( 'NONE', *, *, #31855, .T. ) ;
#3178=EDGE_LOOP ( 'NONE', ( #37082, #26865, #38253, #32350 ) ) ;
#3190=AXIS2_PLACEMENT_3D ( 'NONE', #42358, #6738, #5715 ) ;
#3194=DIRECTION ( 'NONE',  ( -1.000000000000000000, 0.000000000000000000, 0.000000000000000000 ) ) ;
#3195=AXIS2_PLACEMENT_3D ( 'NONE', #8025, #24433, #814 ) ;
#3203=VECTOR ( 'NONE', #36022, 1000.000000000000000 ) ;
#3204=FACE_OUTER_BOUND ( 'NONE', #38418, .T. ) ;
#3206=AXIS2_PLACEMENT_3D ( 'NONE', #34230, #836, #7398 ) ;
#3210=VECTOR ( 'NONE', #11095, 1000.000000000000000 ) ;
#3213=ORIENTED_EDGE ( 'NONE', *, *, #4490, .F. ) ;
#3216=DIRECTION ( 'NONE',  ( 0.000000000000000000, 9.408669700213191589E-16, -1.000000000000000000 ) ) ;
#3217=EDGE_CURVE ( 'NONE', #28773, #11934, #1018, .T. ) ;
#3219=CARTESIAN_POINT ( 'NONE',  ( 17.99999999999999645, 0.000000000000000000, 0.000000000000000000 ) ) ;
#3220=DIRECTION ( 'NONE',  ( 1.000000000000000000, 0.000000000000000000, -0.000000000000000000 ) ) ;
#3221=ORIENTED_EDGE ( 'NONE', *, *, #28772, .T. ) ;
#3222=CARTESIAN_POINT ( 'NONE',  ( 17.99999999999999645, 110.1579703617969130, -21.29539948940136540 ) ) ;
#3224=DIRECTION ( 'NONE',  ( 0.000000000000000000, -0.7525707698561440173, 0.6585113790650322096 ) ) ;
#3227=ORIENTED_EDGE ( 'NONE', *, *, #38286, .T. ) ;
#3228=CARTESIAN_POINT ( 'NONE',  ( 17.99999999999999645, 0.000000000000000000, 0.000000000000000000 ) ) ;
#3229=DIRECTION ( 'NONE',  ( 1.000000000000000000, 0.000000000000000000, 0.000000000000000000 ) ) ;
#3230=AXIS2_PLACEMENT_3D ( 'NONE', #28717, #38493, #11925 ) ;
#3235=AXIS2_PLACEMENT_3D ( 'NONE', #9171, #42099, #38840 ) ;
#3237=AXIS2_PLACEMENT_3D ( 'NONE', #37023, #7129, #30713 ) ;
#3243=CARTESIAN_POINT ( 'NONE',  ( 17.99999999999999645, -93.26762629039376407, -76.29967815892449323 ) ) ;
#3244=DIRECTION ( 'NONE',  ( 0.000000000000000000, 0.000000000000000000, -1.000000000000000000 ) ) ;
#3246=EDGE_CURVE ( 'NONE', #11411, #1814, #14507, .T. ) ;
#3250=DIRECTION ( 'NONE',  ( 0.000000000000000000, 0.000000000000000000, 1.000000000000000000 ) ) ;
#3252=ORIENTED_EDGE ( 'NONE', *, *, #35087, .F. ) ;
#3257=ORIENTED_EDGE ( 'NONE', *, *, #20791, .F. ) ;
#3258=AXIS2_PLACEMENT_3D ( 'NONE', #36683, #6809, #23424 ) ;
#3268=CARTESIAN_POINT ( 'NONE',  ( 17.99999999999999645, 75.03166794516924654, -94.29071961951432002 ) ) ;
#3269=VECTOR ( 'NONE', #19363, 1000.000000000000000 ) ;
#3273=ORIENTED_EDGE ( 'NONE', *, *, #40965, .F. ) ;
#3274=CARTESIAN_POINT ( 'NONE',  ( 0.000000000000000000, 0.000000000000000000, 0.000000000000000000 ) ) ;
#3277=DIRECTION ( 'NONE',  ( -1.000000000000000000, 0.000000000000000000, -0.000000000000000000 ) ) ;
#3282=EDGE_CURVE ( 'NONE', #28903, #844, #15676, .T. ) ;
#3285=EDGE_CURVE ( 'NONE', #41485, #38794, #40001, .T. ) ;
#3287=ORIENTED_EDGE ( 'NONE', *, *, #27542, .F. ) ;
#3290=AXIS2_PLACEMENT_3D ( 'NONE', #14630, #27488, #30761 ) ;
#3293=CIRCLE ( 'NONE', #10303, 59.00000000000000000 ) ;
#3297=DIRECTION ( 'NONE',  ( 0.000000000000000000, 0.000000000000000000, -1.000000000000000000 ) ) ;
#3298=CYLINDRICAL_SURFACE ( 'NONE', #19370, 59.00000000000000000 ) ;
#3301=DIRECTION ( 'NONE',  ( -1.000000000000000000, -0.000000000000000000, -0.000000000000000000 ) ) ;
#3302=CARTESIAN_POINT ( 'NONE',  ( 17.99999999999999645, 0.000000000000000000, 0.000000000000000000 ) ) ;
#3303=ORIENTED_EDGE ( 'NONE', *, *, #8562, .T. ) ;
#3306=CARTESIAN_POINT ( 'NONE',  ( -10.00000000000000000, 0.000000000000000000, 0.000000000000000000 ) ) ;
#3309=AXIS2_PLACEMENT_3D ( 'NONE', #11976, #18330, #18122 ) ;
#3310=VERTEX_POINT ( 'NONE', #2014 ) ;
#3311=DIRECTION ( 'NONE',  ( 0.000000000000000000, 0.000000000000000000, 1.000000000000000000 ) ) ;
#3312=DIRECTION ( 'NONE',  ( 0.000000000000000000, -0.9213119778704165208, 0.3888241754733123834 ) ) ;
#3313=ORIENTED_EDGE ( 'NONE', *, *, #25017, .T. ) ;
#3314=DIRECTION ( 'NONE',  ( 0.000000000000000000, 0.000000000000000000, 1.000000000000000000 ) ) ;
#3315=ORIENTED_EDGE ( 'NONE', *, *, #30009, .F. ) ;
#3320=VERTEX_POINT ( 'NONE', #1588 ) ;
#3325=AXIS2_PLACEMENT_3D ( 'NONE', #28846, #12269, #28437 ) ;
#3326=EDGE_CURVE ( 'NONE', #25336, #12545, #35405, .T. ) ;
#3327=AXIS2_PLACEMENT_3D ( 'NONE', #21633, #1929, #15290 ) ;
#3328=ORIENTED_EDGE ( 'NONE', *, *, #31058, .T. ) ;
#3332=AXIS2_PLACEMENT_3D ( 'NONE', #9001, #22142, #31927 ) ;
#3334=AXIS2_PLACEMENT_3D ( 'NONE', #3087, #22807, #26692 ) ;
#3335=CIRCLE ( 'NONE', #8230, 116.0000000000000000 ) ;
#3338=CARTESIAN_POINT ( 'NONE',  ( 8.999999999999998224, -94.52951811191512377, -67.23221107124996365 ) ) ;
#3343=DIRECTION ( 'NONE',  ( -1.000000000000000000, 0.000000000000000000, -0.000000000000000000 ) ) ;
#3348=DIRECTION ( 'NONE',  ( 1.000000000000000000, 0.000000000000000000, 0.000000000000000000 ) ) ;
#3350=ADVANCED_FACE ( 'NONE', ( #41290 ), #31067, .F. ) ;
#3351=EDGE_CURVE ( 'NONE', #13484, #36189, #21307, .T. ) ;
#3352=EDGE_CURVE ( 'NONE', #14329, #18075, #37967, .T. ) ;
#3355=DIRECTION ( 'NONE',  ( 0.000000000000000000, 0.8477344278896686847, 0.5304209081197459597 ) ) ;
#3356=DIRECTION ( 'NONE',  ( 0.000000000000000000, 0.8747630845319590565, 0.4845508703326540934 ) ) ;
#3357=AXIS2_PLACEMENT_3D ( 'NONE', #30775, #30570, #27732 ) ;
#3362=DIRECTION ( 'NONE',  ( -1.000000000000000000, 0.000000000000000000, 0.000000000000000000 ) ) ;
#3365=CARTESIAN_POINT ( 'NONE',  ( 17.99999999999999645, 97.97378550988226209, 62.10585602713792497 ) ) ;
#3370=CARTESIAN_POINT ( 'NONE',  ( 0.000000000000000000, -115.6826031496112677, 8.575274253897077870 ) ) ;
#3371=EDGE_CURVE ( 'NONE', #10707, #17317, #8013, .T. ) ;
#3381=CARTESIAN_POINT ( 'NONE',  ( 17.99999999999999645, -108.8684555192048435, 27.12806418649580564 ) ) ;
#3382=DIRECTION ( 'NONE',  ( -1.000000000000000000, -0.000000000000000000, -0.000000000000000000 ) ) ;
#3384=CARTESIAN_POINT ( 'NONE',  ( 17.99999999999999645, 40.13512380273970592, 113.6206972269522737 ) ) ;
#3385=AXIS2_PLACEMENT_3D ( 'NONE', #3579, #83, #747 ) ;
#3387=CYLINDRICAL_SURFACE ( 'NONE', #34669, 59.00000000000000000 ) ;
#3392=ORIENTED_EDGE ( 'NONE', *, *, #27091, .T. ) ;
#3396=EDGE_CURVE ( 'NONE', #12907, #10944, #26834, .T. ) ;
#3398=ORIENTED_EDGE ( 'NONE', *, *, #21737, .F. ) ;
#3400=EDGE_CURVE ( 'NONE', #18706, #36637, #1154, .T. ) ;
#3401=EDGE_CURVE ( 'NONE', #8016, #22923, #4651, .T. ) ;
#3402=DIRECTION ( 'NONE',  ( -1.000000000000000000, -0.000000000000000000, -0.000000000000000000 ) ) ;
#3403=VERTEX_POINT ( 'NONE', #29731 ) ;
#3405=ORIENTED_EDGE ( 'NONE', *, *, #38798, .T. ) ;
#3412=ORIENTED_EDGE ( 'NONE', *, *, #5313, .F. ) ;
#3414=ADVANCED_FACE ( 'NONE', ( #32975 ), #15577, .F. ) ;
#3415=CARTESIAN_POINT ( 'NONE',  ( 17.99999999999999645, 0.000000000000000000, 0.000000000000000000 ) ) ;
#3417=AXIS2_PLACEMENT_3D ( 'NONE', #7248, #39965, #30186 ) ;
#3421=CARTESIAN_POINT ( 'NONE',  ( 0.000000000000000000, 0.000000000000000000, 0.000000000000000000 ) ) ;
#3427=ORIENTED_EDGE ( 'NONE', *, *, #31055, .T. ) ;
#3429=FACE_OUTER_BOUND ( 'NONE', #4282, .T. ) ;
#3431=EDGE_CURVE ( 'NONE', #9950, #42699, #11557, .T. ) ;
#3432=ORIENTED_EDGE ( 'NONE', *, *, #42431, .T. ) ;
#3436=DIRECTION ( 'NONE',  ( -1.000000000000000000, -0.000000000000000000, 0.000000000000000000 ) ) ;
#3438=DIRECTION ( 'NONE',  ( 0.000000000000000000, -0.1062934856473523731, -0.9943348002101385363 ) ) ;
#3439=DIRECTION ( 'NONE',  ( -1.000000000000000000, -0.000000000000000000, -0.000000000000000000 ) ) ;
#3442=ORIENTED_EDGE ( 'NONE', *, *, #42111, .F. ) ;
#3445=DIRECTION ( 'NONE',  ( 0.000000000000000000, 0.000000000000000000, 1.000000000000000000 ) ) ;
#3448=CYLINDRICAL_SURFACE ( 'NONE', #35268, 120.5010000000000190 ) ;
#3452=CARTESIAN_POINT ( 'NONE',  ( 17.99999999999999645, 109.1131968883995000, 26.12628443612074847 ) ) ;
#3460=DIRECTION ( 'NONE',  ( -1.000000000000000000, -0.000000000000000000, -0.000000000000000000 ) ) ;
#3461=EDGE_CURVE ( 'NONE', #12095, #30629, #19918, .T. ) ;
#3462=FACE_OUTER_BOUND ( 'NONE', #12214, .T. ) ;
#3463=VERTEX_POINT ( 'NONE', #12514 ) ;
#3464=PLANE ( 'NONE',  #37863 ) ;
#3465=CARTESIAN_POINT ( 'NONE',  ( 17.99999999999999645, 116.4607004671432406, -30.94182036827089632 ) ) ;
#3468=DIRECTION ( 'NONE',  ( 1.000000000000000000, 0.000000000000000000, 0.000000000000000000 ) ) ;
#3471=AXIS2_PLACEMENT_3D ( 'NONE', #7304, #20895, #16746 ) ;
#3472=VERTEX_POINT ( 'NONE', #25827 ) ;
#3473=DIRECTION ( 'NONE',  ( 0.000000000000000000, 0.5963673585384969833, 0.8027116379309670036 ) ) ;
#3476=EDGE_LOOP ( 'NONE', ( #18282, #15572, #12571, #5791 ) ) ;
#3479=VERTEX_POINT ( 'NONE', #42142 ) ;
#3482=ORIENTED_EDGE ( 'NONE', *, *, #2076, .F. ) ;
#3483=CARTESIAN_POINT ( 'NONE',  ( 17.99999999999999645, 0.000000000000000000, 0.000000000000000000 ) ) ;
#3484=DIRECTION ( 'NONE',  ( -1.000000000000000000, -0.000000000000000000, -0.000000000000000000 ) ) ;
#3485=CARTESIAN_POINT ( 'NONE',  ( 0.000000000000000000, 0.000000000000000000, 0.000000000000000000 ) ) ;
#3494=DIRECTION ( 'NONE',  ( 0.000000000000000000, 0.000000000000000000, 1.000000000000000000 ) ) ;
#3499=ORIENTED_EDGE ( 'NONE', *, *, #35905, .F. ) ;
#3501=CIRCLE ( 'NONE', #32125, 120.5010000000000332 ) ;
#3503=VERTEX_POINT ( 'NONE', #43002 ) ;
#3508=EDGE_CURVE ( 'NONE', #41968, #27228, #31730, .T. ) ;
#3511=ADVANCED_FACE ( 'NONE', ( #29302 ), #12300, .F. ) ;
#3512=DIRECTION ( 'NONE',  ( 0.000000000000000000, 1.246648735278247733E-14, -1.000000000000000000 ) ) ;
#3513=CARTESIAN_POINT ( 'NONE',  ( -10.00000000000000000, 0.000000000000000000, 0.000000000000000000 ) ) ;
#3514=VERTEX_POINT ( 'NONE', #32341 ) ;
#3515=DIRECTION ( 'NONE',  ( 0.000000000000000000, -0.5076658003388467844, 0.8615540813938020737 ) ) ;
#3519=ORIENTED_EDGE ( 'NONE', *, *, #40732, .F. ) ;
#3520=DIRECTION ( 'NONE',  ( -1.000000000000000000, 0.000000000000000000, -0.000000000000000000 ) ) ;
#3521=CARTESIAN_POINT ( 'NONE',  ( 17.99999999999999645, 88.00363688980654331, -82.31555682352568226 ) ) ;
#3523=CARTESIAN_POINT ( 'NONE',  ( 17.99999999999999645, -79.94368240339484544, 90.16373242487880191 ) ) ;
#3524=ORIENTED_EDGE ( 'NONE', *, *, #40908, .T. ) ;
#3527=CIRCLE ( 'NONE', #27271, 58.99999999999999289 ) ;
#3528=EDGE_CURVE ( 'NONE', #18244, #43150, #35203, .T. ) ;
#3531=ORIENTED_EDGE ( 'NONE', *, *, #22081, .F. ) ;
#3532=AXIS2_PLACEMENT_3D ( 'NONE', #27090, #40357, #10491 ) ;
#3535=ADVANCED_FACE ( 'NONE', ( #23202 ), #16004, .F. ) ;
#3542=AXIS2_PLACEMENT_3D ( 'NONE', #18125, #30739, #31176 ) ;
#3544=CARTESIAN_POINT ( 'NONE',  ( 17.99999999999999645, -47.31079789947416003, -105.9135893174955783 ) ) ;
#3545=DIRECTION ( 'NONE',  ( 0.000000000000000000, 0.000000000000000000, 1.000000000000000000 ) ) ;
#3547=CARTESIAN_POINT ( 'NONE',  ( 0.000000000000000000, -111.9370513079666409, -44.61600100275288838 ) ) ;
#3554=ORIENTED_EDGE ( 'NONE', *, *, #18854, .F. ) ;
#3557=ADVANCED_FACE ( 'NONE', ( #12935 ), #23412, .F. ) ;
#3558=AXIS2_PLACEMENT_3D ( 'NONE', #32123, #22550, #15774 ) ;
#3561=CARTESIAN_POINT ( 'NONE',  ( 17.99999999999999645, -112.5220807139885864, 28.19186676675805003 ) ) ;
#3565=AXIS2_PLACEMENT_3D ( 'NONE', #39691, #35796, #3473 ) ;
#3567=EDGE_LOOP ( 'NONE', ( #27316, #14935, #34912, #26420 ) ) ;
#3568=LINE ( 'NONE', #36746, #7466 ) ;
#3570=CIRCLE ( 'NONE', #11279, 59.00000000000000000 ) ;
#3571=DIRECTION ( 'NONE',  ( 0.000000000000000000, 0.000000000000000000, 1.000000000000000000 ) ) ;
#3574=VERTEX_POINT ( 'NONE', #6567 ) ;
#3576=CARTESIAN_POINT ( 'NONE',  ( 17.99999999999999645, 0.000000000000000000, 0.000000000000000000 ) ) ;
#3579=CARTESIAN_POINT ( 'NONE',  ( 17.99999999999999645, -18.35539002514457252, 110.6858262410709273 ) ) ;
#3580=EDGE_LOOP ( 'NONE', ( #33920, #37527, #3531, #22237 ) ) ;
#3584=EDGE_CURVE ( 'NONE', #5508, #13710, #31041, .T. ) ;
#3585=CARTESIAN_POINT ( 'NONE',  ( 17.99999999999999645, 114.1529630473454944, -38.59523323561318620 ) ) ;
#3586=ORIENTED_EDGE ( 'NONE', *, *, #35904, .T. ) ;
#3588=DIRECTION ( 'NONE',  ( 1.000000000000000000, 0.000000000000000000, 0.000000000000000000 ) ) ;
#3589=AXIS2_PLACEMENT_3D ( 'NONE', #435, #9839, #13802 ) ;
#3590=DIRECTION ( 'NONE',  ( 0.000000000000000000, 0.000000000000000000, 1.000000000000000000 ) ) ;
#3592=AXIS2_PLACEMENT_3D ( 'NONE', #19386, #42240, #13252 ) ;
#3593=LINE ( 'NONE', #23936, #4743 ) ;
#3596=ORIENTED_EDGE ( 'NONE', *, *, #1485, .T. ) ;
#3597=DIRECTION ( 'NONE',  ( 1.000000000000000000, 0.000000000000000000, 0.000000000000000000 ) ) ;
#3598=EDGE_CURVE ( 'NONE', #21981, #214, #36591, .T. ) ;
#3603=CARTESIAN_POINT ( 'NONE',  ( 17.99999999999999645, 120.3696465864706937, -5.624871700594833435 ) ) ;
#3605=DIRECTION ( 'NONE',  ( -1.000000000000000000, -0.000000000000000000, 0.000000000000000000 ) ) ;
#3606=ORIENTED_EDGE ( 'NONE', *, *, #27487, .F. ) ;
#3612=VERTEX_POINT ( 'NONE', #34069 ) ;
#3614=CYLINDRICAL_SURFACE ( 'NONE', #1093, 116.0000000000000000 ) ;
#3618=AXIS2_PLACEMENT_3D ( 'NONE', #39453, #7601, #34008 ) ;
#3619=ORIENTED_EDGE ( 'NONE', *, *, #41115, .T. ) ;
#3624=CIRCLE ( 'NONE', #4352, 59.00000000000000000 ) ;
#3625=DIRECTION ( 'NONE',  ( 1.000000000000000000, 0.000000000000000000, 0.000000000000000000 ) ) ;
#3626=ORIENTED_EDGE ( 'NONE', *, *, #4639, .T. ) ;
#3633=EDGE_LOOP ( 'NONE', ( #11787, #36386, #10623, #35076 ) ) ;
#3636=EDGE_CURVE ( 'NONE', #19286, #12767, #12859, .T. ) ;
#3637=CYLINDRICAL_SURFACE ( 'NONE', #16929, 120.5010000000000190 ) ;
#3640=ORIENTED_EDGE ( 'NONE', *, *, #37174, .T. ) ;
#3641=CARTESIAN_POINT ( 'NONE',  ( 0.000000000000000000, 0.000000000000000000, 0.000000000000000000 ) ) ;
#3643=CARTESIAN_POINT ( 'NONE',  ( 17.99999999999999645, -97.97378550988267421, 62.10585602713726416 ) ) ;
#3644=ORIENTED_EDGE ( 'NONE', *, *, #36823, .F. ) ;
#3650=ORIENTED_EDGE ( 'NONE', *, *, #18105, .F. ) ;
#3652=DIRECTION ( 'NONE',  ( 0.000000000000000000, 0.000000000000000000, 1.000000000000000000 ) ) ;
#3654=AXIS2_PLACEMENT_3D ( 'NONE', #39401, #32032, #2114 ) ;
#3658=DIRECTION ( 'NONE',  ( 1.000000000000000000, 0.000000000000000000, 0.000000000000000000 ) ) ;
#3659=CARTESIAN_POINT ( 'NONE',  ( 0.000000000000000000, -80.02407177073008882, 78.64108602299921813 ) ) ;
#3660=LINE ( 'NONE', #825, #35094 ) ;
#3667=ORIENTED_EDGE ( 'NONE', *, *, #19953, .T. ) ;
#3670=CIRCLE ( 'NONE', #28125, 59.00000000000000000 ) ;
#3675=VERTEX_POINT ( 'NONE', #10293 ) ;
#3676=DIRECTION ( 'NONE',  ( -1.000000000000000000, -0.000000000000000000, 0.000000000000000000 ) ) ;
#3677=CARTESIAN_POINT ( 'NONE',  ( 0.000000000000000000, -103.4151313792875158, 61.85306461934376188 ) ) ;
#3681=DIRECTION ( 'NONE',  ( -1.000000000000000000, 0.000000000000000000, 0.000000000000000000 ) ) ;
#3688=ORIENTED_EDGE ( 'NONE', *, *, #27487, .T. ) ;
#3689=CYLINDRICAL_SURFACE ( 'NONE', #1465, 59.00000000000000000 ) ;
#3693=EDGE_LOOP ( 'NONE', ( #17942, #8577, #41892, #26605 ) ) ;
#3695=DIRECTION ( 'NONE',  ( -1.000000000000000000, 0.000000000000000000, -0.000000000000000000 ) ) ;
#3697=AXIS2_PLACEMENT_3D ( 'NONE', #1156, #7929, #18444 ) ;
#3698=CYLINDRICAL_SURFACE ( 'NONE', #23904, 116.0000000000000000 ) ;
#3699=DIRECTION ( 'NONE',  ( -1.000000000000000000, 0.000000000000000000, -0.000000000000000000 ) ) ;
#3700=AXIS2_PLACEMENT_3D ( 'NONE', #34480, #7214, #42833 ) ;
#3701=DIRECTION ( 'NONE',  ( -1.000000000000000000, -0.000000000000000000, -0.000000000000000000 ) ) ;
#3704=AXIS2_PLACEMENT_3D ( 'NONE', #7177, #624, #20769 ) ;
#3709=VERTEX_POINT ( 'NONE', #33203 ) ;
#3713=CIRCLE ( 'NONE', #34390, 116.0000000000000000 ) ;
#3714=ORIENTED_EDGE ( 'NONE', *, *, #35671, .F. ) ;
#3716=DIRECTION ( 'NONE',  ( 0.000000000000000000, 0.000000000000000000, 1.000000000000000000 ) ) ;
#3723=AXIS2_PLACEMENT_3D ( 'NONE', #1819, #5096, #41523 ) ;
#3724=ORIENTED_EDGE ( 'NONE', *, *, #20212, .F. ) ;
#3725=CARTESIAN_POINT ( 'NONE',  ( 17.99999999999999645, -91.51415974874549875, -64.91094698989387268 ) ) ;
#3726=VECTOR ( 'NONE', #40532, 1000.000000000000000 ) ;
#3729=VERTEX_POINT ( 'NONE', #37758 ) ;
#3731=ORIENTED_EDGE ( 'NONE', *, *, #16995, .F. ) ;
#3735=CARTESIAN_POINT ( 'NONE',  ( 0.000000000000000000, -25.18647942089668490, -113.2326863338530245 ) ) ;
#3738=ORIENTED_EDGE ( 'NONE', *, *, #11922, .F. ) ;
#3744=DIRECTION ( 'NONE',  ( 0.000000000000000000, 0.5528000653611888637, 0.8333139190825179510 ) ) ;
#3746=CIRCLE ( 'NONE', #3054, 120.5010000000000190 ) ;
#3748=EDGE_CURVE ( 'NONE', #10857, #40564, #22792, .T. ) ;
#3752=VERTEX_POINT ( 'NONE', #14455 ) ;
#3753=DIRECTION ( 'NONE',  ( 1.000000000000000000, 0.000000000000000000, 0.000000000000000000 ) ) ;
#3759=DIRECTION ( 'NONE',  ( 1.000000000000000000, 0.000000000000000000, 0.000000000000000000 ) ) ;
#3771=EDGE_CURVE ( 'NONE', #32964, #16728, #10031, .T. ) ;
#3775=VERTEX_POINT ( 'NONE', #31011 ) ;
#3777=CARTESIAN_POINT ( 'NONE',  ( 0.000000000000000000, 0.000000000000000000, 0.000000000000000000 ) ) ;
#3781=VERTEX_POINT ( 'NONE', #4827 ) ;
#3785=CARTESIAN_POINT ( 'NONE',  ( 17.99999999999999645, 16.77566611177777034, 119.3275660838943111 ) ) ;
#3786=DIRECTION ( 'NONE',  ( 0.000000000000000000, 0.000000000000000000, 1.000000000000000000 ) ) ;
#3792=LINE ( 'NONE', #40248, #19571 ) ;
#3795=DIRECTION ( 'NONE',  ( 0.000000000000000000, 0.000000000000000000, 1.000000000000000000 ) ) ;
#3797=VECTOR ( 'NONE', #9925, 1000.000000000000000 ) ;
#3799=DIRECTION ( 'NONE',  ( 0.000000000000000000, -0.1062934856473723155, 0.9943348002101364269 ) ) ;
#3800=DIRECTION ( 'NONE',  ( 0.000000000000000000, -0.8993121301712230231, 0.4373073204588476259 ) ) ;
#3804=EDGE_CURVE ( 'NONE', #22071, #8700, #17221, .T. ) ;
#3806=ORIENTED_EDGE ( 'NONE', *, *, #32676, .F. ) ;
#3810=CARTESIAN_POINT ( 'NONE',  ( -10.00000000000000000, 0.000000000000000000, 0.000000000000000000 ) ) ;
#3811=DIRECTION ( 'NONE',  ( 0.000000000000000000, 0.5076658003388409002, -0.8615540813938055154 ) ) ;
#3813=CARTESIAN_POINT ( 'NONE',  ( 0.000000000000000000, 100.8494052988171035, 65.95368414178945216 ) ) ;
#3814=EDGE_LOOP ( 'NONE', ( #38003, #26831, #17447, #26161 ) ) ;
#3822=VERTEX_POINT ( 'NONE', #41241 ) ;
#3825=DIRECTION ( 'NONE',  ( -1.000000000000000000, -0.000000000000000000, -0.000000000000000000 ) ) ;
#3827=AXIS2_PLACEMENT_3D ( 'NONE', #23482, #10794, #30219 ) ;
#3829=DIRECTION ( 'NONE',  ( -1.000000000000000000, 0.000000000000000000, 0.000000000000000000 ) ) ;
#3831=VERTEX_POINT ( 'NONE', #34485 ) ;
#3832=DIRECTION ( 'NONE',  ( 1.000000000000000000, 0.000000000000000000, 0.000000000000000000 ) ) ;
#3833=ORIENTED_EDGE ( 'NONE', *, *, #15165, .F. ) ;
#3837=EDGE_LOOP ( 'NONE', ( #42775, #25495, #18855, #27797 ) ) ;
#3842=DIRECTION ( 'NONE',  ( -1.000000000000000000, -0.000000000000000000, -0.000000000000000000 ) ) ;
#3845=CYLINDRICAL_SURFACE ( 'NONE', #27375, 120.5010000000000190 ) ;
#3846=CIRCLE ( 'NONE', #28303, 116.0000000000000000 ) ;
#3848=AXIS2_PLACEMENT_3D ( 'NONE', #15262, #21383, #38755 ) ;
#3849=AXIS2_PLACEMENT_3D ( 'NONE', #21216, #34050, #11368 ) ;
#3852=CARTESIAN_POINT ( 'NONE',  ( 0.000000000000000000, 0.000000000000000000, 0.000000000000000000 ) ) ;
#3854=LINE ( 'NONE', #807, #30305 ) ;
#3860=VECTOR ( 'NONE', #37212, 1000.000000000000000 ) ;
#3861=ADVANCED_FACE ( 'NONE', ( #41890 ), #4369, .F. ) ;
#3868=DIRECTION ( 'NONE',  ( -1.000000000000000000, -0.000000000000000000, -0.000000000000000000 ) ) ;
#3870=LINE ( 'NONE', #27257, #37770 ) ;
#3873=CARTESIAN_POINT ( 'NONE',  ( 17.99999999999999645, 101.8011932243955613, -55.61040422519224791 ) ) ;
#3878=EDGE_CURVE ( 'NONE', #5006, #2034, #28269, .T. ) ;
#3880=AXIS2_PLACEMENT_3D ( 'NONE', #20307, #16821, #26821 ) ;
#3883=EDGE_CURVE ( 'NONE', #42828, #25049, #22701, .T. ) ;
#3885=AXIS2_PLACEMENT_3D ( 'NONE', #27697, #21171, #18334 ) ;
#3889=DIRECTION ( 'NONE',  ( 1.000000000000000000, 0.000000000000000000, 0.000000000000000000 ) ) ;
#3891=CIRCLE ( 'NONE', #23451, 116.0000000000000000 ) ;
#3892=ORIENTED_EDGE ( 'NONE', *, *, #4926, .T. ) ;
#3895=ORIENTED_EDGE ( 'NONE', *, *, #22492, .F. ) ;
#3897=CARTESIAN_POINT ( 'NONE',  ( 17.99999999999999645, 80.02407177073062883, -78.64108602299866391 ) ) ;
#3900=DIRECTION ( 'NONE',  ( 0.000000000000000000, -0.9714298932647074114, -0.2373266998711251186 ) ) ;
#3902=CIRCLE ( 'NONE', #40852, 116.0000000000000000 ) ;
#3903=ORIENTED_EDGE ( 'NONE', *, *, #27957, .T. ) ;
#3905=ORIENTED_EDGE ( 'NONE', *, *, #18105, .T. ) ;
#3908=ORIENTED_EDGE ( 'NONE', *, *, #42184, .T. ) ;
#3909=CARTESIAN_POINT ( 'NONE',  ( 0.000000000000000000, 114.8812324315177023, -16.07179003769037351 ) ) ;
#3912=EDGE_CURVE ( 'NONE', #15607, #40494, #30331, .T. ) ;
#3913=AXIS2_PLACEMENT_3D ( 'NONE', #4064, #26789, #17438 ) ;
#3914=CARTESIAN_POINT ( 'NONE',  ( 0.000000000000000000, 112.5120133921113563, -43.14554256760899875 ) ) ;
#3918=CARTESIAN_POINT ( 'NONE',  ( 17.99999999999999645, -57.69704296431110890, -105.7900857083235451 ) ) ;
#3922=AXIS2_PLACEMENT_3D ( 'NONE', #39300, #32351, #3297 ) ;
#3923=DIRECTION ( 'NONE',  ( 1.000000000000000000, 0.000000000000000000, 0.000000000000000000 ) ) ;
#3924=CARTESIAN_POINT ( 'NONE',  ( 17.99999999999999645, 76.48293397876373945, -82.08917884620232996 ) ) ;
#3925=CARTESIAN_POINT ( 'NONE',  ( 0.000000000000000000, -83.58328028049713510, 80.43528614701295965 ) ) ;
#3926=ORIENTED_EDGE ( 'NONE', *, *, #4610, .T. ) ;
#3931=ORIENTED_EDGE ( 'NONE', *, *, #1573, .T. ) ;
#3937=ADVANCED_FACE ( 'NONE', ( #39240 ), #15738, .F. ) ;
#3941=EDGE_CURVE ( 'NONE', #40301, #39732, #29654, .T. ) ;
#3943=FACE_OUTER_BOUND ( 'NONE', #12053, .T. ) ;
#3953=DIRECTION ( 'NONE',  ( 0.000000000000000000, 0.000000000000000000, 1.000000000000000000 ) ) ;
#3955=VECTOR ( 'NONE', #11182, 1000.000000000000000 ) ;
#3956=AXIS2_PLACEMENT_3D ( 'NONE', #23497, #43088, #13236 ) ;
#3957=EDGE_CURVE ( 'NONE', #5769, #31074, #10841, .T. ) ;
#3958=ORIENTED_EDGE ( 'NONE', *, *, #18939, .F. ) ;
#3959=AXIS2_PLACEMENT_3D ( 'NONE', #38952, #39592, #35881 ) ;
#3963=DIRECTION ( 'NONE',  ( 0.000000000000000000, 0.000000000000000000, 1.000000000000000000 ) ) ;
#3964=ORIENTED_EDGE ( 'NONE', *, *, #7020, .F. ) ;
#3965=CYLINDRICAL_SURFACE ( 'NONE', #21904, 59.00000000000000000 ) ;
#3969=ORIENTED_EDGE ( 'NONE', *, *, #30636, .T. ) ;
#3972=EDGE_LOOP ( 'NONE', ( #9165, #35992, #22533, #36015 ) ) ;
#3975=ORIENTED_EDGE ( 'NONE', *, *, #6023, .F. ) ;
#3977=ORIENTED_EDGE ( 'NONE', *, *, #27373, .T. ) ;
#3979=CIRCLE ( 'NONE', #39514, 58.99999999999998579 ) ;
#3980=DIRECTION ( 'NONE',  ( -1.000000000000000000, 0.000000000000000000, 0.000000000000000000 ) ) ;
#3985=AXIS2_PLACEMENT_3D ( 'NONE', #17943, #852, #27504 ) ;
#3987=VECTOR ( 'NONE', #18870, 1000.000000000000000 ) ;
#3991=CIRCLE ( 'NONE', #24238, 59.00000000000001421 ) ;
#3997=VERTEX_POINT ( 'NONE', #5882 ) ;
#3999=EDGE_LOOP ( 'NONE', ( #8976, #38022, #35165, #3667 ) ) ;
#4004=EDGE_CURVE ( 'NONE', #34488, #6470, #19924, .T. ) ;
#4006=DIRECTION ( 'NONE',  ( 1.000000000000000000, 0.000000000000000000, 0.000000000000000000 ) ) ;
#4007=VERTEX_POINT ( 'NONE', #25359 ) ;
#4008=LINE ( 'NONE', #10801, #42275 ) ;
#4013=DIRECTION ( 'NONE',  ( -1.000000000000000000, 0.000000000000000000, -0.000000000000000000 ) ) ;
#4014=ORIENTED_EDGE ( 'NONE', *, *, #12743, .T. ) ;
#4015=ORIENTED_EDGE ( 'NONE', *, *, #18657, .F. ) ;
#4018=VECTOR ( 'NONE', #25260, 1000.000000000000000 ) ;
#4026=ORIENTED_EDGE ( 'NONE', *, *, #41534, .T. ) ;
#4028=ADVANCED_FACE ( 'NONE', ( #5675 ), #19032, .F. ) ;
#4029=CARTESIAN_POINT ( 'NONE',  ( 0.000000000000000000, -76.48293397876204835, -82.08917884620389316 ) ) ;
#4035=DIRECTION ( 'NONE',  ( -1.000000000000000000, 0.000000000000000000, 0.000000000000000000 ) ) ;
#4038=CARTESIAN_POINT ( 'NONE',  ( 8.999999999999998224, -95.31344542257689056, -66.11616384574544725 ) ) ;
#4040=CIRCLE ( 'NONE', #28492, 116.0000000000000000 ) ;
#4042=CIRCLE ( 'NONE', #28493, 120.5010000000000332 ) ;
#4045=EDGE_CURVE ( 'NONE', #8548, #33465, #32441, .T. ) ;
#4051=CARTESIAN_POINT ( 'NONE',  ( 0.000000000000000000, 0.000000000000000000, 0.000000000000000000 ) ) ;
#4052=DIRECTION ( 'NONE',  ( 0.000000000000000000, 0.000000000000000000, 1.000000000000000000 ) ) ;
#4055=AXIS2_PLACEMENT_3D ( 'NONE', #23203, #10512, #6363 ) ;
#4062=EDGE_CURVE ( 'NONE', #36925, #33209, #31771, .T. ) ;
#4064=CARTESIAN_POINT ( 'NONE',  ( 17.99999999999999645, 0.000000000000000000, 0.000000000000000000 ) ) ;
#4066=EDGE_CURVE ( 'NONE', #3320, #2012, #39393, .T. ) ;
#4071=DIRECTION ( 'NONE',  ( 1.000000000000000000, 0.000000000000000000, 0.000000000000000000 ) ) ;
#4073=CARTESIAN_POINT ( 'NONE',  ( 17.99999999999999645, 120.4984140710909202, 0.7894348306988416830 ) ) ;
#4074=VECTOR ( 'NONE', #13344, 1000.000000000000000 ) ;
#4075=CYLINDRICAL_SURFACE ( 'NONE', #37095, 59.00000000000000000 ) ;
#4076=CIRCLE ( 'NONE', #11822, 59.00000000000000000 ) ;
#4083=ORIENTED_EDGE ( 'NONE', *, *, #17424, .T. ) ;
#4087=DIRECTION ( 'NONE',  ( 0.000000000000000000, 0.9968120070307499025, 0.07978610555308651708 ) ) ;
#4091=DIRECTION ( 'NONE',  ( -1.000000000000000000, -0.000000000000000000, -0.000000000000000000 ) ) ;
#4092=ORIENTED_EDGE ( 'NONE', *, *, #23023, .T. ) ;
#4093=CARTESIAN_POINT ( 'NONE',  ( 17.99999999999999645, -101.1403355683150096, 56.80345518653453496 ) ) ;
#4094=EDGE_CURVE ( 'NONE', #34149, #13162, #21379, .T. ) ;
#4098=DIRECTION ( 'NONE',  ( 0.000000000000000000, 0.5963673585385025344, -0.8027116379309628957 ) ) ;
#4100=EDGE_CURVE ( 'NONE', #36343, #5127, #12175, .T. ) ;
#4101=DIRECTION ( 'NONE',  ( -1.000000000000000000, -0.000000000000000000, 0.000000000000000000 ) ) ;
#4104=EDGE_LOOP ( 'NONE', ( #10081, #5809, #34680, #13639 ) ) ;
#4108=AXIS2_PLACEMENT_3D ( 'NONE', #41040, #21254, #34504 ) ;
#4109=ADVANCED_FACE ( 'NONE', ( #31374 ), #31162, .F. ) ;
#4110=CARTESIAN_POINT ( 'NONE',  ( 17.99999999999999645, 23.10276247328255650, -118.2656051737067600 ) ) ;
#4111=DIRECTION ( 'NONE',  ( 0.000000000000000000, 0.000000000000000000, 1.000000000000000000 ) ) ;
#4112=ADVANCED_FACE ( 'NONE', ( #34851 ), #21159, .F. ) ;
#4113=LINE ( 'NONE', #10915, #17791 ) ;
#4114=DIRECTION ( 'NONE',  ( 0.000000000000000000, 0.000000000000000000, 1.000000000000000000 ) ) ;
#4115=VERTEX_POINT ( 'NONE', #14811 ) ;
#4117=DIRECTION ( 'NONE',  ( -1.000000000000000000, -0.000000000000000000, 0.000000000000000000 ) ) ;
#4118=CARTESIAN_POINT ( 'NONE',  ( 17.99999999999999645, 111.8797445107943531, 8.437727291344614855 ) ) ;
#4119=EDGE_LOOP ( 'NONE', ( #27143, #6630, #29121, #38639 ) ) ;
#4124=ORIENTED_EDGE ( 'NONE', *, *, #23110, .F. ) ;
#4127=ORIENTED_EDGE ( 'NONE', *, *, #12070, .F. ) ;
#4128=FACE_OUTER_BOUND ( 'NONE', #11854, .T. ) ;
#4129=ORIENTED_EDGE ( 'NONE', *, *, #7629, .T. ) ;
#4130=CARTESIAN_POINT ( 'NONE',  ( 0.000000000000000000, 84.62908780824989208, -85.78116633471202590 ) ) ;
#4131=AXIS2_PLACEMENT_3D ( 'NONE', #32656, #39305, #32150 ) ;
#4133=CARTESIAN_POINT ( 'NONE',  ( 17.99999999999999645, 0.000000000000000000, 0.000000000000000000 ) ) ;
#4137=CIRCLE ( 'NONE', #28575, 58.99999999999999289 ) ;
#4139=ADVANCED_FACE ( 'NONE', ( #5169 ), #4963, .F. ) ;
#4143=EDGE_LOOP ( 'NONE', ( #3926, #5413, #31657, #7925 ) ) ;
#4145=DIRECTION ( 'NONE',  ( 0.000000000000000000, 3.022535141193487712E-14, -1.000000000000000000 ) ) ;
#4150=LINE ( 'NONE', #30594, #10683 ) ;
#4154=CYLINDRICAL_SURFACE ( 'NONE', #33265, 59.00000000000000000 ) ;
#4156=CARTESIAN_POINT ( 'NONE',  ( 17.99999999999999645, 105.3681574666269256, -38.54638589714782881 ) ) ;
#4161=AXIS2_PLACEMENT_3D ( 'NONE', #1287, #14635, #11344 ) ;
#4162=CIRCLE ( 'NONE', #2751, 116.0000000000000000 ) ;
#4163=CYLINDRICAL_SURFACE ( 'NONE', #39435, 116.0000000000000000 ) ;
#4171=ORIENTED_EDGE ( 'NONE', *, *, #21769, .F. ) ;
#4172=FACE_OUTER_BOUND ( 'NONE', #40555, .T. ) ;
#4173=DIRECTION ( 'NONE',  ( 1.000000000000000000, 0.000000000000000000, 0.000000000000000000 ) ) ;
#4174=ORIENTED_EDGE ( 'NONE', *, *, #31497, .F. ) ;
#4175=DIRECTION ( 'NONE',  ( -1.000000000000000000, 0.000000000000000000, 0.000000000000000000 ) ) ;
#4176=FACE_OUTER_BOUND ( 'NONE', #36811, .T. ) ;
#4177=VERTEX_POINT ( 'NONE', #29890 ) ;
#4178=LINE ( 'NONE', #7473, #1268 ) ;
#4179=VERTEX_POINT ( 'NONE', #9995 ) ;
#4183=ORIENTED_EDGE ( 'NONE', *, *, #854, .T. ) ;
#4186=AXIS2_PLACEMENT_3D ( 'NONE', #12664, #8518, #38607 ) ;
#4189=EDGE_CURVE ( 'NONE', #37469, #10174, #6498, .T. ) ;
#4192=AXIS2_PLACEMENT_3D ( 'NONE', #38765, #19394, #35912 ) ;
#4193=ORIENTED_EDGE ( 'NONE', *, *, #38339, .T. ) ;
#4198=VECTOR ( 'NONE', #38327, 1000.000000000000000 ) ;
#4199=VECTOR ( 'NONE', #30884, 1000.000000000000000 ) ;
#4202=DIRECTION ( 'NONE',  ( -1.000000000000000000, -0.000000000000000000, -0.000000000000000000 ) ) ;
#4206=DIRECTION ( 'NONE',  ( 0.000000000000000000, 0.9407002666710319039, 0.3392388661180338882 ) ) ;
#4207=ORIENTED_EDGE ( 'NONE', *, *, #5374, .T. ) ;
#4209=DIRECTION ( 'NONE',  ( 0.000000000000000000, 0.000000000000000000, 1.000000000000000000 ) ) ;
#4211=DIRECTION ( 'NONE',  ( 0.000000000000000000, 0.000000000000000000, 1.000000000000000000 ) ) ;
#4215=ORIENTED_EDGE ( 'NONE', *, *, #9916, .T. ) ;
#4216=CIRCLE ( 'NONE', #34194, 59.00000000000000711 ) ;
#4223=EDGE_CURVE ( 'NONE', #10476, #21840, #5289, .T. ) ;
#4225=DIRECTION ( 'NONE',  ( 0.000000000000000000, 0.3641605752528168094, 0.9313361774523405412 ) ) ;
#4227=CARTESIAN_POINT ( 'NONE',  ( 0.000000000000000000, 90.81729652456166946, 72.16798910853647442 ) ) ;
#4236=DIRECTION ( 'NONE',  ( -1.000000000000000000, -0.000000000000000000, -0.000000000000000000 ) ) ;
#4237=FACE_OUTER_BOUND ( 'NONE', #13780, .T. ) ;
#4238=VECTOR ( 'NONE', #33566, 1000.000000000000000 ) ;
#4239=ORIENTED_EDGE ( 'NONE', *, *, #35830, .T. ) ;
#4240=CARTESIAN_POINT ( 'NONE',  ( 0.000000000000000000, -109.4038418350900059, -50.51029986767660773 ) ) ;
#4241=EDGE_LOOP ( 'NONE', ( #32530, #25409, #4394, #4891 ) ) ;
#4244=EDGE_CURVE ( 'NONE', #13499, #20659, #19994, .T. ) ;
#4246=CARTESIAN_POINT ( 'NONE',  ( 0.000000000000000000, 80.74349901498408144, 77.90224541347306797 ) ) ;
#4248=EDGE_CURVE ( 'NONE', #20315, #14728, #5319, .T. ) ;
#4250=ORIENTED_EDGE ( 'NONE', *, *, #34628, .F. ) ;
#4252=DIRECTION ( 'NONE',  ( -1.000000000000000000, 0.000000000000000000, 0.000000000000000000 ) ) ;
#4253=CARTESIAN_POINT ( 'NONE',  ( 0.000000000000000000, -83.49789599728724454, -86.88263557826851979 ) ) ;
#4255=CARTESIAN_POINT ( 'NONE',  ( 17.99999999999999645, 2.418575551220858877, 120.4767259403369053 ) ) ;
#4262=EDGE_CURVE ( 'NONE', #27389, #18211, #33873, .T. ) ;
#4264=DIRECTION ( 'NONE',  ( 1.000000000000000000, 0.000000000000000000, 0.000000000000000000 ) ) ;
#4265=ORIENTED_EDGE ( 'NONE', *, *, #17602, .F. ) ;
#4267=ORIENTED_EDGE ( 'NONE', *, *, #19133, .T. ) ;
#4269=CIRCLE ( 'NONE', #5009, 120.5010000000000332 ) ;
#4279=CARTESIAN_POINT ( 'NONE',  ( 17.99999999999999645, -109.1131968884000258, 26.12628443611856355 ) ) ;
#4281=DIRECTION ( 'NONE',  ( 0.000000000000000000, 0.000000000000000000, 1.000000000000000000 ) ) ;
#4282=EDGE_LOOP ( 'NONE', ( #39399, #26149, #25064, #141 ) ) ;
#4285=DIRECTION ( 'NONE',  ( 0.000000000000000000, 0.2631025642275152121, 0.9647678688145175929 ) ) ;
#4288=AXIS2_PLACEMENT_3D ( 'NONE', #16302, #19168, #6246 ) ;
#4289=ORIENTED_EDGE ( 'NONE', *, *, #12463, .T. ) ;
#4290=LINE ( 'NONE', #15025, #22102 ) ;
#4296=VERTEX_POINT ( 'NONE', #12076 ) ;
#4301=EDGE_CURVE ( 'NONE', #18949, #21981, #8803, .T. ) ;
#4304=VERTEX_POINT ( 'NONE', #34963 ) ;
#4313=CARTESIAN_POINT ( 'NONE',  ( -10.00000000000000000, 0.000000000000000000, 0.000000000000000000 ) ) ;
#4314=ADVANCED_FACE ( 'NONE', ( #40739 ), #20956, .F. ) ;
#4315=DIRECTION ( 'NONE',  ( 1.000000000000000000, 0.000000000000000000, 0.000000000000000000 ) ) ;
#4319=CIRCLE ( 'NONE', #125, 59.00000000000000711 ) ;
#4324=EDGE_CURVE ( 'NONE', #32742, #28827, #30740, .T. ) ;
#4326=VECTOR ( 'NONE', #35971, 1000.000000000000000 ) ;
#4327=DIRECTION ( 'NONE',  ( 1.000000000000000000, -0.000000000000000000, 0.000000000000000000 ) ) ;
#4328=DIRECTION ( 'NONE',  ( 1.000000000000000000, 0.000000000000000000, 0.000000000000000000 ) ) ;
#4334=FACE_OUTER_BOUND ( 'NONE', #31231, .T. ) ;
#4335=ORIENTED_EDGE ( 'NONE', *, *, #31361, .F. ) ;
#4337=DIRECTION ( 'NONE',  ( 0.000000000000000000, 0.000000000000000000, 1.000000000000000000 ) ) ;
#4342=ORIENTED_EDGE ( 'NONE', *, *, #25053, .T. ) ;
#4345=EDGE_CURVE ( 'NONE', #6806, #16376, #7157, .T. ) ;
#4348=ORIENTED_EDGE ( 'NONE', *, *, #5297, .F. ) ;
#4351=VERTEX_POINT ( 'NONE', #30102 ) ;
#4352=AXIS2_PLACEMENT_3D ( 'NONE', #143, #801, #13507 ) ;
#4354=DIRECTION ( 'NONE',  ( 0.000000000000000000, 0.000000000000000000, 1.000000000000000000 ) ) ;
#4355=ORIENTED_EDGE ( 'NONE', *, *, #13030, .F. ) ;
#4360=EDGE_CURVE ( 'NONE', #3320, #31004, #24157, .T. ) ;
#4361=DIRECTION ( 'NONE',  ( 1.000000000000000000, 0.000000000000000000, 0.000000000000000000 ) ) ;
#4362=DIRECTION ( 'NONE',  ( -1.000000000000000000, 0.000000000000000000, 0.000000000000000000 ) ) ;
#4369=CYLINDRICAL_SURFACE ( 'NONE', #4551, 59.00000000000000000 ) ;
#4371=EDGE_LOOP ( 'NONE', ( #33595, #23159, #19710, #31319 ) ) ;
#4376=EDGE_CURVE ( 'NONE', #37783, #10089, #42917, .T. ) ;
#4378=DIRECTION ( 'NONE',  ( 0.000000000000000000, 0.8993121301712174720, 0.4373073204588591723 ) ) ;
#4382=DIRECTION ( 'NONE',  ( 0.000000000000000000, -0.9968120070307493474, -0.07978610555309334496 ) ) ;
#4384=ORIENTED_EDGE ( 'NONE', *, *, #15602, .T. ) ;
#4388=CIRCLE ( 'NONE', #41327, 120.5010000000000474 ) ;
#4391=ADVANCED_FACE ( 'NONE', ( #30948 ), #33778, .F. ) ;
#4393=DIRECTION ( 'NONE',  ( -1.000000000000000000, -0.000000000000000000, -0.000000000000000000 ) ) ;
#4394=ORIENTED_EDGE ( 'NONE', *, *, #24254, .T. ) ;
#4396=ORIENTED_EDGE ( 'NONE', *, *, #30179, .F. ) ;
#4398=ORIENTED_EDGE ( 'NONE', *, *, #30577, .F. ) ;
#4402=VERTEX_POINT ( 'NONE', #17250 ) ;
#4408=ORIENTED_EDGE ( 'NONE', *, *, #33506, .F. ) ;
#4409=VECTOR ( 'NONE', #22961, 1000.000000000000000 ) ;
#4411=EDGE_CURVE ( 'NONE', #40482, #35201, #14171, .T. ) ;
#4412=DIRECTION ( 'NONE',  ( 0.000000000000000000, 0.9826841245925214130, -0.1852887240871113894 ) ) ;
#4415=FACE_OUTER_BOUND ( 'NONE', #19079, .T. ) ;
#4419=AXIS2_PLACEMENT_3D ( 'NONE', #17524, #39779, #33261 ) ;
#4421=DIRECTION ( 'NONE',  ( 1.000000000000000000, -0.000000000000000000, -0.000000000000000000 ) ) ;
#4423=DIRECTION ( 'NONE',  ( 1.000000000000000000, 0.000000000000000000, 0.000000000000000000 ) ) ;
#4424=ORIENTED_EDGE ( 'NONE', *, *, #19959, .T. ) ;
#4426=ORIENTED_EDGE ( 'NONE', *, *, #19419, .F. ) ;
#4427=EDGE_CURVE ( 'NONE', #42118, #10039, #13718, .T. ) ;
#4429=CARTESIAN_POINT ( 'NONE',  ( 8.999999999999998224, -106.6051926090974007, 45.73109345704783379 ) ) ;
#4433=EDGE_CURVE ( 'NONE', #34842, #5268, #40831, .T. ) ;
#4434=EDGE_CURVE ( 'NONE', #31940, #36886, #10224, .T. ) ;
#4436=CIRCLE ( 'NONE', #2339, 58.99999999999999289 ) ;
#4437=ORIENTED_EDGE ( 'NONE', *, *, #41870, .T. ) ;
#4439=ORIENTED_EDGE ( 'NONE', *, *, #3771, .F. ) ;
#4441=DIRECTION ( 'NONE',  ( 0.000000000000000000, 0.000000000000000000, 1.000000000000000000 ) ) ;
#4442=CARTESIAN_POINT ( 'NONE',  ( 17.99999999999999645, -51.27532863109435368, 99.79535634195110561 ) ) ;
#4443=CARTESIAN_POINT ( 'NONE',  ( 17.99999999999999645, 0.000000000000000000, 0.000000000000000000 ) ) ;
#4448=DIRECTION ( 'NONE',  ( -1.000000000000000000, -0.000000000000000000, 0.000000000000000000 ) ) ;
#4450=CARTESIAN_POINT ( 'NONE',  ( 9.000000000000001776, 13.00789606333630566, -115.2683592318613819 ) ) ;
#4451=CIRCLE ( 'NONE', #28873, 120.5010000000000190 ) ;
#4452=ORIENTED_EDGE ( 'NONE', *, *, #42125, .F. ) ;
#4453=CYLINDRICAL_SURFACE ( 'NONE', #41743, 59.00000000000000000 ) ;
#4457=AXIS2_PLACEMENT_3D ( 'NONE', #5451, #35110, #42292 ) ;
#4460=ORIENTED_EDGE ( 'NONE', *, *, #6305, .T. ) ;
#4462=CIRCLE ( 'NONE', #8651, 116.0000000000000000 ) ;
#4465=EDGE_CURVE ( 'NONE', #40313, #42137, #1689, .T. ) ;
#4467=ORIENTED_EDGE ( 'NONE', *, *, #42735, .F. ) ;
#4468=DIRECTION ( 'NONE',  ( 0.000000000000000000, 0.000000000000000000, 1.000000000000000000 ) ) ;
#4469=VERTEX_POINT ( 'NONE', #8670 ) ;
#4473=LINE ( 'NONE', #6896, #8062 ) ;
#4477=EDGE_LOOP ( 'NONE', ( #40614, #38803, #13504, #15692 ) ) ;
#4478=DIRECTION ( 'NONE',  ( -1.000000000000000000, 0.000000000000000000, 0.000000000000000000 ) ) ;
#4479=ORIENTED_EDGE ( 'NONE', *, *, #35792, .F. ) ;
#4481=VERTEX_POINT ( 'NONE', #41620 ) ;
#4490=EDGE_CURVE ( 'NONE', #5055, #2401, #17185, .T. ) ;
#4491=CIRCLE ( 'NONE', #6574, 58.99999999999999289 ) ;
#4492=ORIENTED_EDGE ( 'NONE', *, *, #6268, .F. ) ;
#4494=EDGE_LOOP ( 'NONE', ( #42346, #32881, #40537, #10585 ) ) ;
#4496=AXIS2_PLACEMENT_3D ( 'NONE', #32148, #22574, #2861 ) ;
#4498=VECTOR ( 'NONE', #4478, 1000.000000000000000 ) ;
#4500=ORIENTED_EDGE ( 'NONE', *, *, #28256, .F. ) ;
#4501=CARTESIAN_POINT ( 'NONE',  ( 17.99999999999999645, -107.5680526044917542, -31.89649718262205269 ) ) ;
#4503=DIRECTION ( 'NONE',  ( -1.000000000000000000, -0.000000000000000000, 0.000000000000000000 ) ) ;
#4506=DIRECTION ( 'NONE',  ( -1.000000000000000000, -0.000000000000000000, -0.000000000000000000 ) ) ;
#4507=VERTEX_POINT ( 'NONE', #11772 ) ;
#4508=ADVANCED_FACE ( 'NONE', ( #28123 ), #1906, .F. ) ;
#4515=DIRECTION ( 'NONE',  ( 0.000000000000000000, 0.4132121857683728194, 0.9106347728549155640 ) ) ;
#4516=ORIENTED_EDGE ( 'NONE', *, *, #39991, .T. ) ;
#4525=DIRECTION ( 'NONE',  ( -1.000000000000000000, 0.000000000000000000, 0.000000000000000000 ) ) ;
#4526=CYLINDRICAL_SURFACE ( 'NONE', #22383, 59.00000000000000000 ) ;
#4528=AXIS2_PLACEMENT_3D ( 'NONE', #6066, #39204, #42913 ) ;
#4530=DIRECTION ( 'NONE',  ( -1.000000000000000000, -0.000000000000000000, -0.000000000000000000 ) ) ;
#4531=AXIS2_PLACEMENT_3D ( 'NONE', #38981, #9103, #22458 ) ;
#4536=DIRECTION ( 'NONE',  ( 1.000000000000000000, 0.000000000000000000, 0.000000000000000000 ) ) ;
#4537=DIRECTION ( 'NONE',  ( 0.000000000000000000, 0.9968120070307504577, -0.07978610555307970309 ) ) ;
#4541=EDGE_CURVE ( 'NONE', #20905, #30050, #20983, .T. ) ;
#4545=DIRECTION ( 'NONE',  ( -1.000000000000000000, -0.000000000000000000, -0.000000000000000000 ) ) ;
#4547=VECTOR ( 'NONE', #14119, 1000.000000000000000 ) ;
#4548=ADVANCED_FACE ( 'NONE', ( #31386 ), #4526, .F. ) ;
#4549=CARTESIAN_POINT ( 'NONE',  ( 17.99999999999999645, 101.8011932243948081, 55.61040422519366189 ) ) ;
#4551=AXIS2_PLACEMENT_3D ( 'NONE', #18185, #24507, #37548 ) ;
#4552=DIRECTION ( 'NONE',  ( 1.000000000000000000, 0.000000000000000000, 0.000000000000000000 ) ) ;
#4558=LINE ( 'NONE', #1065, #10428 ) ;
#4564=DIRECTION ( 'NONE',  ( 0.000000000000000000, 0.000000000000000000, 1.000000000000000000 ) ) ;
#4568=CYLINDRICAL_SURFACE ( 'NONE', #21513, 59.00000000000001421 ) ;
#4569=VERTEX_POINT ( 'NONE', #40962 ) ;
#4572=VERTEX_POINT ( 'NONE', #7813 ) ;
#4573=DIRECTION ( 'NONE',  ( 0.000000000000000000, 0.000000000000000000, 1.000000000000000000 ) ) ;
#4577=FACE_OUTER_BOUND ( 'NONE', #37114, .T. ) ;
#4578=ORIENTED_EDGE ( 'NONE', *, *, #23142, .T. ) ;
#4580=EDGE_CURVE ( 'NONE', #36933, #29613, #39715, .T. ) ;
#4586=CIRCLE ( 'NONE', #38723, 58.99999999999999289 ) ;
#4587=ORIENTED_EDGE ( 'NONE', *, *, #41897, .T. ) ;
#4592=ORIENTED_EDGE ( 'NONE', *, *, #13945, .T. ) ;
#4594=CARTESIAN_POINT ( 'NONE',  ( 17.99999999999999645, -34.74871106919691499, 106.6808302961370600 ) ) ;
#4596=AXIS2_PLACEMENT_3D ( 'NONE', #35027, #41987, #25251 ) ;
#4598=ORIENTED_EDGE ( 'NONE', *, *, #13653, .T. ) ;
#4599=VECTOR ( 'NONE', #4327, 1000.000000000000000 ) ;
#4603=ADVANCED_FACE ( 'NONE', ( #15675 ), #2111, .F. ) ;
#4605=AXIS2_PLACEMENT_3D ( 'NONE', #34403, #28550, #30931 ) ;
#4607=CARTESIAN_POINT ( 'NONE',  ( 8.999999999999998224, 95.31344542257733110, 66.11616384574480776 ) ) ;
#4610=EDGE_CURVE ( 'NONE', #553, #19975, #42669, .T. ) ;
#4616=VERTEX_POINT ( 'NONE', #15473 ) ;
#4617=CIRCLE ( 'NONE', #34583, 59.00000000000000000 ) ;
#4625=VECTOR ( 'NONE', #9495, 1000.000000000000000 ) ;
#4626=ORIENTED_EDGE ( 'NONE', *, *, #24773, .T. ) ;
#4627=AXIS2_PLACEMENT_3D ( 'NONE', #20820, #34075, #6808 ) ;
#4628=DIRECTION ( 'NONE',  ( 1.000000000000000000, 0.000000000000000000, 0.000000000000000000 ) ) ;
#4632=MECHANICAL_DESIGN_GEOMETRIC_PRESENTATION_REPRESENTATION('',(#442),#33228);
#4634=ORIENTED_EDGE ( 'NONE', *, *, #27292, .F. ) ;
#4636=CIRCLE ( 'NONE', #22132, 58.99999999999999289 ) ;
#4639=EDGE_CURVE ( 'NONE', #1932, #33553, #31417, .T. ) ;
#4646=DIRECTION ( 'NONE',  ( -1.000000000000000000, 0.000000000000000000, 0.000000000000000000 ) ) ;
#4649=DIRECTION ( 'NONE',  ( 1.000000000000000000, 0.000000000000000000, 0.000000000000000000 ) ) ;
#4650=ORIENTED_EDGE ( 'NONE', *, *, #5217, .T. ) ;
#4651=LINE ( 'NONE', #19711, #29647 ) ;
#4654=CIRCLE ( 'NONE', #28364, 59.00000000000000000 ) ;
#4657=ADVANCED_FACE ( 'NONE', ( #39619 ), #23097, .F. ) ;
#4661=VECTOR ( 'NONE', #9289, 1000.000000000000000 ) ;
#4663=CARTESIAN_POINT ( 'NONE',  ( 17.99999999999999645, 12.43843445475471832, -111.5058645182328405 ) ) ;
#4667=DIRECTION ( 'NONE',  ( -1.000000000000000000, 0.000000000000000000, 0.000000000000000000 ) ) ;
#4671=ORIENTED_EDGE ( 'NONE', *, *, #23903, .T. ) ;
#4672=FACE_OUTER_BOUND ( 'NONE', #35090, .T. ) ;
#4673=ORIENTED_EDGE ( 'NONE', *, *, #5303, .F. ) ;
#4679=ORIENTED_EDGE ( 'NONE', *, *, #7553, .F. ) ;
#4680=ORIENTED_EDGE ( 'NONE', *, *, #7946, .T. ) ;
#4681=CARTESIAN_POINT ( 'NONE',  ( 17.99999999999999645, 34.03109950475727175, 115.5957406979051285 ) ) ;
#4687=DIRECTION ( 'NONE',  ( -1.000000000000000000, 0.000000000000000000, 0.000000000000000000 ) ) ;
#4689=AXIS2_PLACEMENT_3D ( 'NONE', #17767, #27137, #37575 ) ;
#4695=AXIS2_PLACEMENT_3D ( 'NONE', #2080, #18514, #39155 ) ;
#4698=ADVANCED_FACE ( 'NONE', ( #25727 ), #29403, .F. ) ;
#4700=DIRECTION ( 'NONE',  ( -1.000000000000000000, 0.000000000000000000, 0.000000000000000000 ) ) ;
#4703=EDGE_CURVE ( 'NONE', #17388, #3320, #9308, .T. ) ;
#4706=CYLINDRICAL_SURFACE ( 'NONE', #34918, 59.00000000000000000 ) ;
#4707=ORIENTED_EDGE ( 'NONE', *, *, #8268, .T. ) ;
#4709=DIRECTION ( 'NONE',  ( 0.000000000000000000, -0.3641605752528294104, 0.9313361774523356562 ) ) ;
#4715=CARTESIAN_POINT ( 'NONE',  ( -10.00000000000000000, 0.000000000000000000, 0.000000000000000000 ) ) ;
#4719=CARTESIAN_POINT ( 'NONE',  ( 8.999999999999998224, -48.55277268144396174, 105.3500273609078306 ) ) ;
#4720=CIRCLE ( 'NONE', #33280, 59.00000000000001421 ) ;
#4725=EDGE_CURVE ( 'NONE', #35938, #8548, #35495, .T. ) ;
#4726=ORIENTED_EDGE ( 'NONE', *, *, #19657, .F. ) ;
#4729=EDGE_LOOP ( 'NONE', ( #15050, #32759, #17049, #31835 ) ) ;
#4731=( NAMED_UNIT ( * ) PLANE_ANGLE_UNIT ( ) SI_UNIT ( $, .RADIAN. ) );
#4733=EDGE_CURVE ( 'NONE', #37469, #10305, #2109, .T. ) ;
#4734=VECTOR ( 'NONE', #26636, 1000.000000000000000 ) ;
#4737=CARTESIAN_POINT ( 'NONE',  ( 0.000000000000000000, -6.854627147197943415, -115.7972974066014018 ) ) ;
#4741=DIRECTION ( 'NONE',  ( 1.000000000000000000, 0.000000000000000000, 0.000000000000000000 ) ) ;
#4743=VECTOR ( 'NONE', #37203, 1000.000000000000000 ) ;
#4748=DIRECTION ( 'NONE',  ( -1.000000000000000000, 0.000000000000000000, 0.000000000000000000 ) ) ;
#4751=ORIENTED_EDGE ( 'NONE', *, *, #7351, .F. ) ;
#4755=CIRCLE ( 'NONE', #38872, 59.00000000000000711 ) ;
#4757=VECTOR ( 'NONE', #9820, 1000.000000000000000 ) ;
#4758=CARTESIAN_POINT ( 'NONE',  ( 0.000000000000000000, 0.000000000000000000, 0.000000000000000000 ) ) ;
#4760=EDGE_CURVE ( 'NONE', #13499, #10354, #39825, .T. ) ;
#4763=DIRECTION ( 'NONE',  ( -1.000000000000000000, -0.000000000000000000, -0.000000000000000000 ) ) ;
#4764=DIRECTION ( 'NONE',  ( 1.000000000000000000, 0.000000000000000000, 0.000000000000000000 ) ) ;
#4778=CARTESIAN_POINT ( 'NONE',  ( 0.000000000000000000, 0.000000000000000000, 0.000000000000000000 ) ) ;
#4780=ORIENTED_EDGE ( 'NONE', *, *, #24395, .F. ) ;
#4784=DIRECTION ( 'NONE',  ( -1.000000000000000000, 0.000000000000000000, 0.000000000000000000 ) ) ;
#4786=CARTESIAN_POINT ( 'NONE',  ( 17.99999999999999645, 86.84764344322962870, 76.89919913989776035 ) ) ;
#4790=EDGE_LOOP ( 'NONE', ( #15274, #12760, #15288, #9893 ) ) ;
#4791=CARTESIAN_POINT ( 'NONE',  ( 0.000000000000000000, -35.72777019205738469, 106.3569410558016273 ) ) ;
#4793=VECTOR ( 'NONE', #17597, 1000.000000000000000 ) ;
#4794=EDGE_LOOP ( 'NONE', ( #36301, #9854, #30019, #3969 ) ) ;
#4801=DIRECTION ( 'NONE',  ( 0.000000000000000000, 0.000000000000000000, 1.000000000000000000 ) ) ;
#4802=ORIENTED_EDGE ( 'NONE', *, *, #16393, .F. ) ;
#4805=CYLINDRICAL_SURFACE ( 'NONE', #4908, 59.00000000000000000 ) ;
#4806=CARTESIAN_POINT ( 'NONE',  ( 0.000000000000000000, -120.2856157092987388, 7.201503623196430226 ) ) ;
#4809=ADVANCED_FACE ( 'NONE', ( #20681 ), #27410, .F. ) ;
#4810=DIRECTION ( 'NONE',  ( -1.000000000000000000, -0.000000000000000000, 0.000000000000000000 ) ) ;
#4812=CYLINDRICAL_SURFACE ( 'NONE', #30819, 116.0000000000000000 ) ;
#4814=DIRECTION ( 'NONE',  ( -1.000000000000000000, 0.000000000000000000, 0.000000000000000000 ) ) ;
#4818=CARTESIAN_POINT ( 'NONE',  ( 0.000000000000000000, -11.65176648921111635, 115.4133282497342066 ) ) ;
#4819=CARTESIAN_POINT ( 'NONE',  ( 17.99999999999999645, 63.24564713401931471, -102.5693868539688651 ) ) ;
#4820=AXIS2_PLACEMENT_3D ( 'NONE', #18845, #6120, #29062 ) ;
#4827=CARTESIAN_POINT ( 'NONE',  ( 0.000000000000000000, 110.0562500189205224, -49.07252625220001363 ) ) ;
#4835=DIRECTION ( 'NONE',  ( 0.000000000000000000, 0.000000000000000000, 1.000000000000000000 ) ) ;
#4840=ORIENTED_EDGE ( 'NONE', *, *, #33144, .F. ) ;
#4848=EDGE_LOOP ( 'NONE', ( #34423, #26540, #39063, #13815 ) ) ;
#4849=DIRECTION ( 'NONE',  ( 1.000000000000000000, 0.000000000000000000, 0.000000000000000000 ) ) ;
#4852=ORIENTED_EDGE ( 'NONE', *, *, #6733, .F. ) ;
#4855=ORIENTED_EDGE ( 'NONE', *, *, #2254, .T. ) ;
#4858=DIRECTION ( 'NONE',  ( 0.000000000000000000, -0.2113826236296314776, 0.9774033898178651203 ) ) ;
#4860=DIRECTION ( 'NONE',  ( 1.000000000000000000, 0.000000000000000000, 0.000000000000000000 ) ) ;
#4866=DIRECTION ( 'NONE',  ( -1.000000000000000000, -0.000000000000000000, 0.000000000000000000 ) ) ;
#4868=EDGE_LOOP ( 'NONE', ( #42384, #32946, #18201, #5 ) ) ;
#4869=EDGE_CURVE ( 'NONE', #37579, #2622, #14121, .T. ) ;
#4871=CARTESIAN_POINT ( 'NONE',  ( 17.99999999999999645, 0.000000000000000000, 0.000000000000000000 ) ) ;
#4880=ORIENTED_EDGE ( 'NONE', *, *, #2094, .T. ) ;
#4882=ORIENTED_EDGE ( 'NONE', *, *, #38246, .T. ) ;
#4883=EDGE_LOOP ( 'NONE', ( #22935, #20869, #39550, #28800 ) ) ;
#4886=CARTESIAN_POINT ( 'NONE',  ( 0.000000000000000000, 101.1403355683146117, 56.80345518653518866 ) ) ;
#4887=CYLINDRICAL_SURFACE ( 'NONE', #3723, 59.00000000000000000 ) ;
#4888=EDGE_CURVE ( 'NONE', #35775, #21277, #36961, .T. ) ;
#4889=ORIENTED_EDGE ( 'NONE', *, *, #22311, .T. ) ;
#4890=FACE_OUTER_BOUND ( 'NONE', #30091, .T. ) ;
#4891=ORIENTED_EDGE ( 'NONE', *, *, #33750, .T. ) ;
#4892=LINE ( 'NONE', #34994, #4793 ) ;
#4893=EDGE_CURVE ( 'NONE', #2622, #5158, #728, .T. ) ;
#4896=CARTESIAN_POINT ( 'NONE',  ( 0.000000000000000000, 5.492704054966705662, 115.8698847939556344 ) ) ;
#4897=DIRECTION ( 'NONE',  ( 0.000000000000000000, 0.000000000000000000, 1.000000000000000000 ) ) ;
#4898=ORIENTED_EDGE ( 'NONE', *, *, #22087, .T. ) ;
#4899=ORIENTED_EDGE ( 'NONE', *, *, #39655, .T. ) ;
#4900=DIRECTION ( 'NONE',  ( 0.000000000000000000, 0.000000000000000000, 1.000000000000000000 ) ) ;
#4901=CARTESIAN_POINT ( 'NONE',  ( 17.99999999999999645, 0.000000000000000000, 0.000000000000000000 ) ) ;
#4902=CIRCLE ( 'NONE', #41097, 59.00000000000000000 ) ;
#4903=ORIENTED_EDGE ( 'NONE', *, *, #30581, .F. ) ;
#4904=DIRECTION ( 'NONE',  ( 1.000000000000000000, 0.000000000000000000, 0.000000000000000000 ) ) ;
#4905=ORIENTED_EDGE ( 'NONE', *, *, #14002, .T. ) ;
#4906=VECTOR ( 'NONE', #4687, 1000.000000000000000 ) ;
#4908=AXIS2_PLACEMENT_3D ( 'NONE', #8296, #18166, #34692 ) ;
#4909=LINE ( 'NONE', #1844, #4906 ) ;
#4914=VERTEX_POINT ( 'NONE', #102 ) ;
#4919=EDGE_LOOP ( 'NONE', ( #15446, #35529, #22324, #19970 ) ) ;
#4921=ORIENTED_EDGE ( 'NONE', *, *, #8792, .T. ) ;
#4926=EDGE_CURVE ( 'NONE', #23473, #25436, #25855, .T. ) ;
#4929=ORIENTED_EDGE ( 'NONE', *, *, #15849, .T. ) ;
#4930=EDGE_CURVE ( 'NONE', #39721, #40482, #41126, .T. ) ;
#4932=FACE_OUTER_BOUND ( 'NONE', #30822, .T. ) ;
#4935=EDGE_LOOP ( 'NONE', ( #40444, #11667, #32012, #9538 ) ) ;
#4938=CARTESIAN_POINT ( 'NONE',  ( 17.99999999999999645, -63.55543939553702160, -97.03971415477388973 ) ) ;
#4941=CIRCLE ( 'NONE', #26528, 130.0000000000000000 ) ;
#4943=ORIENTED_EDGE ( 'NONE', *, *, #25789, .T. ) ;
#4944=DIRECTION ( 'NONE',  ( 0.000000000000000000, 0.5076658003388409002, -0.8615540813938056264 ) ) ;
#4947=CYLINDRICAL_SURFACE ( 'NONE', #6648, 58.99999999999998579 ) ;
#4948=ADVANCED_FACE ( 'NONE', ( #36995 ), #7108, .F. ) ;
#4952=LINE ( 'NONE', #34187, #5202 ) ;
#4957=ORIENTED_EDGE ( 'NONE', *, *, #31037, .F. ) ;
#4961=EDGE_CURVE ( 'NONE', #29560, #384, #6320, .T. ) ;
#4962=LINE ( 'NONE', #8449, #30022 ) ;
#4963=CYLINDRICAL_SURFACE ( 'NONE', #366, 59.00000000000000000 ) ;
#4971=CIRCLE ( 'NONE', #21054, 59.00000000000000000 ) ;
#4974=DIRECTION ( 'NONE',  ( 0.000000000000000000, 0.000000000000000000, 1.000000000000000000 ) ) ;
#4978=ADVANCED_FACE ( 'NONE', ( #41333 ), #38295, .F. ) ;
#4980=CARTESIAN_POINT ( 'NONE',  ( 0.000000000000000000, 0.000000000000000000, 0.000000000000000000 ) ) ;
#4981=DIRECTION ( 'NONE',  ( 0.000000000000000000, 0.000000000000000000, 1.000000000000000000 ) ) ;
#4982=EDGE_CURVE ( 'NONE', #8937, #13915, #11963, .T. ) ;
#4984=VERTEX_POINT ( 'NONE', #1857 ) ;
#4986=CARTESIAN_POINT ( 'NONE',  ( 17.99999999999999645, 120.2856157092987957, -7.201503623195590009 ) ) ;
#4996=ADVANCED_FACE ( 'NONE', ( #27637 ), #21337, .F. ) ;
#4999=EDGE_CURVE ( 'NONE', #3403, #37380, #41114, .T. ) ;
#5001=CIRCLE ( 'NONE', #30089, 116.0000000000000000 ) ;
#5003=ORIENTED_EDGE ( 'NONE', *, *, #39073, .T. ) ;
#5006=VERTEX_POINT ( 'NONE', #41780 ) ;
#5009=AXIS2_PLACEMENT_3D ( 'NONE', #7378, #20738, #34002 ) ;
#5010=VERTEX_POINT ( 'NONE', #4255 ) ;
#5011=LINE ( 'NONE', #14857, #41953 ) ;
#5013=FACE_OUTER_BOUND ( 'NONE', #32700, .T. ) ;
#5019=DIRECTION ( 'NONE',  ( 0.000000000000000000, 0.000000000000000000, 1.000000000000000000 ) ) ;
#5027=ADVANCED_FACE ( 'NONE', ( #31545 ), #4706, .F. ) ;
#5028=ORIENTED_EDGE ( 'NONE', *, *, #42625, .T. ) ;
#5030=CIRCLE ( 'NONE', #34299, 58.99999999999999289 ) ;
#5042=FACE_OUTER_BOUND ( 'NONE', #20843, .T. ) ;
#5045=EDGE_CURVE ( 'NONE', #28564, #14100, #12635, .T. ) ;
#5046=DIRECTION ( 'NONE',  ( 0.000000000000000000, -0.7525707698561440173, 0.6585113790650322096 ) ) ;
#5049=CIRCLE ( 'NONE', #158, 120.5010000000000190 ) ;
#5052=ORIENTED_EDGE ( 'NONE', *, *, #25762, .F. ) ;
#5053=CARTESIAN_POINT ( 'NONE',  ( 17.99999999999999645, 83.49789599728782719, 86.88263557826796557 ) ) ;
#5055=VERTEX_POINT ( 'NONE', #20907 ) ;
#5056=DIRECTION ( 'NONE',  ( 0.000000000000000000, 0.000000000000000000, 1.000000000000000000 ) ) ;
#5057=CARTESIAN_POINT ( 'NONE',  ( 0.000000000000000000, 0.000000000000000000, 0.000000000000000000 ) ) ;
#5062=ORIENTED_EDGE ( 'NONE', *, *, #18769, .F. ) ;
#5075=CYLINDRICAL_SURFACE ( 'NONE', #32548, 116.0000000000000000 ) ;
#5077=CARTESIAN_POINT ( 'NONE',  ( 0.000000000000000000, 114.8812324315175033, 16.07179003769187986 ) ) ;
#5079=AXIS2_PLACEMENT_3D ( 'NONE', #12135, #2901, #2265 ) ;
#5080=CARTESIAN_POINT ( 'NONE',  ( 17.99999999999999645, 0.000000000000000000, 0.000000000000000000 ) ) ;
#5081=ORIENTED_EDGE ( 'NONE', *, *, #23327, .F. ) ;
#5084=CARTESIAN_POINT ( 'NONE',  ( 0.000000000000000000, -115.9387338813861987, 3.769613505535687636 ) ) ;
#5085=ORIENTED_EDGE ( 'NONE', *, *, #10352, .F. ) ;
#5091=EDGE_LOOP ( 'NONE', ( #17118, #33569, #21105, #3596 ) ) ;
#5093=CARTESIAN_POINT ( 'NONE',  ( 0.000000000000000000, 66.49630760163600485, 90.36876423296011751 ) ) ;
#5096=DIRECTION ( 'NONE',  ( -1.000000000000000000, 0.000000000000000000, 0.000000000000000000 ) ) ;
#5100=DIRECTION ( 'NONE',  ( -1.000000000000000000, -0.000000000000000000, 0.000000000000000000 ) ) ;
#5102=EDGE_CURVE ( 'NONE', #25078, #32554, #35585, .T. ) ;
#5106=EDGE_LOOP ( 'NONE', ( #3724, #38063, #24079, #42426 ) ) ;
#5109=DIRECTION ( 'NONE',  ( -1.000000000000000000, -0.000000000000000000, 0.000000000000000000 ) ) ;
#5111=CIRCLE ( 'NONE', #16981, 120.5010000000000190 ) ;
#5118=DIRECTION ( 'NONE',  ( -1.000000000000000000, 0.000000000000000000, 0.000000000000000000 ) ) ;
#5120=DIRECTION ( 'NONE',  ( 0.000000000000000000, 0.000000000000000000, 1.000000000000000000 ) ) ;
#5127=VERTEX_POINT ( 'NONE', #21973 ) ;
#5132=EDGE_CURVE ( 'NONE', #5549, #14617, #32180, .T. ) ;
#5133=DIRECTION ( 'NONE',  ( 0.000000000000000000, 0.000000000000000000, 1.000000000000000000 ) ) ;
#5137=DIRECTION ( 'NONE',  ( -1.000000000000000000, -0.000000000000000000, -0.000000000000000000 ) ) ;
#5140=DIRECTION ( 'NONE',  ( 0.000000000000000000, 0.000000000000000000, 1.000000000000000000 ) ) ;
#5141=VERTEX_POINT ( 'NONE', #38712 ) ;
#5142=LINE ( 'NONE', #41793, #4018 ) ;
#5146=DIRECTION ( 'NONE',  ( -1.000000000000000000, -0.000000000000000000, -0.000000000000000000 ) ) ;
#5148=EDGE_LOOP ( 'NONE', ( #31660, #30323, #41809, #40796 ) ) ;
#5149=DIRECTION ( 'NONE',  ( 0.000000000000000000, 0.000000000000000000, 1.000000000000000000 ) ) ;
#5152=DIRECTION ( 'NONE',  ( 1.000000000000000000, 0.000000000000000000, 0.000000000000000000 ) ) ;
#5155=ORIENTED_EDGE ( 'NONE', *, *, #8850, .F. ) ;
#5158=VERTEX_POINT ( 'NONE', #15421 ) ;
#5159=DIRECTION ( 'NONE',  ( -1.000000000000000000, 0.000000000000000000, -0.000000000000000000 ) ) ;
#5160=VECTOR ( 'NONE', #32489, 1000.000000000000000 ) ;
#5164=ORIENTED_EDGE ( 'NONE', *, *, #31561, .F. ) ;
#5166=DIRECTION ( 'NONE',  ( -1.000000000000000000, 0.000000000000000000, 0.000000000000000000 ) ) ;
#5168=DIRECTION ( 'NONE',  ( 0.000000000000000000, 0.9407002666710319039, 0.3392388661180338882 ) ) ;
#5169=FACE_OUTER_BOUND ( 'NONE', #41361, .T. ) ;
#5170=AXIS2_PLACEMENT_3D ( 'NONE', #23123, #33978, #17222 ) ;
#5171=VERTEX_POINT ( 'NONE', #42618 ) ;
#5173=ORIENTED_EDGE ( 'NONE', *, *, #7615, .T. ) ;
#5174=CARTESIAN_POINT ( 'NONE',  ( 17.99999999999999645, 19.12429268481714928, 114.4126803693779948 ) ) ;
#5176=DIRECTION ( 'NONE',  ( 0.000000000000000000, 0.2113826236296247330, -0.9774033898178666746 ) ) ;
#5178=CARTESIAN_POINT ( 'NONE',  ( 9.000000000000001776, -101.8011932243944386, -55.61040422519432980 ) ) ;
#5181=DIRECTION ( 'NONE',  ( -1.000000000000000000, -0.000000000000000000, -0.000000000000000000 ) ) ;
#5184=AXIS2_PLACEMENT_3D ( 'NONE', #38405, #1970, #24946 ) ;
#5186=DIRECTION ( 'NONE',  ( -1.000000000000000000, -0.000000000000000000, 0.000000000000000000 ) ) ;
#5187=DIRECTION ( 'NONE',  ( 0.000000000000000000, 0.8747630845319623871, -0.4845508703326482647 ) ) ;
#5190=ORIENTED_EDGE ( 'NONE', *, *, #29366, .F. ) ;
#5191=CARTESIAN_POINT ( 'NONE',  ( 17.99999999999999645, 111.7974656912331426, -9.465682155094398809 ) ) ;
#5201=EDGE_CURVE ( 'NONE', #2622, #21205, #42556, .T. ) ;
#5202=VECTOR ( 'NONE', #11513, 1000.000000000000000 ) ;
#5207=CYLINDRICAL_SURFACE ( 'NONE', #23740, 59.00000000000000000 ) ;
#5208=ORIENTED_EDGE ( 'NONE', *, *, #35205, .F. ) ;
#5209=DIRECTION ( 'NONE',  ( -1.000000000000000000, 0.000000000000000000, -0.000000000000000000 ) ) ;
#5216=VERTEX_POINT ( 'NONE', #26293 ) ;
#5217=EDGE_CURVE ( 'NONE', #43150, #23930, #9050, .T. ) ;
#5218=CARTESIAN_POINT ( 'NONE',  ( 0.000000000000000000, 66.49630760163724119, -90.36876423295917959 ) ) ;
#5221=CYLINDRICAL_SURFACE ( 'NONE', #29135, 120.5010000000000190 ) ;
#5223=CIRCLE ( 'NONE', #13625, 120.5010000000000190 ) ;
#5225=EDGE_LOOP ( 'NONE', ( #14781, #27174, #36143, #24895 ) ) ;
#5226=LINE ( 'NONE', #11581, #17060 ) ;
#5227=VERTEX_POINT ( 'NONE', #22403 ) ;
#5231=AXIS2_PLACEMENT_3D ( 'NONE', #34425, #4530, #26444 ) ;
#5236=DIRECTION ( 'NONE',  ( 0.000000000000000000, 0.000000000000000000, 1.000000000000000000 ) ) ;
#5237=CARTESIAN_POINT ( 'NONE',  ( 0.000000000000000000, -98.69720329640996681, 60.94966826379877745 ) ) ;
#5238=EDGE_CURVE ( 'NONE', #39353, #20934, #11935, .T. ) ;
#5239=ADVANCED_FACE ( 'NONE', ( #35449 ), #9259, .F. ) ;
#5241=DIRECTION ( 'NONE',  ( -1.000000000000000000, -0.000000000000000000, -0.000000000000000000 ) ) ;
#5242=ADVANCED_FACE ( 'NONE', ( #42413 ), #2895, .F. ) ;
#5243=EDGE_CURVE ( 'NONE', #1492, #12095, #32610, .T. ) ;
#5244=DIRECTION ( 'NONE',  ( 0.000000000000000000, -1.332282330596594362E-14, -1.000000000000000000 ) ) ;
#5248=ORIENTED_EDGE ( 'NONE', *, *, #12173, .F. ) ;
#5261=DIRECTION ( 'NONE',  ( -1.000000000000000000, -0.000000000000000000, -0.000000000000000000 ) ) ;
#5268=VERTEX_POINT ( 'NONE', #31980 ) ;
#5275=VERTEX_POINT ( 'NONE', #20627 ) ;
#5281=ORIENTED_EDGE ( 'NONE', *, *, #31581, .T. ) ;
#5282=CARTESIAN_POINT ( 'NONE',  ( 17.99999999999999645, 112.5120133921113563, -43.14554256760899875 ) ) ;
#5284=CIRCLE ( 'NONE', #41525, 58.99999999999998579 ) ;
#5285=DIRECTION ( 'NONE',  ( 1.000000000000000000, 0.000000000000000000, 0.000000000000000000 ) ) ;
#5289=LINE ( 'NONE', #31921, #29712 ) ;
#5292=AXIS2_PLACEMENT_3D ( 'NONE', #7112, #13690, #3811 ) ;
#5297=EDGE_CURVE ( 'NONE', #3781, #10000, #2137, .T. ) ;
#5299=DIRECTION ( 'NONE',  ( -1.000000000000000000, 0.000000000000000000, 0.000000000000000000 ) ) ;
#5300=DIRECTION ( 'NONE',  ( 0.000000000000000000, -0.7525707698561440173, 0.6585113790650324317 ) ) ;
#5301=VERTEX_POINT ( 'NONE', #20408 ) ;
#5303=EDGE_CURVE ( 'NONE', #41672, #25049, #9696, .T. ) ;
#5305=FACE_OUTER_BOUND ( 'NONE', #37404, .T. ) ;
#5308=CARTESIAN_POINT ( 'NONE',  ( 17.99999999999999645, -98.39501399267926729, -53.91376164787777014 ) ) ;
#5309=CARTESIAN_POINT ( 'NONE',  ( 8.999999999999998224, 110.8621702203448649, 34.14058016547577523 ) ) ;
#5313=EDGE_CURVE ( 'NONE', #31622, #37525, #32120, .T. ) ;
#5314=ORIENTED_EDGE ( 'NONE', *, *, #25942, .F. ) ;
#5315=DIRECTION ( 'NONE',  ( 0.000000000000000000, 0.000000000000000000, 1.000000000000000000 ) ) ;
#5316=LINE ( 'NONE', #5530, #22121 ) ;
#5318=DIRECTION ( 'NONE',  ( -1.000000000000000000, -0.000000000000000000, 0.000000000000000000 ) ) ;
#5319=CIRCLE ( 'NONE', #21412, 58.99999999999999289 ) ;
#5320=AXIS2_PLACEMENT_3D ( 'NONE', #12604, #36781, #6673 ) ;
#5321=CIRCLE ( 'NONE', #36660, 120.5010000000000332 ) ;
#5322=DIRECTION ( 'NONE',  ( 1.000000000000000000, 0.000000000000000000, 0.000000000000000000 ) ) ;
#5323=VERTEX_POINT ( 'NONE', #13863 ) ;
#5325=ORIENTED_EDGE ( 'NONE', *, *, #21329, .F. ) ;
#5328=AXIS2_PLACEMENT_3D ( 'NONE', #6164, #25837, #29741 ) ;
#5332=DIRECTION ( 'NONE',  ( 0.000000000000000000, 0.3140767120219495334, -0.9493976084683810601 ) ) ;
#5336=CARTESIAN_POINT ( 'NONE',  ( 17.99999999999999645, -17.33727698085246871, 110.8498592715972961 ) ) ;
#5337=CIRCLE ( 'NONE', #8820, 120.5010000000000332 ) ;
#5339=CARTESIAN_POINT ( 'NONE',  ( 0.000000000000000000, -110.8621702203446659, -34.14058016547651420 ) ) ;
#5344=AXIS2_PLACEMENT_3D ( 'NONE', #16927, #30210, #23689 ) ;
#5348=EDGE_CURVE ( 'NONE', #28845, #12939, #15459, .T. ) ;
#5350=DIRECTION ( 'NONE',  ( -1.000000000000000000, 0.000000000000000000, 0.000000000000000000 ) ) ;
#5351=EDGE_CURVE ( 'NONE', #22453, #36212, #26584, .T. ) ;
#5353=CIRCLE ( 'NONE', #16417, 59.00000000000000000 ) ;
#5354=ORIENTED_EDGE ( 'NONE', *, *, #36093, .T. ) ;
#5357=ORIENTED_EDGE ( 'NONE', *, *, #37444, .T. ) ;
#5358=DIRECTION ( 'NONE',  ( -1.000000000000000000, -0.000000000000000000, -0.000000000000000000 ) ) ;
#5361=DIRECTION ( 'NONE',  ( -1.000000000000000000, -0.000000000000000000, 0.000000000000000000 ) ) ;
#5362=CIRCLE ( 'NONE', #31127, 59.00000000000000000 ) ;
#5363=VERTEX_POINT ( 'NONE', #3547 ) ;
#5366=CIRCLE ( 'NONE', #6751, 59.00000000000000711 ) ;
#5367=AXIS2_PLACEMENT_3D ( 'NONE', #3106, #2256, #35851 ) ;
#5369=ORIENTED_EDGE ( 'NONE', *, *, #19092, .F. ) ;
#5370=DIRECTION ( 'NONE',  ( 0.000000000000000000, 0.000000000000000000, 1.000000000000000000 ) ) ;
#5374=EDGE_CURVE ( 'NONE', #39340, #37783, #537, .T. ) ;
#5375=CARTESIAN_POINT ( 'NONE',  ( 17.99999999999999645, 0.000000000000000000, 0.000000000000000000 ) ) ;
#5378=ORIENTED_EDGE ( 'NONE', *, *, #38040, .F. ) ;
#5379=( LENGTH_UNIT ( ) NAMED_UNIT ( * ) SI_UNIT ( .MILLI., .METRE. ) );
#5380=DIRECTION ( 'NONE',  ( 0.000000000000000000, -0.3641605752528294104, 0.9313361774523356562 ) ) ;
#5381=AXIS2_PLACEMENT_3D ( 'NONE', #27387, #26527, #36750 ) ;
#5382=FACE_OUTER_BOUND ( 'NONE', #4494, .T. ) ;
#5383=VERTEX_POINT ( 'NONE', #10346 ) ;
#5386=CARTESIAN_POINT ( 'NONE',  ( 9.000000000000001776, -109.3506818544112917, 38.70953859160975696 ) ) ;
#5387=VECTOR ( 'NONE', #7452, 1000.000000000000000 ) ;
#5389=AXIS2_PLACEMENT_3D ( 'NONE', #37134, #41265, #27557 ) ;
#5398=ORIENTED_EDGE ( 'NONE', *, *, #1304, .F. ) ;
#5400=CARTESIAN_POINT ( 'NONE',  ( 0.000000000000000000, -115.5737863835462917, 9.934782381633276316 ) ) ;
#5402=CARTESIAN_POINT ( 'NONE',  ( -10.00000000000000000, 0.000000000000000000, 0.000000000000000000 ) ) ;
#5406=ORIENTED_EDGE ( 'NONE', *, *, #15582, .T. ) ;
#5410=CYLINDRICAL_SURFACE ( 'NONE', #22528, 59.00000000000000000 ) ;
#5411=CARTESIAN_POINT ( 'NONE',  ( 0.000000000000000000, -79.18387647320821543, 84.76976882518735579 ) ) ;
#5413=ORIENTED_EDGE ( 'NONE', *, *, #38339, .F. ) ;
#5414=DIRECTION ( 'NONE',  ( 1.000000000000000000, 0.000000000000000000, 0.000000000000000000 ) ) ;
#5415=ORIENTED_EDGE ( 'NONE', *, *, #39381, .F. ) ;
#5416=VECTOR ( 'NONE', #26624, 1000.000000000000000 ) ;
#5417=ADVANCED_FACE ( 'NONE', ( #17137 ), #36726, .F. ) ;
#5418=VECTOR ( 'NONE', #421, 1000.000000000000000 ) ;
#5419=FACE_OUTER_BOUND ( 'NONE', #15549, .T. ) ;
#5421=AXIS2_PLACEMENT_3D ( 'NONE', #23404, #33411, #3494 ) ;
#5422=VECTOR ( 'NONE', #24357, 1000.000000000000000 ) ;
#5423=EDGE_CURVE ( 'NONE', #39508, #38342, #9617, .T. ) ;
#5428=VERTEX_POINT ( 'NONE', #30203 ) ;
#5431=CYLINDRICAL_SURFACE ( 'NONE', #3327, 59.00000000000000000 ) ;
#5433=CARTESIAN_POINT ( 'NONE',  ( 17.99999999999999645, -40.37724737309996215, -104.6802291180871265 ) ) ;
#5434=ORIENTED_EDGE ( 'NONE', *, *, #301, .F. ) ;
#5437=ORIENTED_EDGE ( 'NONE', *, *, #37646, .F. ) ;
#5440=ADVANCED_FACE ( 'NONE', ( #13635 ), #23249, .F. ) ;
#5442=EDGE_CURVE ( 'NONE', #38197, #22945, #40966, .T. ) ;
#5446=ORIENTED_EDGE ( 'NONE', *, *, #36778, .F. ) ;
#5447=AXIS2_PLACEMENT_3D ( 'NONE', #29002, #35092, #35310 ) ;
#5448=VECTOR ( 'NONE', #8422, 1000.000000000000000 ) ;
#5449=VERTEX_POINT ( 'NONE', #31286 ) ;
#5450=CIRCLE ( 'NONE', #3332, 116.0000000000000000 ) ;
#5451=CARTESIAN_POINT ( 'NONE',  ( 17.99999999999999645, 107.2703412112694963, 32.88383143828500721 ) ) ;
#5454=CARTESIAN_POINT ( 'NONE',  ( 0.000000000000000000, -23.85344185397118011, -113.5209818126993611 ) ) ;
#5455=CARTESIAN_POINT ( 'NONE',  ( 8.999999999999998224, 87.74575819880170968, 75.87280091124503656 ) ) ;
#5456=AXIS2_PLACEMENT_3D ( 'NONE', #15548, #28844, #42108 ) ;
#5461=EDGE_CURVE ( 'NONE', #1856, #24349, #6119, .T. ) ;
#5462=ORIENTED_EDGE ( 'NONE', *, *, #681, .F. ) ;
#5464=VERTEX_POINT ( 'NONE', #5077 ) ;
#5465=DIRECTION ( 'NONE',  ( 0.000000000000000000, 0.000000000000000000, 1.000000000000000000 ) ) ;
#5466=DIRECTION ( 'NONE',  ( -1.000000000000000000, 0.000000000000000000, 0.000000000000000000 ) ) ;
#5472=CARTESIAN_POINT ( 'NONE',  ( 17.99999999999999645, -80.02407177073008882, 78.64108602299921813 ) ) ;
#5473=EDGE_CURVE ( 'NONE', #9695, #16188, #11431, .T. ) ;
#5475=ORIENTED_EDGE ( 'NONE', *, *, #6842, .T. ) ;
#5477=EDGE_CURVE ( 'NONE', #27783, #7249, #18055, .T. ) ;
#5481=CARTESIAN_POINT ( 'NONE',  ( 17.99999999999999645, 97.19627249181192497, -71.22763238166385236 ) ) ;
#5483=DIRECTION ( 'NONE',  ( 0.000000000000000000, 0.1590634960190723812, -0.9872683547213445543 ) ) ;
#5486=ORIENTED_EDGE ( 'NONE', *, *, #4639, .F. ) ;
#5487=DIRECTION ( 'NONE',  ( 0.000000000000000000, 0.000000000000000000, 1.000000000000000000 ) ) ;
#5491=EDGE_CURVE ( 'NONE', #24229, #26181, #24340, .T. ) ;
#5492=CARTESIAN_POINT ( 'NONE',  ( 17.99999999999999645, 112.5120133921107737, 43.14554256761054063 ) ) ;
#5498=ORIENTED_EDGE ( 'NONE', *, *, #13346, .F. ) ;
#5499=CARTESIAN_POINT ( 'NONE',  ( -10.00000000000000000, 0.000000000000000000, 0.000000000000000000 ) ) ;
#5501=VERTEX_POINT ( 'NONE', #20859 ) ;
#5502=CARTESIAN_POINT ( 'NONE',  ( 17.99999999999999645, 0.6819280456844267757, -115.9979955608738607 ) ) ;
#5503=AXIS2_PLACEMENT_3D ( 'NONE', #16741, #6878, #10590 ) ;
#5504=EDGE_CURVE ( 'NONE', #17317, #15115, #40854, .T. ) ;
#5505=VECTOR ( 'NONE', #25907, 1000.000000000000000 ) ;
#5506=CARTESIAN_POINT ( 'NONE',  ( 17.99999999999999645, -108.8880088604279166, 39.99251838045924501 ) ) ;
#5508=VERTEX_POINT ( 'NONE', #11220 ) ;
#5512=CARTESIAN_POINT ( 'NONE',  ( 17.99999999999999645, 0.000000000000000000, 0.000000000000000000 ) ) ;
#5514=DIRECTION ( 'NONE',  ( 0.000000000000000000, 0.000000000000000000, 1.000000000000000000 ) ) ;
#5516=ORIENTED_EDGE ( 'NONE', *, *, #41897, .F. ) ;
#5517=EDGE_CURVE ( 'NONE', #416, #23951, #2642, .T. ) ;
#5518=DIRECTION ( 'NONE',  ( 0.000000000000000000, 0.000000000000000000, 1.000000000000000000 ) ) ;
#5523=CARTESIAN_POINT ( 'NONE',  ( 17.99999999999999645, -78.75547124681429523, 91.20343606296975736 ) ) ;
#5524=VERTEX_POINT ( 'NONE', #7491 ) ;
#5527=EDGE_LOOP ( 'NONE', ( #27665, #5666, #16051, #9460 ) ) ;
#5530=CARTESIAN_POINT ( 'NONE',  ( 17.99999999999999645, 57.69704296431184787, 105.7900857083231472 ) ) ;
#5531=CIRCLE ( 'NONE', #13931, 59.00000000000000000 ) ;
#5532=DIRECTION ( 'NONE',  ( -1.000000000000000000, 0.000000000000000000, 0.000000000000000000 ) ) ;
#5533=CIRCLE ( 'NONE', #2726, 116.0000000000000000 ) ;
#5534=DIRECTION ( 'NONE',  ( 0.000000000000000000, 0.000000000000000000, 1.000000000000000000 ) ) ;
#5538=LINE ( 'NONE', #38263, #18718 ) ;
#5539=ORIENTED_EDGE ( 'NONE', *, *, #17119, .F. ) ;
#5540=CYLINDRICAL_SURFACE ( 'NONE', #10363, 116.0000000000000000 ) ;
#5542=EDGE_CURVE ( 'NONE', #1492, #22195, #41662, .T. ) ;
#5543=ADVANCED_FACE ( 'NONE', ( #4415 ), #37802, .F. ) ;
#5549=VERTEX_POINT ( 'NONE', #9207 ) ;
#5550=CYLINDRICAL_SURFACE ( 'NONE', #17993, 59.00000000000000000 ) ;
#5553=CARTESIAN_POINT ( 'NONE',  ( 17.99999999999999645, -120.3696465864706369, 5.624871700595674540 ) ) ;
#5556=ORIENTED_EDGE ( 'NONE', *, *, #30381, .F. ) ;
#5557=CARTESIAN_POINT ( 'NONE',  ( 17.99999999999999645, -73.78980555658671392, 95.26571049921967926 ) ) ;
#5559=EDGE_LOOP ( 'NONE', ( #39796, #41266, #9743, #7292 ) ) ;
#5562=AXIS2_PLACEMENT_3D ( 'NONE', #5499, #32116, #26217 ) ;
#5565=CARTESIAN_POINT ( 'NONE',  ( 17.99999999999999645, 0.000000000000000000, 0.000000000000000000 ) ) ;
#5567=CARTESIAN_POINT ( 'NONE',  ( 8.999999999999998224, 97.97378550988308632, -62.10585602713663178 ) ) ;
#5570=DIRECTION ( 'NONE',  ( -1.000000000000000000, -0.000000000000000000, 0.000000000000000000 ) ) ;
#5572=CARTESIAN_POINT ( 'NONE',  ( 0.000000000000000000, 35.78484819117633720, 110.3423972910434117 ) ) ;
#5575=EDGE_CURVE ( 'NONE', #23951, #25725, #38879, .T. ) ;
#5576=DIRECTION ( 'NONE',  ( -1.000000000000000000, -0.000000000000000000, -0.000000000000000000 ) ) ;
#5577=EDGE_LOOP ( 'NONE', ( #34210, #39106, #40941, #34667 ) ) ;
#5579=DIRECTION ( 'NONE',  ( 0.000000000000000000, -0.8183027759081623609, -0.5747874102144165942 ) ) ;
#5583=EDGE_LOOP ( 'NONE', ( #9345, #24294, #13935, #24520 ) ) ;
#5585=ORIENTED_EDGE ( 'NONE', *, *, #41064, .T. ) ;
#5586=AXIS2_PLACEMENT_3D ( 'NONE', #18532, #1894, #31582 ) ;
#5587=CIRCLE ( 'NONE', #31393, 59.00000000000000000 ) ;
#5588=LINE ( 'NONE', #8868, #37385 ) ;
#5591=EDGE_CURVE ( 'NONE', #8366, #38244, #5450, .T. ) ;
#5592=DIRECTION ( 'NONE',  ( -1.000000000000000000, -0.000000000000000000, -0.000000000000000000 ) ) ;
#5596=EDGE_CURVE ( 'NONE', #32579, #28564, #33319, .T. ) ;
#5598=ORIENTED_EDGE ( 'NONE', *, *, #43160, .F. ) ;
#5600=DIRECTION ( 'NONE',  ( 0.000000000000000000, -0.6382441836448262684, 0.7698339834299010587 ) ) ;
#5613=DIRECTION ( 'NONE',  ( -1.000000000000000000, 0.000000000000000000, -0.000000000000000000 ) ) ;
#5614=ORIENTED_EDGE ( 'NONE', *, *, #42203, .T. ) ;
#5615=CIRCLE ( 'NONE', #12610, 58.99999999999999289 ) ;
#5616=CARTESIAN_POINT ( 'NONE',  ( 0.000000000000000000, 0.000000000000000000, 0.000000000000000000 ) ) ;
#5618=AXIS2_PLACEMENT_3D ( 'NONE', #9036, #5757, #22393 ) ;
#5621=ORIENTED_EDGE ( 'NONE', *, *, #39526, .F. ) ;
#5625=CYLINDRICAL_SURFACE ( 'NONE', #18488, 116.0000000000000000 ) ;
#5628=ORIENTED_EDGE ( 'NONE', *, *, #27229, .F. ) ;
#5630=CARTESIAN_POINT ( 'NONE',  ( 0.000000000000000000, -46.12538073176427389, 111.3235835452210125 ) ) ;
#5631=ORIENTED_EDGE ( 'NONE', *, *, #8893, .F. ) ;
#5635=CARTESIAN_POINT ( 'NONE',  ( 17.99999999999999645, 16.77566611177940104, -119.3275660838940553 ) ) ;
#5636=LINE ( 'NONE', #16126, #11592 ) ;
#5638=ADVANCED_FACE ( 'NONE', ( #22770 ), #38658, .F. ) ;
#5639=CARTESIAN_POINT ( 'NONE',  ( 17.99999999999999645, 86.84764344323065188, -76.89919913989662348 ) ) ;
#5641=LINE ( 'NONE', #22691, #41136 ) ;
#5642=ORIENTED_EDGE ( 'NONE', *, *, #31701, .T. ) ;
#5645=CIRCLE ( 'NONE', #35591, 59.00000000000000000 ) ;
#5648=DIRECTION ( 'NONE',  ( -1.000000000000000000, -0.000000000000000000, 0.000000000000000000 ) ) ;
#5649=EDGE_CURVE ( 'NONE', #17781, #22195, #3293, .T. ) ;
#5652=ADVANCED_FACE ( 'NONE', ( #2639 ), #19281, .F. ) ;
#5653=ORIENTED_EDGE ( 'NONE', *, *, #4465, .T. ) ;
#5657=DIRECTION ( 'NONE',  ( -1.000000000000000000, -0.000000000000000000, -0.000000000000000000 ) ) ;
#5661=EDGE_LOOP ( 'NONE', ( #31563, #40413, #28059, #961 ) ) ;
#5663=ORIENTED_EDGE ( 'NONE', *, *, #25017, .F. ) ;
#5666=ORIENTED_EDGE ( 'NONE', *, *, #17547, .F. ) ;
#5667=DIRECTION ( 'NONE',  ( 1.000000000000000000, 0.000000000000000000, 0.000000000000000000 ) ) ;
#5669=EDGE_CURVE ( 'NONE', #16679, #30476, #15213, .T. ) ;
#5673=EDGE_CURVE ( 'NONE', #5841, #36212, #21921, .T. ) ;
#5675=FACE_OUTER_BOUND ( 'NONE', #6334, .T. ) ;
#5676=AXIS2_PLACEMENT_3D ( 'NONE', #36010, #8986, #38646 ) ;
#5677=EDGE_CURVE ( 'NONE', #38358, #31625, #25666, .T. ) ;
#5682=DIRECTION ( 'NONE',  ( -1.000000000000000000, -0.000000000000000000, -0.000000000000000000 ) ) ;
#5687=PRODUCT ( 'internal spur gear_iso_ISO - Internal spur gear 2M 118T 20PA 18FW ---S118S260OD 1.0AF', 'internal spur gear_iso_ISO - Internal spur gear 2M 118T 20PA 18FW ---S118S260OD 1.0AF', '', ( #10013 ) ) ;
#5691=DIRECTION ( 'NONE',  ( 0.000000000000000000, 0.3140767120219429276, 0.9493976084683832806 ) ) ;
#5696=LINE ( 'NONE', #38425, #33257 ) ;
#5698=ADVANCED_FACE ( 'NONE', ( #20356 ), #30363, .F. ) ;
#5699=VERTEX_POINT ( 'NONE', #9847 ) ;
#5700=CARTESIAN_POINT ( 'NONE',  ( 17.99999999999999645, -84.09610293794020208, -74.27057253243097534 ) ) ;
#5703=VERTEX_POINT ( 'NONE', #36234 ) ;
#5705=VECTOR ( 'NONE', #7846, 1000.000000000000000 ) ;
#5710=CARTESIAN_POINT ( 'NONE',  ( 17.99999999999999645, -67.32409792376445523, -89.75376489259431878 ) ) ;
#5713=DIRECTION ( 'NONE',  ( 0.000000000000000000, 0.000000000000000000, 1.000000000000000000 ) ) ;
#5715=DIRECTION ( 'NONE',  ( 0.000000000000000000, 0.000000000000000000, 1.000000000000000000 ) ) ;
#5717=VERTEX_POINT ( 'NONE', #445 ) ;
#5719=ADVANCED_FACE ( 'NONE', ( #7000 ), #36445, .F. ) ;
#5720=ORIENTED_EDGE ( 'NONE', *, *, #1110, .F. ) ;
#5727=CIRCLE ( 'NONE', #30138, 120.5010000000000474 ) ;
#5728=ORIENTED_EDGE ( 'NONE', *, *, #11920, .F. ) ;
#5730=VERTEX_POINT ( 'NONE', #9644 ) ;
#5733=EDGE_CURVE ( 'NONE', #27433, #9297, #27741, .T. ) ;
#5735=DIRECTION ( 'NONE',  ( 0.000000000000000000, 0.000000000000000000, 1.000000000000000000 ) ) ;
#5737=DIRECTION ( 'NONE',  ( 1.000000000000000000, 0.000000000000000000, 0.000000000000000000 ) ) ;
#5741=DIRECTION ( 'NONE',  ( -1.000000000000000000, 0.000000000000000000, 0.000000000000000000 ) ) ;
#5746=EDGE_LOOP ( 'NONE', ( #39123, #42293, #12435, #13480 ) ) ;
#5748=ORIENTED_EDGE ( 'NONE', *, *, #37318, .T. ) ;
#5752=DIRECTION ( 'NONE',  ( 1.000000000000000000, 0.000000000000000000, -0.000000000000000000 ) ) ;
#5753=ORIENTED_EDGE ( 'NONE', *, *, #40195, .T. ) ;
#5755=ADVANCED_FACE ( 'NONE', ( #20568 ), #32970, .F. ) ;
#5756=ORIENTED_EDGE ( 'NONE', *, *, #24118, .F. ) ;
#5757=DIRECTION ( 'NONE',  ( -1.000000000000000000, 0.000000000000000000, 0.000000000000000000 ) ) ;
#5763=FACE_OUTER_BOUND ( 'NONE', #36648, .T. ) ;
#5764=DIRECTION ( 'NONE',  ( 1.000000000000000000, 0.000000000000000000, 0.000000000000000000 ) ) ;
#5765=AXIS2_PLACEMENT_3D ( 'NONE', #9733, #26334, #5600 ) ;
#5766=DIRECTION ( 'NONE',  ( 0.000000000000000000, 0.000000000000000000, 1.000000000000000000 ) ) ;
#5767=ORIENTED_EDGE ( 'NONE', *, *, #5575, .F. ) ;
#5769=VERTEX_POINT ( 'NONE', #16659 ) ;
#5770=DIRECTION ( 'NONE',  ( 0.000000000000000000, 0.7865515558026436871, -0.6175246149461904865 ) ) ;
#5777=ORIENTED_EDGE ( 'NONE', *, *, #9722, .F. ) ;
#5778=ADVANCED_FACE ( 'NONE', ( #3048 ), #29502, .F. ) ;
#5780=CARTESIAN_POINT ( 'NONE',  ( 17.99999999999999645, 0.000000000000000000, 0.000000000000000000 ) ) ;
#5781=ORIENTED_EDGE ( 'NONE', *, *, #35251, .T. ) ;
#5786=CARTESIAN_POINT ( 'NONE',  ( 0.000000000000000000, 0.000000000000000000, 0.000000000000000000 ) ) ;
#5787=ADVANCED_FACE ( 'NONE', ( #30156 ), #10061, .F. ) ;
#5789=ORIENTED_EDGE ( 'NONE', *, *, #12855, .F. ) ;
#5791=ORIENTED_EDGE ( 'NONE', *, *, #25713, .T. ) ;
#5793=CYLINDRICAL_SURFACE ( 'NONE', #20743, 59.00000000000000000 ) ;
#5794=DIRECTION ( 'NONE',  ( -1.000000000000000000, 0.000000000000000000, 0.000000000000000000 ) ) ;
#5796=CYLINDRICAL_SURFACE ( 'NONE', #9845, 120.5010000000000190 ) ;
#5799=EDGE_CURVE ( 'NONE', #26752, #38997, #16872, .T. ) ;
#5802=CIRCLE ( 'NONE', #35111, 58.99999999999999289 ) ;
#5805=ADVANCED_FACE ( 'NONE', ( #20799 ), #34061, .F. ) ;
#5806=DIRECTION ( 'NONE',  ( 1.000000000000000000, 0.000000000000000000, 0.000000000000000000 ) ) ;
#5809=ORIENTED_EDGE ( 'NONE', *, *, #13030, .T. ) ;
#5810=ORIENTED_EDGE ( 'NONE', *, *, #32657, .T. ) ;
#5811=DIRECTION ( 'NONE',  ( -1.000000000000000000, 0.000000000000000000, -0.000000000000000000 ) ) ;
#5812=CARTESIAN_POINT ( 'NONE',  ( 17.99999999999999645, -114.1157422997284669, 20.82300072952894610 ) ) ;
#5817=FACE_OUTER_BOUND ( 'NONE', #9061, .T. ) ;
#5819=DIRECTION ( 'NONE',  ( 0.000000000000000000, 0.000000000000000000, 1.000000000000000000 ) ) ;
#5820=EDGE_LOOP ( 'NONE', ( #29759, #30479, #41113, #19566 ) ) ;
#5822=VERTEX_POINT ( 'NONE', #14012 ) ;
#5823=CIRCLE ( 'NONE', #7916, 59.00000000000000000 ) ;
#5824=DIRECTION ( 'NONE',  ( 0.000000000000000000, 0.05322217484217219019, 0.9985826956767622775 ) ) ;
#5829=EDGE_CURVE ( 'NONE', #5268, #29453, #30590, .T. ) ;
#5831=EDGE_CURVE ( 'NONE', #33525, #34589, #16604, .T. ) ;
#5832=DIRECTION ( 'NONE',  ( 0.000000000000000000, 0.000000000000000000, 1.000000000000000000 ) ) ;
#5841=VERTEX_POINT ( 'NONE', #34267 ) ;
#5843=EDGE_CURVE ( 'NONE', #2052, #30264, #34476, .T. ) ;
#5849=CARTESIAN_POINT ( 'NONE',  ( 0.000000000000000000, 0.000000000000000000, 0.000000000000000000 ) ) ;
#5850=CARTESIAN_POINT ( 'NONE',  ( 0.000000000000000000, -86.84764344322910290, -76.89919913989835720 ) ) ;
#5851=ORIENTED_EDGE ( 'NONE', *, *, #33988, .T. ) ;
#5853=CARTESIAN_POINT ( 'NONE',  ( 0.000000000000000000, -86.84764344323014029, 76.89919913989720612 ) ) ;
#5855=DIRECTION ( 'NONE',  ( 0.000000000000000000, 0.7865515558026436871, -0.6175246149461902645 ) ) ;
#5856=VERTEX_POINT ( 'NONE', #4819 ) ;
#5857=ADVANCED_FACE ( 'NONE', ( #7438 ), #1530, .F. ) ;
#5858=EDGE_CURVE ( 'NONE', #34567, #19682, #4451, .T. ) ;
#5859=EDGE_LOOP ( 'NONE', ( #25757, #36871, #28869, #12411 ) ) ;
#5862=CARTESIAN_POINT ( 'NONE',  ( 17.99999999999999645, 0.000000000000000000, 0.000000000000000000 ) ) ;
#5863=DIRECTION ( 'NONE',  ( -1.000000000000000000, -0.000000000000000000, 0.000000000000000000 ) ) ;
#5865=CARTESIAN_POINT ( 'NONE',  ( 17.99999999999999645, -109.4038418350900059, -50.51029986767660773 ) ) ;
#5870=ORIENTED_EDGE ( 'NONE', *, *, #41967, .T. ) ;
#5873=ORIENTED_EDGE ( 'NONE', *, *, #37787, .T. ) ;
#5876=EDGE_CURVE ( 'NONE', #30917, #29560, #14882, .T. ) ;
#5877=FACE_OUTER_BOUND ( 'NONE', #42942, .T. ) ;
#5880=AXIS2_PLACEMENT_3D ( 'NONE', #3421, #16999, #26377 ) ;
#5882=CARTESIAN_POINT ( 'NONE',  ( 0.000000000000000000, -11.65176648920959757, -115.4133282497343487 ) ) ;
#5886=EDGE_CURVE ( 'NONE', #37125, #35721, #27971, .T. ) ;
#5888=CARTESIAN_POINT ( 'NONE',  ( 17.99999999999999645, -58.30069736313732420, 100.2847380560565256 ) ) ;
#5890=FACE_OUTER_BOUND ( 'NONE', #37355, .T. ) ;
#5891=EDGE_CURVE ( 'NONE', #26858, #8245, #24965, .T. ) ;
#5894=LINE ( 'NONE', #36205, #54 ) ;
#5895=ORIENTED_EDGE ( 'NONE', *, *, #35579, .F. ) ;
#5901=CARTESIAN_POINT ( 'NONE',  ( 17.99999999999999645, -111.7974656912330715, 9.465682155095141326 ) ) ;
#5902=AXIS2_PLACEMENT_3D ( 'NONE', #18291, #7770, #1866 ) ;
#5905=ORIENTED_EDGE ( 'NONE', *, *, #17284, .F. ) ;
#5906=EDGE_CURVE ( 'NONE', #40508, #8627, #2104, .T. ) ;
#5909=ORIENTED_EDGE ( 'NONE', *, *, #30581, .T. ) ;
#5910=CARTESIAN_POINT ( 'NONE',  ( 17.99999999999999645, -79.18387647320821543, 84.76976882518735579 ) ) ;
#5912=ORIENTED_EDGE ( 'NONE', *, *, #32267, .T. ) ;
#5915=CARTESIAN_POINT ( 'NONE',  ( 0.000000000000000000, -99.97660604679919061, -67.26937820704989690 ) ) ;
#5916=ORIENTED_EDGE ( 'NONE', *, *, #32138, .T. ) ;
#5919=CARTESIAN_POINT ( 'NONE',  ( 17.99999999999999645, 72.00556975657703163, 86.04342158279412445 ) ) ;
#5924=CIRCLE ( 'NONE', #42136, 120.5010000000000332 ) ;
#5926=ORIENTED_EDGE ( 'NONE', *, *, #40859, .T. ) ;
#5928=ORIENTED_EDGE ( 'NONE', *, *, #32480, .T. ) ;
#5929=DIRECTION ( 'NONE',  ( 1.000000000000000000, 0.000000000000000000, 0.000000000000000000 ) ) ;
#5931=ORIENTED_EDGE ( 'NONE', *, *, #16505, .T. ) ;
#5935=ADVANCED_FACE ( 'NONE', ( #37749 ), #7866, .F. ) ;
#5937=EDGE_LOOP ( 'NONE', ( #27562, #24563, #10407, #27378 ) ) ;
#5938=ORIENTED_EDGE ( 'NONE', *, *, #14457, .T. ) ;
#5939=CYLINDRICAL_SURFACE ( 'NONE', #21417, 120.5010000000000190 ) ;
#5941=FACE_OUTER_BOUND ( 'NONE', #33826, .T. ) ;
#5943=FACE_OUTER_BOUND ( 'NONE', #35611, .T. ) ;
#5945=CARTESIAN_POINT ( 'NONE',  ( 17.99999999999999645, 0.000000000000000000, 0.000000000000000000 ) ) ;
#5948=ORIENTED_EDGE ( 'NONE', *, *, #26794, .F. ) ;
#5952=DIRECTION ( 'NONE',  ( -1.000000000000000000, 0.000000000000000000, -0.000000000000000000 ) ) ;
#5953=DIRECTION ( 'NONE',  ( 1.000000000000000000, 0.000000000000000000, 0.000000000000000000 ) ) ;
#5954=EDGE_LOOP ( 'NONE', ( #40867, #3731, #36935, #14311 ) ) ;
#5955=DIRECTION ( 'NONE',  ( -1.000000000000000000, -0.000000000000000000, -0.000000000000000000 ) ) ;
#5956=AXIS2_PLACEMENT_3D ( 'NONE', #15461, #1252, #11524 ) ;
#5962=VERTEX_POINT ( 'NONE', #3925 ) ;
#5963=AXIS2_PLACEMENT_3D ( 'NONE', #10192, #6915, #20275 ) ;
#5964=DIRECTION ( 'NONE',  ( -1.000000000000000000, 0.000000000000000000, -0.000000000000000000 ) ) ;
#5967=CIRCLE ( 'NONE', #33130, 120.5010000000000190 ) ;
#5970=CARTESIAN_POINT ( 'NONE',  ( 17.99999999999999645, 107.2885202478273783, -54.86040852957203384 ) ) ;
#5972=AXIS2_PLACEMENT_3D ( 'NONE', #5919, #13363, #22765 ) ;
#5973=ORIENTED_EDGE ( 'NONE', *, *, #2844, .T. ) ;
#5974=FACE_OUTER_BOUND ( 'NONE', #37328, .T. ) ;
#5978=DIRECTION ( 'NONE',  ( -1.000000000000000000, 0.000000000000000000, 0.000000000000000000 ) ) ;
#5980=CARTESIAN_POINT ( 'NONE',  ( 17.99999999999999645, -42.87700105098682002, 107.7847984684003393 ) ) ;
#5981=ORIENTED_EDGE ( 'NONE', *, *, #17609, .F. ) ;
#5982=DIRECTION ( 'NONE',  ( -1.000000000000000000, 0.000000000000000000, -0.000000000000000000 ) ) ;
#5983=EDGE_CURVE ( 'NONE', #19271, #710, #39712, .T. ) ;
#5984=ORIENTED_EDGE ( 'NONE', *, *, #23591, .T. ) ;
#5986=DIRECTION ( 'NONE',  ( 0.000000000000000000, 0.5963673585385027565, -0.8027116379309627847 ) ) ;
#5990=DIRECTION ( 'NONE',  ( 0.000000000000000000, 0.5963673585385025344, -0.8027116379309628957 ) ) ;
#5991=CIRCLE ( 'NONE', #42914, 120.5010000000000332 ) ;
#5992=EDGE_LOOP ( 'NONE', ( #35502, #22317, #135, #35553 ) ) ;
#5996=DIRECTION ( 'NONE',  ( 0.000000000000000000, -0.3140767120219362107, -0.9493976084683853900 ) ) ;
#5997=EDGE_CURVE ( 'NONE', #39703, #5769, #42089, .T. ) ;
#5998=AXIS2_PLACEMENT_3D ( 'NONE', #14518, #17803, #34335 ) ;
#5999=ORIENTED_EDGE ( 'NONE', *, *, #24247, .F. ) ;
#6001=EDGE_CURVE ( 'NONE', #10513, #31219, #38336, .T. ) ;
#6006=CIRCLE ( 'NONE', #35951, 59.00000000000000000 ) ;
#6009=VERTEX_POINT ( 'NONE', #28613 ) ;
#6010=CARTESIAN_POINT ( 'NONE',  ( 17.99999999999999645, 115.5737863835462349, 9.934782381634081005 ) ) ;
#6012=CARTESIAN_POINT ( 'NONE',  ( 9.000000000000001776, 104.6166166098452379, -50.11350645393572023 ) ) ;
#6013=DIRECTION ( 'NONE',  ( 0.000000000000000000, 0.000000000000000000, 1.000000000000000000 ) ) ;
#6014=DIRECTION ( 'NONE',  ( 1.000000000000000000, 0.000000000000000000, 0.000000000000000000 ) ) ;
#6018=DIRECTION ( 'NONE',  ( -1.000000000000000000, 0.000000000000000000, 0.000000000000000000 ) ) ;
#6021=ADVANCED_FACE ( 'NONE', ( #35550 ), #25353, .F. ) ;
#6023=EDGE_CURVE ( 'NONE', #16211, #19378, #30010, .T. ) ;
#6024=DIRECTION ( 'NONE',  ( -1.000000000000000000, 0.000000000000000000, 0.000000000000000000 ) ) ;
#6027=EDGE_CURVE ( 'NONE', #13915, #8937, #11896, .T. ) ;
#6028=CIRCLE ( 'NONE', #1855, 59.00000000000000000 ) ;
#6029=AXIS2_PLACEMENT_3D ( 'NONE', #18938, #32831, #29369 ) ;
#6034=CARTESIAN_POINT ( 'NONE',  ( 17.99999999999999645, -84.77518783075045405, -73.49448960231443095 ) ) ;
#6037=FACE_OUTER_BOUND ( 'NONE', #40237, .T. ) ;
#6041=ORIENTED_EDGE ( 'NONE', *, *, #41870, .F. ) ;
#6043=VECTOR ( 'NONE', #1627, 1000.000000000000000 ) ;
#6044=VERTEX_POINT ( 'NONE', #25147 ) ;
#6045=CYLINDRICAL_SURFACE ( 'NONE', #15543, 59.00000000000000000 ) ;
#6047=AXIS2_PLACEMENT_3D ( 'NONE', #42615, #42186, #12346 ) ;
#6050=ORIENTED_EDGE ( 'NONE', *, *, #13450, .T. ) ;
#6052=CARTESIAN_POINT ( 'NONE',  ( 0.000000000000000000, 83.58328028049768932, -80.43528614701241963 ) ) ;
#6061=AXIS2_PLACEMENT_3D ( 'NONE', #5093, #41301, #11447 ) ;
#6062=ORIENTED_EDGE ( 'NONE', *, *, #2691, .F. ) ;
#6063=AXIS2_PLACEMENT_3D ( 'NONE', #15335, #1763, #11392 ) ;
#6065=DIRECTION ( 'NONE',  ( 0.000000000000000000, 0.000000000000000000, -1.000000000000000000 ) ) ;
#6066=CARTESIAN_POINT ( 'NONE',  ( 17.99999999999999645, -98.39501399267926729, -53.91376164787777014 ) ) ;
#6068=FACE_OUTER_BOUND ( 'NONE', #25706, .T. ) ;
#6069=ORIENTED_EDGE ( 'NONE', *, *, #39271, .F. ) ;
#6074=CARTESIAN_POINT ( 'NONE',  ( 17.99999999999999645, -114.6488492393081913, 37.09625815499973100 ) ) ;
#6076=ORIENTED_EDGE ( 'NONE', *, *, #9105, .T. ) ;
#6077=DIRECTION ( 'NONE',  ( -1.000000000000000000, -0.000000000000000000, -0.000000000000000000 ) ) ;
#6078=ADVANCED_FACE ( 'NONE', ( #5877 ), #19233, .F. ) ;
#6080=EDGE_CURVE ( 'NONE', #10403, #33606, #12601, .T. ) ;
#6085=DIRECTION ( 'NONE',  ( 0.000000000000000000, 0.000000000000000000, 1.000000000000000000 ) ) ;
#6086=ORIENTED_EDGE ( 'NONE', *, *, #13707, .T. ) ;
#6091=DIRECTION ( 'NONE',  ( 1.000000000000000000, 0.000000000000000000, 0.000000000000000000 ) ) ;
#6094=CARTESIAN_POINT ( 'NONE',  ( 17.99999999999999645, 27.83061035787113369, -117.2431154827794586 ) ) ;
#6097=VECTOR ( 'NONE', #28500, 1000.000000000000000 ) ;
#6098=CARTESIAN_POINT ( 'NONE',  ( 17.99999999999999645, 0.000000000000000000, 0.000000000000000000 ) ) ;
#6099=ORIENTED_EDGE ( 'NONE', *, *, #9535, .F. ) ;
#6100=LINE ( 'NONE', #42307, #2236 ) ;
#6106=DIRECTION ( 'NONE',  ( 0.000000000000000000, 0.7525707698561353576, 0.6585113790650422017 ) ) ;
#6107=ORIENTED_EDGE ( 'NONE', *, *, #43108, .F. ) ;
#6111=FACE_OUTER_BOUND ( 'NONE', #4371, .T. ) ;
#6112=CIRCLE ( 'NONE', #9582, 59.00000000000000000 ) ;
#6113=CARTESIAN_POINT ( 'NONE',  ( 17.99999999999999645, 0.000000000000000000, 0.000000000000000000 ) ) ;
#6114=CARTESIAN_POINT ( 'NONE',  ( 17.99999999999999645, 0.000000000000000000, 0.000000000000000000 ) ) ;
#6115=CIRCLE ( 'NONE', #31894, 59.00000000000000000 ) ;
#6117=ORIENTED_EDGE ( 'NONE', *, *, #10122, .F. ) ;
#6119=CIRCLE ( 'NONE', #29169, 120.5010000000000332 ) ;
#6120=DIRECTION ( 'NONE',  ( 1.000000000000000000, 0.000000000000000000, 0.000000000000000000 ) ) ;
#6125=AXIS2_PLACEMENT_3D ( 'NONE', #26423, #13340, #10032 ) ;
#6127=EDGE_CURVE ( 'NONE', #19436, #17354, #696, .T. ) ;
#6128=ORIENTED_EDGE ( 'NONE', *, *, #32748, .F. ) ;
#6130=EDGE_LOOP ( 'NONE', ( #35914, #39415, #8592, #13142 ) ) ;
#6135=ORIENTED_EDGE ( 'NONE', *, *, #42606, .F. ) ;
#6141=EDGE_CURVE ( 'NONE', #28841, #16818, #35555, .T. ) ;
#6142=FACE_OUTER_BOUND ( 'NONE', #32478, .T. ) ;
#6144=DIRECTION ( 'NONE',  ( 1.000000000000000000, 0.000000000000000000, 0.000000000000000000 ) ) ;
#6149=CARTESIAN_POINT ( 'NONE',  ( -10.00000000000000000, 0.000000000000000000, 0.000000000000000000 ) ) ;
#6151=ORIENTED_EDGE ( 'NONE', *, *, #16164, .T. ) ;
#6154=ORIENTED_EDGE ( 'NONE', *, *, #6001, .T. ) ;
#6157=ORIENTED_EDGE ( 'NONE', *, *, #3246, .T. ) ;
#6158=CARTESIAN_POINT ( 'NONE',  ( 0.000000000000000000, -111.1352304691228596, 15.40237066878559524 ) ) ;
#6162=ORIENTED_EDGE ( 'NONE', *, *, #39422, .T. ) ;
#6164=CARTESIAN_POINT ( 'NONE',  ( 17.99999999999999645, -95.38615066513943930, -59.07414607872924250 ) ) ;
#6165=DIRECTION ( 'NONE',  ( 0.000000000000000000, 0.1590634960190654978, 0.9872683547213455535 ) ) ;
#6166=FACE_OUTER_BOUND ( 'NONE', #23004, .T. ) ;
#6168=DIRECTION ( 'NONE',  ( 1.000000000000000000, 0.000000000000000000, 0.000000000000000000 ) ) ;
#6170=DIRECTION ( 'NONE',  ( 1.000000000000000000, 0.000000000000000000, 0.000000000000000000 ) ) ;
#6171=ORIENTED_EDGE ( 'NONE', *, *, #14526, .F. ) ;
#6173=LINE ( 'NONE', #19732, #22876 ) ;
#6177=EDGE_CURVE ( 'NONE', #36925, #25806, #34881, .T. ) ;
#6178=LINE ( 'NONE', #19523, #34500 ) ;
#6179=VERTEX_POINT ( 'NONE', #22949 ) ;
#6181=VERTEX_POINT ( 'NONE', #26185 ) ;
#6182=CIRCLE ( 'NONE', #42397, 59.00000000000000000 ) ;
#6184=CARTESIAN_POINT ( 'NONE',  ( 17.99999999999999645, 100.8494052988171035, 65.95368414178945216 ) ) ;
#6185=ORIENTED_EDGE ( 'NONE', *, *, #7899, .T. ) ;
#6189=ORIENTED_EDGE ( 'NONE', *, *, #43108, .T. ) ;
#6190=DIRECTION ( 'NONE',  ( 1.000000000000000000, 0.000000000000000000, 0.000000000000000000 ) ) ;
#6193=DIRECTION ( 'NONE',  ( -1.000000000000000000, -0.000000000000000000, -0.000000000000000000 ) ) ;
#6194=ORIENTED_EDGE ( 'NONE', *, *, #1250, .T. ) ;
#6197=CYLINDRICAL_SURFACE ( 'NONE', #9850, 59.00000000000000000 ) ;
#6199=FACE_OUTER_BOUND ( 'NONE', #13127, .T. ) ;
#6200=VERTEX_POINT ( 'NONE', #39458 ) ;
#6201=CARTESIAN_POINT ( 'NONE',  ( 17.99999999999999645, -84.09610293794020208, -74.27057253243097534 ) ) ;
#6202=EDGE_LOOP ( 'NONE', ( #20790, #7046, #427, #34379 ) ) ;
#6208=DIRECTION ( 'NONE',  ( -1.000000000000000000, -0.000000000000000000, -0.000000000000000000 ) ) ;
#6209=CIRCLE ( 'NONE', #1318, 116.0000000000000000 ) ;
#6211=VECTOR ( 'NONE', #37128, 1000.000000000000000 ) ;
#6215=ORIENTED_EDGE ( 'NONE', *, *, #42389, .T. ) ;
#6216=CARTESIAN_POINT ( 'NONE',  ( 17.99999999999999645, 40.13512380274120517, -113.6206972269517905 ) ) ;
#6218=CARTESIAN_POINT ( 'NONE',  ( 17.99999999999999645, 35.54274411428215075, -115.1399337407602701 ) ) ;
#6225=ORIENTED_EDGE ( 'NONE', *, *, #28948, .T. ) ;
#6227=DIRECTION ( 'NONE',  ( 0.000000000000000000, 0.1062934856473656403, -0.9943348002101370930 ) ) ;
#6233=DIRECTION ( 'NONE',  ( 0.000000000000000000, 0.000000000000000000, 1.000000000000000000 ) ) ;
#6235=FACE_OUTER_BOUND ( 'NONE', #26805, .T. ) ;
#6240=AXIS2_PLACEMENT_3D ( 'NONE', #27727, #27283, #40553 ) ;
#6242=CARTESIAN_POINT ( 'NONE',  ( 17.99999999999999645, -41.33768078145568836, 104.3046912715539918 ) ) ;
#6246=DIRECTION ( 'NONE',  ( 0.000000000000000000, 0.000000000000000000, -1.000000000000000000 ) ) ;
#6249=EDGE_CURVE ( 'NONE', #23796, #32501, #41851, .T. ) ;
#6254=ORIENTED_EDGE ( 'NONE', *, *, #24685, .F. ) ;
#6255=CARTESIAN_POINT ( 'NONE',  ( 0.000000000000000000, -41.60679253225836760, 108.2814610871944581 ) ) ;
#6256=CYLINDRICAL_SURFACE ( 'NONE', #31749, 59.00000000000000000 ) ;
#6259=VERTEX_POINT ( 'NONE', #16825 ) ;
#6260=DIRECTION ( 'NONE',  ( -1.000000000000000000, 0.000000000000000000, -0.000000000000000000 ) ) ;
#6262=AXIS2_PLACEMENT_3D ( 'NONE', #5402, #18328, #31589 ) ;
#6265=DIRECTION ( 'NONE',  ( -1.000000000000000000, -0.000000000000000000, -0.000000000000000000 ) ) ;
#6268=EDGE_CURVE ( 'NONE', #10288, #30398, #15426, .T. ) ;
#6271=ORIENTED_EDGE ( 'NONE', *, *, #29299, .T. ) ;
#6276=CARTESIAN_POINT ( 'NONE',  ( -10.00000000000000000, 0.000000000000000000, 130.0000000000000000 ) ) ;
#6280=EDGE_CURVE ( 'NONE', #30344, #12090, #722, .T. ) ;
#6286=DIRECTION ( 'NONE',  ( -1.000000000000000000, 0.000000000000000000, 0.000000000000000000 ) ) ;
#6289=EDGE_CURVE ( 'NONE', #40994, #19328, #17513, .T. ) ;
#6290=ORIENTED_EDGE ( 'NONE', *, *, #8562, .F. ) ;
#6291=FACE_OUTER_BOUND ( 'NONE', #17517, .T. ) ;
#6295=DIRECTION ( 'NONE',  ( 0.000000000000000000, 0.000000000000000000, 1.000000000000000000 ) ) ;
#6297=DIRECTION ( 'NONE',  ( -1.000000000000000000, -0.000000000000000000, -0.000000000000000000 ) ) ;
#6299=CYLINDRICAL_SURFACE ( 'NONE', #11598, 120.5010000000000190 ) ;
#6303=ORIENTED_EDGE ( 'NONE', *, *, #3371, .F. ) ;
#6305=EDGE_CURVE ( 'NONE', #815, #36642, #36262, .T. ) ;
#6313=AXIS2_PLACEMENT_3D ( 'NONE', #19659, #32926, #16371 ) ;
#6315=VERTEX_POINT ( 'NONE', #7607 ) ;
#6317=EDGE_CURVE ( 'NONE', #26249, #2667, #4216, .T. ) ;
#6318=EDGE_CURVE ( 'NONE', #11189, #10403, #27926, .T. ) ;
#6320=CIRCLE ( 'NONE', #38398, 120.5010000000000332 ) ;
#6324=DIRECTION ( 'NONE',  ( 0.000000000000000000, 0.000000000000000000, 1.000000000000000000 ) ) ;
#6328=CARTESIAN_POINT ( 'NONE',  ( -10.00000000000000000, 0.000000000000000000, 0.000000000000000000 ) ) ;
#6334=EDGE_LOOP ( 'NONE', ( #27411, #28099, #42166, #41563 ) ) ;
#6337=ORIENTED_EDGE ( 'NONE', *, *, #19099, .F. ) ;
#6339=ORIENTED_EDGE ( 'NONE', *, *, #41841, .F. ) ;
#6340=ORIENTED_EDGE ( 'NONE', *, *, #4345, .T. ) ;
#6343=VERTEX_POINT ( 'NONE', #41181 ) ;
#6344=DIRECTION ( 'NONE',  ( -1.000000000000000000, -0.000000000000000000, -0.000000000000000000 ) ) ;
#6345=EDGE_CURVE ( 'NONE', #30314, #10921, #28647, .T. ) ;
#6347=EDGE_CURVE ( 'NONE', #41792, #18580, #7166, .T. ) ;
#6348=AXIS2_PLACEMENT_3D ( 'NONE', #21771, #18491, #17628 ) ;
#6349=CYLINDRICAL_SURFACE ( 'NONE', #36598, 59.00000000000000000 ) ;
#6351=CARTESIAN_POINT ( 'NONE',  ( 17.99999999999999645, 0.000000000000000000, 0.000000000000000000 ) ) ;
#6354=LINE ( 'NONE', #28864, #40518 ) ;
#6356=VECTOR ( 'NONE', #35888, 1000.000000000000000 ) ;
#6362=DIRECTION ( 'NONE',  ( -1.000000000000000000, 0.000000000000000000, 0.000000000000000000 ) ) ;
#6363=DIRECTION ( 'NONE',  ( 0.000000000000000000, 0.000000000000000000, 1.000000000000000000 ) ) ;
#6366=EDGE_CURVE ( 'NONE', #27833, #27156, #26546, .T. ) ;
#6371=ORIENTED_EDGE ( 'NONE', *, *, #8792, .F. ) ;
#6372=ORIENTED_EDGE ( 'NONE', *, *, #37248, .F. ) ;
#6376=CARTESIAN_POINT ( 'NONE',  ( 17.99999999999999645, 0.000000000000000000, 0.000000000000000000 ) ) ;
#6378=CARTESIAN_POINT ( 'NONE',  ( 17.99999999999999645, -57.40245293794601622, -96.40140491896693220 ) ) ;
#6379=ORIENTED_EDGE ( 'NONE', *, *, #2911, .T. ) ;
#6380=LINE ( 'NONE', #16682, #25062 ) ;
#6381=AXIS2_PLACEMENT_3D ( 'NONE', #35166, #31694, #1795 ) ;
#6382=CARTESIAN_POINT ( 'NONE',  ( 17.99999999999999645, 0.000000000000000000, 0.000000000000000000 ) ) ;
#6384=ADVANCED_FACE ( 'NONE', ( #31398 ), #37701, .F. ) ;
#6386=CARTESIAN_POINT ( 'NONE',  ( 17.99999999999999645, 84.77518783075197462, -73.49448960231268302 ) ) ;
#6387=CIRCLE ( 'NONE', #2201, 116.0000000000000000 ) ;
#6388=DIRECTION ( 'NONE',  ( -1.000000000000000000, -0.000000000000000000, -0.000000000000000000 ) ) ;
#6392=DIRECTION ( 'NONE',  ( 1.000000000000000000, 0.000000000000000000, 0.000000000000000000 ) ) ;
#6394=VERTEX_POINT ( 'NONE', #17471 ) ;
#6400=ORIENTED_EDGE ( 'NONE', *, *, #15539, .F. ) ;
#6407=LINE ( 'NONE', #25875, #1086 ) ;
#6410=VERTEX_POINT ( 'NONE', #11328 ) ;
#6417=CARTESIAN_POINT ( 'NONE',  ( 17.99999999999999645, 0.000000000000000000, 0.000000000000000000 ) ) ;
#6418=VERTEX_POINT ( 'NONE', #20521 ) ;
#6420=DIRECTION ( 'NONE',  ( 1.000000000000000000, 0.000000000000000000, -0.000000000000000000 ) ) ;
#6421=AXIS2_PLACEMENT_3D ( 'NONE', #28821, #2794, #5465 ) ;
#6422=ORIENTED_EDGE ( 'NONE', *, *, #21583, .T. ) ;
#6426=EDGE_CURVE ( 'NONE', #39003, #38848, #32789, .T. ) ;
#6428=EDGE_CURVE ( 'NONE', #34324, #10921, #14008, .T. ) ;
#6431=DIRECTION ( 'NONE',  ( 1.000000000000000000, 0.000000000000000000, 0.000000000000000000 ) ) ;
#6432=EDGE_LOOP ( 'NONE', ( #4650, #35982, #42516, #3049 ) ) ;
#6433=CYLINDRICAL_SURFACE ( 'NONE', #16573, 116.0000000000000000 ) ;
#6435=CARTESIAN_POINT ( 'NONE',  ( 0.000000000000000000, 63.24564713401931471, -102.5693868539688793 ) ) ;
#6438=DIRECTION ( 'NONE',  ( 1.000000000000000000, 0.000000000000000000, 0.000000000000000000 ) ) ;
#6439=FACE_OUTER_BOUND ( 'NONE', #25381, .T. ) ;
#6440=CIRCLE ( 'NONE', #30849, 58.99999999999999289 ) ;
#6441=CYLINDRICAL_SURFACE ( 'NONE', #42421, 59.00000000000000000 ) ;
#6442=DIRECTION ( 'NONE',  ( -1.000000000000000000, 0.000000000000000000, 0.000000000000000000 ) ) ;
#6446=LINE ( 'NONE', #16528, #2113 ) ;
#6451=DIRECTION ( 'NONE',  ( -1.000000000000000000, -0.000000000000000000, -0.000000000000000000 ) ) ;
#6454=DIRECTION ( 'NONE',  ( 0.000000000000000000, 0.000000000000000000, 1.000000000000000000 ) ) ;
#6455=DIRECTION ( 'NONE',  ( 1.000000000000000000, 0.000000000000000000, 0.000000000000000000 ) ) ;
#6458=CARTESIAN_POINT ( 'NONE',  ( 17.99999999999999645, 0.5156212287294736907, -112.1962860721878315 ) ) ;
#6459=VERTEX_POINT ( 'NONE', #9704 ) ;
#6463=FACE_OUTER_BOUND ( 'NONE', #117, .T. ) ;
#6466=ORIENTED_EDGE ( 'NONE', *, *, #19144, .T. ) ;
#6467=AXIS2_PLACEMENT_3D ( 'NONE', #15223, #18494, #24602 ) ;
#6470=VERTEX_POINT ( 'NONE', #18931 ) ;
#6474=EDGE_CURVE ( 'NONE', #7274, #2948, #3902, .T. ) ;
#6475=ORIENTED_EDGE ( 'NONE', *, *, #12603, .T. ) ;
#6476=VERTEX_POINT ( 'NONE', #38720 ) ;
#6484=DIRECTION ( 'NONE',  ( -1.000000000000000000, -0.000000000000000000, 0.000000000000000000 ) ) ;
#6485=ORIENTED_EDGE ( 'NONE', *, *, #37444, .F. ) ;
#6489=VERTEX_POINT ( 'NONE', #2482 ) ;
#6490=CYLINDRICAL_SURFACE ( 'NONE', #34537, 59.00000000000000000 ) ;
#6492=VERTEX_POINT ( 'NONE', #32190 ) ;
#6493=VECTOR ( 'NONE', #4117, 1000.000000000000000 ) ;
#6494=ORIENTED_EDGE ( 'NONE', *, *, #35349, .T. ) ;
#6498=LINE ( 'NONE', #810, #23474 ) ;
#6500=DIRECTION ( 'NONE',  ( -1.000000000000000000, 0.000000000000000000, 0.000000000000000000 ) ) ;
#6503=DIRECTION ( 'NONE',  ( -1.000000000000000000, 0.000000000000000000, -0.000000000000000000 ) ) ;
#6504=VERTEX_POINT ( 'NONE', #2269 ) ;
#6506=LINE ( 'NONE', #154, #28668 ) ;
#6511=ORIENTED_EDGE ( 'NONE', *, *, #38520, .T. ) ;
#6512=CARTESIAN_POINT ( 'NONE',  ( 0.000000000000000000, -84.62908780824929522, 85.78116633471262276 ) ) ;
#6514=AXIS2_PLACEMENT_3D ( 'NONE', #16242, #22809, #19318 ) ;
#6516=LINE ( 'NONE', #2596, #21224 ) ;
#6518=CIRCLE ( 'NONE', #31613, 59.00000000000000000 ) ;
#6521=AXIS2_PLACEMENT_3D ( 'NONE', #34015, #4101, #24450 ) ;
#6525=EDGE_CURVE ( 'NONE', #40651, #35461, #23491, .T. ) ;
#6526=CARTESIAN_POINT ( 'NONE',  ( 17.99999999999999645, 98.39501399267960835, -53.91376164787712355 ) ) ;
#6527=CYLINDRICAL_SURFACE ( 'NONE', #29996, 116.0000000000000000 ) ;
#6529=VERTEX_POINT ( 'NONE', #35864 ) ;
#6531=FACE_OUTER_BOUND ( 'NONE', #18503, .T. ) ;
#6535=DIRECTION ( 'NONE',  ( -1.000000000000000000, -0.000000000000000000, -0.000000000000000000 ) ) ;
#6539=VERTEX_POINT ( 'NONE', #25681 ) ;
#6540=AXIS2_PLACEMENT_3D ( 'NONE', #40306, #23772, #34411 ) ;
#6542=ORIENTED_EDGE ( 'NONE', *, *, #1784, .T. ) ;
#6543=AXIS2_PLACEMENT_3D ( 'NONE', #10576, #23266, #23702 ) ;
#6545=EDGE_CURVE ( 'NONE', #14651, #8183, #33894, .T. ) ;
#6550=EDGE_CURVE ( 'NONE', #43080, #34294, #39447, .T. ) ;
#6556=FACE_OUTER_BOUND ( 'NONE', #18742, .T. ) ;
#6557=AXIS2_PLACEMENT_3D ( 'NONE', #4501, #27891, #17874 ) ;
#6559=FACE_OUTER_BOUND ( 'NONE', #5954, .T. ) ;
#6563=VERTEX_POINT ( 'NONE', #8846 ) ;
#6565=AXIS2_PLACEMENT_3D ( 'NONE', #41685, #7873, #35131 ) ;
#6566=ORIENTED_EDGE ( 'NONE', *, *, #9611, .F. ) ;
#6567=CARTESIAN_POINT ( 'NONE',  ( 0.000000000000000000, -5.492704054967489924, 115.8698847939556202 ) ) ;
#6568=DIRECTION ( 'NONE',  ( 0.000000000000000000, 0.4132121857683791477, -0.9106347728549126774 ) ) ;
#6574=AXIS2_PLACEMENT_3D ( 'NONE', #12867, #36389, #13095 ) ;
#6576=EDGE_LOOP ( 'NONE', ( #36896, #32679, #25136, #2161 ) ) ;
#6581=ADVANCED_FACE ( 'NONE', ( #23256 ), #26937, .F. ) ;
#6582=DIRECTION ( 'NONE',  ( 0.000000000000000000, 1.881733940042638318E-15, -1.000000000000000000 ) ) ;
#6584=CARTESIAN_POINT ( 'NONE',  ( 17.99999999999999645, 118.8387007424473580, -19.94628303336373065 ) ) ;
#6591=ORIENTED_EDGE ( 'NONE', *, *, #42266, .T. ) ;
#6593=DIRECTION ( 'NONE',  ( -1.000000000000000000, -0.000000000000000000, 0.000000000000000000 ) ) ;
#6594=VERTEX_POINT ( 'NONE', #718 ) ;
#6601=ORIENTED_EDGE ( 'NONE', *, *, #1152, .T. ) ;
#6603=ORIENTED_EDGE ( 'NONE', *, *, #39520, .T. ) ;
#6604=CARTESIAN_POINT ( 'NONE',  ( 0.000000000000000000, 0.000000000000000000, 0.000000000000000000 ) ) ;
#6607=EDGE_CURVE ( 'NONE', #25436, #21133, #42939, .T. ) ;
#6609=CIRCLE ( 'NONE', #41461, 59.00000000000000711 ) ;
#6611=CARTESIAN_POINT ( 'NONE',  ( 0.000000000000000000, -79.94368240339484544, 90.16373242487880191 ) ) ;
#6618=CIRCLE ( 'NONE', #3827, 120.5010000000000190 ) ;
#6620=DIRECTION ( 'NONE',  ( -1.000000000000000000, 0.000000000000000000, 0.000000000000000000 ) ) ;
#6623=ORIENTED_EDGE ( 'NONE', *, *, #18658, .T. ) ;
#6628=DIRECTION ( 'NONE',  ( -1.000000000000000000, -0.000000000000000000, -0.000000000000000000 ) ) ;
#6630=ORIENTED_EDGE ( 'NONE', *, *, #5132, .F. ) ;
#6634=CARTESIAN_POINT ( 'NONE',  ( 17.99999999999999645, -6.486220790509180212, 112.0098273076987283 ) ) ;
#6636=CIRCLE ( 'NONE', #13649, 120.5010000000000332 ) ;
#6637=DIRECTION ( 'NONE',  ( -1.000000000000000000, -0.000000000000000000, 0.000000000000000000 ) ) ;
#6639=DIRECTION ( 'NONE',  ( -1.000000000000000000, 0.000000000000000000, 0.000000000000000000 ) ) ;
#6641=AXIS2_PLACEMENT_3D ( 'NONE', #20346, #3040, #16410 ) ;
#6642=AXIS2_PLACEMENT_3D ( 'NONE', #19613, #2546, #9114 ) ;
#6644=ORIENTED_EDGE ( 'NONE', *, *, #38571, .F. ) ;
#6646=ORIENTED_EDGE ( 'NONE', *, *, #17278, .T. ) ;
#6648=AXIS2_PLACEMENT_3D ( 'NONE', #31567, #14581, #14795 ) ;
#6655=DIRECTION ( 'NONE',  ( 0.000000000000000000, -0.4132121857683850874, 0.9106347728549100129 ) ) ;
#6657=FACE_OUTER_BOUND ( 'NONE', #33150, .T. ) ;
#6658=CARTESIAN_POINT ( 'NONE',  ( 0.000000000000000000, 119.8996782608629985, 12.02323392193396856 ) ) ;
#6659=ORIENTED_EDGE ( 'NONE', *, *, #27078, .T. ) ;
#6661=DIRECTION ( 'NONE',  ( -1.000000000000000000, -0.000000000000000000, -0.000000000000000000 ) ) ;
#6662=EDGE_CURVE ( 'NONE', #6179, #31565, #31829, .T. ) ;
#6665=ORIENTED_EDGE ( 'NONE', *, *, #11380, .T. ) ;
#6671=DIRECTION ( 'NONE',  ( -1.000000000000000000, 0.000000000000000000, 0.000000000000000000 ) ) ;
#6672=AXIS2_PLACEMENT_3D ( 'NONE', #12469, #32290, #2375 ) ;
#6673=DIRECTION ( 'NONE',  ( 0.000000000000000000, -0.8183027759081622499, -0.5747874102144165942 ) ) ;
#6677=EDGE_CURVE ( 'NONE', #8548, #11411, #12339, .T. ) ;
#6687=AXIS2_PLACEMENT_3D ( 'NONE', #38154, #38788, #31611 ) ;
#6689=AXIS2_PLACEMENT_3D ( 'NONE', #38602, #31441, #34914 ) ;
#6695=DIRECTION ( 'NONE',  ( -1.000000000000000000, -0.000000000000000000, 0.000000000000000000 ) ) ;
#6702=CARTESIAN_POINT ( 'NONE',  ( 17.99999999999999645, -40.37724737309996215, -104.6802291180871265 ) ) ;
#6705=CIRCLE ( 'NONE', #19297, 116.0000000000000000 ) ;
#6710=ORIENTED_EDGE ( 'NONE', *, *, #4869, .T. ) ;
#6711=CARTESIAN_POINT ( 'NONE',  ( 17.99999999999999645, -40.13512380273891011, -113.6206972269525863 ) ) ;
#6716=DIRECTION ( 'NONE',  ( -1.000000000000000000, 0.000000000000000000, 0.000000000000000000 ) ) ;
#6717=LINE ( 'NONE', #27033, #29458 ) ;
#6719=EDGE_LOOP ( 'NONE', ( #7514, #4905, #19906, #5870 ) ) ;
#6723=DIRECTION ( 'NONE',  ( 0.000000000000000000, 0.000000000000000000, 1.000000000000000000 ) ) ;
#6728=AXIS2_PLACEMENT_3D ( 'NONE', #19132, #2905, #5990 ) ;
#6730=CARTESIAN_POINT ( 'NONE',  ( 0.000000000000000000, -95.38615066514023511, 59.07414607872794932 ) ) ;
#6733=EDGE_CURVE ( 'NONE', #36312, #41379, #31138, .T. ) ;
#6734=ORIENTED_EDGE ( 'NONE', *, *, #27091, .F. ) ;
#6735=FILL_AREA_STYLE_COLOUR ( '', #193 ) ;
#6738=DIRECTION ( 'NONE',  ( -1.000000000000000000, -0.000000000000000000, -0.000000000000000000 ) ) ;
#6739=VECTOR ( 'NONE', #38318, 1000.000000000000000 ) ;
#6742=CARTESIAN_POINT ( 'NONE',  ( 0.000000000000000000, -0.5156212287272186057, -112.1962860721878172 ) ) ;
#6744=DIRECTION ( 'NONE',  ( 1.000000000000000000, 0.000000000000000000, 0.000000000000000000 ) ) ;
#6746=AXIS2_PLACEMENT_3D ( 'NONE', #9607, #22959, #36200 ) ;
#6751=AXIS2_PLACEMENT_3D ( 'NONE', #19016, #41435, #8504 ) ;
#6753=CYLINDRICAL_SURFACE ( 'NONE', #9465, 59.00000000000000711 ) ;
#6755=CARTESIAN_POINT ( 'NONE',  ( 17.99999999999999645, 110.1579703617966430, 21.29539948940285043 ) ) ;
#6756=EDGE_CURVE ( 'NONE', #37390, #39824, #11415, .T. ) ;
#6758=CARTESIAN_POINT ( 'NONE',  ( 9.000000000000001776, -37.07968990261553444, 109.9140418541956308 ) ) ;
#6759=DIRECTION ( 'NONE',  ( 0.000000000000000000, 0.000000000000000000, 1.000000000000000000 ) ) ;
#6761=ORIENTED_EDGE ( 'NONE', *, *, #36375, .T. ) ;
#6768=CARTESIAN_POINT ( 'NONE',  ( 0.000000000000000000, 0.000000000000000000, 0.000000000000000000 ) ) ;
#6773=VECTOR ( 'NONE', #2395, 1000.000000000000000 ) ;
#6774=VERTEX_POINT ( 'NONE', #8154 ) ;
#6775=CIRCLE ( 'NONE', #37422, 58.99999999999999289 ) ;
#6776=CYLINDRICAL_SURFACE ( 'NONE', #31359, 59.00000000000000000 ) ;
#6779=ORIENTED_EDGE ( 'NONE', *, *, #39520, .F. ) ;
#6780=DIRECTION ( 'NONE',  ( 1.000000000000000000, -0.000000000000000000, -0.000000000000000000 ) ) ;
#6781=CARTESIAN_POINT ( 'NONE',  ( 17.99999999999999645, 29.36437154451999021, 116.8684075565137164 ) ) ;
#6782=AXIS2_PLACEMENT_3D ( 'NONE', #39725, #20363, #6568 ) ;
#6783=LINE ( 'NONE', #30148, #20646 ) ;
#6789=CARTESIAN_POINT ( 'NONE',  ( -10.00000000000000000, 0.000000000000000000, 0.000000000000000000 ) ) ;
#6796=FACE_OUTER_BOUND ( 'NONE', #37297, .T. ) ;
#6798=ORIENTED_EDGE ( 'NONE', *, *, #40797, .F. ) ;
#6804=AXIS2_PLACEMENT_3D ( 'NONE', #42768, #40151, #10287 ) ;
#6805=CIRCLE ( 'NONE', #33290, 120.5010000000000190 ) ;
#6806=VERTEX_POINT ( 'NONE', #11439 ) ;
#6808=DIRECTION ( 'NONE',  ( 0.000000000000000000, 0.000000000000000000, 1.000000000000000000 ) ) ;
#6809=DIRECTION ( 'NONE',  ( 1.000000000000000000, 0.000000000000000000, 0.000000000000000000 ) ) ;
#6818=DIRECTION ( 'NONE',  ( 0.000000000000000000, 0.000000000000000000, 1.000000000000000000 ) ) ;
#6819=AXIS2_PLACEMENT_3D ( 'NONE', #27199, #16965, #24156 ) ;
#6821=CYLINDRICAL_SURFACE ( 'NONE', #29813, 59.00000000000000000 ) ;
#6824=DIRECTION ( 'NONE',  ( 1.000000000000000000, 0.000000000000000000, 0.000000000000000000 ) ) ;
#6825=ORIENTED_EDGE ( 'NONE', *, *, #8743, .T. ) ;
#6827=ORIENTED_EDGE ( 'NONE', *, *, #31058, .F. ) ;
#6828=CARTESIAN_POINT ( 'NONE',  ( 17.99999999999999645, -87.92975456462950490, 69.68953103478128241 ) ) ;
#6833=CIRCLE ( 'NONE', #13121, 59.00000000000000000 ) ;
#6835=EDGE_LOOP ( 'NONE', ( #35609, #3619, #39600, #15456 ) ) ;
#6837=EDGE_CURVE ( 'NONE', #3479, #25483, #40643, .T. ) ;
#6839=VECTOR ( 'NONE', #34761, 1000.000000000000000 ) ;
#6842=EDGE_CURVE ( 'NONE', #12550, #22817, #6518, .T. ) ;
#6846=DIRECTION ( 'NONE',  ( -1.000000000000000000, -0.000000000000000000, 0.000000000000000000 ) ) ;
#6848=DIRECTION ( 'NONE',  ( 0.000000000000000000, 0.000000000000000000, 1.000000000000000000 ) ) ;
#6849=VERTEX_POINT ( 'NONE', #5084 ) ;
#6855=DIRECTION ( 'NONE',  ( 0.000000000000000000, 0.5963673585385027565, -0.8027116379309627847 ) ) ;
#6856=EDGE_CURVE ( 'NONE', #35938, #12319, #35751, .T. ) ;
#6857=ORIENTED_EDGE ( 'NONE', *, *, #31360, .F. ) ;
#6858=CARTESIAN_POINT ( 'NONE',  ( 0.000000000000000000, -6.486220790507708500, -112.0098273076987994 ) ) ;
#6863=EDGE_CURVE ( 'NONE', #9503, #35353, #26724, .T. ) ;
#6864=ADVANCED_FACE ( 'NONE', ( #37809 ), #38452, .F. ) ;
#6866=AXIS2_PLACEMENT_3D ( 'NONE', #11456, #27607, #1392 ) ;
#6867=EDGE_LOOP ( 'NONE', ( #32271, #29422, #773, #36267 ) ) ;
#6868=DIRECTION ( 'NONE',  ( 0.000000000000000000, -0.2113826236296315053, 0.9774033898178651203 ) ) ;
#6872=CARTESIAN_POINT ( 'NONE',  ( 9.000000000000001776, 110.8621702203453339, -34.14058016547421914 ) ) ;
#6874=ORIENTED_EDGE ( 'NONE', *, *, #2413, .T. ) ;
#6878=DIRECTION ( 'NONE',  ( -1.000000000000000000, -0.000000000000000000, 0.000000000000000000 ) ) ;
#6879=EDGE_LOOP ( 'NONE', ( #21079, #30222, #25018, #21706 ) ) ;
#6882=CARTESIAN_POINT ( 'NONE',  ( 17.99999999999999645, 112.5220807139884016, 28.19186676675879255 ) ) ;
#6884=ORIENTED_EDGE ( 'NONE', *, *, #12070, .T. ) ;
#6888=ADVANCED_FACE ( 'NONE', ( #22356 ), #29510, .F. ) ;
#6889=DIRECTION ( 'NONE',  ( -1.000000000000000000, 0.000000000000000000, 0.000000000000000000 ) ) ;
#6890=LINE ( 'NONE', #33304, #42919 ) ;
#6893=DIRECTION ( 'NONE',  ( 0.000000000000000000, -0.7865515558026479059, 0.6175246149461850464 ) ) ;
#6894=ORIENTED_EDGE ( 'NONE', *, *, #25287, .T. ) ;
#6896=CARTESIAN_POINT ( 'NONE',  ( 9.000000000000001776, -29.86146780999875716, -112.0905559814581665 ) ) ;
#6898=CARTESIAN_POINT ( 'NONE',  ( 17.99999999999999645, 0.000000000000000000, 0.000000000000000000 ) ) ;
#6899=VERTEX_POINT ( 'NONE', #25622 ) ;
#6901=ORIENTED_EDGE ( 'NONE', *, *, #15925, .T. ) ;
#6903=ORIENTED_EDGE ( 'NONE', *, *, #36381, .F. ) ;
#6904=FACE_OUTER_BOUND ( 'NONE', #41201, .T. ) ;
#6914=LINE ( 'NONE', #34131, #17381 ) ;
#6915=DIRECTION ( 'NONE',  ( -1.000000000000000000, 0.000000000000000000, 0.000000000000000000 ) ) ;
#6917=AXIS2_PLACEMENT_3D ( 'NONE', #33703, #7298, #3786 ) ;
#6923=AXIS2_PLACEMENT_3D ( 'NONE', #13339, #3468, #13129 ) ;
#6924=EDGE_CURVE ( 'NONE', #36681, #42716, #8619, .T. ) ;
#6927=VERTEX_POINT ( 'NONE', #19501 ) ;
#6932=CARTESIAN_POINT ( 'NONE',  ( 0.000000000000000000, 0.000000000000000000, 0.000000000000000000 ) ) ;
#6940=EDGE_CURVE ( 'NONE', #34149, #28377, #17006, .T. ) ;
#6942=ORIENTED_EDGE ( 'NONE', *, *, #2892, .T. ) ;
#6943=DIRECTION ( 'NONE',  ( -1.000000000000000000, 0.000000000000000000, 0.000000000000000000 ) ) ;
#6945=ORIENTED_EDGE ( 'NONE', *, *, #34059, .T. ) ;
#6949=VECTOR ( 'NONE', #17211, 1000.000000000000000 ) ;
#6950=AXIS2_PLACEMENT_3D ( 'NONE', #24322, #4628, #18004 ) ;
#6952=VERTEX_POINT ( 'NONE', #2016 ) ;
#6956=DIRECTION ( 'NONE',  ( -1.000000000000000000, -0.000000000000000000, -0.000000000000000000 ) ) ;
#6960=EDGE_CURVE ( 'NONE', #11221, #23796, #12515, .T. ) ;
#6962=DIRECTION ( 'NONE',  ( 0.000000000000000000, 0.000000000000000000, 1.000000000000000000 ) ) ;
#6963=DIRECTION ( 'NONE',  ( 0.000000000000000000, 0.000000000000000000, 1.000000000000000000 ) ) ;
#6967=DIRECTION ( 'NONE',  ( 0.000000000000000000, 0.000000000000000000, 1.000000000000000000 ) ) ;
#6971=DIRECTION ( 'NONE',  ( -1.000000000000000000, 0.000000000000000000, 0.000000000000000000 ) ) ;
#6972=AXIS2_PLACEMENT_3D ( 'NONE', #20980, #9866, #23219 ) ;
#6975=VERTEX_POINT ( 'NONE', #5523 ) ;
#6976=ADVANCED_FACE ( 'NONE', ( #42777 ), #38889, .F. ) ;
#6977=DIRECTION ( 'NONE',  ( 0.000000000000000000, 0.000000000000000000, 1.000000000000000000 ) ) ;
#6979=CIRCLE ( 'NONE', #30708, 116.0000000000000000 ) ;
#6982=ORIENTED_EDGE ( 'NONE', *, *, #35256, .T. ) ;
#6989=DIRECTION ( 'NONE',  ( -1.000000000000000000, -0.000000000000000000, -0.000000000000000000 ) ) ;
#6990=ORIENTED_EDGE ( 'NONE', *, *, #42389, .F. ) ;
#6993=ADVANCED_FACE ( 'NONE', ( #2647 ), #39092, .F. ) ;
#6996=EDGE_CURVE ( 'NONE', #7217, #12907, #15578, .T. ) ;
#6997=CARTESIAN_POINT ( 'NONE',  ( 0.000000000000000000, -84.09610293794020208, -74.27057253243097534 ) ) ;
#6999=AXIS2_PLACEMENT_3D ( 'NONE', #26761, #10164, #6893 ) ;
#7000=FACE_OUTER_BOUND ( 'NONE', #19164, .T. ) ;
#7007=AXIS2_PLACEMENT_3D ( 'NONE', #6604, #33449, #17352 ) ;
#7008=VECTOR ( 'NONE', #20732, 1000.000000000000000 ) ;
#7010=ORIENTED_EDGE ( 'NONE', *, *, #5669, .F. ) ;
#7012=CARTESIAN_POINT ( 'NONE',  ( 0.000000000000000000, 58.30069736313799211, -100.2847380560561419 ) ) ;
#7017=CARTESIAN_POINT ( 'NONE',  ( 17.99999999999999645, 0.000000000000000000, 0.000000000000000000 ) ) ;
#7019=CARTESIAN_POINT ( 'NONE',  ( 8.999999999999998224, -69.72480978689983999, -92.70626138606085931 ) ) ;
#7020=EDGE_CURVE ( 'NONE', #35191, #16394, #12301, .T. ) ;
#7025=CARTESIAN_POINT ( 'NONE',  ( 17.99999999999999645, 97.19627249181095863, 71.22763238166520239 ) ) ;
#7026=EDGE_LOOP ( 'NONE', ( #2298, #26518, #18903, #17958 ) ) ;
#7030=VERTEX_POINT ( 'NONE', #454 ) ;
#7034=CARTESIAN_POINT ( 'NONE',  ( 0.000000000000000000, 73.78980555658606022, 95.26571049922013401 ) ) ;
#7035=AXIS2_PLACEMENT_3D ( 'NONE', #13460, #10152, #23505 ) ;
#7037=DIRECTION ( 'NONE',  ( 1.000000000000000000, 0.000000000000000000, 0.000000000000000000 ) ) ;
#7041=EDGE_LOOP ( 'NONE', ( #4014, #35497, #9920, #27224 ) ) ;
#7042=CARTESIAN_POINT ( 'NONE',  ( 17.99999999999999645, -64.69195966009822030, -96.28577441832322847 ) ) ;
#7046=ORIENTED_EDGE ( 'NONE', *, *, #42457, .F. ) ;
#7048=ADVANCED_FACE ( 'NONE', ( #6796 ), #30598, .F. ) ;
#7053=FACE_OUTER_BOUND ( 'NONE', #30563, .T. ) ;
#7054=ORIENTED_EDGE ( 'NONE', *, *, #6940, .T. ) ;
#7056=VERTEX_POINT ( 'NONE', #13374 ) ;
#7057=DIRECTION ( 'NONE',  ( -1.000000000000000000, 0.000000000000000000, -0.000000000000000000 ) ) ;
#7065=CARTESIAN_POINT ( 'NONE',  ( 0.000000000000000000, 0.000000000000000000, 0.000000000000000000 ) ) ;
#7068=ORIENTED_EDGE ( 'NONE', *, *, #25814, .T. ) ;
#7073=DIRECTION ( 'NONE',  ( -1.000000000000000000, -0.000000000000000000, -0.000000000000000000 ) ) ;
#7075=ORIENTED_EDGE ( 'NONE', *, *, #16584, .F. ) ;
#7077=ORIENTED_EDGE ( 'NONE', *, *, #26985, .F. ) ;
#7082=LINE ( 'NONE', #36525, #29634 ) ;
#7084=ORIENTED_EDGE ( 'NONE', *, *, #2425, .T. ) ;
#7085=DIRECTION ( 'NONE',  ( -1.000000000000000000, 0.000000000000000000, 0.000000000000000000 ) ) ;
#7086=DIRECTION ( 'NONE',  ( 0.000000000000000000, -1.243708525996931132E-14, -1.000000000000000000 ) ) ;
#7089=EDGE_LOOP ( 'NONE', ( #15824, #34928, #2506, #5938 ) ) ;
#7092=FACE_OUTER_BOUND ( 'NONE', #11632, .T. ) ;
#7093=ORIENTED_EDGE ( 'NONE', *, *, #17909, .F. ) ;
#7095=CARTESIAN_POINT ( 'NONE',  ( 17.99999999999999645, -88.56657216608570593, -68.87840567546012949 ) ) ;
#7096=AXIS2_PLACEMENT_3D ( 'NONE', #36436, #30586, #27303 ) ;
#7102=FACE_OUTER_BOUND ( 'NONE', #7503, .T. ) ;
#7104=EDGE_CURVE ( 'NONE', #23547, #2401, #11924, .T. ) ;
#7105=VECTOR ( 'NONE', #13990, 1000.000000000000000 ) ;
#7106=LINE ( 'NONE', #17409, #4547 ) ;
#7108=CYLINDRICAL_SURFACE ( 'NONE', #37679, 59.00000000000000000 ) ;
#7110=VECTOR ( 'NONE', #16205, 1000.000000000000000 ) ;
#7111=CARTESIAN_POINT ( 'NONE',  ( 0.000000000000000000, 11.65176648921190150, -115.4133282497341355 ) ) ;
#7112=CARTESIAN_POINT ( 'NONE',  ( 17.99999999999999645, 57.40245293794667703, 96.40140491896650587 ) ) ;
#7114=DIRECTION ( 'NONE',  ( 0.000000000000000000, 0.000000000000000000, 1.000000000000000000 ) ) ;
#7117=ORIENTED_EDGE ( 'NONE', *, *, #10567, .T. ) ;
#7119=ORIENTED_EDGE ( 'NONE', *, *, #21769, .T. ) ;
#7120=CYLINDRICAL_SURFACE ( 'NONE', #22900, 59.00000000000000000 ) ;
#7124=CARTESIAN_POINT ( 'NONE',  ( 0.000000000000000000, 0.000000000000000000, 0.000000000000000000 ) ) ;
#7127=DIRECTION ( 'NONE',  ( 1.000000000000000000, 0.000000000000000000, 0.000000000000000000 ) ) ;
#7128=ORIENTED_EDGE ( 'NONE', *, *, #6289, .T. ) ;
#7129=DIRECTION ( 'NONE',  ( 1.000000000000000000, 0.000000000000000000, 0.000000000000000000 ) ) ;
#7130=AXIS2_PLACEMENT_3D ( 'NONE', #21474, #18408, #5483 ) ;
#7131=DIRECTION ( 'NONE',  ( 0.000000000000000000, 1.331914804436429787E-14, -1.000000000000000000 ) ) ;
#7132=CIRCLE ( 'NONE', #18350, 58.99999999999998579 ) ;
#7135=DIRECTION ( 'NONE',  ( 0.000000000000000000, 0.000000000000000000, 1.000000000000000000 ) ) ;
#7136=ORIENTED_EDGE ( 'NONE', *, *, #22618, .T. ) ;
#7137=CARTESIAN_POINT ( 'NONE',  ( 0.000000000000000000, -110.3490479609630910, 38.71798610214488434 ) ) ;
#7143=DIRECTION ( 'NONE',  ( 0.000000000000000000, 0.000000000000000000, 1.000000000000000000 ) ) ;
#7152=EDGE_CURVE ( 'NONE', #29060, #31074, #3058, .T. ) ;
#7153=EDGE_CURVE ( 'NONE', #25529, #30264, #42279, .T. ) ;
#7156=CYLINDRICAL_SURFACE ( 'NONE', #17534, 116.0000000000000000 ) ;
#7157=LINE ( 'NONE', #34003, #16492 ) ;
#7159=ORIENTED_EDGE ( 'NONE', *, *, #13876, .F. ) ;
#7160=AXIS2_PLACEMENT_3D ( 'NONE', #43114, #33080, #30480 ) ;
#7163=ORIENTED_EDGE ( 'NONE', *, *, #19658, .F. ) ;
#7164=CYLINDRICAL_SURFACE ( 'NONE', #41296, 59.00000000000000000 ) ;
#7166=LINE ( 'NONE', #21406, #41763 ) ;
#7169=CIRCLE ( 'NONE', #169, 116.0000000000000000 ) ;
#7171=EDGE_LOOP ( 'NONE', ( #11799, #34309, #36782, #30069 ) ) ;
#7175=DIRECTION ( 'NONE',  ( 0.000000000000000000, 0.3641605752528230266, -0.9313361774523380987 ) ) ;
#7177=CARTESIAN_POINT ( 'NONE',  ( 17.99999999999999645, 23.21237537461745859, 109.7700237000592836 ) ) ;
#7178=ADVANCED_FACE ( 'NONE', ( #8098 ), #7446, .F. ) ;
#7183=DIRECTION ( 'NONE',  ( 0.000000000000000000, 0.000000000000000000, 1.000000000000000000 ) ) ;
#7186=FACE_OUTER_BOUND ( 'NONE', #37879, .T. ) ;
#7190=VERTEX_POINT ( 'NONE', #30803 ) ;
#7192=CYLINDRICAL_SURFACE ( 'NONE', #41334, 59.00000000000000000 ) ;
#7195=FACE_OUTER_BOUND ( 'NONE', #35684, .T. ) ;
#7196=CYLINDRICAL_SURFACE ( 'NONE', #41575, 120.5010000000000190 ) ;
#7198=CARTESIAN_POINT ( 'NONE',  ( 17.99999999999999645, 111.8797445107944810, -8.437727291343108504 ) ) ;
#7202=ORIENTED_EDGE ( 'NONE', *, *, #25448, .F. ) ;
#7203=DIRECTION ( 'NONE',  ( 0.000000000000000000, 0.9714298932647106311, -0.2373266998711119624 ) ) ;
#7211=ORIENTED_EDGE ( 'NONE', *, *, #15710, .T. ) ;
#7214=DIRECTION ( 'NONE',  ( -1.000000000000000000, -0.000000000000000000, -0.000000000000000000 ) ) ;
#7217=VERTEX_POINT ( 'NONE', #34487 ) ;
#7219=EDGE_CURVE ( 'NONE', #30344, #42093, #33945, .T. ) ;
#7221=ORIENTED_EDGE ( 'NONE', *, *, #21450, .F. ) ;
#7223=CYLINDRICAL_SURFACE ( 'NONE', #8742, 59.00000000000000000 ) ;
#7227=VERTEX_POINT ( 'NONE', #31243 ) ;
#7229=VECTOR ( 'NONE', #28599, 1000.000000000000000 ) ;
#7239=DIRECTION ( 'NONE',  ( 1.000000000000000000, 0.000000000000000000, 0.000000000000000000 ) ) ;
#7246=VECTOR ( 'NONE', #25949, 1000.000000000000000 ) ;
#7247=ORIENTED_EDGE ( 'NONE', *, *, #6141, .F. ) ;
#7248=CARTESIAN_POINT ( 'NONE',  ( 0.000000000000000000, 0.000000000000000000, 0.000000000000000000 ) ) ;
#7249=VERTEX_POINT ( 'NONE', #11171 ) ;
#7254=EDGE_CURVE ( 'NONE', #2432, #41661, #20761, .T. ) ;
#7257=EDGE_LOOP ( 'NONE', ( #38505, #28046, #33452, #11319 ) ) ;
#7260=CARTESIAN_POINT ( 'NONE',  ( 0.000000000000000000, 0.000000000000000000, 0.000000000000000000 ) ) ;
#7262=VERTEX_POINT ( 'NONE', #1329 ) ;
#7263=DIRECTION ( 'NONE',  ( 0.000000000000000000, 0.000000000000000000, 1.000000000000000000 ) ) ;
#7264=AXIS2_PLACEMENT_3D ( 'NONE', #2100, #38537, #8661 ) ;
#7266=ADVANCED_FACE ( 'NONE', ( #7661 ), #4154, .F. ) ;
#7267=AXIS2_PLACEMENT_3D ( 'NONE', #41009, #34257, #17724 ) ;
#7269=CIRCLE ( 'NONE', #13596, 116.0000000000000000 ) ;
#7274=VERTEX_POINT ( 'NONE', #24292 ) ;
#7275=AXIS2_PLACEMENT_3D ( 'NONE', #34433, #25309, #8680 ) ;
#7281=CARTESIAN_POINT ( 'NONE',  ( 17.99999999999999645, 15.21076497709875497, -119.5371223922153519 ) ) ;
#7283=CARTESIAN_POINT ( 'NONE',  ( 17.99999999999999645, -71.21168426767167148, 86.70160608319299911 ) ) ;
#7284=ORIENTED_EDGE ( 'NONE', *, *, #31822, .T. ) ;
#7285=CARTESIAN_POINT ( 'NONE',  ( 0.000000000000000000, -17.33727698085101565, -110.8498592715975519 ) ) ;
#7289=ADVANCED_FACE ( 'NONE', ( #7876 ), #41242, .F. ) ;
#7290=FACE_OUTER_BOUND ( 'NONE', #5577, .T. ) ;
#7291=CARTESIAN_POINT ( 'NONE',  ( 17.99999999999999645, 0.000000000000000000, 0.000000000000000000 ) ) ;
#7292=ORIENTED_EDGE ( 'NONE', *, *, #8749, .T. ) ;
#7293=ORIENTED_EDGE ( 'NONE', *, *, #30326, .F. ) ;
#7298=DIRECTION ( 'NONE',  ( -1.000000000000000000, -0.000000000000000000, 0.000000000000000000 ) ) ;
#7304=CARTESIAN_POINT ( 'NONE',  ( 0.000000000000000000, 0.000000000000000000, 0.000000000000000000 ) ) ;
#7305=CARTESIAN_POINT ( 'NONE',  ( 17.99999999999999645, -109.3506818544112917, 38.70953859160975696 ) ) ;
#7307=AXIS2_PLACEMENT_3D ( 'NONE', #10141, #529, #13883 ) ;
#7308=ORIENTED_EDGE ( 'NONE', *, *, #13297, .F. ) ;
#7309=CARTESIAN_POINT ( 'NONE',  ( 17.99999999999999645, 0.000000000000000000, 0.000000000000000000 ) ) ;
#7312=UNCERTAINTY_MEASURE_WITH_UNIT (LENGTH_MEASURE( 1.000000000000000082E-05 ), #38714, 'distance_accuracy_value', 'NONE');
#7314=ORIENTED_EDGE ( 'NONE', *, *, #21729, .T. ) ;
#7315=CARTESIAN_POINT ( 'NONE',  ( 17.99999999999999645, -111.9370513079672520, 44.61600100275137493 ) ) ;
#7319=CARTESIAN_POINT ( 'NONE',  ( 17.99999999999999645, -74.56001736500675747, 88.86396238369010803 ) ) ;
#7321=EDGE_CURVE ( 'NONE', #29070, #22351, #5894, .T. ) ;
#7326=CIRCLE ( 'NONE', #1756, 116.0000000000000000 ) ;
#7330=LINE ( 'NONE', #565, #35124 ) ;
#7331=EDGE_LOOP ( 'NONE', ( #17431, #34256, #4673, #25255 ) ) ;
#7333=CIRCLE ( 'NONE', #20620, 120.5010000000000332 ) ;
#7334=ORIENTED_EDGE ( 'NONE', *, *, #25839, .T. ) ;
#7335=DIRECTION ( 'NONE',  ( -1.000000000000000000, 0.000000000000000000, 0.000000000000000000 ) ) ;
#7336=CIRCLE ( 'NONE', #35918, 120.5010000000000190 ) ;
#7341=DIRECTION ( 'NONE',  ( 0.000000000000000000, 0.000000000000000000, 1.000000000000000000 ) ) ;
#7342=AXIS2_PLACEMENT_3D ( 'NONE', #12747, #5953, #31961 ) ;
#7343=ORIENTED_EDGE ( 'NONE', *, *, #2745, .F. ) ;
#7346=DIRECTION ( 'NONE',  ( -1.000000000000000000, 0.000000000000000000, 0.000000000000000000 ) ) ;
#7348=DIRECTION ( 'NONE',  ( 0.000000000000000000, 0.000000000000000000, -1.000000000000000000 ) ) ;
#7351=EDGE_CURVE ( 'NONE', #2623, #34294, #16855, .T. ) ;
#7353=ORIENTED_EDGE ( 'NONE', *, *, #29125, .F. ) ;
#7354=CYLINDRICAL_SURFACE ( 'NONE', #27485, 59.00000000000000000 ) ;
#7358=CARTESIAN_POINT ( 'NONE',  ( 0.000000000000000000, 98.39501399267960835, -53.91376164787712355 ) ) ;
#7361=CARTESIAN_POINT ( 'NONE',  ( 9.000000000000001776, -115.5737863835462917, 9.934782381633290527 ) ) ;
#7366=CARTESIAN_POINT ( 'NONE',  ( 0.000000000000000000, 54.09091620264857880, -102.6166301549512525 ) ) ;
#7367=ORIENTED_EDGE ( 'NONE', *, *, #36779, .F. ) ;
#7372=CIRCLE ( 'NONE', #403, 116.0000000000000000 ) ;
#7373=CIRCLE ( 'NONE', #31783, 116.0000000000000000 ) ;
#7377=ORIENTED_EDGE ( 'NONE', *, *, #31649, .T. ) ;
#7378=CARTESIAN_POINT ( 'NONE',  ( 0.000000000000000000, 0.000000000000000000, 0.000000000000000000 ) ) ;
#7379=CARTESIAN_POINT ( 'NONE',  ( 8.999999999999998224, 90.81729652456265001, -72.16798910853526650 ) ) ;
#7380=AXIS2_PLACEMENT_3D ( 'NONE', #899, #20834, #41263 ) ;
#7381=ORIENTED_EDGE ( 'NONE', *, *, #40228, .F. ) ;
#7383=LINE ( 'NONE', #607, #25969 ) ;
#7384=EDGE_CURVE ( 'NONE', #27389, #36617, #42534, .T. ) ;
#7386=ORIENTED_EDGE ( 'NONE', *, *, #31905, .T. ) ;
#7387=CARTESIAN_POINT ( 'NONE',  ( 8.999999999999998224, 94.52951811191559273, 67.23221107124935259 ) ) ;
#7388=DIRECTION ( 'NONE',  ( 0.000000000000000000, 0.2113826236296247607, -0.9774033898178666746 ) ) ;
#7389=CARTESIAN_POINT ( 'NONE',  ( 17.99999999999999645, -23.85344185397118011, -113.5209818126993611 ) ) ;
#7391=CIRCLE ( 'NONE', #33180, 120.5010000000000190 ) ;
#7396=CIRCLE ( 'NONE', #36628, 59.00000000000000000 ) ;
#7398=DIRECTION ( 'NONE',  ( 0.000000000000000000, 0.000000000000000000, 1.000000000000000000 ) ) ;
#7400=LINE ( 'NONE', #20765, #29134 ) ;
#7404=EDGE_CURVE ( 'NONE', #9027, #22175, #21682, .T. ) ;
#7405=EDGE_CURVE ( 'NONE', #10476, #6849, #41840, .T. ) ;
#7407=ORIENTED_EDGE ( 'NONE', *, *, #38040, .T. ) ;
#7409=DIRECTION ( 'NONE',  ( 1.000000000000000000, 0.000000000000000000, 0.000000000000000000 ) ) ;
#7415=CARTESIAN_POINT ( 'NONE',  ( 17.99999999999999645, 0.000000000000000000, 0.000000000000000000 ) ) ;
#7417=CARTESIAN_POINT ( 'NONE',  ( 0.000000000000000000, -42.87700105098682002, 107.7847984684003393 ) ) ;
#7421=FACE_OUTER_BOUND ( 'NONE', #34288, .T. ) ;
#7422=VERTEX_POINT ( 'NONE', #2385 ) ;
#7423=DIRECTION ( 'NONE',  ( 0.000000000000000000, 0.000000000000000000, 1.000000000000000000 ) ) ;
#7426=CYLINDRICAL_SURFACE ( 'NONE', #35318, 120.5010000000000190 ) ;
#7427=ORIENTED_EDGE ( 'NONE', *, *, #30677, .T. ) ;
#7428=DIRECTION ( 'NONE',  ( 0.000000000000000000, 0.000000000000000000, 1.000000000000000000 ) ) ;
#7431=ORIENTED_EDGE ( 'NONE', *, *, #3878, .F. ) ;
#7432=AXIS2_PLACEMENT_3D ( 'NONE', #725, #14086, #18247 ) ;
#7437=CIRCLE ( 'NONE', #37394, 59.00000000000000711 ) ;
#7438=FACE_OUTER_BOUND ( 'NONE', #28502, .T. ) ;
#7441=VECTOR ( 'NONE', #38812, 1000.000000000000000 ) ;
#7446=CYLINDRICAL_SURFACE ( 'NONE', #38830, 59.00000000000000000 ) ;
#7448=DIRECTION ( 'NONE',  ( -1.000000000000000000, -0.000000000000000000, 0.000000000000000000 ) ) ;
#7452=DIRECTION ( 'NONE',  ( -1.000000000000000000, 0.000000000000000000, 0.000000000000000000 ) ) ;
#7453=AXIS2_PLACEMENT_3D ( 'NONE', #37182, #289, #10582 ) ;
#7455=ADVANCED_FACE ( 'NONE', ( #36413 ), #12682, .F. ) ;
#7458=CIRCLE ( 'NONE', #34656, 116.0000000000000000 ) ;
#7459=CIRCLE ( 'NONE', #14505, 59.00000000000000000 ) ;
#7460=ADVANCED_FACE ( 'NONE', ( #35568 ), #6527, .F. ) ;
#7465=FACE_OUTER_BOUND ( 'NONE', #42255, .T. ) ;
#7466=VECTOR ( 'NONE', #16939, 1000.000000000000000 ) ;
#7467=AXIS2_PLACEMENT_3D ( 'NONE', #30771, #27498, #40770 ) ;
#7468=ORIENTED_EDGE ( 'NONE', *, *, #41312, .T. ) ;
#7472=ORIENTED_EDGE ( 'NONE', *, *, #25257, .T. ) ;
#7473=CARTESIAN_POINT ( 'NONE',  ( 9.000000000000001776, -19.12429268481792732, 114.4126803693778669 ) ) ;
#7475=FACE_OUTER_BOUND ( 'NONE', #13927, .T. ) ;
#7477=EDGE_LOOP ( 'NONE', ( #10023, #34154, #23674, #11104 ) ) ;
#7478=CYLINDRICAL_SURFACE ( 'NONE', #15346, 116.0000000000000000 ) ;
#7479=ORIENTED_EDGE ( 'NONE', *, *, #31172, .F. ) ;
#7485=VERTEX_POINT ( 'NONE', #26419 ) ;
#7488=CARTESIAN_POINT ( 'NONE',  ( 17.99999999999999645, -103.5682682299991342, 43.14958040911493242 ) ) ;
#7490=DIRECTION ( 'NONE',  ( 0.000000000000000000, 0.000000000000000000, 1.000000000000000000 ) ) ;
#7491=CARTESIAN_POINT ( 'NONE',  ( 0.000000000000000000, 68.61497464550593861, 99.05794392877625398 ) ) ;
#7492=AXIS2_PLACEMENT_3D ( 'NONE', #8747, #21886, #15540 ) ;
#7496=AXIS2_PLACEMENT_3D ( 'NONE', #42997, #23841, #19706 ) ;
#7497=LINE ( 'NONE', #506, #28276 ) ;
#7499=DIRECTION ( 'NONE',  ( -1.000000000000000000, -0.000000000000000000, -0.000000000000000000 ) ) ;
#7502=VECTOR ( 'NONE', #23656, 1000.000000000000000 ) ;
#7503=EDGE_LOOP ( 'NONE', ( #34663, #17288, #4289, #23338 ) ) ;
#7506=AXIS2_PLACEMENT_3D ( 'NONE', #16538, #33073, #9304 ) ;
#7507=EDGE_LOOP ( 'NONE', ( #31674, #25176, #11373, #29442 ) ) ;
#7509=DIRECTION ( 'NONE',  ( 0.000000000000000000, 0.5528000653611945259, -0.8333139190825141762 ) ) ;
#7511=ADVANCED_FACE ( 'NONE', ( #33805 ), #20535, .F. ) ;
#7513=ADVANCED_FACE ( 'NONE', ( #4334 ), #13770, .F. ) ;
#7514=ORIENTED_EDGE ( 'NONE', *, *, #39271, .T. ) ;
#7516=VERTEX_POINT ( 'NONE', #3465 ) ;
#7521=ORIENTED_EDGE ( 'NONE', *, *, #39650, .T. ) ;
#7522=ORIENTED_EDGE ( 'NONE', *, *, #9634, .F. ) ;
#7526=EDGE_CURVE ( 'NONE', #7516, #25306, #26498, .T. ) ;
#7528=CARTESIAN_POINT ( 'NONE',  ( 17.99999999999999645, -103.4151313792875158, 61.85306461934377609 ) ) ;
#7533=VERTEX_POINT ( 'NONE', #27493 ) ;
#7536=CARTESIAN_POINT ( 'NONE',  ( -10.00000000000000000, 0.000000000000000000, 0.000000000000000000 ) ) ;
#7539=ORIENTED_EDGE ( 'NONE', *, *, #15188, .T. ) ;
#7541=CARTESIAN_POINT ( 'NONE',  ( -10.00000000000000000, 0.000000000000000000, 0.000000000000000000 ) ) ;
#7543=CARTESIAN_POINT ( 'NONE',  ( 17.99999999999999645, 117.6086855750634470, 26.24286718912143712 ) ) ;
#7545=ORIENTED_EDGE ( 'NONE', *, *, #10834, .F. ) ;
#7547=EDGE_CURVE ( 'NONE', #36084, #23269, #25831, .T. ) ;
#7550=CARTESIAN_POINT ( 'NONE',  ( 0.000000000000000000, 115.9750404417044081, -2.406240749597859718 ) ) ;
#7551=CARTESIAN_POINT ( 'NONE',  ( 17.99999999999999645, -116.0452958106482981, 32.46506308663420270 ) ) ;
#7553=EDGE_CURVE ( 'NONE', #8886, #22817, #34238, .T. ) ;
#7556=ORIENTED_EDGE ( 'NONE', *, *, #21032, .T. ) ;
#7558=DIRECTION ( 'NONE',  ( 1.000000000000000000, 0.000000000000000000, 0.000000000000000000 ) ) ;
#7562=CARTESIAN_POINT ( 'NONE',  ( -10.00000000000000000, 0.000000000000000000, 0.000000000000000000 ) ) ;
#7566=LINE ( 'NONE', #9967, #6949 ) ;
#7568=VERTEX_POINT ( 'NONE', #33589 ) ;
#7571=SURFACE_STYLE_USAGE ( .BOTH. , #37457 ) ;
#7573=CARTESIAN_POINT ( 'NONE',  ( 0.000000000000000000, -93.26762629039475883, 76.29967815892324268 ) ) ;
#7575=DIRECTION ( 'NONE',  ( 0.000000000000000000, 0.5076658003388351270, 0.8615540813938089570 ) ) ;
#7576=ORIENTED_EDGE ( 'NONE', *, *, #31830, .F. ) ;
#7580=DIRECTION ( 'NONE',  ( 0.000000000000000000, -0.9574220383620022368, -0.2886919473396315494 ) ) ;
#7582=DIRECTION ( 'NONE',  ( -1.000000000000000000, -0.000000000000000000, 0.000000000000000000 ) ) ;
#7585=FACE_OUTER_BOUND ( 'NONE', #15462, .T. ) ;
#7594=CYLINDRICAL_SURFACE ( 'NONE', #30025, 59.00000000000000711 ) ;
#7596=LINE ( 'NONE', #33999, #18577 ) ;
#7597=ORIENTED_EDGE ( 'NONE', *, *, #40437, .T. ) ;
#7598=CARTESIAN_POINT ( 'NONE',  ( 17.99999999999999645, -23.21237537461820466, 109.7700237000591414 ) ) ;
#7601=DIRECTION ( 'NONE',  ( -1.000000000000000000, 0.000000000000000000, 0.000000000000000000 ) ) ;
#7603=ADVANCED_FACE ( 'NONE', ( #30561 ), #409, .F. ) ;
#7604=ORIENTED_EDGE ( 'NONE', *, *, #16720, .F. ) ;
#7607=CARTESIAN_POINT ( 'NONE',  ( 0.000000000000000000, 98.69720329641039314, -60.94966826379810243 ) ) ;
#7614=VECTOR ( 'NONE', #27125, 1000.000000000000000 ) ;
#7615=EDGE_CURVE ( 'NONE', #26682, #24778, #6979, .T. ) ;
#7617=CARTESIAN_POINT ( 'NONE',  ( 0.000000000000000000, 0.000000000000000000, 0.000000000000000000 ) ) ;
#7618=FACE_OUTER_BOUND ( 'NONE', #22126, .T. ) ;
#7619=FACE_OUTER_BOUND ( 'NONE', #43128, .T. ) ;
#7621=CARTESIAN_POINT ( 'NONE',  ( 17.99999999999999645, -84.62908780824814414, -85.78116633471378805 ) ) ;
#7623=EDGE_CURVE ( 'NONE', #28961, #25672, #15381, .T. ) ;
#7624=ORIENTED_EDGE ( 'NONE', *, *, #1679, .F. ) ;
#7626=CARTESIAN_POINT ( 'NONE',  ( 17.99999999999999645, 98.39501399267960835, -53.91376164787712355 ) ) ;
#7629=EDGE_CURVE ( 'NONE', #5449, #3132, #20770, .T. ) ;
#7630=CARTESIAN_POINT ( 'NONE',  ( 0.000000000000000000, 1.592040838891559450E-14, -130.0000000000000000 ) ) ;
#7633=DIRECTION ( 'NONE',  ( -1.000000000000000000, -0.000000000000000000, -0.000000000000000000 ) ) ;
#7637=EDGE_LOOP ( 'NONE', ( #42082, #31979, #29703, #28487 ) ) ;
#7641=VECTOR ( 'NONE', #16189, 1000.000000000000000 ) ;
#7643=DIRECTION ( 'NONE',  ( -1.000000000000000000, 0.000000000000000000, -0.000000000000000000 ) ) ;
#7648=EDGE_CURVE ( 'NONE', #40120, #35216, #1062, .T. ) ;
#7652=EDGE_CURVE ( 'NONE', #25306, #21207, #15298, .T. ) ;
#7653=CARTESIAN_POINT ( 'NONE',  ( 17.99999999999999645, 0.000000000000000000, 0.000000000000000000 ) ) ;
#7661=FACE_OUTER_BOUND ( 'NONE', #5820, .T. ) ;
#7663=DIRECTION ( 'NONE',  ( -1.000000000000000000, 0.000000000000000000, 0.000000000000000000 ) ) ;
#7667=CIRCLE ( 'NONE', #41803, 59.00000000000000000 ) ;
#7668=CARTESIAN_POINT ( 'NONE',  ( 17.99999999999999645, -52.19040376560366923, -99.31985817764231683 ) ) ;
#7669=CARTESIAN_POINT ( 'NONE',  ( 0.000000000000000000, -112.5220807139885864, 28.19186676675805003 ) ) ;
#7671=VECTOR ( 'NONE', #38576, 1000.000000000000000 ) ;
#7673=DIRECTION ( 'NONE',  ( 0.000000000000000000, 0.000000000000000000, 1.000000000000000000 ) ) ;
#7677=DIRECTION ( 'NONE',  ( 0.000000000000000000, 0.000000000000000000, 1.000000000000000000 ) ) ;
#7679=ORIENTED_EDGE ( 'NONE', *, *, #34743, .T. ) ;
#7681=DIRECTION ( 'NONE',  ( -1.000000000000000000, -0.000000000000000000, -0.000000000000000000 ) ) ;
#7684=FACE_OUTER_BOUND ( 'NONE', #14262, .T. ) ;
#7685=VERTEX_POINT ( 'NONE', #14638 ) ;
#7687=CYLINDRICAL_SURFACE ( 'NONE', #32073, 59.00000000000000000 ) ;
#7688=EDGE_LOOP ( 'NONE', ( #12648, #38296, #10764, #29972 ) ) ;
#7690=AXIS2_PLACEMENT_3D ( 'NONE', #18610, #22300, #15733 ) ;
#7691=ORIENTED_EDGE ( 'NONE', *, *, #38715, .T. ) ;
#7693=VECTOR ( 'NONE', #3165, 1000.000000000000000 ) ;
#7698=AXIS2_PLACEMENT_3D ( 'NONE', #40462, #752, #88 ) ;
#7699=CIRCLE ( 'NONE', #2781, 59.00000000000000000 ) ;
#7700=VECTOR ( 'NONE', #31221, 1000.000000000000000 ) ;
#7701=CARTESIAN_POINT ( 'NONE',  ( 0.000000000000000000, -64.69195966009822030, -96.28577441832322847 ) ) ;
#7702=DIRECTION ( 'NONE',  ( 0.000000000000000000, 0.000000000000000000, 1.000000000000000000 ) ) ;
#7705=AXIS2_PLACEMENT_3D ( 'NONE', #33339, #10864, #10642 ) ;
#7707=DIRECTION ( 'NONE',  ( 0.000000000000000000, 0.000000000000000000, 1.000000000000000000 ) ) ;
#7708=ORIENTED_EDGE ( 'NONE', *, *, #39074, .T. ) ;
#7712=CARTESIAN_POINT ( 'NONE',  ( 17.99999999999999645, 0.000000000000000000, 0.000000000000000000 ) ) ;
#7720=AXIS2_PLACEMENT_3D ( 'NONE', #40748, #4315, #4098 ) ;
#7721=ORIENTED_EDGE ( 'NONE', *, *, #6940, .F. ) ;
#7726=VECTOR ( 'NONE', #36292, 1000.000000000000000 ) ;
#7730=DIRECTION ( 'NONE',  ( -1.000000000000000000, -0.000000000000000000, -0.000000000000000000 ) ) ;
#7733=AXIS2_PLACEMENT_3D ( 'NONE', #15413, #26280, #9464 ) ;
#7735=VECTOR ( 'NONE', #23277, 1000.000000000000000 ) ;
#7736=CARTESIAN_POINT ( 'NONE',  ( 0.000000000000000000, 51.27532863109366446, 99.79535634195144667 ) ) ;
#7738=EDGE_CURVE ( 'NONE', #25961, #41859, #10480, .T. ) ;
#7739=ORIENTED_EDGE ( 'NONE', *, *, #17389, .F. ) ;
#7746=VERTEX_POINT ( 'NONE', #38368 ) ;
#7749=AXIS2_PLACEMENT_3D ( 'NONE', #9006, #42573, #12938 ) ;
#7751=DIRECTION ( 'NONE',  ( 0.000000000000000000, -7.056502275159893199E-15, -1.000000000000000000 ) ) ;
#7752=ORIENTED_EDGE ( 'NONE', *, *, #34213, .T. ) ;
#7754=LINE ( 'NONE', #17624, #29150 ) ;
#7755=ADVANCED_FACE ( 'NONE', ( #11348 ), #41648, .F. ) ;
#7756=DIRECTION ( 'NONE',  ( 1.000000000000000000, 0.000000000000000000, 0.000000000000000000 ) ) ;
#7757=ORIENTED_EDGE ( 'NONE', *, *, #24547, .F. ) ;
#7758=CARTESIAN_POINT ( 'NONE',  ( 17.99999999999999645, 51.27532863109366446, 99.79535634195144667 ) ) ;
#7760=CIRCLE ( 'NONE', #35623, 116.0000000000000000 ) ;
#7765=DIRECTION ( 'NONE',  ( 0.000000000000000000, -0.9968120070307493474, -0.07978610555309324781 ) ) ;
#7770=DIRECTION ( 'NONE',  ( 1.000000000000000000, 0.000000000000000000, 0.000000000000000000 ) ) ;
#7774=EDGE_CURVE ( 'NONE', #43001, #27783, #35317, .T. ) ;
#7775=VERTEX_POINT ( 'NONE', #8283 ) ;
#7776=FACE_OUTER_BOUND ( 'NONE', #35032, .T. ) ;
#7777=CARTESIAN_POINT ( 'NONE',  ( 17.99999999999999645, 59.07817985939141181, -105.0250430397503294 ) ) ;
#7780=DIRECTION ( 'NONE',  ( 0.000000000000000000, -0.5963673585385078635, 0.8027116379309587879 ) ) ;
#7781=ORIENTED_EDGE ( 'NONE', *, *, #27248, .F. ) ;
#7784=CYLINDRICAL_SURFACE ( 'NONE', #11641, 59.00000000000000000 ) ;
#7785=DIRECTION ( 'NONE',  ( 1.000000000000000000, -0.000000000000000000, 0.000000000000000000 ) ) ;
#7786=LINE ( 'NONE', #21798, #6739 ) ;
#7787=ORIENTED_EDGE ( 'NONE', *, *, #40653, .T. ) ;
#7790=CARTESIAN_POINT ( 'NONE',  ( 0.000000000000000000, 96.25468616236661035, 72.49500943364525085 ) ) ;
#7793=CIRCLE ( 'NONE', #828, 120.5010000000000190 ) ;
#7795=APPLICATION_CONTEXT ( 'automotive_design' ) ;
#7798=CARTESIAN_POINT ( 'NONE',  ( 0.000000000000000000, 97.97378550988308632, -62.10585602713662468 ) ) ;
#7800=AXIS2_PLACEMENT_3D ( 'NONE', #18052, #31740, #24366 ) ;
#7805=CARTESIAN_POINT ( 'NONE',  ( 0.000000000000000000, 108.8684555192050425, -27.12806418649509865 ) ) ;
#7811=ORIENTED_EDGE ( 'NONE', *, *, #29679, .F. ) ;
#7812=CARTESIAN_POINT ( 'NONE',  ( 9.000000000000001776, 29.86146780999950323, 112.0905559814579675 ) ) ;
#7813=CARTESIAN_POINT ( 'NONE',  ( 17.99999999999999645, 64.69195966010022403, -96.28577441832183581 ) ) ;
#7815=ORIENTED_EDGE ( 'NONE', *, *, #29179, .F. ) ;
#7816=CARTESIAN_POINT ( 'NONE',  ( 17.99999999999999645, -112.1702510623870666, 2.471285140322257323 ) ) ;
#7832=DIRECTION ( 'NONE',  ( -1.000000000000000000, -0.000000000000000000, -0.000000000000000000 ) ) ;
#7833=DIRECTION ( 'NONE',  ( 0.000000000000000000, 0.000000000000000000, 1.000000000000000000 ) ) ;
#7835=FACE_OUTER_BOUND ( 'NONE', #34167, .T. ) ;
#7839=EDGE_LOOP ( 'NONE', ( #38943, #13836, #25595, #19842 ) ) ;
#7841=DIRECTION ( 'NONE',  ( 0.000000000000000000, 0.000000000000000000, 1.000000000000000000 ) ) ;
#7846=DIRECTION ( 'NONE',  ( -1.000000000000000000, -0.000000000000000000, 0.000000000000000000 ) ) ;
#7847=DIRECTION ( 'NONE',  ( 0.000000000000000000, 0.000000000000000000, 1.000000000000000000 ) ) ;
#7848=ORIENTED_EDGE ( 'NONE', *, *, #23782, .F. ) ;
#7851=CIRCLE ( 'NONE', #23211, 58.99999999999999289 ) ;
#7852=CARTESIAN_POINT ( 'NONE',  ( 17.99999999999999645, 63.24564713401792204, 102.5693868539697178 ) ) ;
#7853=ORIENTED_EDGE ( 'NONE', *, *, #16627, .F. ) ;
#7856=VERTEX_POINT ( 'NONE', #16130 ) ;
#7858=CARTESIAN_POINT ( 'NONE',  ( 17.99999999999999645, 83.49789599728902090, -86.88263557826680028 ) ) ;
#7860=ORIENTED_EDGE ( 'NONE', *, *, #11291, .T. ) ;
#7862=EDGE_CURVE ( 'NONE', #2989, #15836, #5641, .T. ) ;
#7863=AXIS2_PLACEMENT_3D ( 'NONE', #3228, #389, #33573 ) ;
#7865=CARTESIAN_POINT ( 'NONE',  ( 17.99999999999999645, -83.58328028049608349, -80.43528614701409651 ) ) ;
#7866=CYLINDRICAL_SURFACE ( 'NONE', #25154, 120.5010000000000190 ) ;
#7872=ORIENTED_EDGE ( 'NONE', *, *, #23023, .F. ) ;
#7873=DIRECTION ( 'NONE',  ( -1.000000000000000000, -0.000000000000000000, -0.000000000000000000 ) ) ;
#7876=FACE_OUTER_BOUND ( 'NONE', #34785, .T. ) ;
#7883=CYLINDRICAL_SURFACE ( 'NONE', #1162, 116.0000000000000000 ) ;
#7885=CARTESIAN_POINT ( 'NONE',  ( 0.000000000000000000, 52.88069566989454273, 103.2454939717370905 ) ) ;
#7888=VERTEX_POINT ( 'NONE', #5850 ) ;
#7890=ORIENTED_EDGE ( 'NONE', *, *, #39115, .F. ) ;
#7892=AXIS2_PLACEMENT_3D ( 'NONE', #38084, #4264, #14127 ) ;
#7899=EDGE_CURVE ( 'NONE', #714, #2641, #28796, .T. ) ;
#7901=DIRECTION ( 'NONE',  ( 0.000000000000000000, -0.9968120070307509017, 0.07978610555307326380 ) ) ;
#7902=ORIENTED_EDGE ( 'NONE', *, *, #36421, .F. ) ;
#7903=CARTESIAN_POINT ( 'NONE',  ( 0.000000000000000000, 111.7974656912330005, 9.465682155095883843 ) ) ;
#7904=EDGE_LOOP ( 'NONE', ( #35000, #7624, #13097, #16086 ) ) ;
#7911=CIRCLE ( 'NONE', #208, 116.0000000000000000 ) ;
#7912=DIRECTION ( 'NONE',  ( 0.000000000000000000, -0.5963673585384915432, -0.8027116379309710004 ) ) ;
#7915=ORIENTED_EDGE ( 'NONE', *, *, #2030, .T. ) ;
#7916=AXIS2_PLACEMENT_3D ( 'NONE', #42326, #32518, #12259 ) ;
#7919=LINE ( 'NONE', #21281, #11685 ) ;
#7921=CARTESIAN_POINT ( 'NONE',  ( 0.000000000000000000, 11.41303419184972689, 111.6154788735836405 ) ) ;
#7925=ORIENTED_EDGE ( 'NONE', *, *, #39381, .T. ) ;
#7929=DIRECTION ( 'NONE',  ( 1.000000000000000000, 0.000000000000000000, 0.000000000000000000 ) ) ;
#7930=ORIENTED_EDGE ( 'NONE', *, *, #30038, .F. ) ;
#7936=CIRCLE ( 'NONE', #39269, 58.99999999999998579 ) ;
#7945=DIRECTION ( 'NONE',  ( 0.000000000000000000, 0.000000000000000000, 1.000000000000000000 ) ) ;
#7946=EDGE_CURVE ( 'NONE', #29277, #21041, #40063, .T. ) ;
#7950=VERTEX_POINT ( 'NONE', #795 ) ;
#7955=AXIS2_PLACEMENT_3D ( 'NONE', #19767, #33031, #3117 ) ;
#7958=VERTEX_POINT ( 'NONE', #7137 ) ;
#7961=EDGE_CURVE ( 'NONE', #15394, #30264, #41867, .T. ) ;
#7964=AXIS2_PLACEMENT_3D ( 'NONE', #24929, #2353, #28396 ) ;
#7966=DIRECTION ( 'NONE',  ( 0.000000000000000000, 0.000000000000000000, 1.000000000000000000 ) ) ;
#7970=CIRCLE ( 'NONE', #39990, 116.0000000000000000 ) ;
#7971=CARTESIAN_POINT ( 'NONE',  ( 17.99999999999999645, -0.5156212287272186057, -112.1962860721878172 ) ) ;
#7973=DIRECTION ( 'NONE',  ( -1.000000000000000000, -0.000000000000000000, -0.000000000000000000 ) ) ;
#7975=FILL_AREA_STYLE ('',( #6735 ) ) ;
#7982=AXIS2_PLACEMENT_3D ( 'NONE', #2693, #16266, #30003 ) ;
#7983=DIRECTION ( 'NONE',  ( 0.000000000000000000, 0.000000000000000000, -1.000000000000000000 ) ) ;
#7988=DIRECTION ( 'NONE',  ( 0.000000000000000000, 0.5528000653611888637, 0.8333139190825179510 ) ) ;
#7994=CARTESIAN_POINT ( 'NONE',  ( 0.000000000000000000, 120.4984140710909344, -0.7894348306988346886 ) ) ;
#7997=AXIS2_PLACEMENT_3D ( 'NONE', #26039, #2229, #25640 ) ;
#8003=CARTESIAN_POINT ( 'NONE',  ( 0.000000000000000000, -57.40245293794732362, 96.40140491896615060 ) ) ;
#8012=ADVANCED_FACE ( 'NONE', ( #17225 ), #16578, .F. ) ;
#8013=CIRCLE ( 'NONE', #15705, 59.00000000000001421 ) ;
#8015=DIRECTION ( 'NONE',  ( 0.000000000000000000, -0.9213119778704166318, 0.3888241754733122724 ) ) ;
#8016=VERTEX_POINT ( 'NONE', #138 ) ;
#8018=ORIENTED_EDGE ( 'NONE', *, *, #32064, .T. ) ;
#8019=CARTESIAN_POINT ( 'NONE',  ( 17.99999999999999645, 0.000000000000000000, 0.000000000000000000 ) ) ;
#8022=ADVANCED_FACE ( 'NONE', ( #13500 ), #14152, .F. ) ;
#8025=CARTESIAN_POINT ( 'NONE',  ( 17.99999999999999645, -6.486220790507708500, -112.0098273076987994 ) ) ;
#8026=AXIS2_PLACEMENT_3D ( 'NONE', #22548, #15992, #36014 ) ;
#8028=CARTESIAN_POINT ( 'NONE',  ( 17.99999999999999645, 0.000000000000000000, 0.000000000000000000 ) ) ;
#8030=ORIENTED_EDGE ( 'NONE', *, *, #9227, .T. ) ;
#8031=CIRCLE ( 'NONE', #11541, 116.0000000000000000 ) ;
#8032=CARTESIAN_POINT ( 'NONE',  ( 0.000000000000000000, 24.22031524826126514, -109.5520369638034879 ) ) ;
#8040=AXIS2_PLACEMENT_3D ( 'NONE', #2666, #38689, #16030 ) ;
#8045=EDGE_LOOP ( 'NONE', ( #42682, #18932, #21792, #5748 ) ) ;
#8048=DIRECTION ( 'NONE',  ( 0.000000000000000000, 0.9213119778704139673, -0.3888241754733183231 ) ) ;
#8050=ORIENTED_EDGE ( 'NONE', *, *, #4248, .T. ) ;
#8052=CARTESIAN_POINT ( 'NONE',  ( 0.000000000000000000, -114.6488492393081913, 37.09625815499973100 ) ) ;
#8053=VECTOR ( 'NONE', #7643, 1000.000000000000000 ) ;
#8054=DIRECTION ( 'NONE',  ( 0.000000000000000000, 0.000000000000000000, 1.000000000000000000 ) ) ;
#8061=ORIENTED_EDGE ( 'NONE', *, *, #27032, .T. ) ;
#8062=VECTOR ( 'NONE', #1210, 1000.000000000000000 ) ;
#8069=ORIENTED_EDGE ( 'NONE', *, *, #27597, .F. ) ;
#8072=DIRECTION ( 'NONE',  ( 1.000000000000000000, 0.000000000000000000, 0.000000000000000000 ) ) ;
#8079=CYLINDRICAL_SURFACE ( 'NONE', #3849, 116.0000000000000000 ) ;
#8080=VERTEX_POINT ( 'NONE', #13289 ) ;
#8082=DIRECTION ( 'NONE',  ( 0.000000000000000000, 0.9826841245925203028, 0.1852887240871181618 ) ) ;
#8085=DIRECTION ( 'NONE',  ( -1.000000000000000000, 0.000000000000000000, 0.000000000000000000 ) ) ;
#8086=CIRCLE ( 'NONE', #37322, 59.00000000000000711 ) ;
#8087=VERTEX_POINT ( 'NONE', #30513 ) ;
#8089=CIRCLE ( 'NONE', #19966, 116.0000000000000000 ) ;
#8092=EDGE_CURVE ( 'NONE', #1587, #27890, #33489, .T. ) ;
#8095=DIRECTION ( 'NONE',  ( 0.000000000000000000, 0.000000000000000000, 1.000000000000000000 ) ) ;
#8096=DIRECTION ( 'NONE',  ( 0.000000000000000000, -0.9996456111234522934, -0.02662052143778445915 ) ) ;
#8097=ADVANCED_FACE ( 'NONE', ( #11090 ), #38109, .F. ) ;
#8098=FACE_OUTER_BOUND ( 'NONE', #42977, .T. ) ;
#8100=CIRCLE ( 'NONE', #12291, 116.0000000000000000 ) ;
#8105=CIRCLE ( 'NONE', #13699, 120.5010000000000332 ) ;
#8106=CARTESIAN_POINT ( 'NONE',  ( 9.000000000000001776, 98.69720329641039314, -60.94966826379810243 ) ) ;
#8107=DIRECTION ( 'NONE',  ( -1.000000000000000000, 0.000000000000000000, 0.000000000000000000 ) ) ;
#8110=EDGE_CURVE ( 'NONE', #33918, #17817, #21028, .T. ) ;
#8114=DIRECTION ( 'NONE',  ( -1.000000000000000000, 0.000000000000000000, 0.000000000000000000 ) ) ;
#8117=VECTOR ( 'NONE', #4866, 1000.000000000000000 ) ;
#8120=ORIENTED_EDGE ( 'NONE', *, *, #11107, .T. ) ;
#8123=ORIENTED_EDGE ( 'NONE', *, *, #31324, .T. ) ;
#8131=EDGE_CURVE ( 'NONE', #12660, #14763, #40944, .T. ) ;
#8133=CIRCLE ( 'NONE', #1140, 59.00000000000000000 ) ;
#8134=EDGE_CURVE ( 'NONE', #8627, #2879, #23781, .T. ) ;
#8135=CARTESIAN_POINT ( 'NONE',  ( 0.000000000000000000, 18.35539002514530793, -110.6858262410707994 ) ) ;
#8136=ORIENTED_EDGE ( 'NONE', *, *, #42928, .F. ) ;
#8138=AXIS2_PLACEMENT_3D ( 'NONE', #39870, #19646, #32912 ) ;
#8143=DIRECTION ( 'NONE',  ( 0.000000000000000000, -0.9213119778704086382, -0.3888241754733307021 ) ) ;
#8145=DIRECTION ( 'NONE',  ( -1.000000000000000000, 0.000000000000000000, 0.000000000000000000 ) ) ;
#8149=DIRECTION ( 'NONE',  ( -1.000000000000000000, 0.000000000000000000, 0.000000000000000000 ) ) ;
#8151=DIRECTION ( 'NONE',  ( 0.000000000000000000, 0.1590634960190723812, -0.9872683547213445543 ) ) ;
#8153=EDGE_CURVE ( 'NONE', #26461, #32652, #4941, .T. ) ;
#8154=CARTESIAN_POINT ( 'NONE',  ( 17.99999999999999645, 53.40478689619730090, 108.0204598100367548 ) ) ;
#8158=AXIS2_PLACEMENT_3D ( 'NONE', #34125, #34776, #27598 ) ;
#8160=CIRCLE ( 'NONE', #40866, 116.0000000000000000 ) ;
#8162=AXIS2_PLACEMENT_3D ( 'NONE', #29819, #25906, #6655 ) ;
#8166=DIRECTION ( 'NONE',  ( 0.000000000000000000, 0.000000000000000000, -1.000000000000000000 ) ) ;
#8167=VECTOR ( 'NONE', #24360, 1000.000000000000000 ) ;
#8168=CARTESIAN_POINT ( 'NONE',  ( 17.99999999999999645, -96.25468616236614139, -72.49500943364587613 ) ) ;
#8170=VECTOR ( 'NONE', #29084, 1000.000000000000000 ) ;
#8172=DIRECTION ( 'NONE',  ( 1.000000000000000000, 0.000000000000000000, 0.000000000000000000 ) ) ;
#8183=VERTEX_POINT ( 'NONE', #7790 ) ;
#8187=EDGE_CURVE ( 'NONE', #42630, #2738, #40450, .T. ) ;
#8191=DIRECTION ( 'NONE',  ( -1.000000000000000000, 0.000000000000000000, -0.000000000000000000 ) ) ;
#8194=FACE_OUTER_BOUND ( 'NONE', #36119, .T. ) ;
#8197=CIRCLE ( 'NONE', #8877, 59.00000000000000000 ) ;
#8199=EDGE_CURVE ( 'NONE', #9794, #20914, #27250, .T. ) ;
#8201=CARTESIAN_POINT ( 'NONE',  ( 17.99999999999999645, -5.456439917444183330, -112.0647122740742390 ) ) ;
#8206=LINE ( 'NONE', #14331, #30878 ) ;
#8212=CARTESIAN_POINT ( 'NONE',  ( 17.99999999999999645, 0.000000000000000000, 0.000000000000000000 ) ) ;
#8215=ADVANCED_FACE ( 'NONE', ( #31366 ), #14588, .F. ) ;
#8216=CARTESIAN_POINT ( 'NONE',  ( 0.000000000000000000, 0.000000000000000000, 0.000000000000000000 ) ) ;
#8217=ORIENTED_EDGE ( 'NONE', *, *, #42164, .F. ) ;
#8219=DIRECTION ( 'NONE',  ( 0.000000000000000000, 0.000000000000000000, 1.000000000000000000 ) ) ;
#8224=ORIENTED_EDGE ( 'NONE', *, *, #8397, .T. ) ;
#8226=ORIENTED_EDGE ( 'NONE', *, *, #10834, .T. ) ;
#8228=CARTESIAN_POINT ( 'NONE',  ( 0.000000000000000000, -120.4984140710909202, -0.7894348306996294973 ) ) ;
#8230=AXIS2_PLACEMENT_3D ( 'NONE', #37567, #21043, #18847 ) ;
#8234=ORIENTED_EDGE ( 'NONE', *, *, #26069, .F. ) ;
#8238=VERTEX_POINT ( 'NONE', #17876 ) ;
#8243=DIRECTION ( 'NONE',  ( 0.000000000000000000, 0.9968120070307504577, -0.07978610555307977248 ) ) ;
#8244=DIRECTION ( 'NONE',  ( 1.000000000000000000, 0.000000000000000000, 0.000000000000000000 ) ) ;
#8245=VERTEX_POINT ( 'NONE', #41364 ) ;
#8246=DIRECTION ( 'NONE',  ( 0.000000000000000000, 0.000000000000000000, 1.000000000000000000 ) ) ;
#8247=ORIENTED_EDGE ( 'NONE', *, *, #8682, .F. ) ;
#8251=CIRCLE ( 'NONE', #27066, 116.0000000000000000 ) ;
#8255=ORIENTED_EDGE ( 'NONE', *, *, #22136, .F. ) ;
#8257=CARTESIAN_POINT ( 'NONE',  ( -10.00000000000000000, 0.000000000000000000, 0.000000000000000000 ) ) ;
#8258=ORIENTED_EDGE ( 'NONE', *, *, #15006, .F. ) ;
#8266=EDGE_CURVE ( 'NONE', #16946, #40970, #25707, .T. ) ;
#8268=EDGE_CURVE ( 'NONE', #18966, #16222, #22431, .T. ) ;
#8269=CARTESIAN_POINT ( 'NONE',  ( 17.99999999999999645, -91.65951123222531294, 71.09524597798055368 ) ) ;
#8277=FACE_OUTER_BOUND ( 'NONE', #40523, .T. ) ;
#8280=FACE_OUTER_BOUND ( 'NONE', #10413, .T. ) ;
#8281=ORIENTED_EDGE ( 'NONE', *, *, #43094, .T. ) ;
#8283=CARTESIAN_POINT ( 'NONE',  ( 17.99999999999999645, 8.827181066045881153, 120.1772519049559662 ) ) ;
#8288=ORIENTED_EDGE ( 'NONE', *, *, #15660, .T. ) ;
#8289=CARTESIAN_POINT ( 'NONE',  ( 17.99999999999999645, -59.07817985938929439, -105.0250430397515089 ) ) ;
#8292=CARTESIAN_POINT ( 'NONE',  ( 17.99999999999999645, 0.000000000000000000, 0.000000000000000000 ) ) ;
#8294=DIRECTION ( 'NONE',  ( -1.000000000000000000, 0.000000000000000000, 0.000000000000000000 ) ) ;
#8296=CARTESIAN_POINT ( 'NONE',  ( 17.99999999999999645, -75.72520367775034345, -82.78868281116056949 ) ) ;
#8299=CARTESIAN_POINT ( 'NONE',  ( 0.000000000000000000, -21.55123232222555529, 118.5581519187671518 ) ) ;
#8300=ORIENTED_EDGE ( 'NONE', *, *, #35134, .F. ) ;
#8301=CYLINDRICAL_SURFACE ( 'NONE', #40535, 59.00000000000000000 ) ;
#8305=AXIS2_PLACEMENT_3D ( 'NONE', #7358, #4071, #797 ) ;
#8306=CARTESIAN_POINT ( 'NONE',  ( 17.99999999999999645, -79.94368240339484544, 90.16373242487880191 ) ) ;
#8311=DIRECTION ( 'NONE',  ( -1.000000000000000000, 0.000000000000000000, 0.000000000000000000 ) ) ;
#8316=ORIENTED_EDGE ( 'NONE', *, *, #41115, .F. ) ;
#8321=DIRECTION ( 'NONE',  ( -1.000000000000000000, 0.000000000000000000, 0.000000000000000000 ) ) ;
#8322=ADVANCED_FACE ( 'NONE', ( #12588 ), #5796, .F. ) ;
#8327=EDGE_LOOP ( 'NONE', ( #20804, #26585, #13554, #42176 ) ) ;
#8331=AXIS2_PLACEMENT_3D ( 'NONE', #13307, #2990, #29445 ) ;
#8336=ORIENTED_EDGE ( 'NONE', *, *, #35197, .F. ) ;
#8340=EDGE_CURVE ( 'NONE', #7274, #39353, #32421, .T. ) ;
#8341=ORIENTED_EDGE ( 'NONE', *, *, #28631, .T. ) ;
#8344=VERTEX_POINT ( 'NONE', #18956 ) ;
#8346=DIRECTION ( 'NONE',  ( -1.000000000000000000, -0.000000000000000000, 0.000000000000000000 ) ) ;
#8348=CARTESIAN_POINT ( 'NONE',  ( 17.99999999999999645, 68.63002662989875091, -93.51962064069435598 ) ) ;
#8352=DIRECTION ( 'NONE',  ( 1.000000000000000000, 0.000000000000000000, 0.000000000000000000 ) ) ;
#8357=ORIENTED_EDGE ( 'NONE', *, *, #6863, .T. ) ;
#8358=CYLINDRICAL_SURFACE ( 'NONE', #12970, 120.5010000000000190 ) ;
#8359=CIRCLE ( 'NONE', #38989, 59.00000000000000000 ) ;
#8361=CARTESIAN_POINT ( 'NONE',  ( 0.000000000000000000, -88.56657216608570593, -68.87840567546012949 ) ) ;
#8362=CIRCLE ( 'NONE', #38990, 59.00000000000000000 ) ;
#8364=CIRCLE ( 'NONE', #28605, 120.5010000000000190 ) ;
#8366=VERTEX_POINT ( 'NONE', #15869 ) ;
#8368=EDGE_CURVE ( 'NONE', #10198, #16946, #28696, .T. ) ;
#8369=ORIENTED_EDGE ( 'NONE', *, *, #43064, .F. ) ;
#8371=DIRECTION ( 'NONE',  ( -1.000000000000000000, 0.000000000000000000, 0.000000000000000000 ) ) ;
#8373=CARTESIAN_POINT ( 'NONE',  ( 0.000000000000000000, -100.8494052988175298, 65.95368414178875582 ) ) ;
#8375=CARTESIAN_POINT ( 'NONE',  ( 17.99999999999999645, -112.5120133921104753, -43.14554256761131512 ) ) ;
#8378=VERTEX_POINT ( 'NONE', #25484 ) ;
#8381=VECTOR ( 'NONE', #35125, 1000.000000000000000 ) ;
#8388=AXIS2_PLACEMENT_3D ( 'NONE', #24905, #28584, #21422 ) ;
#8389=EDGE_CURVE ( 'NONE', #38794, #11221, #39791, .T. ) ;
#8393=AXIS2_PLACEMENT_3D ( 'NONE', #30238, #9936, #23285 ) ;
#8397=EDGE_CURVE ( 'NONE', #35404, #40182, #23806, .T. ) ;
#8400=CARTESIAN_POINT ( 'NONE',  ( 0.000000000000000000, 35.54274411428055913, 115.1399337407607959 ) ) ;
#8404=DIRECTION ( 'NONE',  ( 0.000000000000000000, 0.000000000000000000, 1.000000000000000000 ) ) ;
#8406=ORIENTED_EDGE ( 'NONE', *, *, #41186, .F. ) ;
#8410=DIRECTION ( 'NONE',  ( 0.000000000000000000, 0.8183027759081702435, -0.5747874102144052699 ) ) ;
#8411=DIRECTION ( 'NONE',  ( 0.000000000000000000, 0.000000000000000000, 1.000000000000000000 ) ) ;
#8414=DIRECTION ( 'NONE',  ( -1.000000000000000000, 0.000000000000000000, 0.000000000000000000 ) ) ;
#8420=AXIS2_PLACEMENT_3D ( 'NONE', #30411, #486, #3096 ) ;
#8422=DIRECTION ( 'NONE',  ( -1.000000000000000000, 0.000000000000000000, 0.000000000000000000 ) ) ;
#8428=AXIS2_PLACEMENT_3D ( 'NONE', #34620, #1665, #1011 ) ;
#8430=VERTEX_POINT ( 'NONE', #33493 ) ;
#8431=CYLINDRICAL_SURFACE ( 'NONE', #42981, 116.0000000000000000 ) ;
#8433=CARTESIAN_POINT ( 'NONE',  ( 17.99999999999999645, 47.31079789947484926, 105.9135893174952656 ) ) ;
#8435=DIRECTION ( 'NONE',  ( -1.000000000000000000, -0.000000000000000000, -0.000000000000000000 ) ) ;
#8436=ORIENTED_EDGE ( 'NONE', *, *, #29956, .T. ) ;
#8438=CARTESIAN_POINT ( 'NONE',  ( 0.000000000000000000, 0.000000000000000000, 0.000000000000000000 ) ) ;
#8439=ORIENTED_EDGE ( 'NONE', *, *, #986, .F. ) ;
#8440=DIRECTION ( 'NONE',  ( 1.000000000000000000, 0.000000000000000000, 0.000000000000000000 ) ) ;
#8442=ORIENTED_EDGE ( 'NONE', *, *, #10611, .F. ) ;
#8445=EDGE_CURVE ( 'NONE', #1680, #42118, #30230, .T. ) ;
#8447=ADVANCED_FACE ( 'NONE', ( #3143 ), #40454, .F. ) ;
#8448=EDGE_CURVE ( 'NONE', #39845, #31846, #9137, .T. ) ;
#8449=CARTESIAN_POINT ( 'NONE',  ( 9.000000000000001776, 6.854627147200274884, -115.7972974066012881 ) ) ;
#8454=ORIENTED_EDGE ( 'NONE', *, *, #37718, .T. ) ;
#8458=DIRECTION ( 'NONE',  ( 1.000000000000000000, 0.000000000000000000, 0.000000000000000000 ) ) ;
#8459=CIRCLE ( 'NONE', #32835, 116.0000000000000000 ) ;
#8461=ORIENTED_EDGE ( 'NONE', *, *, #42063, .T. ) ;
#8462=CARTESIAN_POINT ( 'NONE',  ( 0.000000000000000000, 0.000000000000000000, 0.000000000000000000 ) ) ;
#8464=AXIS2_PLACEMENT_3D ( 'NONE', #21069, #706, #13415 ) ;
#8465=CYLINDRICAL_SURFACE ( 'NONE', #20439, 59.00000000000000000 ) ;
#8468=EDGE_LOOP ( 'NONE', ( #29319, #34464, #6901, #4215 ) ) ;
#8470=DIRECTION ( 'NONE',  ( -1.000000000000000000, 0.000000000000000000, 0.000000000000000000 ) ) ;
#8471=EDGE_CURVE ( 'NONE', #23588, #6470, #32129, .T. ) ;
#8474=ORIENTED_EDGE ( 'NONE', *, *, #42095, .F. ) ;
#8478=CIRCLE ( 'NONE', #33547, 58.99999999999999289 ) ;
#8480=VECTOR ( 'NONE', #23292, 1000.000000000000000 ) ;
#8481=CARTESIAN_POINT ( 'NONE',  ( 0.000000000000000000, 92.25992191227393846, 77.51514567967427638 ) ) ;
#8484=CARTESIAN_POINT ( 'NONE',  ( 17.99999999999999645, 111.2721026680458749, 14.38025178762809908 ) ) ;
#8485=VERTEX_POINT ( 'NONE', #16518 ) ;
#8486=DIRECTION ( 'NONE',  ( 0.000000000000000000, -0.05322217484216511946, -0.9985826956767627216 ) ) ;
#8491=AXIS2_PLACEMENT_3D ( 'NONE', #6997, #17075, #206 ) ;
#8492=ORIENTED_EDGE ( 'NONE', *, *, #6127, .T. ) ;
#8493=CARTESIAN_POINT ( 'NONE',  ( 0.000000000000000000, -80.74349901498459303, 77.90224541347254217 ) ) ;
#8494=CYLINDRICAL_SURFACE ( 'NONE', #35425, 120.5010000000000190 ) ;
#8499=EDGE_CURVE ( 'NONE', #25660, #15814, #36529, .T. ) ;
#8502=ORIENTED_EDGE ( 'NONE', *, *, #411, .T. ) ;
#8503=CARTESIAN_POINT ( 'NONE',  ( 0.000000000000000000, 105.3681574666269256, -38.54638589714782881 ) ) ;
#8504=DIRECTION ( 'NONE',  ( 0.000000000000000000, 0.9996456111234526265, -0.02662052143777152158 ) ) ;
#8506=EDGE_CURVE ( 'NONE', #13412, #24013, #40480, .T. ) ;
#8509=CYLINDRICAL_SURFACE ( 'NONE', #25280, 116.0000000000000000 ) ;
#8512=AXIS2_PLACEMENT_3D ( 'NONE', #2862, #39102, #9663 ) ;
#8516=DIRECTION ( 'NONE',  ( -1.000000000000000000, 0.000000000000000000, -0.000000000000000000 ) ) ;
#8518=DIRECTION ( 'NONE',  ( 1.000000000000000000, 0.000000000000000000, 0.000000000000000000 ) ) ;
#8522=CIRCLE ( 'NONE', #17631, 59.00000000000001421 ) ;
#8526=ORIENTED_EDGE ( 'NONE', *, *, #8743, .F. ) ;
#8529=DIRECTION ( 'NONE',  ( -1.000000000000000000, 0.000000000000000000, 0.000000000000000000 ) ) ;
#8532=AXIS2_PLACEMENT_3D ( 'NONE', #24440, #14390, #22032 ) ;
#8541=AXIS2_PLACEMENT_3D ( 'NONE', #1453, #8654, #11305 ) ;
#8546=ORIENTED_EDGE ( 'NONE', *, *, #16994, .F. ) ;
#8548=VERTEX_POINT ( 'NONE', #37186 ) ;
#8549=CARTESIAN_POINT ( 'NONE',  ( 0.000000000000000000, -93.26762629039376407, -76.29967815892449323 ) ) ;
#8559=EDGE_CURVE ( 'NONE', #25806, #20272, #14102, .T. ) ;
#8561=CARTESIAN_POINT ( 'NONE',  ( 17.99999999999999645, 100.6739960869724655, -49.52796165323157851 ) ) ;
#8562=EDGE_CURVE ( 'NONE', #37783, #40263, #23711, .T. ) ;
#8566=VECTOR ( 'NONE', #33952, 1000.000000000000000 ) ;
#8569=DIRECTION ( 'NONE',  ( -1.000000000000000000, -0.000000000000000000, -0.000000000000000000 ) ) ;
#8571=CARTESIAN_POINT ( 'NONE',  ( 17.99999999999999645, 17.33727698085173330, 110.8498592715974098 ) ) ;
#8575=CIRCLE ( 'NONE', #20453, 59.00000000000000000 ) ;
#8577=ORIENTED_EDGE ( 'NONE', *, *, #11974, .F. ) ;
#8582=DIRECTION ( 'NONE',  ( 0.000000000000000000, 0.9407002666710341243, -0.3392388661180278930 ) ) ;
#8583=ORIENTED_EDGE ( 'NONE', *, *, #13119, .F. ) ;
#8586=LINE ( 'NONE', #42801, #27103 ) ;
#8588=CARTESIAN_POINT ( 'NONE',  ( 0.000000000000000000, 110.3490479609632615, -20.28201389785435182 ) ) ;
#8592=ORIENTED_EDGE ( 'NONE', *, *, #2958, .T. ) ;
#8593=EDGE_CURVE ( 'NONE', #38227, #32590, #2845, .T. ) ;
#8595=VECTOR ( 'NONE', #26201, 1000.000000000000000 ) ;
#8596=ORIENTED_EDGE ( 'NONE', *, *, #25211, .F. ) ;
#8598=ORIENTED_EDGE ( 'NONE', *, *, #3080, .F. ) ;
#8600=ORIENTED_EDGE ( 'NONE', *, *, #9916, .F. ) ;
#8602=EDGE_CURVE ( 'NONE', #41947, #13537, #8459, .T. ) ;
#8608=DIRECTION ( 'NONE',  ( 0.000000000000000000, 0.000000000000000000, 1.000000000000000000 ) ) ;
#8610=ADVANCED_FACE ( 'NONE', ( #15197 ), #17607, .F. ) ;
#8611=DIRECTION ( 'NONE',  ( 0.000000000000000000, -0.3140767120219556952, 0.9493976084683790617 ) ) ;
#8612=ORIENTED_EDGE ( 'NONE', *, *, #7321, .T. ) ;
#8613=DIRECTION ( 'NONE',  ( 0.000000000000000000, 0.3140767120219428166, 0.9493976084683832806 ) ) ;
#8617=DIRECTION ( 'NONE',  ( 0.000000000000000000, 0.000000000000000000, 1.000000000000000000 ) ) ;
#8619=CIRCLE ( 'NONE', #33684, 116.0000000000000000 ) ;
#8621=CYLINDRICAL_SURFACE ( 'NONE', #30918, 59.00000000000000000 ) ;
#8622=VERTEX_POINT ( 'NONE', #18263 ) ;
#8624=LINE ( 'NONE', #24609, #38636 ) ;
#8626=ADVANCED_FACE ( 'NONE', ( #14751 ), #31317, .F. ) ;
#8627=VERTEX_POINT ( 'NONE', #4681 ) ;
#8628=CARTESIAN_POINT ( 'NONE',  ( 17.99999999999999645, 0.000000000000000000, 0.000000000000000000 ) ) ;
#8630=DIRECTION ( 'NONE',  ( -1.000000000000000000, 0.000000000000000000, -0.000000000000000000 ) ) ;
#8633=FACE_OUTER_BOUND ( 'NONE', #33017, .T. ) ;
#8636=DIRECTION ( 'NONE',  ( 0.000000000000000000, 0.000000000000000000, 1.000000000000000000 ) ) ;
#8637=ORIENTED_EDGE ( 'NONE', *, *, #18227, .F. ) ;
#8638=CIRCLE ( 'NONE', #17718, 120.5010000000000190 ) ;
#8639=DIRECTION ( 'NONE',  ( 0.000000000000000000, -1.599473849036242511E-14, -1.000000000000000000 ) ) ;
#8646=CARTESIAN_POINT ( 'NONE',  ( -10.00000000000000000, 0.000000000000000000, 0.000000000000000000 ) ) ;
#8647=CIRCLE ( 'NONE', #4457, 59.00000000000000711 ) ;
#8648=EDGE_CURVE ( 'NONE', #18183, #26358, #26620, .T. ) ;
#8651=AXIS2_PLACEMENT_3D ( 'NONE', #19563, #35874, #26097 ) ;
#8654=DIRECTION ( 'NONE',  ( -1.000000000000000000, -0.000000000000000000, -0.000000000000000000 ) ) ;
#8655=AXIS2_PLACEMENT_3D ( 'NONE', #29625, #13061, #26361 ) ;
#8661=DIRECTION ( 'NONE',  ( 0.000000000000000000, 0.000000000000000000, 1.000000000000000000 ) ) ;
#8665=DIRECTION ( 'NONE',  ( 1.000000000000000000, 0.000000000000000000, 0.000000000000000000 ) ) ;
#8666=EDGE_CURVE ( 'NONE', #35643, #1340, #33552, .T. ) ;
#8667=CARTESIAN_POINT ( 'NONE',  ( -10.00000000000000000, 0.000000000000000000, 0.000000000000000000 ) ) ;
#8668=CARTESIAN_POINT ( 'NONE',  ( 17.99999999999999645, 0.000000000000000000, 0.000000000000000000 ) ) ;
#8670=CARTESIAN_POINT ( 'NONE',  ( 0.000000000000000000, 78.18175027177548486, -85.69488855492920720 ) ) ;
#8671=ORIENTED_EDGE ( 'NONE', *, *, #6347, .T. ) ;
#8678=VECTOR ( 'NONE', #17888, 1000.000000000000000 ) ;
#8680=DIRECTION ( 'NONE',  ( 0.000000000000000000, 0.000000000000000000, 1.000000000000000000 ) ) ;
#8682=EDGE_CURVE ( 'NONE', #18274, #10688, #19667, .T. ) ;
#8691=EDGE_LOOP ( 'NONE', ( #21194, #10462, #7293, #6050 ) ) ;
#8693=CYLINDRICAL_SURFACE ( 'NONE', #25029, 116.0000000000000000 ) ;
#8694=DIRECTION ( 'NONE',  ( 0.000000000000000000, 0.5963673585385025344, -0.8027116379309628957 ) ) ;
#8695=DIRECTION ( 'NONE',  ( 0.000000000000000000, 0.000000000000000000, 1.000000000000000000 ) ) ;
#8696=ORIENTED_EDGE ( 'NONE', *, *, #10733, .F. ) ;
#8697=FACE_OUTER_BOUND ( 'NONE', #38538, .T. ) ;
#8700=VERTEX_POINT ( 'NONE', #41314 ) ;
#8703=VERTEX_POINT ( 'NONE', #11690 ) ;
#8704=DIRECTION ( 'NONE',  ( 0.000000000000000000, 0.2631025642275152121, 0.9647678688145175929 ) ) ;
#8706=AXIS2_PLACEMENT_3D ( 'NONE', #7198, #24487, #41218 ) ;
#8707=DIRECTION ( 'NONE',  ( 0.000000000000000000, 0.000000000000000000, 1.000000000000000000 ) ) ;
#8710=ADVANCED_FACE ( 'NONE', ( #1398 ), #24799, .F. ) ;
#8713=VERTEX_POINT ( 'NONE', #34792 ) ;
#8714=AXIS2_PLACEMENT_3D ( 'NONE', #580, #23544, #7348 ) ;
#8715=DIRECTION ( 'NONE',  ( -1.000000000000000000, -0.000000000000000000, -0.000000000000000000 ) ) ;
#8716=DIRECTION ( 'NONE',  ( 1.000000000000000000, 0.000000000000000000, 0.000000000000000000 ) ) ;
#8718=CIRCLE ( 'NONE', #24107, 116.0000000000000000 ) ;
#8719=DIRECTION ( 'NONE',  ( -1.000000000000000000, 0.000000000000000000, -0.000000000000000000 ) ) ;
#8720=CARTESIAN_POINT ( 'NONE',  ( 0.000000000000000000, 115.0622509503834578, -14.72000021165029082 ) ) ;
#8725=FACE_OUTER_BOUND ( 'NONE', #25213, .T. ) ;
#8727=DIRECTION ( 'NONE',  ( 0.000000000000000000, 0.4132121857683791477, -0.9106347728549126774 ) ) ;
#8732=ORIENTED_EDGE ( 'NONE', *, *, #42266, .F. ) ;
#8733=CARTESIAN_POINT ( 'NONE',  ( 0.000000000000000000, 0.000000000000000000, 0.000000000000000000 ) ) ;
#8739=EDGE_CURVE ( 'NONE', #28542, #16567, #5001, .T. ) ;
#8742=AXIS2_PLACEMENT_3D ( 'NONE', #23850, #17975, #31245 ) ;
#8743=EDGE_CURVE ( 'NONE', #19682, #8854, #23840, .T. ) ;
#8746=AXIS2_PLACEMENT_3D ( 'NONE', #12823, #15899, #107 ) ;
#8747=CARTESIAN_POINT ( 'NONE',  ( 17.99999999999999645, -12.43843445475394027, 111.5058645182329116 ) ) ;
#8749=EDGE_CURVE ( 'NONE', #36535, #16214, #13343, .T. ) ;
#8750=DIRECTION ( 'NONE',  ( 0.000000000000000000, 0.7164567402983115230, 0.6976315211349884970 ) ) ;
#8755=ORIENTED_EDGE ( 'NONE', *, *, #27028, .F. ) ;
#8761=CARTESIAN_POINT ( 'NONE',  ( 17.99999999999999645, 29.36437154452156761, -116.8684075565133043 ) ) ;
#8762=ORIENTED_EDGE ( 'NONE', *, *, #8187, .T. ) ;
#8763=ORIENTED_EDGE ( 'NONE', *, *, #38033, .T. ) ;
#8764=LINE ( 'NONE', #28645, #7641 ) ;
#8770=CARTESIAN_POINT ( 'NONE',  ( 17.99999999999999645, -110.1579703617964725, -21.29539948940357164 ) ) ;
#8777=CIRCLE ( 'NONE', #4596, 120.5010000000000190 ) ;
#8781=VECTOR ( 'NONE', #26442, 1000.000000000000000 ) ;
#8785=VECTOR ( 'NONE', #9343, 1000.000000000000000 ) ;
#8792=EDGE_CURVE ( 'NONE', #40190, #38713, #28012, .T. ) ;
#8797=ORIENTED_EDGE ( 'NONE', *, *, #6474, .F. ) ;
#8800=CARTESIAN_POINT ( 'NONE',  ( -10.00000000000000000, 0.000000000000000000, 0.000000000000000000 ) ) ;
#8803=CIRCLE ( 'NONE', #31114, 59.00000000000000711 ) ;
#8806=CYLINDRICAL_SURFACE ( 'NONE', #23714, 120.5010000000000190 ) ;
#8809=EDGE_LOOP ( 'NONE', ( #25606, #615, #43086, #38960 ) ) ;
#8810=LINE ( 'NONE', #35825, #35431 ) ;
#8812=CIRCLE ( 'NONE', #37360, 59.00000000000000711 ) ;
#8814=CIRCLE ( 'NONE', #31816, 120.5010000000000332 ) ;
#8815=CARTESIAN_POINT ( 'NONE',  ( 17.99999999999999645, 115.9750404417044081, -2.406240749597859718 ) ) ;
#8817=ORIENTED_EDGE ( 'NONE', *, *, #27096, .T. ) ;
#8819=CARTESIAN_POINT ( 'NONE',  ( 17.99999999999999645, -30.01658535635337444, 108.1077105353196970 ) ) ;
#8820=AXIS2_PLACEMENT_3D ( 'NONE', #15657, #12592, #19379 ) ;
#8823=VERTEX_POINT ( 'NONE', #42540 ) ;
#8828=ADVANCED_FACE ( 'NONE', ( #12690 ), #19473, .F. ) ;
#8833=DIRECTION ( 'NONE',  ( -1.000000000000000000, -0.000000000000000000, -0.000000000000000000 ) ) ;
#8836=EDGE_LOOP ( 'NONE', ( #7431, #6903, #10664, #39928 ) ) ;
#8840=VECTOR ( 'NONE', #2807, 1000.000000000000000 ) ;
#8841=DIRECTION ( 'NONE',  ( -1.000000000000000000, -0.000000000000000000, -0.000000000000000000 ) ) ;
#8842=DIRECTION ( 'NONE',  ( 0.000000000000000000, 0.000000000000000000, -1.000000000000000000 ) ) ;
#8843=AXIS2_PLACEMENT_3D ( 'NONE', #23076, #12798, #13024 ) ;
#8845=DIRECTION ( 'NONE',  ( 1.000000000000000000, 0.000000000000000000, 0.000000000000000000 ) ) ;
#8846=CARTESIAN_POINT ( 'NONE',  ( 17.99999999999999645, -59.47573314508800735, 99.59235496188593117 ) ) ;
#8847=COLOUR_RGB ( '', 0.72549020, 0.75294118, 0.79215686) ;
#8848=ORIENTED_EDGE ( 'NONE', *, *, #8666, .F. ) ;
#8850=EDGE_CURVE ( 'NONE', #21953, #6529, #6387, .T. ) ;
#8853=AXIS2_PLACEMENT_3D ( 'NONE', #38926, #39335, #22400 ) ;
#8854=VERTEX_POINT ( 'NONE', #35998 ) ;
#8855=CARTESIAN_POINT ( 'NONE',  ( 17.99999999999999645, 46.83041522348636931, -101.9567785075596618 ) ) ;
#8861=EDGE_CURVE ( 'NONE', #27302, #33525, #9622, .T. ) ;
#8863=CYLINDRICAL_SURFACE ( 'NONE', #13788, 116.0000000000000000 ) ;
#8867=CIRCLE ( 'NONE', #40894, 116.0000000000000000 ) ;
#8868=CARTESIAN_POINT ( 'NONE',  ( 8.999999999999998224, 106.6051926090971023, 45.73109345704855855 ) ) ;
#8870=DIRECTION ( 'NONE',  ( 1.000000000000000000, 0.000000000000000000, 0.000000000000000000 ) ) ;
#8871=ORIENTED_EDGE ( 'NONE', *, *, #37193, .T. ) ;
#8875=CIRCLE ( 'NONE', #15873, 59.00000000000000000 ) ;
#8876=CARTESIAN_POINT ( 'NONE',  ( 0.000000000000000000, 0.000000000000000000, 0.000000000000000000 ) ) ;
#8877=AXIS2_PLACEMENT_3D ( 'NONE', #2282, #35468, #9068 ) ;
#8881=FACE_OUTER_BOUND ( 'NONE', #29516, .T. ) ;
#8882=CIRCLE ( 'NONE', #33263, 59.00000000000000000 ) ;
#8883=AXIS2_PLACEMENT_3D ( 'NONE', #1102, #34070, #18186 ) ;
#8885=FACE_OUTER_BOUND ( 'NONE', #35224, .T. ) ;
#8886=VERTEX_POINT ( 'NONE', #23818 ) ;
#8887=ORIENTED_EDGE ( 'NONE', *, *, #37368, .T. ) ;
#8888=CARTESIAN_POINT ( 'NONE',  ( 9.000000000000001776, -63.55543939553702160, -97.03971415477388973 ) ) ;
#8892=CYLINDRICAL_SURFACE ( 'NONE', #29242, 59.00000000000001421 ) ;
#8893=EDGE_CURVE ( 'NONE', #36084, #16529, #17592, .T. ) ;
#8896=ORIENTED_EDGE ( 'NONE', *, *, #36085, .T. ) ;
#8898=ORIENTED_EDGE ( 'NONE', *, *, #26928, .F. ) ;
#8899=CARTESIAN_POINT ( 'NONE',  ( 0.000000000000000000, -31.17727234463771424, 111.7317219465818852 ) ) ;
#8900=CYLINDRICAL_SURFACE ( 'NONE', #4531, 59.00000000000000000 ) ;
#8906=EDGE_CURVE ( 'NONE', #714, #5010, #14091, .T. ) ;
#8908=CARTESIAN_POINT ( 'NONE',  ( 17.99999999999999645, 119.0898412705476943, -18.38751498043618682 ) ) ;
#8917=EDGE_CURVE ( 'NONE', #14512, #5171, #41922, .T. ) ;
#8918=VERTEX_POINT ( 'NONE', #7417 ) ;
#8920=AXIS2_PLACEMENT_3D ( 'NONE', #8667, #2306, #18770 ) ;
#8923=DIRECTION ( 'NONE',  ( -1.000000000000000000, -0.000000000000000000, -0.000000000000000000 ) ) ;
#8926=FACE_OUTER_BOUND ( 'NONE', #17684, .T. ) ;
#8928=ORIENTED_EDGE ( 'NONE', *, *, #878, .F. ) ;
#8930=FACE_OUTER_BOUND ( 'NONE', #25854, .T. ) ;
#8931=ORIENTED_EDGE ( 'NONE', *, *, #37193, .F. ) ;
#8932=AXIS2_PLACEMENT_3D ( 'NONE', #5901, #11849, #25174 ) ;
#8937=VERTEX_POINT ( 'NONE', #7630 ) ;
#8938=LINE ( 'NONE', #25761, #40668 ) ;
#8940=ORIENTED_EDGE ( 'NONE', *, *, #42636, .F. ) ;
#8942=FACE_OUTER_BOUND ( 'NONE', #5937, .T. ) ;
#8943=DIRECTION ( 'NONE',  ( 0.000000000000000000, -0.6783118362696222148, 0.7347741508630615259 ) ) ;
#8944=EDGE_CURVE ( 'NONE', #1122, #31468, #14421, .T. ) ;
#8945=CARTESIAN_POINT ( 'NONE',  ( 17.99999999999999645, -68.63002662989681824, -93.51962064069581970 ) ) ;
#8946=CARTESIAN_POINT ( 'NONE',  ( 0.000000000000000000, -119.7318547011700502, -13.59315897125848238 ) ) ;
#8947=ORIENTED_EDGE ( 'NONE', *, *, #5829, .T. ) ;
#8950=CARTESIAN_POINT ( 'NONE',  ( 8.999999999999998224, 42.87700105098606684, 107.7847984684006377 ) ) ;
#8952=DIRECTION ( 'NONE',  ( 0.000000000000000000, 0.000000000000000000, -1.000000000000000000 ) ) ;
#8953=DIRECTION ( 'NONE',  ( 1.000000000000000000, 0.000000000000000000, 0.000000000000000000 ) ) ;
#8958=ORIENTED_EDGE ( 'NONE', *, *, #7648, .F. ) ;
#8961=ORIENTED_EDGE ( 'NONE', *, *, #21888, .F. ) ;
#8966=CARTESIAN_POINT ( 'NONE',  ( 0.000000000000000000, 29.36437154452156761, -116.8684075565133043 ) ) ;
#8968=EDGE_CURVE ( 'NONE', #2829, #34305, #33815, .T. ) ;
#8970=DIRECTION ( 'NONE',  ( 0.000000000000000000, 0.000000000000000000, 1.000000000000000000 ) ) ;
#8973=ORIENTED_EDGE ( 'NONE', *, *, #36026, .T. ) ;
#8975=DIRECTION ( 'NONE',  ( -1.000000000000000000, -0.000000000000000000, -0.000000000000000000 ) ) ;
#8976=ORIENTED_EDGE ( 'NONE', *, *, #32064, .F. ) ;
#8978=ORIENTED_EDGE ( 'NONE', *, *, #12353, .T. ) ;
#8979=CARTESIAN_POINT ( 'NONE',  ( 17.99999999999999645, -97.97378550988183576, -62.10585602713859288 ) ) ;
#8980=VERTEX_POINT ( 'NONE', #187 ) ;
#8983=ADVANCED_FACE ( 'NONE', ( #7186 ), #13555, .F. ) ;
#8985=ORIENTED_EDGE ( 'NONE', *, *, #17797, .T. ) ;
#8986=DIRECTION ( 'NONE',  ( 1.000000000000000000, 0.000000000000000000, 0.000000000000000000 ) ) ;
#8990=ADVANCED_FACE ( 'NONE', ( #10261 ), #13778, .F. ) ;
#8991=ADVANCED_FACE ( 'NONE', ( #20335 ), #27500, .F. ) ;
#8994=ORIENTED_EDGE ( 'NONE', *, *, #9326, .T. ) ;
#8999=DIRECTION ( 'NONE',  ( 1.000000000000000000, 0.000000000000000000, 0.000000000000000000 ) ) ;
#9001=CARTESIAN_POINT ( 'NONE',  ( 0.000000000000000000, 0.000000000000000000, 0.000000000000000000 ) ) ;
#9003=CARTESIAN_POINT ( 'NONE',  ( 17.99999999999999645, 45.89132998248050654, 102.3829004574631512 ) ) ;
#9004=VERTEX_POINT ( 'NONE', #37083 ) ;
#9005=CARTESIAN_POINT ( 'NONE',  ( 17.99999999999999645, 0.000000000000000000, 0.000000000000000000 ) ) ;
#9006=CARTESIAN_POINT ( 'NONE',  ( 17.99999999999999645, -72.00556975657760006, 86.04342158279364128 ) ) ;
#9010=ORIENTED_EDGE ( 'NONE', *, *, #6756, .T. ) ;
#9016=CARTESIAN_POINT ( 'NONE',  ( 0.000000000000000000, -41.60679253225688967, -108.2814610871950265 ) ) ;
#9018=DIRECTION ( 'NONE',  ( -1.000000000000000000, 0.000000000000000000, 0.000000000000000000 ) ) ;
#9020=CARTESIAN_POINT ( 'NONE',  ( 17.99999999999999645, 0.000000000000000000, 0.000000000000000000 ) ) ;
#9024=CARTESIAN_POINT ( 'NONE',  ( 17.99999999999999645, -119.0898412705473532, -18.38751498043852806 ) ) ;
#9027=VERTEX_POINT ( 'NONE', #40774 ) ;
#9029=ORIENTED_EDGE ( 'NONE', *, *, #7774, .F. ) ;
#9031=EDGE_LOOP ( 'NONE', ( #7708, #33134, #31158, #602 ) ) ;
#9033=ORIENTED_EDGE ( 'NONE', *, *, #23835, .T. ) ;
#9036=CARTESIAN_POINT ( 'NONE',  ( 17.99999999999999645, 0.000000000000000000, 0.000000000000000000 ) ) ;
#9038=EDGE_CURVE ( 'NONE', #3997, #15479, #5011, .T. ) ;
#9041=ORIENTED_EDGE ( 'NONE', *, *, #33568, .F. ) ;
#9045=VECTOR ( 'NONE', #37091, 1000.000000000000000 ) ;
#9046=CARTESIAN_POINT ( 'NONE',  ( 0.000000000000000000, -97.97378550988183576, -62.10585602713859288 ) ) ;
#9048=CARTESIAN_POINT ( 'NONE',  ( 0.000000000000000000, 52.19040376560434424, 99.31985817764196156 ) ) ;
#9049=VERTEX_POINT ( 'NONE', #22283 ) ;
#9050=LINE ( 'NONE', #5567, #36302 ) ;
#9053=CARTESIAN_POINT ( 'NONE',  ( 17.99999999999999645, 35.78484819117633720, 110.3423972910434117 ) ) ;
#9057=DIRECTION ( 'NONE',  ( -1.000000000000000000, 0.000000000000000000, -0.000000000000000000 ) ) ;
#9060=DIRECTION ( 'NONE',  ( -1.000000000000000000, 0.000000000000000000, -0.000000000000000000 ) ) ;
#9061=EDGE_LOOP ( 'NONE', ( #35833, #29009, #17004, #27873 ) ) ;
#9066=CARTESIAN_POINT ( 'NONE',  ( 17.99999999999999645, -107.2885202478262698, -54.86040852957422942 ) ) ;
#9068=DIRECTION ( 'NONE',  ( 0.000000000000000000, -0.4610925014493325591, 0.8873520750565681015 ) ) ;
#9069=ORIENTED_EDGE ( 'NONE', *, *, #12046, .T. ) ;
#9070=CARTESIAN_POINT ( 'NONE',  ( 17.99999999999999645, 29.86146780999950323, 112.0905559814579675 ) ) ;
#9071=CIRCLE ( 'NONE', #39723, 116.0000000000000000 ) ;
#9072=AXIS2_PLACEMENT_3D ( 'NONE', #29235, #42504, #32272 ) ;
#9077=ORIENTED_EDGE ( 'NONE', *, *, #26231, .T. ) ;
#9078=DIRECTION ( 'NONE',  ( -1.000000000000000000, 0.000000000000000000, 0.000000000000000000 ) ) ;
#9084=EDGE_CURVE ( 'NONE', #20639, #14493, #15507, .T. ) ;
#9085=CARTESIAN_POINT ( 'NONE',  ( 0.000000000000000000, 0.000000000000000000, 0.000000000000000000 ) ) ;
#9087=ORIENTED_EDGE ( 'NONE', *, *, #31018, .F. ) ;
#9089=LINE ( 'NONE', #22445, #11302 ) ;
#9091=CARTESIAN_POINT ( 'NONE',  ( 17.99999999999999645, -98.39501399267994941, 53.91376164787647696 ) ) ;
#9094=CYLINDRICAL_SURFACE ( 'NONE', #12399, 120.5010000000000190 ) ;
#9099=EDGE_CURVE ( 'NONE', #25078, #40994, #28594, .T. ) ;
#9101=AXIS2_PLACEMENT_3D ( 'NONE', #22236, #35273, #18964 ) ;
#9102=CARTESIAN_POINT ( 'NONE',  ( 17.99999999999999645, -101.1249659627852679, -48.60055280209521555 ) ) ;
#9103=DIRECTION ( 'NONE',  ( -1.000000000000000000, 0.000000000000000000, 0.000000000000000000 ) ) ;
#9104=AXIS2_PLACEMENT_3D ( 'NONE', #39326, #18709, #32171 ) ;
#9105=EDGE_CURVE ( 'NONE', #36755, #33779, #32893, .T. ) ;
#9106=AXIS2_PLACEMENT_3D ( 'NONE', #16353, #23564, #36832 ) ;
#9109=EDGE_LOOP ( 'NONE', ( #18219, #24718, #2225, #22599 ) ) ;
#9112=DIRECTION ( 'NONE',  ( 0.000000000000000000, 0.000000000000000000, 1.000000000000000000 ) ) ;
#9114=DIRECTION ( 'NONE',  ( 0.000000000000000000, 0.8747630845319591675, 0.4845508703326539823 ) ) ;
#9120=VERTEX_POINT ( 'NONE', #38805 ) ;
#9124=LINE ( 'NONE', #25747, #10813 ) ;
#9125=CARTESIAN_POINT ( 'NONE',  ( 17.99999999999999645, 84.09610293794069946, 74.27057253243037849 ) ) ;
#9126=EDGE_LOOP ( 'NONE', ( #17712, #39071, #13862, #7163 ) ) ;
#9130=ORIENTED_EDGE ( 'NONE', *, *, #40938, .T. ) ;
#9133=VECTOR ( 'NONE', #29136, 1000.000000000000000 ) ;
#9137=CIRCLE ( 'NONE', #33523, 59.00000000000000000 ) ;
#9139=EDGE_CURVE ( 'NONE', #3463, #18148, #12703, .T. ) ;
#9147=CARTESIAN_POINT ( 'NONE',  ( 0.000000000000000000, 29.86146780999950323, 112.0905559814579675 ) ) ;
#9149=CARTESIAN_POINT ( 'NONE',  ( 17.99999999999999645, -51.98489025774375705, 108.7109110710159854 ) ) ;
#9150=EDGE_CURVE ( 'NONE', #2165, #18762, #16198, .T. ) ;
#9153=CARTESIAN_POINT ( 'NONE',  ( 17.99999999999999645, 79.94368240339547071, -90.16373242487824768 ) ) ;
#9155=CARTESIAN_POINT ( 'NONE',  ( 17.99999999999999645, 112.1427988504407551, 3.502162136923788083 ) ) ;
#9161=AXIS2_PLACEMENT_3D ( 'NONE', #15361, #24331, #17779 ) ;
#9162=ORIENTED_EDGE ( 'NONE', *, *, #2182, .F. ) ;
#9163=DIRECTION ( 'NONE',  ( -1.000000000000000000, 0.000000000000000000, 0.000000000000000000 ) ) ;
#9165=ORIENTED_EDGE ( 'NONE', *, *, #26503, .T. ) ;
#9167=AXIS2_PLACEMENT_3D ( 'NONE', #33169, #16183, #9824 ) ;
#9171=CARTESIAN_POINT ( 'NONE',  ( 17.99999999999999645, 0.000000000000000000, 0.000000000000000000 ) ) ;
#9172=CARTESIAN_POINT ( 'NONE',  ( 17.99999999999999645, 100.8494052988171035, 65.95368414178945216 ) ) ;
#9174=CYLINDRICAL_SURFACE ( 'NONE', #24679, 59.00000000000000000 ) ;
#9177=ORIENTED_EDGE ( 'NONE', *, *, #38033, .F. ) ;
#9179=DIRECTION ( 'NONE',  ( -1.000000000000000000, -0.000000000000000000, -0.000000000000000000 ) ) ;
#9183=CARTESIAN_POINT ( 'NONE',  ( 17.99999999999999645, -29.02167576844178853, 108.3790330702168774 ) ) ;
#9184=ORIENTED_EDGE ( 'NONE', *, *, #38804, .T. ) ;
#9189=EDGE_LOOP ( 'NONE', ( #7159, #41675, #9033, #42236 ) ) ;
#9191=CIRCLE ( 'NONE', #16165, 58.99999999999998579 ) ;
#9193=ORIENTED_EDGE ( 'NONE', *, *, #22735, .F. ) ;
#9199=CYLINDRICAL_SURFACE ( 'NONE', #3558, 58.99999999999999289 ) ;
#9202=AXIS2_PLACEMENT_3D ( 'NONE', #31494, #24992, #35169 ) ;
#9206=LINE ( 'NONE', #35794, #15113 ) ;
#9207=CARTESIAN_POINT ( 'NONE',  ( 17.99999999999999645, 120.4984140710909344, -0.7894348306988416830 ) ) ;
#9208=ORIENTED_EDGE ( 'NONE', *, *, #16817, .T. ) ;
#9211=DIRECTION ( 'NONE',  ( 0.000000000000000000, 0.000000000000000000, 1.000000000000000000 ) ) ;
#9217=VECTOR ( 'NONE', #24307, 1000.000000000000000 ) ;
#9220=CARTESIAN_POINT ( 'NONE',  ( 0.000000000000000000, -8.827181066046705382, 120.1772519049559378 ) ) ;
#9221=DIRECTION ( 'NONE',  ( -1.000000000000000000, 0.000000000000000000, 0.000000000000000000 ) ) ;
#9222=EDGE_CURVE ( 'NONE', #18461, #39703, #5030, .T. ) ;
#9223=FACE_OUTER_BOUND ( 'NONE', #27021, .T. ) ;
#9227=EDGE_CURVE ( 'NONE', #30882, #16679, #35949, .T. ) ;
#9228=DIRECTION ( 'NONE',  ( 1.000000000000000000, 0.000000000000000000, 0.000000000000000000 ) ) ;
#9235=CIRCLE ( 'NONE', #39178, 58.99999999999999289 ) ;
#9236=DIRECTION ( 'NONE',  ( -1.000000000000000000, -0.000000000000000000, -0.000000000000000000 ) ) ;
#9237=CARTESIAN_POINT ( 'NONE',  ( 8.999999999999998224, 107.1354928292869744, 44.47455650398100602 ) ) ;
#9243=ORIENTED_EDGE ( 'NONE', *, *, #18518, .T. ) ;
#9245=ORIENTED_EDGE ( 'NONE', *, *, #29055, .F. ) ;
#9247=EDGE_LOOP ( 'NONE', ( #11230, #16589, #20794, #223 ) ) ;
#9255=DIRECTION ( 'NONE',  ( -1.000000000000000000, 0.000000000000000000, 0.000000000000000000 ) ) ;
#9257=CARTESIAN_POINT ( 'NONE',  ( 17.99999999999999645, -116.0452958106478434, -32.46506308663576590 ) ) ;
#9258=ORIENTED_EDGE ( 'NONE', *, *, #19237, .T. ) ;
#9259=CYLINDRICAL_SURFACE ( 'NONE', #14048, 59.00000000000000000 ) ;
#9271=DIRECTION ( 'NONE',  ( -1.000000000000000000, 0.000000000000000000, -0.000000000000000000 ) ) ;
#9276=EDGE_CURVE ( 'NONE', #17401, #40745, #39146, .T. ) ;
#9277=CARTESIAN_POINT ( 'NONE',  ( 17.99999999999999645, 96.25468616236661035, 72.49500943364525085 ) ) ;
#9280=ORIENTED_EDGE ( 'NONE', *, *, #19762, .F. ) ;
#9281=DIRECTION ( 'NONE',  ( 0.000000000000000000, 0.000000000000000000, 1.000000000000000000 ) ) ;
#9282=ORIENTED_EDGE ( 'NONE', *, *, #1788, .F. ) ;
#9283=FACE_OUTER_BOUND ( 'NONE', #23562, .T. ) ;
#9286=CARTESIAN_POINT ( 'NONE',  ( 17.99999999999999645, -111.7974656912330715, 9.465682155095141326 ) ) ;
#9288=DIRECTION ( 'NONE',  ( 0.000000000000000000, 0.7865515558026396903, 0.6175246149461955936 ) ) ;
#9289=DIRECTION ( 'NONE',  ( -1.000000000000000000, -0.000000000000000000, 0.000000000000000000 ) ) ;
#9290=DIRECTION ( 'NONE',  ( 1.000000000000000000, -0.000000000000000000, 0.000000000000000000 ) ) ;
#9293=CARTESIAN_POINT ( 'NONE',  ( 17.99999999999999645, -41.60679253225836760, 108.2814610871944581 ) ) ;
#9297=VERTEX_POINT ( 'NONE', #15711 ) ;
#9302=CARTESIAN_POINT ( 'NONE',  ( 17.99999999999999645, 5.456439917444967591, 112.0647122740742105 ) ) ;
#9304=DIRECTION ( 'NONE',  ( 0.000000000000000000, 0.000000000000000000, 1.000000000000000000 ) ) ;
#9307=ORIENTED_EDGE ( 'NONE', *, *, #17115, .T. ) ;
#9308=LINE ( 'NONE', #22662, #23769 ) ;
#9309=ORIENTED_EDGE ( 'NONE', *, *, #15526, .T. ) ;
#9312=FACE_OUTER_BOUND ( 'NONE', #19651, .T. ) ;
#9314=DIRECTION ( 'NONE',  ( -1.000000000000000000, -0.000000000000000000, 0.000000000000000000 ) ) ;
#9316=FACE_OUTER_BOUND ( 'NONE', #25481, .T. ) ;
#9319=DIRECTION ( 'NONE',  ( -1.000000000000000000, 0.000000000000000000, 0.000000000000000000 ) ) ;
#9325=AXIS2_PLACEMENT_3D ( 'NONE', #19856, #42707, #19642 ) ;
#9326=EDGE_CURVE ( 'NONE', #19393, #30398, #39215, .T. ) ;
#9330=DIRECTION ( 'NONE',  ( -1.000000000000000000, -0.000000000000000000, 0.000000000000000000 ) ) ;
#9334=CYLINDRICAL_SURFACE ( 'NONE', #10754, 116.0000000000000000 ) ;
#9337=AXIS2_PLACEMENT_3D ( 'NONE', #24677, #28148, #37514 ) ;
#9338=VERTEX_POINT ( 'NONE', #9780 ) ;
#9340=DIRECTION ( 'NONE',  ( 0.000000000000000000, 1.423061292157245201E-14, -1.000000000000000000 ) ) ;
#9341=ORIENTED_EDGE ( 'NONE', *, *, #33562, .T. ) ;
#9343=DIRECTION ( 'NONE',  ( -1.000000000000000000, 0.000000000000000000, 0.000000000000000000 ) ) ;
#9345=ORIENTED_EDGE ( 'NONE', *, *, #1926, .T. ) ;
#9347=VERTEX_POINT ( 'NONE', #30932 ) ;
#9349=CIRCLE ( 'NONE', #12155, 120.5010000000000190 ) ;
#9351=CARTESIAN_POINT ( 'NONE',  ( 0.000000000000000000, 120.2856157092986678, 7.201503623197233139 ) ) ;
#9354=DIRECTION ( 'NONE',  ( 1.000000000000000000, 0.000000000000000000, 0.000000000000000000 ) ) ;
#9357=CARTESIAN_POINT ( 'NONE',  ( 0.000000000000000000, -103.5682682299991342, 43.14958040911493242 ) ) ;
#9358=VECTOR ( 'NONE', #22941, 1000.000000000000000 ) ;
#9367=CIRCLE ( 'NONE', #2372, 120.5010000000000332 ) ;
#9374=ADVANCED_FACE ( 'NONE', ( #33763 ), #13728, .F. ) ;
#9378=DIRECTION ( 'NONE',  ( 0.000000000000000000, 0.000000000000000000, 1.000000000000000000 ) ) ;
#9383=ORIENTED_EDGE ( 'NONE', *, *, #16817, .F. ) ;
#9385=DIRECTION ( 'NONE',  ( 0.000000000000000000, 0.000000000000000000, 1.000000000000000000 ) ) ;
#9389=ADVANCED_FACE ( 'NONE', ( #7585 ), #3845, .F. ) ;
#9390=CARTESIAN_POINT ( 'NONE',  ( 0.000000000000000000, 0.000000000000000000, 0.000000000000000000 ) ) ;
#9391=CARTESIAN_POINT ( 'NONE',  ( 8.999999999999998224, 86.84764344322962870, 76.89919913989776035 ) ) ;
#9400=ORIENTED_EDGE ( 'NONE', *, *, #2820, .T. ) ;
#9405=CARTESIAN_POINT ( 'NONE',  ( 17.99999999999999645, -51.98489025774233596, -108.7109110710166391 ) ) ;
#9406=CARTESIAN_POINT ( 'NONE',  ( -10.00000000000000000, 0.000000000000000000, 0.000000000000000000 ) ) ;
#9407=EDGE_CURVE ( 'NONE', #20671, #2041, #35020, .T. ) ;
#9408=CARTESIAN_POINT ( 'NONE',  ( 17.99999999999999645, 47.58001226230536673, 110.7096808509485300 ) ) ;
#9409=EDGE_CURVE ( 'NONE', #9666, #14373, #33607, .T. ) ;
#9411=CARTESIAN_POINT ( 'NONE',  ( 17.99999999999999645, 0.000000000000000000, 0.000000000000000000 ) ) ;
#9412=CARTESIAN_POINT ( 'NONE',  ( -10.00000000000000000, 0.000000000000000000, 116.0000000000000000 ) ) ;
#9415=AXIS2_PLACEMENT_3D ( 'NONE', #33503, #37794, #7912 ) ;
#9417=CIRCLE ( 'NONE', #33122, 116.0000000000000000 ) ;
#9424=DIRECTION ( 'NONE',  ( 0.000000000000000000, 0.000000000000000000, 1.000000000000000000 ) ) ;
#9425=ORIENTED_EDGE ( 'NONE', *, *, #19283, .T. ) ;
#9427=DIRECTION ( 'NONE',  ( -1.000000000000000000, -0.000000000000000000, -0.000000000000000000 ) ) ;
#9429=EDGE_CURVE ( 'NONE', #29862, #38233, #3624, .T. ) ;
#9432=ORIENTED_EDGE ( 'NONE', *, *, #10930, .T. ) ;
#9433=ORIENTED_EDGE ( 'NONE', *, *, #25867, .F. ) ;
#9434=CARTESIAN_POINT ( 'NONE',  ( -10.00000000000000000, 0.000000000000000000, 0.000000000000000000 ) ) ;
#9436=DIRECTION ( 'NONE',  ( -1.000000000000000000, -0.000000000000000000, -0.000000000000000000 ) ) ;
#9439=DIRECTION ( 'NONE',  ( -1.000000000000000000, 0.000000000000000000, 0.000000000000000000 ) ) ;
#9442=VERTEX_POINT ( 'NONE', #24208 ) ;
#9446=EDGE_CURVE ( 'NONE', #3132, #35775, #28786, .T. ) ;
#9448=CARTESIAN_POINT ( 'NONE',  ( 17.99999999999999645, 66.49630760163724119, -90.36876423295917959 ) ) ;
#9449=DIRECTION ( 'NONE',  ( 1.000000000000000000, 0.000000000000000000, 0.000000000000000000 ) ) ;
#9451=ORIENTED_EDGE ( 'NONE', *, *, #29330, .F. ) ;
#9457=ORIENTED_EDGE ( 'NONE', *, *, #743, .F. ) ;
#9458=AXIS2_PLACEMENT_3D ( 'NONE', #33475, #37816, #21085 ) ;
#9459=DIRECTION ( 'NONE',  ( 0.000000000000000000, 0.000000000000000000, 1.000000000000000000 ) ) ;
#9460=ORIENTED_EDGE ( 'NONE', *, *, #37170, .T. ) ;
#9464=DIRECTION ( 'NONE',  ( 0.000000000000000000, 0.3140767120219494779, -0.9493976084683810601 ) ) ;
#9465=AXIS2_PLACEMENT_3D ( 'NONE', #33584, #26623, #13543 ) ;
#9468=DIRECTION ( 'NONE',  ( 0.000000000000000000, 0.000000000000000000, 1.000000000000000000 ) ) ;
#9470=EDGE_LOOP ( 'NONE', ( #9786, #7427, #5281, #29328 ) ) ;
#9472=EDGE_CURVE ( 'NONE', #32590, #20200, #6717, .T. ) ;
#9473=CARTESIAN_POINT ( 'NONE',  ( 17.99999999999999645, -68.61497464550663494, 99.05794392877579924 ) ) ;
#9474=LINE ( 'NONE', #22827, #41576 ) ;
#9477=ORIENTED_EDGE ( 'NONE', *, *, #13060, .T. ) ;
#9478=CARTESIAN_POINT ( 'NONE',  ( 17.99999999999999645, -92.10690493017015967, -64.06707842432270184 ) ) ;
#9479=ORIENTED_EDGE ( 'NONE', *, *, #18512, .T. ) ;
#9484=FACE_OUTER_BOUND ( 'NONE', #32292, .T. ) ;
#9488=AXIS2_PLACEMENT_3D ( 'NONE', #22712, #6091, #13521 ) ;
#9489=CIRCLE ( 'NONE', #14405, 116.0000000000000000 ) ;
#9491=DIRECTION ( 'NONE',  ( 0.000000000000000000, 0.000000000000000000, 1.000000000000000000 ) ) ;
#9492=AXIS2_PLACEMENT_3D ( 'NONE', #14938, #25404, #28241 ) ;
#9493=ORIENTED_EDGE ( 'NONE', *, *, #26875, .F. ) ;
#9495=DIRECTION ( 'NONE',  ( -1.000000000000000000, 0.000000000000000000, 0.000000000000000000 ) ) ;
#9500=AXIS2_PLACEMENT_3D ( 'NONE', #17232, #23980, #800 ) ;
#9502=CARTESIAN_POINT ( 'NONE',  ( 0.000000000000000000, -24.22031524825905890, -109.5520369638039710 ) ) ;
#9503=VERTEX_POINT ( 'NONE', #33347 ) ;
#9506=DIRECTION ( 'NONE',  ( 0.000000000000000000, 0.7164567402983162969, -0.6976315211349835010 ) ) ;
#9507=ADVANCED_FACE ( 'NONE', ( #3429 ), #3637, .F. ) ;
#9511=ORIENTED_EDGE ( 'NONE', *, *, #34556, .F. ) ;
#9512=DIRECTION ( 'NONE',  ( 1.000000000000000000, 0.000000000000000000, 0.000000000000000000 ) ) ;
#9513=FACE_OUTER_BOUND ( 'NONE', #32814, .T. ) ;
#9516=ORIENTED_EDGE ( 'NONE', *, *, #37648, .T. ) ;
#9517=DIRECTION ( 'NONE',  ( 0.000000000000000000, -0.2113826236296113270, -0.9774033898178695612 ) ) ;
#9519=EDGE_CURVE ( 'NONE', #10645, #10921, #13942, .T. ) ;
#9521=AXIS2_PLACEMENT_3D ( 'NONE', #18332, #38341, #35068 ) ;
#9522=CIRCLE ( 'NONE', #15141, 59.00000000000000000 ) ;
#9527=CARTESIAN_POINT ( 'NONE',  ( 17.99999999999999645, -112.8457601792513714, -26.86697618949492039 ) ) ;
#9529=AXIS2_PLACEMENT_3D ( 'NONE', #11446, #28478, #5315 ) ;
#9530=DIRECTION ( 'NONE',  ( -1.000000000000000000, 0.000000000000000000, 0.000000000000000000 ) ) ;
#9531=ADVANCED_FACE ( 'NONE', ( #33989 ), #4075, .F. ) ;
#9532=EDGE_CURVE ( 'NONE', #21659, #38310, #17881, .T. ) ;
#9533=CIRCLE ( 'NONE', #31844, 116.0000000000000000 ) ;
#9534=CARTESIAN_POINT ( 'NONE',  ( 17.99999999999999645, -3.996885678772183592, -120.4346956066682424 ) ) ;
#9535=EDGE_CURVE ( 'NONE', #32579, #32669, #7132, .T. ) ;
#9538=ORIENTED_EDGE ( 'NONE', *, *, #18626, .F. ) ;
#9542=FACE_OUTER_BOUND ( 'NONE', #37513, .T. ) ;
#9546=LINE ( 'NONE', #19185, #1628 ) ;
#9551=CARTESIAN_POINT ( 'NONE',  ( 0.000000000000000000, 119.8996782608631406, -12.02323392193236629 ) ) ;
#9552=CIRCLE ( 'NONE', #38813, 116.0000000000000000 ) ;
#9553=ORIENTED_EDGE ( 'NONE', *, *, #16121, .T. ) ;
#9560=CIRCLE ( 'NONE', #21451, 120.5010000000000190 ) ;
#9564=CARTESIAN_POINT ( 'NONE',  ( 0.000000000000000000, -29.02167576844178853, 108.3790330702168774 ) ) ;
#9566=CARTESIAN_POINT ( 'NONE',  ( 9.000000000000001776, 107.1354928292875996, -44.47455650397954230 ) ) ;
#9569=AXIS2_PLACEMENT_3D ( 'NONE', #12712, #6144, #15777 ) ;
#9571=DIRECTION ( 'NONE',  ( -1.000000000000000000, 0.000000000000000000, 0.000000000000000000 ) ) ;
#9572=CIRCLE ( 'NONE', #34640, 120.5010000000000190 ) ;
#9575=DIRECTION ( 'NONE',  ( 1.000000000000000000, 0.000000000000000000, 0.000000000000000000 ) ) ;
#9577=VERTEX_POINT ( 'NONE', #31580 ) ;
#9582=AXIS2_PLACEMENT_3D ( 'NONE', #28901, #35828, #38473 ) ;
#9584=EDGE_CURVE ( 'NONE', #38581, #17370, #42655, .T. ) ;
#9585=ADVANCED_FACE ( 'NONE', ( #24861 ), #21156, .F. ) ;
#9586=CARTESIAN_POINT ( 'NONE',  ( 0.000000000000000000, -41.62036691425451096, -113.0850832732718914 ) ) ;
#9588=AXIS2_PLACEMENT_3D ( 'NONE', #21245, #37123, #10734 ) ;
#9592=ORIENTED_EDGE ( 'NONE', *, *, #38807, .F. ) ;
#9595=VERTEX_POINT ( 'NONE', #38532 ) ;
#9600=DIRECTION ( 'NONE',  ( 0.000000000000000000, 0.000000000000000000, 1.000000000000000000 ) ) ;
#9607=CARTESIAN_POINT ( 'NONE',  ( 17.99999999999999645, -110.1579703617967567, 21.29539948940213634 ) ) ;
#9609=VECTOR ( 'NONE', #13135, 1000.000000000000000 ) ;
#9610=CARTESIAN_POINT ( 'NONE',  ( 17.99999999999999645, -12.43843445475394027, 111.5058645182329116 ) ) ;
#9611=EDGE_CURVE ( 'NONE', #34305, #27015, #10637, .T. ) ;
#9617=CIRCLE ( 'NONE', #15939, 116.0000000000000000 ) ;
#9622=LINE ( 'NONE', #11902, #13394 ) ;
#9624=DIRECTION ( 'NONE',  ( -1.000000000000000000, -0.000000000000000000, -0.000000000000000000 ) ) ;
#9627=ORIENTED_EDGE ( 'NONE', *, *, #27639, .T. ) ;
#9629=CARTESIAN_POINT ( 'NONE',  ( 17.99999999999999645, -16.77566611177701006, -119.3275660838943963 ) ) ;
#9631=ORIENTED_EDGE ( 'NONE', *, *, #16170, .F. ) ;
#9632=CYLINDRICAL_SURFACE ( 'NONE', #35626, 120.5010000000000190 ) ;
#9634=EDGE_CURVE ( 'NONE', #30173, #1677, #165, .T. ) ;
#9644=CARTESIAN_POINT ( 'NONE',  ( 17.99999999999999645, -34.03109950475653989, -115.5957406979053133 ) ) ;
#9653=CARTESIAN_POINT ( 'NONE',  ( -10.00000000000000000, 0.000000000000000000, 0.000000000000000000 ) ) ;
#9654=ORIENTED_EDGE ( 'NONE', *, *, #40797, .T. ) ;
#9655=CARTESIAN_POINT ( 'NONE',  ( 0.000000000000000000, -40.13512380273891011, -113.6206972269525863 ) ) ;
#9658=ORIENTED_EDGE ( 'NONE', *, *, #42203, .F. ) ;
#9660=DIRECTION ( 'NONE',  ( 0.000000000000000000, 0.000000000000000000, 1.000000000000000000 ) ) ;
#9661=DIRECTION ( 'NONE',  ( 0.000000000000000000, 0.000000000000000000, 1.000000000000000000 ) ) ;
#9662=DIRECTION ( 'NONE',  ( 0.000000000000000000, 0.000000000000000000, 1.000000000000000000 ) ) ;
#9663=DIRECTION ( 'NONE',  ( 0.000000000000000000, 0.000000000000000000, 1.000000000000000000 ) ) ;
#9665=DIRECTION ( 'NONE',  ( 0.000000000000000000, 0.000000000000000000, 1.000000000000000000 ) ) ;
#9666=VERTEX_POINT ( 'NONE', #35054 ) ;
#9668=EDGE_LOOP ( 'NONE', ( #11309, #22460, #12446, #8763 ) ) ;
#9673=CIRCLE ( 'NONE', #15293, 58.99999999999999289 ) ;
#9675=CARTESIAN_POINT ( 'NONE',  ( -10.00000000000000000, 0.000000000000000000, 0.000000000000000000 ) ) ;
#9676=ORIENTED_EDGE ( 'NONE', *, *, #41591, .T. ) ;
#9678=ORIENTED_EDGE ( 'NONE', *, *, #20978, .F. ) ;
#9685=ORIENTED_EDGE ( 'NONE', *, *, #34517, .T. ) ;
#9687=ADVANCED_FACE ( 'NONE', ( #41816 ), #1249, .F. ) ;
#9690=ORIENTED_EDGE ( 'NONE', *, *, #10949, .F. ) ;
#9693=CARTESIAN_POINT ( 'NONE',  ( 17.99999999999999645, -69.90696807222551001, 98.15042952503490881 ) ) ;
#9695=VERTEX_POINT ( 'NONE', #2725 ) ;
#9696=LINE ( 'NONE', #33668, #7726 ) ;
#9698=EDGE_CURVE ( 'NONE', #18411, #31896, #28097, .T. ) ;
#9704=CARTESIAN_POINT ( 'NONE',  ( 17.99999999999999645, -116.4607004671426438, -30.94182036827323756 ) ) ;
#9706=ORIENTED_EDGE ( 'NONE', *, *, #24960, .F. ) ;
#9710=ORIENTED_EDGE ( 'NONE', *, *, #14381, .F. ) ;
#9711=CARTESIAN_POINT ( 'NONE',  ( 17.99999999999999645, -12.43843445475238063, -111.5058645182330963 ) ) ;
#9719=ORIENTED_EDGE ( 'NONE', *, *, #42636, .T. ) ;
#9720=ADVANCED_FACE ( 'NONE', ( #25712 ), #23081, .F. ) ;
#9722=EDGE_CURVE ( 'NONE', #22119, #35461, #36121, .T. ) ;
#9727=CYLINDRICAL_SURFACE ( 'NONE', #3956, 116.0000000000000000 ) ;
#9728=DIRECTION ( 'NONE',  ( -1.000000000000000000, 0.000000000000000000, 0.000000000000000000 ) ) ;
#9729=CARTESIAN_POINT ( 'NONE',  ( 17.99999999999999645, 103.4151313792879421, -61.85306461934305844 ) ) ;
#9730=VERTEX_POINT ( 'NONE', #39382 ) ;
#9732=AXIS2_PLACEMENT_3D ( 'NONE', #20187, #16695, #33880 ) ;
#9733=CARTESIAN_POINT ( 'NONE',  ( 17.99999999999999645, 0.000000000000000000, 0.000000000000000000 ) ) ;
#9737=DIRECTION ( 'NONE',  ( -1.000000000000000000, 0.000000000000000000, 0.000000000000000000 ) ) ;
#9740=CARTESIAN_POINT ( 'NONE',  ( 17.99999999999999645, -115.9750404417043939, -2.406240749598616446 ) ) ;
#9743=ORIENTED_EDGE ( 'NONE', *, *, #19512, .T. ) ;
#9744=CARTESIAN_POINT ( 'NONE',  ( 17.99999999999999645, -47.58001226230465619, -110.7096808509488284 ) ) ;
#9748=DIRECTION ( 'NONE',  ( -1.000000000000000000, -0.000000000000000000, 0.000000000000000000 ) ) ;
#9751=CYLINDRICAL_SURFACE ( 'NONE', #23252, 59.00000000000000000 ) ;
#9753=CARTESIAN_POINT ( 'NONE',  ( 0.000000000000000000, -79.18387647320706435, -84.76976882518842160 ) ) ;
#9755=CIRCLE ( 'NONE', #32095, 120.5010000000000332 ) ;
#9756=CIRCLE ( 'NONE', #17467, 116.0000000000000000 ) ;
#9757=LINE ( 'NONE', #32459, #22704 ) ;
#9758=ORIENTED_EDGE ( 'NONE', *, *, #6366, .T. ) ;
#9764=EDGE_CURVE ( 'NONE', #6594, #34488, #1592, .T. ) ;
#9765=CARTESIAN_POINT ( 'NONE',  ( 17.99999999999999645, 24.22031524825977300, 109.5520369638038289 ) ) ;
#9770=CARTESIAN_POINT ( 'NONE',  ( 9.000000000000001776, -98.69720329640996681, 60.94966826379877745 ) ) ;
#9774=CARTESIAN_POINT ( 'NONE',  ( 17.99999999999999645, 3.996885678773026029, 120.4346956066682424 ) ) ;
#9779=DIRECTION ( 'NONE',  ( 0.000000000000000000, 0.000000000000000000, 1.000000000000000000 ) ) ;
#9780=CARTESIAN_POINT ( 'NONE',  ( 0.000000000000000000, -88.00363688980490906, -82.31555682352745862 ) ) ;
#9784=DIRECTION ( 'NONE',  ( 0.000000000000000000, 9.408669700213191589E-16, -1.000000000000000000 ) ) ;
#9786=ORIENTED_EDGE ( 'NONE', *, *, #41838, .T. ) ;
#9787=AXIS2_PLACEMENT_3D ( 'NONE', #7536, #29828, #14109 ) ;
#9788=FACE_OUTER_BOUND ( 'NONE', #13036, .T. ) ;
#9790=AXIS2_PLACEMENT_3D ( 'NONE', #36862, #179, #6967 ) ;
#9792=VERTEX_POINT ( 'NONE', #12171 ) ;
#9793=DIRECTION ( 'NONE',  ( -1.000000000000000000, 0.000000000000000000, -0.000000000000000000 ) ) ;
#9794=VERTEX_POINT ( 'NONE', #25491 ) ;
#9795=EDGE_CURVE ( 'NONE', #6539, #1566, #41294, .T. ) ;
#9796=CYLINDRICAL_SURFACE ( 'NONE', #12727, 116.0000000000000000 ) ;
#9804=AXIS2_PLACEMENT_3D ( 'NONE', #36619, #3229, #33365 ) ;
#9808=AXIS2_PLACEMENT_3D ( 'NONE', #41564, #7973, #1633 ) ;
#9810=VECTOR ( 'NONE', #10099, 1000.000000000000000 ) ;
#9812=ADVANCED_FACE ( 'NONE', ( #8881 ), #35480, .F. ) ;
#9814=EDGE_CURVE ( 'NONE', #34305, #433, #27921, .T. ) ;
#9820=DIRECTION ( 'NONE',  ( -1.000000000000000000, -0.000000000000000000, 0.000000000000000000 ) ) ;
#9822=AXIS2_PLACEMENT_3D ( 'NONE', #39025, #2359, #15728 ) ;
#9824=DIRECTION ( 'NONE',  ( 0.000000000000000000, 0.05322217484217878214, -0.9985826956767620555 ) ) ;
#9827=CARTESIAN_POINT ( 'NONE',  ( 17.99999999999999645, -103.1672962317648512, -44.09967643725973119 ) ) ;
#9829=ORIENTED_EDGE ( 'NONE', *, *, #22749, .F. ) ;
#9834=ORIENTED_EDGE ( 'NONE', *, *, #8448, .T. ) ;
#9837=DIRECTION ( 'NONE',  ( 0.000000000000000000, -0.9968120070307493474, -0.07978610555309324781 ) ) ;
#9839=DIRECTION ( 'NONE',  ( -1.000000000000000000, 0.000000000000000000, -0.000000000000000000 ) ) ;
#9840=AXIS2_PLACEMENT_3D ( 'NONE', #23456, #23883, #33660 ) ;
#9845=AXIS2_PLACEMENT_3D ( 'NONE', #19154, #29382, #39163 ) ;
#9846=ADVANCED_FACE ( 'NONE', ( #39809 ), #37194, .F. ) ;
#9847=CARTESIAN_POINT ( 'NONE',  ( 17.99999999999999645, -117.6086855750636460, 26.24286718912065552 ) ) ;
#9850=AXIS2_PLACEMENT_3D ( 'NONE', #22399, #43053, #12763 ) ;
#9854=ORIENTED_EDGE ( 'NONE', *, *, #2501, .F. ) ;
#9859=EDGE_LOOP ( 'NONE', ( #30125, #13271, #32907, #33199 ) ) ;
#9861=ADVANCED_FACE ( 'NONE', ( #86 ), #304, .F. ) ;
#9863=EDGE_CURVE ( 'NONE', #12090, #13726, #9071, .T. ) ;
#9864=CARTESIAN_POINT ( 'NONE',  ( 9.000000000000001776, -17.77780072541623113, -114.6296200873377842 ) ) ;
#9866=DIRECTION ( 'NONE',  ( -1.000000000000000000, -0.000000000000000000, -0.000000000000000000 ) ) ;
#9867=ORIENTED_EDGE ( 'NONE', *, *, #20925, .T. ) ;
#9870=CYLINDRICAL_SURFACE ( 'NONE', #2699, 59.00000000000000000 ) ;
#9875=CARTESIAN_POINT ( 'NONE',  ( 17.99999999999999645, 107.5680526044919674, -31.89649718262133149 ) ) ;
#9877=CYLINDRICAL_SURFACE ( 'NONE', #11550, 59.00000000000000000 ) ;
#9880=ORIENTED_EDGE ( 'NONE', *, *, #31649, .F. ) ;
#9882=EDGE_CURVE ( 'NONE', #10144, #5171, #18192, .T. ) ;
#9884=DIRECTION ( 'NONE',  ( 1.000000000000000000, -0.000000000000000000, -0.000000000000000000 ) ) ;
#9889=CARTESIAN_POINT ( 'NONE',  ( 17.99999999999999645, -71.21168426767047777, -86.70160608319397966 ) ) ;
#9890=ORIENTED_EDGE ( 'NONE', *, *, #5649, .F. ) ;
#9893=ORIENTED_EDGE ( 'NONE', *, *, #32240, .T. ) ;
#9896=DIRECTION ( 'NONE',  ( 0.000000000000000000, 0.000000000000000000, 1.000000000000000000 ) ) ;
#9897=DIRECTION ( 'NONE',  ( -1.000000000000000000, 0.000000000000000000, 0.000000000000000000 ) ) ;
#9898=ORIENTED_EDGE ( 'NONE', *, *, #41893, .T. ) ;
#9900=VERTEX_POINT ( 'NONE', #27192 ) ;
#9902=AXIS2_PLACEMENT_3D ( 'NONE', #6098, #19652, #32922 ) ;
#9904=VECTOR ( 'NONE', #43020, 1000.000000000000000 ) ;
#9911=CIRCLE ( 'NONE', #34304, 59.00000000000000000 ) ;
#9915=LINE ( 'NONE', #23263, #26853 ) ;
#9916=EDGE_CURVE ( 'NONE', #27181, #20720, #3792, .T. ) ;
#9917=CYLINDRICAL_SURFACE ( 'NONE', #34435, 59.00000000000000000 ) ;
#9920=ORIENTED_EDGE ( 'NONE', *, *, #37505, .T. ) ;
#9922=ORIENTED_EDGE ( 'NONE', *, *, #33799, .T. ) ;
#9924=CARTESIAN_POINT ( 'NONE',  ( 0.000000000000000000, 27.83061035787114079, -117.2431154827794586 ) ) ;
#9925=DIRECTION ( 'NONE',  ( -1.000000000000000000, 0.000000000000000000, -0.000000000000000000 ) ) ;
#9926=VERTEX_POINT ( 'NONE', #10151 ) ;
#9928=CARTESIAN_POINT ( 'NONE',  ( 0.000000000000000000, 74.56001736500617483, 88.86396238369059120 ) ) ;
#9930=CIRCLE ( 'NONE', #2280, 120.5010000000000474 ) ;
#9931=DIRECTION ( 'NONE',  ( -1.000000000000000000, -0.000000000000000000, 0.000000000000000000 ) ) ;
#9934=EDGE_CURVE ( 'NONE', #10316, #4569, #7699, .T. ) ;
#9936=DIRECTION ( 'NONE',  ( -1.000000000000000000, 0.000000000000000000, 0.000000000000000000 ) ) ;
#9937=VECTOR ( 'NONE', #20722, 1000.000000000000000 ) ;
#9941=CARTESIAN_POINT ( 'NONE',  ( 0.000000000000000000, 73.78980555658731078, -95.26571049921918188 ) ) ;
#9942=CARTESIAN_POINT ( 'NONE',  ( 17.99999999999999645, 98.39501399267960835, 53.91376164787712355 ) ) ;
#9943=CIRCLE ( 'NONE', #33643, 120.5010000000000190 ) ;
#9945=CARTESIAN_POINT ( 'NONE',  ( 17.99999999999999645, 0.000000000000000000, 0.000000000000000000 ) ) ;
#9948=ORIENTED_EDGE ( 'NONE', *, *, #18711, .T. ) ;
#9949=CARTESIAN_POINT ( 'NONE',  ( 17.99999999999999645, 0.000000000000000000, 0.000000000000000000 ) ) ;
#9950=VERTEX_POINT ( 'NONE', #33294 ) ;
#9952=CARTESIAN_POINT ( 'NONE',  ( 17.99999999999999645, -88.00363688980490906, -82.31555682352745862 ) ) ;
#9963=LINE ( 'NONE', #339, #18579 ) ;
#9967=CARTESIAN_POINT ( 'NONE',  ( 8.999999999999998224, 69.72480978690171582, -92.70626138605945243 ) ) ;
#9968=( GEOMETRIC_REPRESENTATION_CONTEXT ( 3 ) GLOBAL_UNCERTAINTY_ASSIGNED_CONTEXT ( ( #1959 ) ) GLOBAL_UNIT_ASSIGNED_CONTEXT ( ( #24390, #37639, #41117 ) ) REPRESENTATION_CONTEXT ( 'NONE', 'WORKASPACE' ) );
#9974=DIRECTION ( 'NONE',  ( 1.000000000000000000, -0.000000000000000000, -0.000000000000000000 ) ) ;
#9979=VERTEX_POINT ( 'NONE', #542 ) ;
#9988=AXIS2_PLACEMENT_3D ( 'NONE', #21876, #12243, #18615 ) ;
#9991=AXIS2_PLACEMENT_3D ( 'NONE', #20534, #39898, #40338 ) ;
#9992=ORIENTED_EDGE ( 'NONE', *, *, #38700, .T. ) ;
#9993=DIRECTION ( 'NONE',  ( -1.000000000000000000, -0.000000000000000000, 0.000000000000000000 ) ) ;
#9995=CARTESIAN_POINT ( 'NONE',  ( 0.000000000000000000, -88.00363688980601751, 82.31555682352626491 ) ) ;
#10000=VERTEX_POINT ( 'NONE', #18063 ) ;
#10002=DIRECTION ( 'NONE',  ( 0.000000000000000000, 0.000000000000000000, 1.000000000000000000 ) ) ;
#10004=AXIS2_PLACEMENT_3D ( 'NONE', #43062, #39572, #23255 ) ;
#10005=LINE ( 'NONE', #160, #13422 ) ;
#10006=DIRECTION ( 'NONE',  ( -1.000000000000000000, -0.000000000000000000, 0.000000000000000000 ) ) ;
#10008=ORIENTED_EDGE ( 'NONE', *, *, #22208, .F. ) ;
#10009=CARTESIAN_POINT ( 'NONE',  ( 0.000000000000000000, -3.996885678773838713, 120.4346956066681713 ) ) ;
#10013=PRODUCT_CONTEXT ( 'NONE', #18697, 'mechanical' ) ;
#10017=ORIENTED_EDGE ( 'NONE', *, *, #21960, .F. ) ;
#10022=LINE ( 'NONE', #16382, #16600 ) ;
#10023=ORIENTED_EDGE ( 'NONE', *, *, #21729, .F. ) ;
#10024=LINE ( 'NONE', #6758, #1647 ) ;
#10025=CARTESIAN_POINT ( 'NONE',  ( 8.999999999999998224, 97.97378550988226209, 62.10585602713793207 ) ) ;
#10027=EDGE_CURVE ( 'NONE', #22504, #26216, #41770, .T. ) ;
#10028=ORIENTED_EDGE ( 'NONE', *, *, #6856, .T. ) ;
#10030=DIRECTION ( 'NONE',  ( 0.000000000000000000, -0.9911528310040056411, -0.1327255272837324085 ) ) ;
#10031=CIRCLE ( 'NONE', #26104, 116.0000000000000000 ) ;
#10032=DIRECTION ( 'NONE',  ( 0.000000000000000000, -0.9574220383620081209, 0.2886919473396123981 ) ) ;
#10033=ORIENTED_EDGE ( 'NONE', *, *, #9535, .T. ) ;
#10037=VERTEX_POINT ( 'NONE', #11049 ) ;
#10038=DIRECTION ( 'NONE',  ( 0.000000000000000000, 0.8993121301712172500, 0.4373073204588593388 ) ) ;
#10039=VERTEX_POINT ( 'NONE', #14544 ) ;
#10041=AXIS2_PLACEMENT_3D ( 'NONE', #3219, #36608, #13520 ) ;
#10042=ORIENTED_EDGE ( 'NONE', *, *, #33568, .T. ) ;
#10043=AXIS2_PLACEMENT_3D ( 'NONE', #21736, #38042, #34990 ) ;
#10046=EDGE_LOOP ( 'NONE', ( #17778, #37315, #32923, #20943 ) ) ;
#10047=FACE_OUTER_BOUND ( 'NONE', #40695, .T. ) ;
#10051=ORIENTED_EDGE ( 'NONE', *, *, #29533, .F. ) ;
#10054=DIRECTION ( 'NONE',  ( -1.000000000000000000, 0.000000000000000000, 0.000000000000000000 ) ) ;
#10055=EDGE_CURVE ( 'NONE', #6806, #40193, #10475, .T. ) ;
#10057=DIRECTION ( 'NONE',  ( -1.000000000000000000, 0.000000000000000000, 0.000000000000000000 ) ) ;
#10059=EDGE_CURVE ( 'NONE', #10843, #5501, #4909, .T. ) ;
#10061=CYLINDRICAL_SURFACE ( 'NONE', #5421, 120.5010000000000190 ) ;
#10062=CARTESIAN_POINT ( 'NONE',  ( 0.000000000000000000, 0.000000000000000000, 0.000000000000000000 ) ) ;
#10064=CIRCLE ( 'NONE', #1717, 59.00000000000000711 ) ;
#10067=DIRECTION ( 'NONE',  ( 1.000000000000000000, 0.000000000000000000, 0.000000000000000000 ) ) ;
#10072=AXIS2_PLACEMENT_3D ( 'NONE', #17012, #37255, #30297 ) ;
#10075=ORIENTED_EDGE ( 'NONE', *, *, #38940, .T. ) ;
#10077=CYLINDRICAL_SURFACE ( 'NONE', #24202, 59.00000000000000000 ) ;
#10078=DIRECTION ( 'NONE',  ( 0.000000000000000000, 0.000000000000000000, 1.000000000000000000 ) ) ;
#10081=ORIENTED_EDGE ( 'NONE', *, *, #19989, .F. ) ;
#10084=CYLINDRICAL_SURFACE ( 'NONE', #15993, 116.0000000000000000 ) ;
#10088=DIRECTION ( 'NONE',  ( 1.000000000000000000, 0.000000000000000000, 0.000000000000000000 ) ) ;
#10089=VERTEX_POINT ( 'NONE', #21963 ) ;
#10090=DIRECTION ( 'NONE',  ( -1.000000000000000000, -0.000000000000000000, -0.000000000000000000 ) ) ;
#10091=ORIENTED_EDGE ( 'NONE', *, *, #15199, .T. ) ;
#10092=DIRECTION ( 'NONE',  ( 0.000000000000000000, 4.469118107601265561E-15, -1.000000000000000000 ) ) ;
#10093=VECTOR ( 'NONE', #14941, 1000.000000000000000 ) ;
#10098=ORIENTED_EDGE ( 'NONE', *, *, #8917, .F. ) ;
#10099=DIRECTION ( 'NONE',  ( 1.000000000000000000, -0.000000000000000000, -0.000000000000000000 ) ) ;
#10102=CARTESIAN_POINT ( 'NONE',  ( 0.000000000000000000, 118.8387007424473580, -19.94628303336371644 ) ) ;
#10107=CARTESIAN_POINT ( 'NONE',  ( 0.000000000000000000, 0.000000000000000000, 0.000000000000000000 ) ) ;
#10111=CYLINDRICAL_SURFACE ( 'NONE', #35235, 59.00000000000000000 ) ;
#10115=EDGE_CURVE ( 'NONE', #13510, #14100, #31535, .T. ) ;
#10121=ORIENTED_EDGE ( 'NONE', *, *, #6127, .F. ) ;
#10122=EDGE_CURVE ( 'NONE', #15605, #16577, #21107, .T. ) ;
#10124=AXIS2_PLACEMENT_3D ( 'NONE', #32137, #25621, #22777 ) ;
#10128=CARTESIAN_POINT ( 'NONE',  ( 17.99999999999999645, -111.9370513079666409, -44.61600100275288838 ) ) ;
#10135=CARTESIAN_POINT ( 'NONE',  ( 17.99999999999999645, 114.6488492393079781, 37.09625815500054102 ) ) ;
#10139=CIRCLE ( 'NONE', #376, 120.5010000000000190 ) ;
#10141=CARTESIAN_POINT ( 'NONE',  ( 17.99999999999999645, 0.000000000000000000, 0.000000000000000000 ) ) ;
#10143=EDGE_CURVE ( 'NONE', #24120, #27034, #21325, .T. ) ;
#10144=VERTEX_POINT ( 'NONE', #1407 ) ;
#10147=CARTESIAN_POINT ( 'NONE',  ( 17.99999999999999645, 0.000000000000000000, 0.000000000000000000 ) ) ;
#10151=CARTESIAN_POINT ( 'NONE',  ( 17.99999999999999645, 5.492704054966705662, 115.8698847939556344 ) ) ;
#10152=DIRECTION ( 'NONE',  ( 1.000000000000000000, 0.000000000000000000, 0.000000000000000000 ) ) ;
#10154=ORIENTED_EDGE ( 'NONE', *, *, #15717, .F. ) ;
#10155=CARTESIAN_POINT ( 'NONE',  ( 17.99999999999999645, 0.000000000000000000, 0.000000000000000000 ) ) ;
#10160=LINE ( 'NONE', #7543, #10283 ) ;
#10161=ADVANCED_FACE ( 'NONE', ( #41552 ), #11697, .F. ) ;
#10163=ORIENTED_EDGE ( 'NONE', *, *, #4434, .T. ) ;
#10164=DIRECTION ( 'NONE',  ( 1.000000000000000000, 0.000000000000000000, 0.000000000000000000 ) ) ;
#10166=ORIENTED_EDGE ( 'NONE', *, *, #11346, .F. ) ;
#10169=DIRECTION ( 'NONE',  ( 0.000000000000000000, 0.000000000000000000, -1.000000000000000000 ) ) ;
#10170=CARTESIAN_POINT ( 'NONE',  ( 0.000000000000000000, 0.000000000000000000, 0.000000000000000000 ) ) ;
#10172=CARTESIAN_POINT ( 'NONE',  ( 17.99999999999999645, -40.13512380274045199, 113.6206972269520179 ) ) ;
#10173=CIRCLE ( 'NONE', #31817, 116.0000000000000000 ) ;
#10174=VERTEX_POINT ( 'NONE', #35438 ) ;
#10177=EDGE_CURVE ( 'NONE', #14877, #5508, #30024, .T. ) ;
#10178=CARTESIAN_POINT ( 'NONE',  ( 17.99999999999999645, 108.8880088604276608, 39.99251838045997687 ) ) ;
#10180=VERTEX_POINT ( 'NONE', #19114 ) ;
#10183=ORIENTED_EDGE ( 'NONE', *, *, #1316, .T. ) ;
#10187=FACE_OUTER_BOUND ( 'NONE', #1181, .T. ) ;
#10188=VERTEX_POINT ( 'NONE', #38704 ) ;
#10192=CARTESIAN_POINT ( 'NONE',  ( 17.99999999999999645, 0.000000000000000000, 0.000000000000000000 ) ) ;
#10193=CIRCLE ( 'NONE', #32500, 120.5010000000000190 ) ;
#10194=CYLINDRICAL_SURFACE ( 'NONE', #34615, 116.0000000000000000 ) ;
#10196=CARTESIAN_POINT ( 'NONE',  ( 9.000000000000001776, 11.65176648921190150, -115.4133282497341355 ) ) ;
#10198=VERTEX_POINT ( 'NONE', #5557 ) ;
#10201=CIRCLE ( 'NONE', #40834, 120.5010000000000332 ) ;
#10203=CARTESIAN_POINT ( 'NONE',  ( 17.99999999999999645, 79.94368240339426279, 90.16373242487935613 ) ) ;
#10206=ORIENTED_EDGE ( 'NONE', *, *, #37688, .F. ) ;
#10207=CARTESIAN_POINT ( 'NONE',  ( 8.999999999999998224, -97.97378550988183576, -62.10585602713859288 ) ) ;
#10213=DIRECTION ( 'NONE',  ( 1.000000000000000000, 0.000000000000000000, 0.000000000000000000 ) ) ;
#10219=DIRECTION ( 'NONE',  ( -1.000000000000000000, -0.000000000000000000, -0.000000000000000000 ) ) ;
#10222=ORIENTED_EDGE ( 'NONE', *, *, #19119, .F. ) ;
#10223=DIRECTION ( 'NONE',  ( 0.000000000000000000, 0.05322217484217877520, -0.9985826956767620555 ) ) ;
#10224=LINE ( 'NONE', #23572, #22757 ) ;
#10225=EDGE_CURVE ( 'NONE', #41306, #2648, #23777, .T. ) ;
#10226=ORIENTED_EDGE ( 'NONE', *, *, #28139, .F. ) ;
#10229=CARTESIAN_POINT ( 'NONE',  ( 17.99999999999999645, 79.18387647320879807, -84.76976882518680156 ) ) ;
#10231=VERTEX_POINT ( 'NONE', #2049 ) ;
#10232=CARTESIAN_POINT ( 'NONE',  ( 0.000000000000000000, -111.2721026680459602, 44.61974821237267719 ) ) ;
#10240=ORIENTED_EDGE ( 'NONE', *, *, #16310, .T. ) ;
#10243=EDGE_CURVE ( 'NONE', #8823, #29283, #3501, .T. ) ;
#10247=AXIS2_PLACEMENT_3D ( 'NONE', #28661, #41501, #11218 ) ;
#10248=FACE_OUTER_BOUND ( 'NONE', #111, .T. ) ;
#10251=DIRECTION ( 'NONE',  ( 0.000000000000000000, -0.4132121857683668797, -0.9106347728549182285 ) ) ;
#10255=CARTESIAN_POINT ( 'NONE',  ( 17.99999999999999645, 0.000000000000000000, 0.000000000000000000 ) ) ;
#10257=EDGE_CURVE ( 'NONE', #30765, #26249, #19535, .T. ) ;
#10260=CIRCLE ( 'NONE', #23533, 59.00000000000001421 ) ;
#10261=FACE_OUTER_BOUND ( 'NONE', #31009, .T. ) ;
#10262=LINE ( 'NONE', #40126, #9609 ) ;
#10265=ORIENTED_EDGE ( 'NONE', *, *, #6525, .F. ) ;
#10266=CIRCLE ( 'NONE', #12382, 59.00000000000000000 ) ;
#10269=CIRCLE ( 'NONE', #14475, 120.5010000000000190 ) ;
#10274=CARTESIAN_POINT ( 'NONE',  ( 17.99999999999999645, 0.000000000000000000, 0.000000000000000000 ) ) ;
#10275=EDGE_CURVE ( 'NONE', #267, #32870, #34893, .T. ) ;
#10280=CYLINDRICAL_SURFACE ( 'NONE', #42621, 116.0000000000000000 ) ;
#10281=EDGE_CURVE ( 'NONE', #1786, #40777, #31423, .T. ) ;
#10282=EDGE_CURVE ( 'NONE', #25436, #34149, #25661, .T. ) ;
#10283=VECTOR ( 'NONE', #6889, 1000.000000000000000 ) ;
#10284=DIRECTION ( 'NONE',  ( -1.000000000000000000, -0.000000000000000000, -0.000000000000000000 ) ) ;
#10287=DIRECTION ( 'NONE',  ( 0.000000000000000000, 0.000000000000000000, 1.000000000000000000 ) ) ;
#10288=VERTEX_POINT ( 'NONE', #42816 ) ;
#10292=EDGE_LOOP ( 'NONE', ( #8973, #18638, #10557, #12955 ) ) ;
#10293=CARTESIAN_POINT ( 'NONE',  ( 17.99999999999999645, 42.87700105098607395, 107.7847984684006377 ) ) ;
#10294=EDGE_CURVE ( 'NONE', #20690, #31728, #25861, .T. ) ;
#10296=CIRCLE ( 'NONE', #1913, 116.0000000000000000 ) ;
#10297=VERTEX_POINT ( 'NONE', #36931 ) ;
#10302=CIRCLE ( 'NONE', #11700, 59.00000000000001421 ) ;
#10303=AXIS2_PLACEMENT_3D ( 'NONE', #35599, #32758, #28665 ) ;
#10305=VERTEX_POINT ( 'NONE', #7042 ) ;
#10306=CYLINDRICAL_SURFACE ( 'NONE', #29071, 120.5010000000000190 ) ;
#10312=CARTESIAN_POINT ( 'NONE',  ( 17.99999999999999645, -110.3490479609633752, 20.28201389785361641 ) ) ;
#10316=VERTEX_POINT ( 'NONE', #23449 ) ;
#10317=EDGE_CURVE ( 'NONE', #34636, #21461, #24508, .T. ) ;
#10321=DIRECTION ( 'NONE',  ( 1.000000000000000000, 0.000000000000000000, 0.000000000000000000 ) ) ;
#10322=VERTEX_POINT ( 'NONE', #13197 ) ;
#10323=CARTESIAN_POINT ( 'NONE',  ( 17.99999999999999645, 0.000000000000000000, 0.000000000000000000 ) ) ;
#10326=ORIENTED_EDGE ( 'NONE', *, *, #11338, .T. ) ;
#10327=DIRECTION ( 'NONE',  ( -1.000000000000000000, 0.000000000000000000, 0.000000000000000000 ) ) ;
#10331=CARTESIAN_POINT ( 'NONE',  ( 17.99999999999999645, -69.72480978690109055, 92.70626138605992139 ) ) ;
#10332=VECTOR ( 'NONE', #15759, 1000.000000000000000 ) ;
#10333=AXIS2_PLACEMENT_3D ( 'NONE', #16390, #29696, #42967 ) ;
#10334=CIRCLE ( 'NONE', #24297, 116.0000000000000000 ) ;
#10337=CARTESIAN_POINT ( 'NONE',  ( 17.99999999999999645, -52.19040376560500505, 99.31985817764160629 ) ) ;
#10340=AXIS2_PLACEMENT_3D ( 'NONE', #12749, #6824, #20181 ) ;
#10345=EDGE_LOOP ( 'NONE', ( #13545, #6734, #9245, #3905 ) ) ;
#10346=CARTESIAN_POINT ( 'NONE',  ( 0.000000000000000000, 118.8387007424470738, 19.94628303336527608 ) ) ;
#10352=EDGE_CURVE ( 'NONE', #16718, #18043, #19602, .T. ) ;
#10353=DIRECTION ( 'NONE',  ( 0.000000000000000000, -0.7865515558026479059, 0.6175246149461850464 ) ) ;
#10354=VERTEX_POINT ( 'NONE', #16699 ) ;
#10358=FACE_OUTER_BOUND ( 'NONE', #25618, .T. ) ;
#10362=CARTESIAN_POINT ( 'NONE',  ( 0.000000000000000000, -100.6739960869714139, -49.52796165323368172 ) ) ;
#10363=AXIS2_PLACEMENT_3D ( 'NONE', #21947, #32362, #2235 ) ;
#10364=VERTEX_POINT ( 'NONE', #10544 ) ;
#10367=CARTESIAN_POINT ( 'NONE',  ( 17.99999999999999645, 40.13512380273970592, 113.6206972269522737 ) ) ;
#10368=FACE_OUTER_BOUND ( 'NONE', #30738, .T. ) ;
#10369=EDGE_CURVE ( 'NONE', #40182, #3503, #39759, .T. ) ;
#10371=DIRECTION ( 'NONE',  ( -1.000000000000000000, 0.000000000000000000, -0.000000000000000000 ) ) ;
#10373=ORIENTED_EDGE ( 'NONE', *, *, #37739, .T. ) ;
#10374=CARTESIAN_POINT ( 'NONE',  ( 9.000000000000001776, -31.17727234463771424, 111.7317219465818852 ) ) ;
#10375=CYLINDRICAL_SURFACE ( 'NONE', #17297, 59.00000000000000000 ) ;
#10376=ADVANCED_FACE ( 'NONE', ( #36279 ), #30630, .F. ) ;
#10379=ORIENTED_EDGE ( 'NONE', *, *, #38446, .F. ) ;
#10382=CARTESIAN_POINT ( 'NONE',  ( 9.000000000000001776, 115.0622509503834578, -14.72000021165029082 ) ) ;
#10383=ORIENTED_EDGE ( 'NONE', *, *, #29504, .T. ) ;
#10386=CARTESIAN_POINT ( 'NONE',  ( 17.99999999999999645, 0.000000000000000000, 0.000000000000000000 ) ) ;
#10389=ADVANCED_FACE ( 'NONE', ( #13406 ), #40194, .F. ) ;
#10394=CARTESIAN_POINT ( 'NONE',  ( 8.999999999999998224, -64.69195966009955612, 96.28577441832231898 ) ) ;
#10398=ORIENTED_EDGE ( 'NONE', *, *, #11544, .T. ) ;
#10400=CARTESIAN_POINT ( 'NONE',  ( 8.999999999999998224, 64.69195966010022403, -96.28577441832183581 ) ) ;
#10402=DIRECTION ( 'NONE',  ( 1.000000000000000000, 0.000000000000000000, 0.000000000000000000 ) ) ;
#10403=VERTEX_POINT ( 'NONE', #10331 ) ;
#10404=DIRECTION ( 'NONE',  ( 0.000000000000000000, -0.5076658003388468954, 0.8615540813938020737 ) ) ;
#10407=ORIENTED_EDGE ( 'NONE', *, *, #29480, .T. ) ;
#10408=CYLINDRICAL_SURFACE ( 'NONE', #12415, 116.0000000000000000 ) ;
#10409=DIRECTION ( 'NONE',  ( 0.000000000000000000, 0.000000000000000000, -1.000000000000000000 ) ) ;
#10413=EDGE_LOOP ( 'NONE', ( #17719, #42045, #32251, #8341 ) ) ;
#10415=VERTEX_POINT ( 'NONE', #23239 ) ;
#10418=EDGE_CURVE ( 'NONE', #29283, #16283, #36275, .T. ) ;
#10419=DIRECTION ( 'NONE',  ( -1.000000000000000000, -0.000000000000000000, -0.000000000000000000 ) ) ;
#10420=AXIS2_PLACEMENT_3D ( 'NONE', #16036, #25859, #19110 ) ;
#10422=CARTESIAN_POINT ( 'NONE',  ( 8.999999999999998224, -95.31344542257777164, 66.11616384574416827 ) ) ;
#10428=VECTOR ( 'NONE', #34241, 1000.000000000000000 ) ;
#10433=CARTESIAN_POINT ( 'NONE',  ( 0.000000000000000000, 0.000000000000000000, 0.000000000000000000 ) ) ;
#10435=ORIENTED_EDGE ( 'NONE', *, *, #5045, .T. ) ;
#10438=ORIENTED_EDGE ( 'NONE', *, *, #3584, .F. ) ;
#10444=EDGE_CURVE ( 'NONE', #1566, #10322, #24326, .T. ) ;
#10445=CARTESIAN_POINT ( 'NONE',  ( 0.000000000000000000, 117.6086855750634470, 26.24286718912143712 ) ) ;
#10446=DIRECTION ( 'NONE',  ( 0.000000000000000000, 0.5963673585384970943, 0.8027116379309668925 ) ) ;
#10447=ORIENTED_EDGE ( 'NONE', *, *, #38715, .F. ) ;
#10450=ORIENTED_EDGE ( 'NONE', *, *, #23626, .T. ) ;
#10451=CIRCLE ( 'NONE', #24411, 120.5010000000000190 ) ;
#10457=DIRECTION ( 'NONE',  ( -1.000000000000000000, 0.000000000000000000, 0.000000000000000000 ) ) ;
#10462=ORIENTED_EDGE ( 'NONE', *, *, #32955, .F. ) ;
#10469=CARTESIAN_POINT ( 'NONE',  ( 17.99999999999999645, 80.74349901498510462, -77.90224541347200216 ) ) ;
#10475=CIRCLE ( 'NONE', #11909, 116.0000000000000000 ) ;
#10476=VERTEX_POINT ( 'NONE', #27798 ) ;
#10477=AXIS2_PLACEMENT_3D ( 'NONE', #21865, #35535, #22288 ) ;
#10480=CIRCLE ( 'NONE', #14683, 59.00000000000000711 ) ;
#10481=ORIENTED_EDGE ( 'NONE', *, *, #3957, .F. ) ;
#10482=DIRECTION ( 'NONE',  ( 0.000000000000000000, 0.000000000000000000, 1.000000000000000000 ) ) ;
#10485=CYLINDRICAL_SURFACE ( 'NONE', #21248, 59.00000000000000000 ) ;
#10488=DIRECTION ( 'NONE',  ( -1.000000000000000000, 0.000000000000000000, 0.000000000000000000 ) ) ;
#10491=DIRECTION ( 'NONE',  ( 0.000000000000000000, 0.000000000000000000, 1.000000000000000000 ) ) ;
#10493=ADVANCED_FACE ( 'NONE', ( #41489 ), #31486, .F. ) ;
#10494=LINE ( 'NONE', #23831, #39395 ) ;
#10508=ORIENTED_EDGE ( 'NONE', *, *, #22354, .F. ) ;
#10509=DIRECTION ( 'NONE',  ( 0.000000000000000000, -0.7164567402983209599, 0.6976315211349787271 ) ) ;
#10511=ADVANCED_FACE ( 'NONE', ( #14489 ), #21058, .F. ) ;
#10512=DIRECTION ( 'NONE',  ( -1.000000000000000000, 0.000000000000000000, 0.000000000000000000 ) ) ;
#10513=VERTEX_POINT ( 'NONE', #41717 ) ;
#10515=CARTESIAN_POINT ( 'NONE',  ( 17.99999999999999645, -119.8996782608629275, -12.02323392193477325 ) ) ;
#10518=VECTOR ( 'NONE', #4525, 1000.000000000000000 ) ;
#10520=CARTESIAN_POINT ( 'NONE',  ( 8.999999999999998224, 73.51007459736429439, 89.73443560133387109 ) ) ;
#10521=CARTESIAN_POINT ( 'NONE',  ( 0.000000000000000000, -45.89132998248120288, 102.3829004574628385 ) ) ;
#10522=CARTESIAN_POINT ( 'NONE',  ( 17.99999999999999645, -119.7318547011702634, 13.59315897125686412 ) ) ;
#10525=ORIENTED_EDGE ( 'NONE', *, *, #34261, .F. ) ;
#10526=FACE_OUTER_BOUND ( 'NONE', #31267, .T. ) ;
#10527=DIRECTION ( 'NONE',  ( 0.000000000000000000, 0.9213119778704114138, 0.3888241754733244848 ) ) ;
#10528=ORIENTED_EDGE ( 'NONE', *, *, #27929, .T. ) ;
#10529=DIRECTION ( 'NONE',  ( 0.000000000000000000, 0.2113826236296247607, -0.9774033898178666746 ) ) ;
#10530=CARTESIAN_POINT ( 'NONE',  ( 17.99999999999999645, 0.000000000000000000, 0.000000000000000000 ) ) ;
#10531=EDGE_LOOP ( 'NONE', ( #15016, #13644, #8871, #14646 ) ) ;
#10534=CARTESIAN_POINT ( 'NONE',  ( 8.999999999999998224, -104.0201923570372173, -51.34003878071168003 ) ) ;
#10536=AXIS2_PLACEMENT_3D ( 'NONE', #35845, #2886, #19329 ) ;
#10543=VERTEX_POINT ( 'NONE', #38228 ) ;
#10544=CARTESIAN_POINT ( 'NONE',  ( 17.99999999999999645, 119.0898412705474385, 18.38751498043773935 ) ) ;
#10545=AXIS2_PLACEMENT_3D ( 'NONE', #36320, #293, #30030 ) ;
#10553=DIRECTION ( 'NONE',  ( 1.000000000000000000, 0.000000000000000000, 0.000000000000000000 ) ) ;
#10555=ORIENTED_EDGE ( 'NONE', *, *, #19658, .T. ) ;
#10556=CARTESIAN_POINT ( 'NONE',  ( 0.000000000000000000, -98.39501399267994941, 53.91376164787647696 ) ) ;
#10557=ORIENTED_EDGE ( 'NONE', *, *, #33010, .F. ) ;
#10559=AXIS2_PLACEMENT_3D ( 'NONE', #11385, #24717, #16176 ) ;
#10562=EDGE_CURVE ( 'NONE', #31846, #37721, #34231, .T. ) ;
#10567=EDGE_CURVE ( 'NONE', #37692, #31975, #4971, .T. ) ;
#10574=DIRECTION ( 'NONE',  ( 1.000000000000000000, 0.000000000000000000, 0.000000000000000000 ) ) ;
#10575=AXIS2_PLACEMENT_3D ( 'NONE', #24139, #21318, #17818 ) ;
#10576=CARTESIAN_POINT ( 'NONE',  ( 17.99999999999999645, 0.000000000000000000, 0.000000000000000000 ) ) ;
#10579=ORIENTED_EDGE ( 'NONE', *, *, #12384, .F. ) ;
#10580=CIRCLE ( 'NONE', #16144, 58.99999999999999289 ) ;
#10582=DIRECTION ( 'NONE',  ( 0.000000000000000000, 0.000000000000000000, 1.000000000000000000 ) ) ;
#10584=ORIENTED_EDGE ( 'NONE', *, *, #11991, .T. ) ;
#10585=ORIENTED_EDGE ( 'NONE', *, *, #41649, .F. ) ;
#10586=CARTESIAN_POINT ( 'NONE',  ( 17.99999999999999645, 0.000000000000000000, 0.000000000000000000 ) ) ;
#10587=CARTESIAN_POINT ( 'NONE',  ( 8.999999999999998224, -54.09091620264651823, -102.6166301549523467 ) ) ;
#10589=LINE ( 'NONE', #4450, #14624 ) ;
#10590=DIRECTION ( 'NONE',  ( 0.000000000000000000, 0.000000000000000000, 1.000000000000000000 ) ) ;
#10595=DIRECTION ( 'NONE',  ( 0.000000000000000000, -3.810511228586342406E-14, -1.000000000000000000 ) ) ;
#10598=AXIS2_PLACEMENT_3D ( 'NONE', #29243, #16365, #16154 ) ;
#10601=CIRCLE ( 'NONE', #830, 116.0000000000000000 ) ;
#10603=AXIS2_PLACEMENT_3D ( 'NONE', #26385, #13296, #33115 ) ;
#10604=LINE ( 'NONE', #10394, #17848 ) ;
#10607=EDGE_LOOP ( 'NONE', ( #12120, #32903, #35241, #30848 ) ) ;
#10608=CIRCLE ( 'NONE', #39147, 120.5010000000000332 ) ;
#10610=LINE ( 'NONE', #3603, #3860 ) ;
#10611=EDGE_CURVE ( 'NONE', #11646, #42007, #29365, .T. ) ;
#10614=CYLINDRICAL_SURFACE ( 'NONE', #17690, 116.0000000000000000 ) ;
#10616=EDGE_CURVE ( 'NONE', #12490, #384, #35163, .T. ) ;
#10623=ORIENTED_EDGE ( 'NONE', *, *, #16228, .F. ) ;
#10628=EDGE_CURVE ( 'NONE', #25554, #27794, #16866, .T. ) ;
#10630=CIRCLE ( 'NONE', #35014, 59.00000000000000711 ) ;
#10632=CARTESIAN_POINT ( 'NONE',  ( 17.99999999999999645, 0.000000000000000000, 0.000000000000000000 ) ) ;
#10633=ORIENTED_EDGE ( 'NONE', *, *, #31645, .T. ) ;
#10634=FILL_AREA_STYLE_COLOUR ( '', #8847 ) ;
#10635=CIRCLE ( 'NONE', #7130, 120.5010000000000190 ) ;
#10637=CIRCLE ( 'NONE', #8541, 116.0000000000000000 ) ;
#10638=CARTESIAN_POINT ( 'NONE',  ( 17.99999999999999645, -21.55123232222391394, -118.5581519187674360 ) ) ;
#10640=DIRECTION ( 'NONE',  ( 0.000000000000000000, 0.000000000000000000, 1.000000000000000000 ) ) ;
#10642=DIRECTION ( 'NONE',  ( 0.000000000000000000, 0.000000000000000000, 1.000000000000000000 ) ) ;
#10645=VERTEX_POINT ( 'NONE', #25607 ) ;
#10646=DIRECTION ( 'NONE',  ( 0.000000000000000000, 0.9714298932647090767, 0.2373266998711184850 ) ) ;
#10647=DIRECTION ( 'NONE',  ( 0.000000000000000000, 0.000000000000000000, 1.000000000000000000 ) ) ;
#10649=CARTESIAN_POINT ( 'NONE',  ( 17.99999999999999645, 97.97378550988308632, -62.10585602713662468 ) ) ;
#10650=ORIENTED_EDGE ( 'NONE', *, *, #11889, .F. ) ;
#10651=DIRECTION ( 'NONE',  ( 1.000000000000000000, 0.000000000000000000, 0.000000000000000000 ) ) ;
#10658=LINE ( 'NONE', #17249, #4238 ) ;
#10660=ORIENTED_EDGE ( 'NONE', *, *, #2376, .T. ) ;
#10662=CARTESIAN_POINT ( 'NONE',  ( 0.000000000000000000, -111.2721026680459602, -14.38025178762732104 ) ) ;
#10664=ORIENTED_EDGE ( 'NONE', *, *, #986, .T. ) ;
#10667=EDGE_CURVE ( 'NONE', #21659, #40725, #15468, .T. ) ;
#10674=AXIS2_PLACEMENT_3D ( 'NONE', #21830, #25104, #38352 ) ;
#10682=DIRECTION ( 'NONE',  ( 1.000000000000000000, 0.000000000000000000, -0.000000000000000000 ) ) ;
#10683=VECTOR ( 'NONE', #658, 1000.000000000000000 ) ;
#10685=CARTESIAN_POINT ( 'NONE',  ( 17.99999999999999645, -115.9750404417044223, 2.406240749597103434 ) ) ;
#10686=DIRECTION ( 'NONE',  ( -1.000000000000000000, -0.000000000000000000, -0.000000000000000000 ) ) ;
#10687=AXIS2_PLACEMENT_3D ( 'NONE', #2607, #32101, #2180 ) ;
#10688=VERTEX_POINT ( 'NONE', #25186 ) ;
#10690=DIRECTION ( 'NONE',  ( 1.000000000000000000, 0.000000000000000000, 0.000000000000000000 ) ) ;
#10693=DIRECTION ( 'NONE',  ( 0.000000000000000000, 0.000000000000000000, 1.000000000000000000 ) ) ;
#10694=CARTESIAN_POINT ( 'NONE',  ( 17.99999999999999645, -51.27532863109435368, 99.79535634195110561 ) ) ;
#10695=ORIENTED_EDGE ( 'NONE', *, *, #15509, .F. ) ;
#10701=EDGE_LOOP ( 'NONE', ( #29596, #4855, #147, #20283 ) ) ;
#10702=CARTESIAN_POINT ( 'NONE',  ( 9.000000000000001776, 58.30069736313667050, 100.2847380560568951 ) ) ;
#10706=FACE_OUTER_BOUND ( 'NONE', #37632, .T. ) ;
#10707=VERTEX_POINT ( 'NONE', #5502 ) ;
#10708=DIRECTION ( 'NONE',  ( 0.000000000000000000, -0.9996456111234522934, -0.02662052143778456323 ) ) ;
#10709=DIRECTION ( 'NONE',  ( -1.000000000000000000, -0.000000000000000000, -0.000000000000000000 ) ) ;
#10712=AXIS2_PLACEMENT_3D ( 'NONE', #32716, #36622, #9600 ) ;
#10714=CARTESIAN_POINT ( 'NONE',  ( 0.000000000000000000, -84.77518783075045405, -73.49448960231443095 ) ) ;
#10715=ADVANCED_FACE ( 'NONE', ( #10047 ), #42985, .F. ) ;
#10719=CIRCLE ( 'NONE', #17704, 116.0000000000000000 ) ;
#10733=EDGE_CURVE ( 'NONE', #1445, #21287, #23621, .T. ) ;
#10734=DIRECTION ( 'NONE',  ( 0.000000000000000000, 0.000000000000000000, 1.000000000000000000 ) ) ;
#10738=CARTESIAN_POINT ( 'NONE',  ( 17.99999999999999645, -63.24564713401724703, -102.5693868539701299 ) ) ;
#10743=CARTESIAN_POINT ( 'NONE',  ( 17.99999999999999645, 0.000000000000000000, 0.000000000000000000 ) ) ;
#10745=ORIENTED_EDGE ( 'NONE', *, *, #21530, .F. ) ;
#10749=ORIENTED_EDGE ( 'NONE', *, *, #30974, .F. ) ;
#10750=CARTESIAN_POINT ( 'NONE',  ( 0.000000000000000000, -6.486220790509180212, 112.0098273076987283 ) ) ;
#10751=ORIENTED_EDGE ( 'NONE', *, *, #34361, .T. ) ;
#10754=AXIS2_PLACEMENT_3D ( 'NONE', #32897, #25537, #12846 ) ;
#10757=FACE_BOUND ( 'NONE', #29880, .T. ) ;
#10762=DIRECTION ( 'NONE',  ( 0.000000000000000000, 0.000000000000000000, 1.000000000000000000 ) ) ;
#10764=ORIENTED_EDGE ( 'NONE', *, *, #8445, .F. ) ;
#10771=FACE_OUTER_BOUND ( 'NONE', #39222, .T. ) ;
#10773=FACE_OUTER_BOUND ( 'NONE', #22096, .T. ) ;
#10775=ADVANCED_FACE ( 'NONE', ( #13568 ), #3689, .F. ) ;
#10776=ORIENTED_EDGE ( 'NONE', *, *, #2610, .T. ) ;
#10778=AXIS2_PLACEMENT_3D ( 'NONE', #39022, #28169, #3438 ) ;
#10779=DIRECTION ( 'NONE',  ( -1.000000000000000000, 0.000000000000000000, 0.000000000000000000 ) ) ;
#10785=CIRCLE ( 'NONE', #8655, 59.00000000000000711 ) ;
#10787=EDGE_CURVE ( 'NONE', #35201, #14512, #27273, .T. ) ;
#10790=EDGE_LOOP ( 'NONE', ( #23825, #2672, #12521, #14057 ) ) ;
#10791=CARTESIAN_POINT ( 'NONE',  ( 17.99999999999999645, 97.19627249181192497, -71.22763238166385236 ) ) ;
#10792=EDGE_CURVE ( 'NONE', #2814, #37962, #16647, .T. ) ;
#10793=CARTESIAN_POINT ( 'NONE',  ( 17.99999999999999645, 111.2721026680460596, -14.38025178762657852 ) ) ;
#10794=DIRECTION ( 'NONE',  ( 1.000000000000000000, 0.000000000000000000, 0.000000000000000000 ) ) ;
#10795=ADVANCED_FACE ( 'NONE', ( #13356 ), #9632, .F. ) ;
#10796=CYLINDRICAL_SURFACE ( 'NONE', #32349, 59.00000000000000000 ) ;
#10800=ORIENTED_EDGE ( 'NONE', *, *, #35787, .F. ) ;
#10801=CARTESIAN_POINT ( 'NONE',  ( 17.99999999999999645, -53.40478689619660457, -108.0204598100370816 ) ) ;
#10802=DIRECTION ( 'NONE',  ( -1.000000000000000000, 0.000000000000000000, 0.000000000000000000 ) ) ;
#10804=LINE ( 'NONE', #20657, #15696 ) ;
#10807=DIRECTION ( 'NONE',  ( -1.000000000000000000, -0.000000000000000000, -0.000000000000000000 ) ) ;
#10810=AXIS2_PLACEMENT_3D ( 'NONE', #11108, #36835, #4087 ) ;
#10812=ORIENTED_EDGE ( 'NONE', *, *, #24248, .F. ) ;
#10813=VECTOR ( 'NONE', #39638, 1000.000000000000000 ) ;
#10815=ORIENTED_EDGE ( 'NONE', *, *, #2105, .T. ) ;
#10818=EDGE_CURVE ( 'NONE', #12767, #38581, #22980, .T. ) ;
#10821=DIRECTION ( 'NONE',  ( 1.000000000000000000, 0.000000000000000000, 0.000000000000000000 ) ) ;
#10824=ORIENTED_EDGE ( 'NONE', *, *, #2444, .F. ) ;
#10830=ORIENTED_EDGE ( 'NONE', *, *, #3352, .F. ) ;
#10832=EDGE_CURVE ( 'NONE', #35433, #22718, #22448, .T. ) ;
#10834=EDGE_CURVE ( 'NONE', #29542, #27165, #27980, .T. ) ;
#10835=DIRECTION ( 'NONE',  ( -1.000000000000000000, -0.000000000000000000, -0.000000000000000000 ) ) ;
#10836=CARTESIAN_POINT ( 'NONE',  ( 0.000000000000000000, 0.000000000000000000, 0.000000000000000000 ) ) ;
#10839=AXIS2_PLACEMENT_3D ( 'NONE', #21335, #14767, #8611 ) ;
#10841=CIRCLE ( 'NONE', #35210, 120.5010000000000190 ) ;
#10842=CARTESIAN_POINT ( 'NONE',  ( 17.99999999999999645, 0.000000000000000000, 0.000000000000000000 ) ) ;
#10843=VERTEX_POINT ( 'NONE', #16408 ) ;
#10846=ORIENTED_EDGE ( 'NONE', *, *, #1734, .T. ) ;
#10855=EDGE_LOOP ( 'NONE', ( #28597, #14293, #14708, #37760 ) ) ;
#10857=VERTEX_POINT ( 'NONE', #34855 ) ;
#10859=CARTESIAN_POINT ( 'NONE',  ( 0.000000000000000000, -31.17727234463623631, -111.7317219465823115 ) ) ;
#10864=DIRECTION ( 'NONE',  ( -1.000000000000000000, 0.000000000000000000, 0.000000000000000000 ) ) ;
#10869=EDGE_CURVE ( 'NONE', #29621, #5301, #31452, .T. ) ;
#10870=DIRECTION ( 'NONE',  ( 1.000000000000000000, 0.000000000000000000, 0.000000000000000000 ) ) ;
#10872=DIRECTION ( 'NONE',  ( 0.000000000000000000, 0.000000000000000000, 1.000000000000000000 ) ) ;
#10874=EDGE_CURVE ( 'NONE', #40855, #36072, #2197, .T. ) ;
#10876=ORIENTED_EDGE ( 'NONE', *, *, #27523, .F. ) ;
#10878=VECTOR ( 'NONE', #24615, 1000.000000000000000 ) ;
#10879=ORIENTED_EDGE ( 'NONE', *, *, #2, .F. ) ;
#10885=CIRCLE ( 'NONE', #40110, 58.99999999999998579 ) ;
#10887=DIRECTION ( 'NONE',  ( -1.000000000000000000, 0.000000000000000000, 0.000000000000000000 ) ) ;
#10890=EDGE_LOOP ( 'NONE', ( #31491, #4898, #12758, #24821 ) ) ;
#10891=LINE ( 'NONE', #816, #23109 ) ;
#10894=ORIENTED_EDGE ( 'NONE', *, *, #38621, .T. ) ;
#10895=CARTESIAN_POINT ( 'NONE',  ( 0.000000000000000000, 0.000000000000000000, 0.000000000000000000 ) ) ;
#10897=ORIENTED_EDGE ( 'NONE', *, *, #14634, .F. ) ;
#10901=CARTESIAN_POINT ( 'NONE',  ( 0.000000000000000000, -41.62036691425604573, 113.0850832732712945 ) ) ;
#10907=AXIS2_PLACEMENT_3D ( 'NONE', #13523, #26816, #40090 ) ;
#10910=CIRCLE ( 'NONE', #16494, 116.0000000000000000 ) ;
#10911=CIRCLE ( 'NONE', #5328, 58.99999999999999289 ) ;
#10912=DIRECTION ( 'NONE',  ( 0.000000000000000000, 0.000000000000000000, 1.000000000000000000 ) ) ;
#10913=CIRCLE ( 'NONE', #24168, 59.00000000000001421 ) ;
#10914=DIRECTION ( 'NONE',  ( 1.000000000000000000, 0.000000000000000000, -0.000000000000000000 ) ) ;
#10915=CARTESIAN_POINT ( 'NONE',  ( 8.999999999999998224, 87.74575819880270444, -75.87280091124384285 ) ) ;
#10916=DIRECTION ( 'NONE',  ( -1.000000000000000000, 0.000000000000000000, -0.000000000000000000 ) ) ;
#10919=DIRECTION ( 'NONE',  ( 0.000000000000000000, -0.2631025642275088838, -0.9647678688145193693 ) ) ;
#10921=VERTEX_POINT ( 'NONE', #5400 ) ;
#10923=DIRECTION ( 'NONE',  ( 1.000000000000000000, -0.000000000000000000, 0.000000000000000000 ) ) ;
#10926=DIRECTION ( 'NONE',  ( 0.000000000000000000, 0.000000000000000000, 1.000000000000000000 ) ) ;
#10927=LINE ( 'NONE', #31857, #36130 ) ;
#10930=EDGE_CURVE ( 'NONE', #15795, #18913, #36337, .T. ) ;
#10935=DIRECTION ( 'NONE',  ( 0.000000000000000000, 0.000000000000000000, 1.000000000000000000 ) ) ;
#10936=ORIENTED_EDGE ( 'NONE', *, *, #4893, .T. ) ;
#10937=DIRECTION ( 'NONE',  ( 0.000000000000000000, 3.551772811830479642E-14, -1.000000000000000000 ) ) ;
#10939=VERTEX_POINT ( 'NONE', #5174 ) ;
#10944=VERTEX_POINT ( 'NONE', #18538 ) ;
#10946=DIRECTION ( 'NONE',  ( -1.000000000000000000, -0.000000000000000000, -0.000000000000000000 ) ) ;
#10947=AXIS2_PLACEMENT_3D ( 'NONE', #37981, #41030, #32097 ) ;
#10949=EDGE_CURVE ( 'NONE', #6259, #2948, #9191, .T. ) ;
#10952=CARTESIAN_POINT ( 'NONE',  ( 9.000000000000001776, 104.6166166098445416, 50.11350645393712000 ) ) ;
#10955=VECTOR ( 'NONE', #31637, 1000.000000000000000 ) ;
#10956=CARTESIAN_POINT ( 'NONE',  ( 8.999999999999998224, 114.8812324315175033, 16.07179003769187986 ) ) ;
#10963=ORIENTED_EDGE ( 'NONE', *, *, #9222, .T. ) ;
#10970=FACE_OUTER_BOUND ( 'NONE', #20394, .T. ) ;
#10972=CIRCLE ( 'NONE', #31871, 59.00000000000000000 ) ;
#10973=ORIENTED_EDGE ( 'NONE', *, *, #3804, .F. ) ;
#10976=DIRECTION ( 'NONE',  ( -1.000000000000000000, 0.000000000000000000, 0.000000000000000000 ) ) ;
#10981=CIRCLE ( 'NONE', #3959, 116.0000000000000000 ) ;
#10983=ADVANCED_FACE ( 'NONE', ( #1899 ), #41822, .T. ) ;
#10984=CARTESIAN_POINT ( 'NONE',  ( 17.99999999999999645, 92.10690493017060021, 64.06707842432207656 ) ) ;
#10986=DIRECTION ( 'NONE',  ( 0.000000000000000000, -2.305124076552231752E-14, -1.000000000000000000 ) ) ;
#10988=ORIENTED_EDGE ( 'NONE', *, *, #13155, .T. ) ;
#10989=PRODUCT_DEFINITION ( 'UNKNOWN', '', #42738, #20456 ) ;
#10993=AXIS2_PLACEMENT_3D ( 'NONE', #7260, #13416, #16707 ) ;
#10995=ORIENTED_EDGE ( 'NONE', *, *, #13364, .T. ) ;
#10998=ORIENTED_EDGE ( 'NONE', *, *, #8559, .F. ) ;
#11006=CARTESIAN_POINT ( 'NONE',  ( 17.99999999999999645, 0.000000000000000000, 0.000000000000000000 ) ) ;
#11008=AXIS2_PLACEMENT_3D ( 'NONE', #29471, #12680, #17040 ) ;
#11009=ORIENTED_EDGE ( 'NONE', *, *, #41477, .F. ) ;
#11013=AXIS2_PLACEMENT_3D ( 'NONE', #23704, #4006, #4225 ) ;
#11018=ORIENTED_EDGE ( 'NONE', *, *, #18917, .F. ) ;
#11021=ORIENTED_EDGE ( 'NONE', *, *, #39407, .F. ) ;
#11022=CIRCLE ( 'NONE', #35382, 120.5010000000000190 ) ;
#11023=VERTEX_POINT ( 'NONE', #9527 ) ;
#11024=CYLINDRICAL_SURFACE ( 'NONE', #5998, 116.0000000000000000 ) ;
#11025=CARTESIAN_POINT ( 'NONE',  ( 17.99999999999999645, 92.25992191227393846, 77.51514567967427638 ) ) ;
#11026=DIRECTION ( 'NONE',  ( 1.000000000000000000, 0.000000000000000000, 0.000000000000000000 ) ) ;
#11027=DIRECTION ( 'NONE',  ( -1.000000000000000000, -0.000000000000000000, 0.000000000000000000 ) ) ;
#11030=ORIENTED_EDGE ( 'NONE', *, *, #22559, .T. ) ;
#11035=FACE_OUTER_BOUND ( 'NONE', #38057, .T. ) ;
#11036=ORIENTED_EDGE ( 'NONE', *, *, #5799, .T. ) ;
#11037=ORIENTED_EDGE ( 'NONE', *, *, #14908, .F. ) ;
#11038=DIRECTION ( 'NONE',  ( 0.000000000000000000, 0.000000000000000000, 1.000000000000000000 ) ) ;
#11040=EDGE_CURVE ( 'NONE', #35433, #5549, #41224, .T. ) ;
#11041=CARTESIAN_POINT ( 'NONE',  ( 0.000000000000000000, -5.456439917445724319, 112.0647122740741963 ) ) ;
#11042=CIRCLE ( 'NONE', #23602, 59.00000000000000000 ) ;
#11043=CARTESIAN_POINT ( 'NONE',  ( 17.99999999999999645, -63.24564713401861837, 102.5693868539693341 ) ) ;
#11049=CARTESIAN_POINT ( 'NONE',  ( 0.000000000000000000, 86.84764344323065188, -76.89919913989662348 ) ) ;
#11050=AXIS2_PLACEMENT_3D ( 'NONE', #12687, #12267, #22742 ) ;
#11056=CARTESIAN_POINT ( 'NONE',  ( 17.99999999999999645, -19.12429268481634281, -114.4126803693781085 ) ) ;
#11059=VERTEX_POINT ( 'NONE', #22883 ) ;
#11063=DIRECTION ( 'NONE',  ( -1.000000000000000000, -0.000000000000000000, 0.000000000000000000 ) ) ;
#11064=DIRECTION ( 'NONE',  ( 0.000000000000000000, 0.000000000000000000, 1.000000000000000000 ) ) ;
#11066=AXIS2_PLACEMENT_3D ( 'NONE', #28386, #18587, #36118 ) ;
#11073=EDGE_CURVE ( 'NONE', #29453, #5323, #31482, .T. ) ;
#11074=ORIENTED_EDGE ( 'NONE', *, *, #13849, .T. ) ;
#11076=EDGE_CURVE ( 'NONE', #27890, #24120, #21777, .T. ) ;
#11077=CARTESIAN_POINT ( 'NONE',  ( 0.000000000000000000, 76.48293397876373945, -82.08917884620232996 ) ) ;
#11080=DIRECTION ( 'NONE',  ( 1.000000000000000000, 0.000000000000000000, 0.000000000000000000 ) ) ;
#11084=CARTESIAN_POINT ( 'NONE',  ( 17.99999999999999645, -57.40245293794732362, 96.40140491896615060 ) ) ;
#11087=ORIENTED_EDGE ( 'NONE', *, *, #24169, .T. ) ;
#11090=FACE_OUTER_BOUND ( 'NONE', #24452, .T. ) ;
#11094=ORIENTED_EDGE ( 'NONE', *, *, #26933, .T. ) ;
#11095=DIRECTION ( 'NONE',  ( 1.000000000000000000, 0.000000000000000000, -0.000000000000000000 ) ) ;
#11100=ADVANCED_FACE ( 'NONE', ( #29606 ), #42878, .F. ) ;
#11102=ORIENTED_EDGE ( 'NONE', *, *, #31360, .T. ) ;
#11104=ORIENTED_EDGE ( 'NONE', *, *, #25870, .F. ) ;
#11107=EDGE_CURVE ( 'NONE', #18324, #27302, #41918, .T. ) ;
#11108=CARTESIAN_POINT ( 'NONE',  ( 0.000000000000000000, 0.000000000000000000, 0.000000000000000000 ) ) ;
#11109=EDGE_CURVE ( 'NONE', #4179, #17128, #37034, .T. ) ;
#11112=CARTESIAN_POINT ( 'NONE',  ( 0.000000000000000000, 0.000000000000000000, 0.000000000000000000 ) ) ;
#11113=DIRECTION ( 'NONE',  ( 0.000000000000000000, 0.000000000000000000, 1.000000000000000000 ) ) ;
#11114=EDGE_LOOP ( 'NONE', ( #17658, #24600, #29715, #368 ) ) ;
#11115=DIRECTION ( 'NONE',  ( 0.000000000000000000, 0.2631025642275152121, 0.9647678688145175929 ) ) ;
#11119=DIRECTION ( 'NONE',  ( 0.000000000000000000, 0.000000000000000000, 1.000000000000000000 ) ) ;
#11124=AXIS2_PLACEMENT_3D ( 'NONE', #31687, #41713, #38001 ) ;
#11125=EDGE_CURVE ( 'NONE', #17817, #42716, #26341, .T. ) ;
#11132=CARTESIAN_POINT ( 'NONE',  ( 0.000000000000000000, 84.09610293794170843, -74.27057253242929846 ) ) ;
#11139=EDGE_LOOP ( 'NONE', ( #5539, #6659, #8406, #29344 ) ) ;
#11141=DIRECTION ( 'NONE',  ( 0.000000000000000000, 0.7164567402983114119, 0.6976315211349884970 ) ) ;
#11142=DIRECTION ( 'NONE',  ( -1.000000000000000000, 0.000000000000000000, 0.000000000000000000 ) ) ;
#11143=ORIENTED_EDGE ( 'NONE', *, *, #22349, .F. ) ;
#11147=DIRECTION ( 'NONE',  ( 0.000000000000000000, 0.000000000000000000, 1.000000000000000000 ) ) ;
#11148=ORIENTED_EDGE ( 'NONE', *, *, #39918, .T. ) ;
#11149=EDGE_CURVE ( 'NONE', #32652, #26461, #30112, .T. ) ;
#11154=AXIS2_PLACEMENT_3D ( 'NONE', #5375, #18738, #14576 ) ;
#11155=CARTESIAN_POINT ( 'NONE',  ( 17.99999999999999645, 0.000000000000000000, 0.000000000000000000 ) ) ;
#11156=ORIENTED_EDGE ( 'NONE', *, *, #1304, .T. ) ;
#11158=CARTESIAN_POINT ( 'NONE',  ( 17.99999999999999645, 0.000000000000000000, 0.000000000000000000 ) ) ;
#11160=DIRECTION ( 'NONE',  ( 0.000000000000000000, 0.000000000000000000, 1.000000000000000000 ) ) ;
#11163=DIRECTION ( 'NONE',  ( -1.000000000000000000, -0.000000000000000000, -0.000000000000000000 ) ) ;
#11164=VERTEX_POINT ( 'NONE', #5812 ) ;
#11168=ORIENTED_EDGE ( 'NONE', *, *, #25701, .F. ) ;
#11170=DIRECTION ( 'NONE',  ( 0.000000000000000000, -0.5076658003388292428, -0.8615540813938125098 ) ) ;
#11171=CARTESIAN_POINT ( 'NONE',  ( 0.000000000000000000, -47.31079789947556691, 105.9135893174949530 ) ) ;
#11172=EDGE_CURVE ( 'NONE', #38476, #22945, #9089, .T. ) ;
#11175=EDGE_CURVE ( 'NONE', #16471, #30860, #25252, .T. ) ;
#11182=DIRECTION ( 'NONE',  ( 1.000000000000000000, -0.000000000000000000, 0.000000000000000000 ) ) ;
#11189=VERTEX_POINT ( 'NONE', #313 ) ;
#11191=ORIENTED_EDGE ( 'NONE', *, *, #12794, .F. ) ;
#11196=FACE_OUTER_BOUND ( 'NONE', #17963, .T. ) ;
#11204=AXIS2_PLACEMENT_3D ( 'NONE', #7653, #37964, #24940 ) ;
#11208=ADVANCED_FACE ( 'NONE', ( #27196 ), #37420, .F. ) ;
#11210=DIRECTION ( 'NONE',  ( 0.000000000000000000, -0.3641605752528102591, -0.9313361774523430947 ) ) ;
#11211=ORIENTED_EDGE ( 'NONE', *, *, #32377, .F. ) ;
#11215=CIRCLE ( 'NONE', #38373, 59.00000000000000711 ) ;
#11216=VECTOR ( 'NONE', #5118, 1000.000000000000000 ) ;
#11217=DIRECTION ( 'NONE',  ( 0.000000000000000000, 0.000000000000000000, 1.000000000000000000 ) ) ;
#11218=DIRECTION ( 'NONE',  ( 0.000000000000000000, 0.000000000000000000, 1.000000000000000000 ) ) ;
#11220=CARTESIAN_POINT ( 'NONE',  ( 17.99999999999999645, 114.1529630473449686, 38.59523323561477781 ) ) ;
#11221=VERTEX_POINT ( 'NONE', #36773 ) ;
#11225=DIRECTION ( 'NONE',  ( 1.000000000000000000, 0.000000000000000000, 0.000000000000000000 ) ) ;
#11229=ORIENTED_EDGE ( 'NONE', *, *, #32748, .T. ) ;
#11230=ORIENTED_EDGE ( 'NONE', *, *, #33183, .T. ) ;
#11231=CARTESIAN_POINT ( 'NONE',  ( 0.000000000000000000, 0.000000000000000000, 116.0000000000000000 ) ) ;
#11239=ORIENTED_EDGE ( 'NONE', *, *, #32486, .T. ) ;
#11244=EDGE_CURVE ( 'NONE', #7856, #36681, #32214, .T. ) ;
#11248=ORIENTED_EDGE ( 'NONE', *, *, #31738, .F. ) ;
#11253=ORIENTED_EDGE ( 'NONE', *, *, #41403, .F. ) ;
#11255=ORIENTED_EDGE ( 'NONE', *, *, #22375, .T. ) ;
#11258=AXIS2_PLACEMENT_3D ( 'NONE', #9653, #12722, #22778 ) ;
#11259=DIRECTION ( 'NONE',  ( 0.000000000000000000, 0.000000000000000000, 1.000000000000000000 ) ) ;
#11264=FACE_OUTER_BOUND ( 'NONE', #24099, .T. ) ;
#11265=DIRECTION ( 'NONE',  ( 1.000000000000000000, -0.000000000000000000, -0.000000000000000000 ) ) ;
#11266=ORIENTED_EDGE ( 'NONE', *, *, #41839, .T. ) ;
#11268=EDGE_LOOP ( 'NONE', ( #9654, #38600, #3519, #12393 ) ) ;
#11271=DIRECTION ( 'NONE',  ( 0.000000000000000000, -0.9574220383620022368, -0.2886919473396314384 ) ) ;
#11272=VECTOR ( 'NONE', #29077, 1000.000000000000000 ) ;
#11274=DIRECTION ( 'NONE',  ( 0.000000000000000000, 0.000000000000000000, 1.000000000000000000 ) ) ;
#11279=AXIS2_PLACEMENT_3D ( 'NONE', #13859, #34316, #4412 ) ;
#11287=ORIENTED_EDGE ( 'NONE', *, *, #42457, .T. ) ;
#11288=DIRECTION ( 'NONE',  ( 1.000000000000000000, 0.000000000000000000, 0.000000000000000000 ) ) ;
#11291=EDGE_CURVE ( 'NONE', #32870, #40129, #28068, .T. ) ;
#11292=LINE ( 'NONE', #1660, #31056 ) ;
#11293=CARTESIAN_POINT ( 'NONE',  ( 17.99999999999999645, -29.86146780999875716, -112.0905559814581665 ) ) ;
#11296=DIRECTION ( 'NONE',  ( 0.000000000000000000, 0.000000000000000000, 1.000000000000000000 ) ) ;
#11298=DIRECTION ( 'NONE',  ( -1.000000000000000000, -0.000000000000000000, -0.000000000000000000 ) ) ;
#11302=VECTOR ( 'NONE', #35691, 1000.000000000000000 ) ;
#11303=ORIENTED_EDGE ( 'NONE', *, *, #35031, .T. ) ;
#11305=DIRECTION ( 'NONE',  ( 0.000000000000000000, 0.000000000000000000, 1.000000000000000000 ) ) ;
#11309=ORIENTED_EDGE ( 'NONE', *, *, #35579, .T. ) ;
#11310=CARTESIAN_POINT ( 'NONE',  ( 17.99999999999999645, -74.56001736500559218, -88.86396238369110279 ) ) ;
#11318=DIRECTION ( 'NONE',  ( 0.000000000000000000, 0.000000000000000000, 1.000000000000000000 ) ) ;
#11319=ORIENTED_EDGE ( 'NONE', *, *, #34572, .T. ) ;
#11324=CARTESIAN_POINT ( 'NONE',  ( 0.000000000000000000, -101.1249659627852679, -48.60055280209521555 ) ) ;
#11327=FACE_OUTER_BOUND ( 'NONE', #2998, .T. ) ;
#11328=CARTESIAN_POINT ( 'NONE',  ( 17.99999999999999645, -27.83061035786878890, -117.2431154827800270 ) ) ;
#11330=CARTESIAN_POINT ( 'NONE',  ( 17.99999999999999645, 72.00556975657821113, -86.04342158279314390 ) ) ;
#11331=CIRCLE ( 'NONE', #37088, 59.00000000000001421 ) ;
#11333=AXIS2_PLACEMENT_3D ( 'NONE', #16676, #42585, #35818 ) ;
#11334=ORIENTED_EDGE ( 'NONE', *, *, #15325, .F. ) ;
#11336=AXIS2_PLACEMENT_3D ( 'NONE', #27237, #40949, #17449 ) ;
#11338=EDGE_CURVE ( 'NONE', #30034, #41672, #4319, .T. ) ;
#11339=AXIS2_PLACEMENT_3D ( 'NONE', #37102, #20566, #26872 ) ;
#11342=EDGE_CURVE ( 'NONE', #32645, #1677, #23184, .T. ) ;
#11344=DIRECTION ( 'NONE',  ( 0.000000000000000000, 0.000000000000000000, 1.000000000000000000 ) ) ;
#11346=EDGE_CURVE ( 'NONE', #19737, #18, #12528, .T. ) ;
#11348=FACE_OUTER_BOUND ( 'NONE', #16599, .T. ) ;
#11355=VERTEX_POINT ( 'NONE', #2438 ) ;
#11357=ORIENTED_EDGE ( 'NONE', *, *, #25958, .T. ) ;
#11359=CYLINDRICAL_SURFACE ( 'NONE', #24728, 59.00000000000000000 ) ;
#11363=ORIENTED_EDGE ( 'NONE', *, *, #42791, .F. ) ;
#11364=ADVANCED_FACE ( 'NONE', ( #19946 ), #39947, .T. ) ;
#11366=VECTOR ( 'NONE', #6024, 1000.000000000000000 ) ;
#11368=DIRECTION ( 'NONE',  ( 0.000000000000000000, 0.000000000000000000, 1.000000000000000000 ) ) ;
#11373=ORIENTED_EDGE ( 'NONE', *, *, #22672, .F. ) ;
#11374=DIRECTION ( 'NONE',  ( 0.000000000000000000, 0.000000000000000000, 1.000000000000000000 ) ) ;
#11379=CYLINDRICAL_SURFACE ( 'NONE', #9988, 59.00000000000000000 ) ;
#11380=EDGE_CURVE ( 'NONE', #20659, #32376, #33604, .T. ) ;
#11383=DIRECTION ( 'NONE',  ( -1.000000000000000000, 0.000000000000000000, 0.000000000000000000 ) ) ;
#11384=DIRECTION ( 'NONE',  ( 1.000000000000000000, 0.000000000000000000, 0.000000000000000000 ) ) ;
#11385=CARTESIAN_POINT ( 'NONE',  ( 17.99999999999999645, 67.32409792376626001, -89.75376489259298296 ) ) ;
#11387=CARTESIAN_POINT ( 'NONE',  ( 17.99999999999999645, -73.78980555658542073, -95.26571049922065981 ) ) ;
#11392=DIRECTION ( 'NONE',  ( 0.000000000000000000, -0.5963673585384915432, -0.8027116379309710004 ) ) ;
#11396=DIRECTION ( 'NONE',  ( 0.000000000000000000, 0.000000000000000000, 1.000000000000000000 ) ) ;
#11398=ORIENTED_EDGE ( 'NONE', *, *, #41983, .T. ) ;
#11406=CARTESIAN_POINT ( 'NONE',  ( 17.99999999999999645, 110.3490479609632615, -20.28201389785435182 ) ) ;
#11411=VERTEX_POINT ( 'NONE', #3070 ) ;
#11413=EDGE_CURVE ( 'NONE', #22001, #719, #41948, .T. ) ;
#11415=CIRCLE ( 'NONE', #205, 59.00000000000000000 ) ;
#11418=EDGE_CURVE ( 'NONE', #9595, #21320, #29315, .T. ) ;
#11425=AXIS2_PLACEMENT_3D ( 'NONE', #6113, #16175, #22736 ) ;
#11429=DIRECTION ( 'NONE',  ( -1.000000000000000000, 0.000000000000000000, -0.000000000000000000 ) ) ;
#11431=LINE ( 'NONE', #11654, #36797 ) ;
#11437=DIRECTION ( 'NONE',  ( 0.000000000000000000, 0.000000000000000000, 1.000000000000000000 ) ) ;
#11439=CARTESIAN_POINT ( 'NONE',  ( 0.000000000000000000, 113.8630351447205697, 22.16324045874448601 ) ) ;
#11440=ORIENTED_EDGE ( 'NONE', *, *, #12212, .F. ) ;
#11441=AXIS2_PLACEMENT_3D ( 'NONE', #16459, #29762, #12330 ) ;
#11443=ORIENTED_EDGE ( 'NONE', *, *, #27127, .F. ) ;
#11446=CARTESIAN_POINT ( 'NONE',  ( 17.99999999999999645, 103.5682682299988500, -43.14958040911561454 ) ) ;
#11447=DIRECTION ( 'NONE',  ( 0.000000000000000000, 0.9911528310040076395, -0.1327255272837190025 ) ) ;
#11451=CARTESIAN_POINT ( 'NONE',  ( 8.999999999999998224, 108.8880088604276608, 39.99251838045997687 ) ) ;
#11456=CARTESIAN_POINT ( 'NONE',  ( 0.000000000000000000, 56.51398178981952469, -96.92493144647394843 ) ) ;
#11457=DIRECTION ( 'NONE',  ( -1.000000000000000000, 0.000000000000000000, 0.000000000000000000 ) ) ;
#11459=CARTESIAN_POINT ( 'NONE',  ( 0.000000000000000000, -97.89532456239460601, -54.81585448086294576 ) ) ;
#11460=ORIENTED_EDGE ( 'NONE', *, *, #3396, .T. ) ;
#11461=ORIENTED_EDGE ( 'NONE', *, *, #1299, .T. ) ;
#11462=CARTESIAN_POINT ( 'NONE',  ( 0.000000000000000000, 0.000000000000000000, 0.000000000000000000 ) ) ;
#11471=EDGE_CURVE ( 'NONE', #6492, #10188, #30608, .T. ) ;
#11472=EDGE_CURVE ( 'NONE', #24485, #25931, #12033, .T. ) ;
#11476=DIRECTION ( 'NONE',  ( 0.000000000000000000, 0.6783118362696172188, -0.7347741508630661889 ) ) ;
#11483=CIRCLE ( 'NONE', #19838, 59.00000000000000000 ) ;
#11485=ORIENTED_EDGE ( 'NONE', *, *, #12039, .T. ) ;
#11488=AXIS2_PLACEMENT_3D ( 'NONE', #27022, #33337, #13934 ) ;
#11489=DIRECTION ( 'NONE',  ( -1.000000000000000000, -0.000000000000000000, 0.000000000000000000 ) ) ;
#11494=EDGE_LOOP ( 'NONE', ( #37141, #23866, #37773, #31073 ) ) ;
#11496=CARTESIAN_POINT ( 'NONE',  ( 8.999999999999998224, -101.1403355683150096, 56.80345518653452785 ) ) ;
#11499=LINE ( 'NONE', #4719, #10878 ) ;
#11505=CARTESIAN_POINT ( 'NONE',  ( 8.999999999999998224, 86.84764344323065188, -76.89919913989662348 ) ) ;
#11506=ORIENTED_EDGE ( 'NONE', *, *, #30981, .T. ) ;
#11508=AXIS2_PLACEMENT_3D ( 'NONE', #26254, #9436, #39530 ) ;
#11510=AXIS2_PLACEMENT_3D ( 'NONE', #42425, #32619, #5996 ) ;
#11513=DIRECTION ( 'NONE',  ( 1.000000000000000000, -0.000000000000000000, -0.000000000000000000 ) ) ;
#11521=DIRECTION ( 'NONE',  ( -1.000000000000000000, -0.000000000000000000, -0.000000000000000000 ) ) ;
#11524=DIRECTION ( 'NONE',  ( 0.000000000000000000, 0.000000000000000000, 1.000000000000000000 ) ) ;
#11526=ORIENTED_EDGE ( 'NONE', *, *, #37170, .F. ) ;
#11527=DIRECTION ( 'NONE',  ( -1.000000000000000000, -0.000000000000000000, -0.000000000000000000 ) ) ;
#11528=VERTEX_POINT ( 'NONE', #10738 ) ;
#11535=DIRECTION ( 'NONE',  ( -1.000000000000000000, -0.000000000000000000, -0.000000000000000000 ) ) ;
#11536=AXIS2_PLACEMENT_3D ( 'NONE', #16093, #29392, #42662 ) ;
#11538=CARTESIAN_POINT ( 'NONE',  ( 0.000000000000000000, 0.000000000000000000, 0.000000000000000000 ) ) ;
#11539=ADVANCED_FACE ( 'NONE', ( #30387 ), #24075, .F. ) ;
#11540=ORIENTED_EDGE ( 'NONE', *, *, #14435, .T. ) ;
#11541=AXIS2_PLACEMENT_3D ( 'NONE', #13284, #26152, #29426 ) ;
#11543=DIRECTION ( 'NONE',  ( -1.000000000000000000, -0.000000000000000000, 0.000000000000000000 ) ) ;
#11544=EDGE_CURVE ( 'NONE', #27409, #30365, #37562, .T. ) ;
#11550=AXIS2_PLACEMENT_3D ( 'NONE', #36475, #6593, #33230 ) ;
#11557=CIRCLE ( 'NONE', #10124, 58.99999999999999289 ) ;
#11562=DIRECTION ( 'NONE',  ( -1.000000000000000000, 0.000000000000000000, -0.000000000000000000 ) ) ;
#11565=LINE ( 'NONE', #24908, #38577 ) ;
#11566=AXIS2_PLACEMENT_3D ( 'NONE', #1082, #14436, #31227 ) ;
#11572=VERTEX_POINT ( 'NONE', #33636 ) ;
#11573=AXIS2_PLACEMENT_3D ( 'NONE', #32872, #41120, #14332 ) ;
#11576=AXIS2_PLACEMENT_3D ( 'NONE', #32353, #42153, #16620 ) ;
#11581=CARTESIAN_POINT ( 'NONE',  ( 17.99999999999999645, 103.4151313792870610, 61.85306461934443689 ) ) ;
#11583=CARTESIAN_POINT ( 'NONE',  ( 0.000000000000000000, -115.5737863835461496, -9.934782381634859050 ) ) ;
#11585=ORIENTED_EDGE ( 'NONE', *, *, #31646, .F. ) ;
#11587=DIRECTION ( 'NONE',  ( -1.000000000000000000, -0.000000000000000000, 0.000000000000000000 ) ) ;
#11589=DIRECTION ( 'NONE',  ( 0.000000000000000000, 0.000000000000000000, 1.000000000000000000 ) ) ;
#11592=VECTOR ( 'NONE', #42693, 1000.000000000000000 ) ;
#11594=FACE_OUTER_BOUND ( 'NONE', #860, .T. ) ;
#11598=AXIS2_PLACEMENT_3D ( 'NONE', #379, #6503, #19863 ) ;
#11599=CIRCLE ( 'NONE', #40798, 59.00000000000001421 ) ;
#11603=VERTEX_POINT ( 'NONE', #10522 ) ;
#11604=AXIS2_PLACEMENT_3D ( 'NONE', #21925, #35177, #40222 ) ;
#11613=CIRCLE ( 'NONE', #4605, 120.5010000000000190 ) ;
#11618=DIRECTION ( 'NONE',  ( -1.000000000000000000, -0.000000000000000000, -0.000000000000000000 ) ) ;
#11620=EDGE_LOOP ( 'NONE', ( #37087, #5984, #5767, #12160 ) ) ;
#11622=ORIENTED_EDGE ( 'NONE', *, *, #17913, .T. ) ;
#11631=AXIS2_PLACEMENT_3D ( 'NONE', #38195, #21672, #14888 ) ;
#11632=EDGE_LOOP ( 'NONE', ( #37577, #23987, #23984, #8671 ) ) ;
#11634=AXIS2_PLACEMENT_3D ( 'NONE', #12147, #15439, #15635 ) ;
#11635=EDGE_CURVE ( 'NONE', #18706, #17459, #10601, .T. ) ;
#11639=ORIENTED_EDGE ( 'NONE', *, *, #4580, .F. ) ;
#11641=AXIS2_PLACEMENT_3D ( 'NONE', #11084, #14355, #14580 ) ;
#11646=VERTEX_POINT ( 'NONE', #27994 ) ;
#11648=CIRCLE ( 'NONE', #24915, 58.99999999999999289 ) ;
#11651=DIRECTION ( 'NONE',  ( 0.000000000000000000, 0.6382441836448211614, -0.7698339834299053885 ) ) ;
#11654=CARTESIAN_POINT ( 'NONE',  ( 17.99999999999999645, -53.40478689619801145, 108.0204598100363711 ) ) ;
#11658=DIRECTION ( 'NONE',  ( 0.000000000000000000, -0.1590634960190789038, 0.9872683547213435551 ) ) ;
#11660=DIRECTION ( 'NONE',  ( 0.000000000000000000, 0.9996456111234524045, 0.02662052143777834251 ) ) ;
#11662=ORIENTED_EDGE ( 'NONE', *, *, #9934, .T. ) ;
#11665=CIRCLE ( 'NONE', #5389, 120.5010000000000190 ) ;
#11667=ORIENTED_EDGE ( 'NONE', *, *, #22378, .T. ) ;
#11669=ADVANCED_FACE ( 'NONE', ( #28201 ), #35364, .F. ) ;
#11676=EDGE_CURVE ( 'NONE', #19109, #5383, #10635, .T. ) ;
#11677=ADVANCED_FACE ( 'NONE', ( #15542 ), #12051, .F. ) ;
#11679=AXIS2_PLACEMENT_3D ( 'NONE', #42993, #13148, #42764 ) ;
#11681=DIRECTION ( 'NONE',  ( 0.000000000000000000, -0.9407002666710297945, -0.3392388661180402165 ) ) ;
#11682=EDGE_LOOP ( 'NONE', ( #35735, #2533, #41529, #15918 ) ) ;
#11685=VECTOR ( 'NONE', #24993, 1000.000000000000000 ) ;
#11687=CARTESIAN_POINT ( 'NONE',  ( 0.000000000000000000, 107.2885202478266251, 54.86040852957352598 ) ) ;
#11690=CARTESIAN_POINT ( 'NONE',  ( 0.000000000000000000, -78.18175027177375114, -85.69488855493077040 ) ) ;
#11692=ORIENTED_EDGE ( 'NONE', *, *, #10667, .T. ) ;
#11694=ORIENTED_EDGE ( 'NONE', *, *, #13591, .F. ) ;
#11697=CYLINDRICAL_SURFACE ( 'NONE', #5618, 120.5010000000000190 ) ;
#11700=AXIS2_PLACEMENT_3D ( 'NONE', #14647, #41868, #12016 ) ;
#11704=ORIENTED_EDGE ( 'NONE', *, *, #6318, .F. ) ;
#11705=CARTESIAN_POINT ( 'NONE',  ( 17.99999999999999645, 73.78980555658732499, -95.26571049921918188 ) ) ;
#11708=CIRCLE ( 'NONE', #507, 59.00000000000000711 ) ;
#11712=DIRECTION ( 'NONE',  ( -1.000000000000000000, 0.000000000000000000, -0.000000000000000000 ) ) ;
#11714=ORIENTED_EDGE ( 'NONE', *, *, #38569, .F. ) ;
#11716=EDGE_LOOP ( 'NONE', ( #39707, #1165, #23073, #20775 ) ) ;
#11728=DIRECTION ( 'NONE',  ( -1.000000000000000000, 0.000000000000000000, -0.000000000000000000 ) ) ;
#11734=DIRECTION ( 'NONE',  ( 0.000000000000000000, -0.7164567402983066380, -0.6976315211349934930 ) ) ;
#11735=CIRCLE ( 'NONE', #20096, 120.5010000000000190 ) ;
#11748=DIRECTION ( 'NONE',  ( 0.000000000000000000, 0.9574220383620042352, 0.2886919473396248881 ) ) ;
#11751=DIRECTION ( 'NONE',  ( 0.000000000000000000, 0.000000000000000000, 1.000000000000000000 ) ) ;
#11752=EDGE_LOOP ( 'NONE', ( #19586, #28428, #18441, #664 ) ) ;
#11753=EDGE_CURVE ( 'NONE', #2648, #36025, #12627, .T. ) ;
#11757=LINE ( 'NONE', #25087, #4198 ) ;
#11764=CARTESIAN_POINT ( 'NONE',  ( 0.000000000000000000, 35.72777019205808813, -106.3569410558013715 ) ) ;
#11766=VECTOR ( 'NONE', #9571, 1000.000000000000000 ) ;
#11768=EDGE_CURVE ( 'NONE', #30521, #39546, #20414, .T. ) ;
#11769=CARTESIAN_POINT ( 'NONE',  ( 17.99999999999999645, 111.9370513079669394, 44.61600100275212100 ) ) ;
#11770=ORIENTED_EDGE ( 'NONE', *, *, #39650, .F. ) ;
#11772=CARTESIAN_POINT ( 'NONE',  ( 0.000000000000000000, -16.77566611177856615, 119.3275660838941832 ) ) ;
#11776=CARTESIAN_POINT ( 'NONE',  ( 17.99999999999999645, -92.25992191227442163, 77.51514567967366531 ) ) ;
#11777=CARTESIAN_POINT ( 'NONE',  ( 0.000000000000000000, 53.40478689619728669, 108.0204598100367548 ) ) ;
#11780=DIRECTION ( 'NONE',  ( 1.000000000000000000, 0.000000000000000000, 0.000000000000000000 ) ) ;
#11781=DIRECTION ( 'NONE',  ( -1.000000000000000000, -0.000000000000000000, -0.000000000000000000 ) ) ;
#11787=ORIENTED_EDGE ( 'NONE', *, *, #34261, .T. ) ;
#11789=CARTESIAN_POINT ( 'NONE',  ( 9.000000000000001776, -0.6819280456836842585, 115.9979955608738607 ) ) ;
#11790=DIRECTION ( 'NONE',  ( 1.000000000000000000, 0.000000000000000000, 0.000000000000000000 ) ) ;
#11793=DIRECTION ( 'NONE',  ( -1.000000000000000000, -0.000000000000000000, -0.000000000000000000 ) ) ;
#11794=VERTEX_POINT ( 'NONE', #5630 ) ;
#11795=DIRECTION ( 'NONE',  ( 1.000000000000000000, 0.000000000000000000, 0.000000000000000000 ) ) ;
#11799=ORIENTED_EDGE ( 'NONE', *, *, #15106, .T. ) ;
#11802=ORIENTED_EDGE ( 'NONE', *, *, #22373, .T. ) ;
#11805=DIRECTION ( 'NONE',  ( 0.000000000000000000, 0.000000000000000000, 1.000000000000000000 ) ) ;
#11808=ORIENTED_EDGE ( 'NONE', *, *, #3636, .T. ) ;
#11809=ORIENTED_EDGE ( 'NONE', *, *, #1790, .T. ) ;
#11810=FACE_OUTER_BOUND ( 'NONE', #12945, .T. ) ;
#11811=ORIENTED_EDGE ( 'NONE', *, *, #37501, .F. ) ;
#11813=LINE ( 'NONE', #5455, #40153 ) ;
#11814=CYLINDRICAL_SURFACE ( 'NONE', #13561, 116.0000000000000000 ) ;
#11815=FACE_OUTER_BOUND ( 'NONE', #13401, .T. ) ;
#11816=ORIENTED_EDGE ( 'NONE', *, *, #8906, .F. ) ;
#11818=ADVANCED_FACE ( 'NONE', ( #10187 ), #23750, .F. ) ;
#11819=FACE_OUTER_BOUND ( 'NONE', #20495, .T. ) ;
#11822=AXIS2_PLACEMENT_3D ( 'NONE', #2929, #33056, #3147 ) ;
#11826=CARTESIAN_POINT ( 'NONE',  ( 17.99999999999999645, 0.000000000000000000, 0.000000000000000000 ) ) ;
#11828=ORIENTED_EDGE ( 'NONE', *, *, #15925, .F. ) ;
#11834=AXIS2_PLACEMENT_3D ( 'NONE', #40973, #4536, #7388 ) ;
#11835=LINE ( 'NONE', #25161, #15171 ) ;
#11836=CARTESIAN_POINT ( 'NONE',  ( 17.99999999999999645, 98.69720329641039314, -60.94966826379810243 ) ) ;
#11837=DIRECTION ( 'NONE',  ( 0.000000000000000000, 0.000000000000000000, -1.000000000000000000 ) ) ;
#11839=ADVANCED_FACE ( 'NONE', ( #36575 ), #30068, .F. ) ;
#11840=ORIENTED_EDGE ( 'NONE', *, *, #25464, .F. ) ;
#11844=VECTOR ( 'NONE', #9530, 1000.000000000000000 ) ;
#11846=ORIENTED_EDGE ( 'NONE', *, *, #34446, .T. ) ;
#11849=DIRECTION ( 'NONE',  ( -1.000000000000000000, 0.000000000000000000, 0.000000000000000000 ) ) ;
#11850=CARTESIAN_POINT ( 'NONE',  ( 17.99999999999999645, -84.77518783075143460, 73.49448960231327987 ) ) ;
#11853=DIRECTION ( 'NONE',  ( -1.000000000000000000, -0.000000000000000000, -0.000000000000000000 ) ) ;
#11854=EDGE_LOOP ( 'NONE', ( #18635, #37168, #20247, #25269 ) ) ;
#11855=CIRCLE ( 'NONE', #25777, 116.0000000000000000 ) ;
#11859=ORIENTED_EDGE ( 'NONE', *, *, #5517, .T. ) ;
#11861=DIRECTION ( 'NONE',  ( 1.000000000000000000, 0.000000000000000000, 0.000000000000000000 ) ) ;
#11862=ORIENTED_EDGE ( 'NONE', *, *, #10317, .F. ) ;
#11865=EDGE_CURVE ( 'NONE', #12185, #15011, #12553, .T. ) ;
#11867=EDGE_CURVE ( 'NONE', #35377, #5501, #26494, .T. ) ;
#11868=CARTESIAN_POINT ( 'NONE',  ( 17.99999999999999645, -2.418575551221673336, 120.4767259403368911 ) ) ;
#11872=EDGE_LOOP ( 'NONE', ( #6710, #26684, #9258, #13730 ) ) ;
#11877=DIRECTION ( 'NONE',  ( 1.000000000000000000, 0.000000000000000000, -0.000000000000000000 ) ) ;
#11885=DIRECTION ( 'NONE',  ( 0.000000000000000000, 0.000000000000000000, 1.000000000000000000 ) ) ;
#11887=DIRECTION ( 'NONE',  ( 0.000000000000000000, 0.000000000000000000, 1.000000000000000000 ) ) ;
#11889=EDGE_CURVE ( 'NONE', #21485, #27034, #4162, .T. ) ;
#11890=CARTESIAN_POINT ( 'NONE',  ( 0.000000000000000000, -101.8011932243951634, 55.61040422519296555 ) ) ;
#11891=ORIENTED_EDGE ( 'NONE', *, *, #3941, .F. ) ;
#11895=LINE ( 'NONE', #28264, #23513 ) ;
#11896=CIRCLE ( 'NONE', #7690, 130.0000000000000000 ) ;
#11898=CARTESIAN_POINT ( 'NONE',  ( 17.99999999999999645, 84.09610293794170843, -74.27057253242929846 ) ) ;
#11900=ORIENTED_EDGE ( 'NONE', *, *, #28593, .T. ) ;
#11902=CARTESIAN_POINT ( 'NONE',  ( 17.99999999999999645, -117.9424311864587480, -24.69967462999156638 ) ) ;
#11906=ORIENTED_EDGE ( 'NONE', *, *, #2285, .T. ) ;
#11907=CARTESIAN_POINT ( 'NONE',  ( 0.000000000000000000, -108.8684555192048435, 27.12806418649580564 ) ) ;
#11909=AXIS2_PLACEMENT_3D ( 'NONE', #38279, #38484, #14760 ) ;
#11911=AXIS2_PLACEMENT_3D ( 'NONE', #4133, #34466, #21651 ) ;
#11912=ORIENTED_EDGE ( 'NONE', *, *, #35671, .T. ) ;
#11920=EDGE_CURVE ( 'NONE', #23147, #33779, #8362, .T. ) ;
#11922=EDGE_CURVE ( 'NONE', #17636, #16359, #7566, .T. ) ;
#11924=CIRCLE ( 'NONE', #41846, 58.99999999999999289 ) ;
#11925=DIRECTION ( 'NONE',  ( 0.000000000000000000, -0.2631025642275284238, 0.9647678688145140402 ) ) ;
#11928=ORIENTED_EDGE ( 'NONE', *, *, #27934, .F. ) ;
#11929=CARTESIAN_POINT ( 'NONE',  ( 0.000000000000000000, 0.000000000000000000, 0.000000000000000000 ) ) ;
#11934=VERTEX_POINT ( 'NONE', #23316 ) ;
#11935=CIRCLE ( 'NONE', #27970, 59.00000000000000000 ) ;
#11940=CARTESIAN_POINT ( 'NONE',  ( 8.999999999999998224, 90.81729652456166946, 72.16798910853647442 ) ) ;
#11943=VECTOR ( 'NONE', #2974, 1000.000000000000000 ) ;
#11946=ORIENTED_EDGE ( 'NONE', *, *, #26763, .F. ) ;
#11948=EDGE_LOOP ( 'NONE', ( #40754, #4587, #4342, #15142 ) ) ;
#11949=CIRCLE ( 'NONE', #3542, 59.00000000000000711 ) ;
#11951=CARTESIAN_POINT ( 'NONE',  ( 17.99999999999999645, 0.000000000000000000, 0.000000000000000000 ) ) ;
#11952=ADVANCED_FACE ( 'NONE', ( #343 ), #13706, .F. ) ;
#11955=CARTESIAN_POINT ( 'NONE',  ( 17.99999999999999645, 0.000000000000000000, 0.000000000000000000 ) ) ;
#11957=CARTESIAN_POINT ( 'NONE',  ( 17.99999999999999645, 80.02407177072956301, 78.64108602299977235 ) ) ;
#11963=CIRCLE ( 'NONE', #9808, 130.0000000000000000 ) ;
#11964=CARTESIAN_POINT ( 'NONE',  ( 17.99999999999999645, -18.35539002514457252, 110.6858262410709273 ) ) ;
#11965=DIRECTION ( 'NONE',  ( 1.000000000000000000, 0.000000000000000000, 0.000000000000000000 ) ) ;
#11966=EDGE_LOOP ( 'NONE', ( #22564, #4437, #36860, #11357 ) ) ;
#11970=CARTESIAN_POINT ( 'NONE',  ( -10.00000000000000000, 0.000000000000000000, 0.000000000000000000 ) ) ;
#11972=DIRECTION ( 'NONE',  ( 1.000000000000000000, 0.000000000000000000, 0.000000000000000000 ) ) ;
#11973=AXIS2_PLACEMENT_3D ( 'NONE', #25811, #2628, #26007 ) ;
#11974=EDGE_CURVE ( 'NONE', #36528, #15552, #34833, .T. ) ;
#11976=CARTESIAN_POINT ( 'NONE',  ( 17.99999999999999645, 0.000000000000000000, 0.000000000000000000 ) ) ;
#11977=EDGE_CURVE ( 'NONE', #35437, #6343, #16046, .T. ) ;
#11982=DIRECTION ( 'NONE',  ( 0.000000000000000000, 0.000000000000000000, 1.000000000000000000 ) ) ;
#11987=CARTESIAN_POINT ( 'NONE',  ( 0.000000000000000000, -119.8996782608629275, -12.02323392193478746 ) ) ;
#11991=EDGE_CURVE ( 'NONE', #23414, #9794, #17466, .T. ) ;
#12001=LINE ( 'NONE', #11789, #12444 ) ;
#12002=FACE_OUTER_BOUND ( 'NONE', #35703, .T. ) ;
#12004=CARTESIAN_POINT ( 'NONE',  ( 0.000000000000000000, 0.000000000000000000, 0.000000000000000000 ) ) ;
#12006=FACE_OUTER_BOUND ( 'NONE', #7257, .T. ) ;
#12009=ORIENTED_EDGE ( 'NONE', *, *, #30013, .T. ) ;
#12016=DIRECTION ( 'NONE',  ( 0.000000000000000000, 0.5076658003388352380, 0.8615540813938089570 ) ) ;
#12018=ORIENTED_EDGE ( 'NONE', *, *, #30914, .F. ) ;
#12019=DIRECTION ( 'NONE',  ( 0.000000000000000000, 0.000000000000000000, 1.000000000000000000 ) ) ;
#12021=DIRECTION ( 'NONE',  ( -1.000000000000000000, 0.000000000000000000, -0.000000000000000000 ) ) ;
#12022=DIRECTION ( 'NONE',  ( -1.000000000000000000, -0.000000000000000000, 0.000000000000000000 ) ) ;
#12024=ADVANCED_FACE ( 'NONE', ( #8633 ), #31352, .F. ) ;
#12027=ORIENTED_EDGE ( 'NONE', *, *, #72, .T. ) ;
#12030=EDGE_CURVE ( 'NONE', #27228, #41800, #41582, .T. ) ;
#12031=AXIS2_PLACEMENT_3D ( 'NONE', #10662, #24003, #39878 ) ;
#12033=CIRCLE ( 'NONE', #15521, 58.99999999999999289 ) ;
#12039=EDGE_CURVE ( 'NONE', #19203, #31163, #38315, .T. ) ;
#12041=DIRECTION ( 'NONE',  ( -1.000000000000000000, 0.000000000000000000, -0.000000000000000000 ) ) ;
#12043=AXIS2_PLACEMENT_3D ( 'NONE', #29249, #15732, #38825 ) ;
#12046=EDGE_CURVE ( 'NONE', #4304, #22351, #30673, .T. ) ;
#12050=CARTESIAN_POINT ( 'NONE',  ( 8.999999999999998224, -91.65951123222436081, -71.09524597798180423 ) ) ;
#12051=CYLINDRICAL_SURFACE ( 'NONE', #16221, 58.99999999999998579 ) ;
#12053=EDGE_LOOP ( 'NONE', ( #21162, #9432, #7377, #16241 ) ) ;
#12055=ORIENTED_EDGE ( 'NONE', *, *, #33121, .F. ) ;
#12061=ORIENTED_EDGE ( 'NONE', *, *, #8861, .T. ) ;
#12064=AXIS2_PLACEMENT_3D ( 'NONE', #27470, #1273, #18340 ) ;
#12066=DIRECTION ( 'NONE',  ( 0.000000000000000000, 0.000000000000000000, -1.000000000000000000 ) ) ;
#12070=EDGE_CURVE ( 'NONE', #2989, #8080, #35509, .T. ) ;
#12076=CARTESIAN_POINT ( 'NONE',  ( 0.000000000000000000, -110.0562500189195561, -49.07252625220222342 ) ) ;
#12080=EDGE_CURVE ( 'NONE', #22453, #18907, #7667, .T. ) ;
#12081=FACE_OUTER_BOUND ( 'NONE', #123, .T. ) ;
#12082=DIRECTION ( 'NONE',  ( 0.000000000000000000, -0.8993121301712230231, 0.4373073204588476259 ) ) ;
#12084=EDGE_CURVE ( 'NONE', #37344, #19147, #29992, .T. ) ;
#12085=ORIENTED_EDGE ( 'NONE', *, *, #1358, .T. ) ;
#12086=DIRECTION ( 'NONE',  ( 1.000000000000000000, 0.000000000000000000, 0.000000000000000000 ) ) ;
#12089=DIRECTION ( 'NONE',  ( -1.000000000000000000, -0.000000000000000000, -0.000000000000000000 ) ) ;
#12090=VERTEX_POINT ( 'NONE', #15638 ) ;
#12095=VERTEX_POINT ( 'NONE', #32410 ) ;
#12101=FACE_OUTER_BOUND ( 'NONE', #29841, .T. ) ;
#12102=ORIENTED_EDGE ( 'NONE', *, *, #5997, .F. ) ;
#12105=FACE_OUTER_BOUND ( 'NONE', #3999, .T. ) ;
#12110=AXIS2_PLACEMENT_3D ( 'NONE', #12355, #5358, #35860 ) ;
#12112=ORIENTED_EDGE ( 'NONE', *, *, #14841, .T. ) ;
#12115=CIRCLE ( 'NONE', #36449, 58.99999999999999289 ) ;
#12116=ORIENTED_EDGE ( 'NONE', *, *, #35010, .F. ) ;
#12118=VERTEX_POINT ( 'NONE', #39586 ) ;
#12120=ORIENTED_EDGE ( 'NONE', *, *, #29246, .T. ) ;
#12123=ADVANCED_FACE ( 'NONE', ( #2706 ), #19778, .F. ) ;
#12124=CARTESIAN_POINT ( 'NONE',  ( -10.00000000000000000, 0.000000000000000000, 0.000000000000000000 ) ) ;
#12128=DIRECTION ( 'NONE',  ( 1.000000000000000000, 0.000000000000000000, 0.000000000000000000 ) ) ;
#12130=DIRECTION ( 'NONE',  ( 0.000000000000000000, 0.000000000000000000, 1.000000000000000000 ) ) ;
#12131=AXIS2_PLACEMENT_3D ( 'NONE', #20388, #17346, #30184 ) ;
#12133=EDGE_CURVE ( 'NONE', #17236, #22453, #2496, .T. ) ;
#12135=CARTESIAN_POINT ( 'NONE',  ( 17.99999999999999645, 108.8684555192046872, 27.12806418649654105 ) ) ;
#12141=ORIENTED_EDGE ( 'NONE', *, *, #6550, .T. ) ;
#12142=CIRCLE ( 'NONE', #17731, 58.99999999999999289 ) ;
#12144=CARTESIAN_POINT ( 'NONE',  ( -10.00000000000000000, 0.000000000000000000, 0.000000000000000000 ) ) ;
#12147=CARTESIAN_POINT ( 'NONE',  ( 17.99999999999999645, 0.000000000000000000, 0.000000000000000000 ) ) ;
#12152=ORIENTED_EDGE ( 'NONE', *, *, #18759, .T. ) ;
#12153=CARTESIAN_POINT ( 'NONE',  ( 17.99999999999999645, 104.2166695095720854, -60.49278301857700768 ) ) ;
#12155=AXIS2_PLACEMENT_3D ( 'NONE', #17668, #40950, #23559 ) ;
#12160=ORIENTED_EDGE ( 'NONE', *, *, #28656, .F. ) ;
#12161=CARTESIAN_POINT ( 'NONE',  ( 17.99999999999999645, 0.000000000000000000, 0.000000000000000000 ) ) ;
#12164=AXIS2_PLACEMENT_3D ( 'NONE', #39866, #9993, #26170 ) ;
#12168=AXIS2_PLACEMENT_3D ( 'NONE', #10362, #29807, #30441 ) ;
#12169=ORIENTED_EDGE ( 'NONE', *, *, #17366, .F. ) ;
#12171=CARTESIAN_POINT ( 'NONE',  ( 17.99999999999999645, 23.10276247328101817, 118.2656051737070726 ) ) ;
#12172=VECTOR ( 'NONE', #6260, 1000.000000000000000 ) ;
#12173=EDGE_CURVE ( 'NONE', #27156, #8183, #35670, .T. ) ;
#12175=LINE ( 'NONE', #35274, #20645 ) ;
#12176=AXIS2_PLACEMENT_3D ( 'NONE', #28325, #21148, #11748 ) ;
#12181=CARTESIAN_POINT ( 'NONE',  ( 0.000000000000000000, 115.6826031496113529, -8.575274253896266075 ) ) ;
#12182=DIRECTION ( 'NONE',  ( -1.000000000000000000, 0.000000000000000000, 0.000000000000000000 ) ) ;
#12184=ORIENTED_EDGE ( 'NONE', *, *, #34556, .T. ) ;
#12185=VERTEX_POINT ( 'NONE', #7366 ) ;
#12188=EDGE_CURVE ( 'NONE', #31468, #12550, #31643, .T. ) ;
#12191=EDGE_CURVE ( 'NONE', #17669, #16188, #20526, .T. ) ;
#12194=DIRECTION ( 'NONE',  ( -1.000000000000000000, 0.000000000000000000, -0.000000000000000000 ) ) ;
#12195=ORIENTED_EDGE ( 'NONE', *, *, #34762, .T. ) ;
#12196=AXIS2_PLACEMENT_3D ( 'NONE', #24870, #35487, #21814 ) ;
#12199=AXIS2_PLACEMENT_3D ( 'NONE', #37607, #1388, #21529 ) ;
#12200=EDGE_CURVE ( 'NONE', #41108, #11023, #4462, .T. ) ;
#12205=VERTEX_POINT ( 'NONE', #12370 ) ;
#12210=ADVANCED_FACE ( 'NONE', ( #36744 ), #9917, .F. ) ;
#12211=ADVANCED_FACE ( 'NONE', ( #13651 ), #36518, .F. ) ;
#12212=EDGE_CURVE ( 'NONE', #7685, #9595, #12839, .T. ) ;
#12214=EDGE_LOOP ( 'NONE', ( #21836, #40479, #18051, #31736 ) ) ;
#12215=DIRECTION ( 'NONE',  ( 1.000000000000000000, 0.000000000000000000, 0.000000000000000000 ) ) ;
#12220=DIRECTION ( 'NONE',  ( -1.000000000000000000, 0.000000000000000000, -0.000000000000000000 ) ) ;
#12221=EDGE_LOOP ( 'NONE', ( #30276, #7093, #38213, #1598 ) ) ;
#12225=ORIENTED_EDGE ( 'NONE', *, *, #18087, .F. ) ;
#12228=DIRECTION ( 'NONE',  ( -1.000000000000000000, 0.000000000000000000, 0.000000000000000000 ) ) ;
#12230=VECTOR ( 'NONE', #22033, 1000.000000000000000 ) ;
#12232=CYLINDRICAL_SURFACE ( 'NONE', #21380, 120.5010000000000190 ) ;
#12234=CARTESIAN_POINT ( 'NONE',  ( 17.99999999999999645, 35.54274411428057334, 115.1399337407607959 ) ) ;
#12235=AXIS2_PLACEMENT_3D ( 'NONE', #17110, #9449, #3312 ) ;
#12236=EDGE_LOOP ( 'NONE', ( #31647, #41593, #26274, #42067 ) ) ;
#12240=CARTESIAN_POINT ( 'NONE',  ( 0.000000000000000000, -64.69195966009955612, 96.28577441832231898 ) ) ;
#12241=CARTESIAN_POINT ( 'NONE',  ( 0.000000000000000000, 0.5156212287279957618, 112.1962860721878172 ) ) ;
#12243=DIRECTION ( 'NONE',  ( -1.000000000000000000, 0.000000000000000000, -0.000000000000000000 ) ) ;
#12245=ORIENTED_EDGE ( 'NONE', *, *, #12993, .T. ) ;
#12252=AXIS2_PLACEMENT_3D ( 'NONE', #24951, #6265, #32880 ) ;
#12254=VECTOR ( 'NONE', #27644, 1000.000000000000000 ) ;
#12255=DIRECTION ( 'NONE',  ( 0.000000000000000000, 0.9968120070307497915, 0.07978610555308651708 ) ) ;
#12258=EDGE_CURVE ( 'NONE', #12380, #25306, #30278, .T. ) ;
#12259=DIRECTION ( 'NONE',  ( 0.000000000000000000, 0.000000000000000000, -1.000000000000000000 ) ) ;
#12262=CIRCLE ( 'NONE', #24141, 120.5010000000000332 ) ;
#12266=DIRECTION ( 'NONE',  ( -1.000000000000000000, 0.000000000000000000, 0.000000000000000000 ) ) ;
#12267=DIRECTION ( 'NONE',  ( -1.000000000000000000, -0.000000000000000000, -0.000000000000000000 ) ) ;
#12269=DIRECTION ( 'NONE',  ( 1.000000000000000000, 0.000000000000000000, 0.000000000000000000 ) ) ;
#12276=ADVANCED_FACE ( 'NONE', ( #33275 ), #10796, .F. ) ;
#12280=AXIS2_PLACEMENT_3D ( 'NONE', #29350, #9897, #22828 ) ;
#12283=ORIENTED_EDGE ( 'NONE', *, *, #23161, .T. ) ;
#12284=AXIS2_PLACEMENT_3D ( 'NONE', #6858, #20216, #2490 ) ;
#12288=AXIS2_PLACEMENT_3D ( 'NONE', #10836, #17843, #27866 ) ;
#12289=CARTESIAN_POINT ( 'NONE',  ( 17.99999999999999645, -111.1352304691228596, 15.40237066878559524 ) ) ;
#12291=AXIS2_PLACEMENT_3D ( 'NONE', #20975, #13974, #27272 ) ;
#12293=CARTESIAN_POINT ( 'NONE',  ( 0.000000000000000000, 0.000000000000000000, 0.000000000000000000 ) ) ;
#12294=EDGE_CURVE ( 'NONE', #20361, #21959, #30221, .T. ) ;
#12299=ORIENTED_EDGE ( 'NONE', *, *, #15891, .T. ) ;
#12300=CYLINDRICAL_SURFACE ( 'NONE', #16414, 59.00000000000000000 ) ;
#12301=LINE ( 'NONE', #39513, #21036 ) ;
#12302=ORIENTED_EDGE ( 'NONE', *, *, #3748, .T. ) ;
#12310=CARTESIAN_POINT ( 'NONE',  ( 17.99999999999999645, -45.89132998248120288, 102.3829004574628385 ) ) ;
#12314=AXIS2_PLACEMENT_3D ( 'NONE', #12817, #42463, #29840 ) ;
#12315=AXIS2_PLACEMENT_3D ( 'NONE', #15857, #22415, #5579 ) ;
#12319=VERTEX_POINT ( 'NONE', #20874 ) ;
#12320=FACE_OUTER_BOUND ( 'NONE', #14060, .T. ) ;
#12323=AXIS2_PLACEMENT_3D ( 'NONE', #2082, #28539, #8639 ) ;
#12330=DIRECTION ( 'NONE',  ( 0.000000000000000000, 0.000000000000000000, 1.000000000000000000 ) ) ;
#12332=AXIS2_PLACEMENT_3D ( 'NONE', #40081, #6500, #6295 ) ;
#12334=CARTESIAN_POINT ( 'NONE',  ( 17.99999999999999645, 0.000000000000000000, 0.000000000000000000 ) ) ;
#12338=DIRECTION ( 'NONE',  ( 0.000000000000000000, 0.8747630845319591675, 0.4845508703326539823 ) ) ;
#12339=CIRCLE ( 'NONE', #5344, 59.00000000000000000 ) ;
#12342=EDGE_LOOP ( 'NONE', ( #16646, #5728, #33541, #41158 ) ) ;
#12346=DIRECTION ( 'NONE',  ( 0.000000000000000000, 0.000000000000000000, 1.000000000000000000 ) ) ;
#12350=CIRCLE ( 'NONE', #21448, 116.0000000000000000 ) ;
#12351=ORIENTED_EDGE ( 'NONE', *, *, #23032, .T. ) ;
#12353=EDGE_CURVE ( 'NONE', #10174, #41147, #42752, .T. ) ;
#12355=CARTESIAN_POINT ( 'NONE',  ( 0.000000000000000000, 0.000000000000000000, 0.000000000000000000 ) ) ;
#12356=FACE_OUTER_BOUND ( 'NONE', #31592, .T. ) ;
#12367=DIRECTION ( 'NONE',  ( -1.000000000000000000, -0.000000000000000000, -0.000000000000000000 ) ) ;
#12370=CARTESIAN_POINT ( 'NONE',  ( 17.99999999999999645, 90.81729652456166946, 72.16798910853647442 ) ) ;
#12371=ADVANCED_FACE ( 'NONE', ( #13875 ), #27171, .F. ) ;
#12373=CARTESIAN_POINT ( 'NONE',  ( 17.99999999999999645, 35.54274411428215075, -115.1399337407602701 ) ) ;
#12374=VERTEX_POINT ( 'NONE', #727 ) ;
#12380=VERTEX_POINT ( 'NONE', #14092 ) ;
#12382=AXIS2_PLACEMENT_3D ( 'NONE', #38841, #5261, #25366 ) ;
#12383=CARTESIAN_POINT ( 'NONE',  ( 0.000000000000000000, 104.6166166098445416, 50.11350645393712000 ) ) ;
#12384=EDGE_CURVE ( 'NONE', #18335, #20343, #17034, .T. ) ;
#12385=AXIS2_PLACEMENT_3D ( 'NONE', #21490, #4849, #18209 ) ;
#12386=CARTESIAN_POINT ( 'NONE',  ( 0.000000000000000000, -69.90696807222551001, 98.15042952503490881 ) ) ;
#12388=CIRCLE ( 'NONE', #29103, 59.00000000000000000 ) ;
#12389=ORIENTED_EDGE ( 'NONE', *, *, #21394, .F. ) ;
#12392=CARTESIAN_POINT ( 'NONE',  ( 17.99999999999999645, 100.8494052988179561, -65.95368414178808791 ) ) ;
#12393=ORIENTED_EDGE ( 'NONE', *, *, #24195, .T. ) ;
#12394=ORIENTED_EDGE ( 'NONE', *, *, #22375, .F. ) ;
#12395=CARTESIAN_POINT ( 'NONE',  ( 17.99999999999999645, 47.58001226230536673, 110.7096808509485300 ) ) ;
#12399=AXIS2_PLACEMENT_3D ( 'NONE', #12815, #32865, #36131 ) ;
#12400=CARTESIAN_POINT ( 'NONE',  ( 17.99999999999999645, -111.2721026680459602, -14.38025178762732104 ) ) ;
#12401=CYLINDRICAL_SURFACE ( 'NONE', #19301, 59.00000000000000000 ) ;
#12404=ORIENTED_EDGE ( 'NONE', *, *, #8187, .F. ) ;
#12406=CARTESIAN_POINT ( 'NONE',  ( 17.99999999999999645, -120.2856157092986393, -7.201503623198056481 ) ) ;
#12409=ADVANCED_FACE ( 'NONE', ( #24568 ), #4887, .F. ) ;
#12411=ORIENTED_EDGE ( 'NONE', *, *, #12212, .T. ) ;
#12413=ORIENTED_EDGE ( 'NONE', *, *, #21243, .T. ) ;
#12414=CIRCLE ( 'NONE', #42328, 116.0000000000000000 ) ;
#12415=AXIS2_PLACEMENT_3D ( 'NONE', #7562, #33963, #30491 ) ;
#12420=EDGE_LOOP ( 'NONE', ( #7787, #3892, #42558, #7054 ) ) ;
#12421=CIRCLE ( 'NONE', #5456, 116.0000000000000000 ) ;
#12425=EDGE_CURVE ( 'NONE', #20914, #27767, #18249, .T. ) ;
#12428=CARTESIAN_POINT ( 'NONE',  ( 0.000000000000000000, 0.000000000000000000, 0.000000000000000000 ) ) ;
#12430=LINE ( 'NONE', #6276, #39425 ) ;
#12432=DIRECTION ( 'NONE',  ( -1.000000000000000000, 0.000000000000000000, 0.000000000000000000 ) ) ;
#12435=ORIENTED_EDGE ( 'NONE', *, *, #10616, .F. ) ;
#12440=AXIS2_PLACEMENT_3D ( 'NONE', #21045, #24315, #5056 ) ;
#12444=VECTOR ( 'NONE', #34882, 1000.000000000000000 ) ;
#12446=ORIENTED_EDGE ( 'NONE', *, *, #10257, .F. ) ;
#12448=VERTEX_POINT ( 'NONE', #8375 ) ;
#12449=CIRCLE ( 'NONE', #26392, 116.0000000000000000 ) ;
#12450=CARTESIAN_POINT ( 'NONE',  ( 0.000000000000000000, 113.8630351447208824, -22.16324045874292636 ) ) ;
#12452=CIRCLE ( 'NONE', #17331, 58.99999999999998579 ) ;
#12453=FACE_OUTER_BOUND ( 'NONE', #272, .T. ) ;
#12460=EDGE_CURVE ( 'NONE', #844, #13292, #28258, .T. ) ;
#12462=DIRECTION ( 'NONE',  ( 0.000000000000000000, 0.000000000000000000, 1.000000000000000000 ) ) ;
#12463=EDGE_CURVE ( 'NONE', #41070, #41968, #28884, .T. ) ;
#12469=CARTESIAN_POINT ( 'NONE',  ( 17.99999999999999645, -101.1249659627852679, -48.60055280209521555 ) ) ;
#12477=DIRECTION ( 'NONE',  ( -1.000000000000000000, -0.000000000000000000, -0.000000000000000000 ) ) ;
#12478=DIRECTION ( 'NONE',  ( -1.000000000000000000, -0.000000000000000000, 0.000000000000000000 ) ) ;
#12479=EDGE_CURVE ( 'NONE', #36212, #5428, #21256, .T. ) ;
#12480=ORIENTED_EDGE ( 'NONE', *, *, #13909, .F. ) ;
#12482=CARTESIAN_POINT ( 'NONE',  ( 17.99999999999999645, 0.000000000000000000, 0.000000000000000000 ) ) ;
#12486=LINE ( 'NONE', #25377, #559 ) ;
#12490=VERTEX_POINT ( 'NONE', #21089 ) ;
#12496=VECTOR ( 'NONE', #27027, 1000.000000000000000 ) ;
#12497=CYLINDRICAL_SURFACE ( 'NONE', #18511, 116.0000000000000000 ) ;
#12498=AXIS2_PLACEMENT_3D ( 'NONE', #19045, #12686, #35994 ) ;
#12501=DIRECTION ( 'NONE',  ( 0.000000000000000000, -0.4132121857683850874, 0.9106347728549100129 ) ) ;
#12503=EDGE_CURVE ( 'NONE', #267, #23227, #7269, .T. ) ;
#12507=EDGE_CURVE ( 'NONE', #32964, #27433, #31304, .T. ) ;
#12509=ORIENTED_EDGE ( 'NONE', *, *, #3598, .F. ) ;
#12511=ADVANCED_FACE ( 'NONE', ( #38678 ), #29520, .F. ) ;
#12514=CARTESIAN_POINT ( 'NONE',  ( 0.000000000000000000, -116.4607004671430417, 30.94182036827165660 ) ) ;
#12515=LINE ( 'NONE', #19289, #14918 ) ;
#12517=ADVANCED_FACE ( 'NONE', ( #6166 ), #28890, .F. ) ;
#12520=ORIENTED_EDGE ( 'NONE', *, *, #41967, .F. ) ;
#12521=ORIENTED_EDGE ( 'NONE', *, *, #29656, .F. ) ;
#12522=DIRECTION ( 'NONE',  ( -1.000000000000000000, -0.000000000000000000, 0.000000000000000000 ) ) ;
#12523=CARTESIAN_POINT ( 'NONE',  ( 0.000000000000000000, -113.8630351447207119, 22.16324045874372572 ) ) ;
#12524=CIRCLE ( 'NONE', #9732, 120.5010000000000190 ) ;
#12526=FACE_OUTER_BOUND ( 'NONE', #21227, .T. ) ;
#12527=AXIS2_PLACEMENT_3D ( 'NONE', #29477, #26207, #22965 ) ;
#12528=LINE ( 'NONE', #39304, #9904 ) ;
#12533=DIRECTION ( 'NONE',  ( 0.000000000000000000, -0.05322217484216513333, -0.9985826956767627216 ) ) ;
#12534=CARTESIAN_POINT ( 'NONE',  ( 17.99999999999999645, 0.000000000000000000, 0.000000000000000000 ) ) ;
#12537=ORIENTED_EDGE ( 'NONE', *, *, #1976, .T. ) ;
#12539=ADVANCED_FACE ( 'NONE', ( #29110 ), #15799, .F. ) ;
#12540=ORIENTED_EDGE ( 'NONE', *, *, #32529, .F. ) ;
#12541=EDGE_CURVE ( 'NONE', #10180, #4179, #16227, .T. ) ;
#12542=DIRECTION ( 'NONE',  ( 0.000000000000000000, -0.6382441836448110584, -0.7698339834299138262 ) ) ;
#12545=VERTEX_POINT ( 'NONE', #12949 ) ;
#12547=VERTEX_POINT ( 'NONE', #22366 ) ;
#12548=DIRECTION ( 'NONE',  ( 0.000000000000000000, -0.3140767120219362107, -0.9493976084683853900 ) ) ;
#12550=VERTEX_POINT ( 'NONE', #32356 ) ;
#12553=CIRCLE ( 'NONE', #42476, 116.0000000000000000 ) ;
#12554=AXIS2_PLACEMENT_3D ( 'NONE', #25604, #35779, #19057 ) ;
#12556=DIRECTION ( 'NONE',  ( -1.000000000000000000, 0.000000000000000000, 0.000000000000000000 ) ) ;
#12557=EDGE_CURVE ( 'NONE', #2034, #6009, #33747, .T. ) ;
#12558=CYLINDRICAL_SURFACE ( 'NONE', #12280, 59.00000000000000000 ) ;
#12559=ORIENTED_EDGE ( 'NONE', *, *, #34461, .F. ) ;
#12561=ORIENTED_EDGE ( 'NONE', *, *, #3461, .T. ) ;
#12562=EDGE_CURVE ( 'NONE', #42396, #40004, #24040, .T. ) ;
#12566=DIRECTION ( 'NONE',  ( 0.000000000000000000, 0.4610925014493267304, -0.8873520750565710991 ) ) ;
#12567=DIRECTION ( 'NONE',  ( 0.000000000000000000, 0.000000000000000000, 1.000000000000000000 ) ) ;
#12569=ADVANCED_FACE ( 'NONE', ( #5943 ), #19090, .F. ) ;
#12570=ADVANCED_FACE ( 'NONE', ( #12526 ), #35196, .F. ) ;
#12571=ORIENTED_EDGE ( 'NONE', *, *, #37208, .T. ) ;
#12572=DIRECTION ( 'NONE',  ( 1.000000000000000000, 0.000000000000000000, 0.000000000000000000 ) ) ;
#12573=DIRECTION ( 'NONE',  ( -1.000000000000000000, 0.000000000000000000, 0.000000000000000000 ) ) ;
#12577=ORIENTED_EDGE ( 'NONE', *, *, #28108, .T. ) ;
#12579=ORIENTED_EDGE ( 'NONE', *, *, #25580, .T. ) ;
#12581=DIRECTION ( 'NONE',  ( 0.000000000000000000, -0.8993121301712141413, -0.4373073204588656671 ) ) ;
#12586=DIRECTION ( 'NONE',  ( -1.000000000000000000, -0.000000000000000000, -0.000000000000000000 ) ) ;
#12587=EDGE_LOOP ( 'NONE', ( #32857, #41197, #40039, #24589 ) ) ;
#12588=FACE_OUTER_BOUND ( 'NONE', #22029, .T. ) ;
#12589=CARTESIAN_POINT ( 'NONE',  ( 0.000000000000000000, -2.418575551221678666, 120.4767259403368911 ) ) ;
#12590=CARTESIAN_POINT ( 'NONE',  ( 17.99999999999999645, -3.996885678773838713, 120.4346956066681713 ) ) ;
#12592=DIRECTION ( 'NONE',  ( 1.000000000000000000, 0.000000000000000000, 0.000000000000000000 ) ) ;
#12593=DIRECTION ( 'NONE',  ( -1.000000000000000000, -0.000000000000000000, -0.000000000000000000 ) ) ;
#12594=DIRECTION ( 'NONE',  ( 1.000000000000000000, 0.000000000000000000, 0.000000000000000000 ) ) ;
#12595=ORIENTED_EDGE ( 'NONE', *, *, #16094, .T. ) ;
#12596=ORIENTED_EDGE ( 'NONE', *, *, #3941, .T. ) ;
#12597=FACE_OUTER_BOUND ( 'NONE', #1343, .T. ) ;
#12598=CARTESIAN_POINT ( 'NONE',  ( 17.99999999999999645, 0.000000000000000000, 0.000000000000000000 ) ) ;
#12600=DIRECTION ( 'NONE',  ( 0.000000000000000000, 0.000000000000000000, 1.000000000000000000 ) ) ;
#12601=CIRCLE ( 'NONE', #36230, 116.0000000000000000 ) ;
#12603=EDGE_CURVE ( 'NONE', #4007, #25961, #12873, .T. ) ;
#12604=CARTESIAN_POINT ( 'NONE',  ( 0.000000000000000000, 12.43843445475471832, -111.5058645182328405 ) ) ;
#12605=AXIS2_PLACEMENT_3D ( 'NONE', #23517, #3597, #16969 ) ;
#12607=DIRECTION ( 'NONE',  ( 0.000000000000000000, 0.000000000000000000, 1.000000000000000000 ) ) ;
#12609=ORIENTED_EDGE ( 'NONE', *, *, #9934, .F. ) ;
#12610=AXIS2_PLACEMENT_3D ( 'NONE', #28337, #21382, #5168 ) ;
#12611=DIRECTION ( 'NONE',  ( 1.000000000000000000, 0.000000000000000000, 0.000000000000000000 ) ) ;
#12612=FACE_OUTER_BOUND ( 'NONE', #33682, .T. ) ;
#12617=ORIENTED_EDGE ( 'NONE', *, *, #30840, .F. ) ;
#12618=AXIS2_PLACEMENT_3D ( 'NONE', #24418, #1885, #27893 ) ;
#12627=LINE ( 'NONE', #36150, #40566 ) ;
#12630=FACE_OUTER_BOUND ( 'NONE', #22026, .T. ) ;
#12631=CARTESIAN_POINT ( 'NONE',  ( 0.000000000000000000, -48.55277268144396174, 105.3500273609078306 ) ) ;
#12635=CIRCLE ( 'NONE', #2832, 58.99999999999998579 ) ;
#12637=EDGE_CURVE ( 'NONE', #41527, #17401, #32574, .T. ) ;
#12641=EDGE_CURVE ( 'NONE', #24346, #30476, #37234, .T. ) ;
#12642=AXIS2_PLACEMENT_3D ( 'NONE', #41612, #31379, #38539 ) ;
#12643=ORIENTED_EDGE ( 'NONE', *, *, #43009, .F. ) ;
#12648=ORIENTED_EDGE ( 'NONE', *, *, #16941, .T. ) ;
#12650=DIRECTION ( 'NONE',  ( -1.000000000000000000, -0.000000000000000000, -0.000000000000000000 ) ) ;
#12651=ORIENTED_EDGE ( 'NONE', *, *, #22498, .F. ) ;
#12653=FACE_OUTER_BOUND ( 'NONE', #38252, .T. ) ;
#12655=CARTESIAN_POINT ( 'NONE',  ( 0.000000000000000000, 0.000000000000000000, 0.000000000000000000 ) ) ;
#12656=DIRECTION ( 'NONE',  ( 0.000000000000000000, 0.000000000000000000, -1.000000000000000000 ) ) ;
#12660=VERTEX_POINT ( 'NONE', #14408 ) ;
#12661=CARTESIAN_POINT ( 'NONE',  ( 8.999999999999998224, 48.55277268144470071, -105.3500273609075180 ) ) ;
#12662=ORIENTED_EDGE ( 'NONE', *, *, #36778, .T. ) ;
#12663=CARTESIAN_POINT ( 'NONE',  ( 9.000000000000001776, 5.492704054966705662, 115.8698847939556344 ) ) ;
#12664=CARTESIAN_POINT ( 'NONE',  ( 17.99999999999999645, 66.49630760163724119, -90.36876423295917959 ) ) ;
#12665=EDGE_CURVE ( 'NONE', #32420, #13665, #2391, .T. ) ;
#12678=VECTOR ( 'NONE', #16706, 1000.000000000000000 ) ;
#12680=DIRECTION ( 'NONE',  ( 1.000000000000000000, 0.000000000000000000, 0.000000000000000000 ) ) ;
#12681=CARTESIAN_POINT ( 'NONE',  ( 17.99999999999999645, -63.24564713401861837, 102.5693868539693341 ) ) ;
#12682=CYLINDRICAL_SURFACE ( 'NONE', #20269, 120.5010000000000190 ) ;
#12683=PRODUCT_DEFINITION_SHAPE ( 'NONE', 'NONE',  #10989 ) ;
#12686=DIRECTION ( 'NONE',  ( -1.000000000000000000, -0.000000000000000000, -0.000000000000000000 ) ) ;
#12687=CARTESIAN_POINT ( 'NONE',  ( 0.000000000000000000, 0.000000000000000000, 0.000000000000000000 ) ) ;
#12690=FACE_OUTER_BOUND ( 'NONE', #26569, .T. ) ;
#12697=ORIENTED_EDGE ( 'NONE', *, *, #8131, .F. ) ;
#12703=CIRCLE ( 'NONE', #26651, 59.00000000000000000 ) ;
#12704=CARTESIAN_POINT ( 'NONE',  ( 17.99999999999999645, -115.9387338813861987, 3.769613505535687636 ) ) ;
#12708=EDGE_CURVE ( 'NONE', #23222, #9027, #4113, .T. ) ;
#12711=VECTOR ( 'NONE', #15567, 1000.000000000000000 ) ;
#12712=CARTESIAN_POINT ( 'NONE',  ( 17.99999999999999645, 84.09610293794170843, -74.27057253242929846 ) ) ;
#12713=DIRECTION ( 'NONE',  ( -1.000000000000000000, 0.000000000000000000, 0.000000000000000000 ) ) ;
#12714=DIRECTION ( 'NONE',  ( -1.000000000000000000, 0.000000000000000000, 0.000000000000000000 ) ) ;
#12716=ORIENTED_EDGE ( 'NONE', *, *, #12463, .F. ) ;
#12717=ADVANCED_FACE ( 'NONE', ( #7618 ), #27940, .F. ) ;
#12720=CARTESIAN_POINT ( 'NONE',  ( 17.99999999999999645, 45.89132998248050654, 102.3829004574631512 ) ) ;
#12722=DIRECTION ( 'NONE',  ( -1.000000000000000000, -0.000000000000000000, -0.000000000000000000 ) ) ;
#12723=ORIENTED_EDGE ( 'NONE', *, *, #16653, .F. ) ;
#12727=AXIS2_PLACEMENT_3D ( 'NONE', #32281, #22295, #2590 ) ;
#12733=CARTESIAN_POINT ( 'NONE',  ( 17.99999999999999645, 0.000000000000000000, 0.000000000000000000 ) ) ;
#12735=CYLINDRICAL_SURFACE ( 'NONE', #27186, 116.0000000000000000 ) ;
#12739=CARTESIAN_POINT ( 'NONE',  ( 17.99999999999999645, 91.51415974874679193, -64.91094698989203948 ) ) ;
#12740=AXIS2_PLACEMENT_3D ( 'NONE', #18178, #14878, #41676 ) ;
#12741=DIRECTION ( 'NONE',  ( 0.000000000000000000, 1.246648735278247733E-14, -1.000000000000000000 ) ) ;
#12743=EDGE_CURVE ( 'NONE', #42396, #35643, #17481, .T. ) ;
#12747=CARTESIAN_POINT ( 'NONE',  ( 0.000000000000000000, -11.41303419184897017, -111.6154788735837116 ) ) ;
#12748=ORIENTED_EDGE ( 'NONE', *, *, #13060, .F. ) ;
#12749=CARTESIAN_POINT ( 'NONE',  ( 17.99999999999999645, 0.000000000000000000, 0.000000000000000000 ) ) ;
#12752=EDGE_LOOP ( 'NONE', ( #41506, #803, #25128, #25578 ) ) ;
#12753=CARTESIAN_POINT ( 'NONE',  ( 0.000000000000000000, 0.000000000000000000, 0.000000000000000000 ) ) ;
#12754=ORIENTED_EDGE ( 'NONE', *, *, #30179, .T. ) ;
#12758=ORIENTED_EDGE ( 'NONE', *, *, #10115, .F. ) ;
#12760=ORIENTED_EDGE ( 'NONE', *, *, #42319, .F. ) ;
#12761=CIRCLE ( 'NONE', #26672, 59.00000000000000000 ) ;
#12763=DIRECTION ( 'NONE',  ( 0.000000000000000000, 0.000000000000000000, 1.000000000000000000 ) ) ;
#12767=VERTEX_POINT ( 'NONE', #36253 ) ;
#12770=EDGE_LOOP ( 'NONE', ( #20260, #22256, #7872, #28700 ) ) ;
#12778=ORIENTED_EDGE ( 'NONE', *, *, #16862, .F. ) ;
#12782=CARTESIAN_POINT ( 'NONE',  ( 0.000000000000000000, 47.58001226230686598, -110.7096808509478763 ) ) ;
#12786=AXIS2_PLACEMENT_3D ( 'NONE', #27865, #41119, #21775 ) ;
#12787=CARTESIAN_POINT ( 'NONE',  ( 0.000000000000000000, 0.000000000000000000, 0.000000000000000000 ) ) ;
#12789=DIRECTION ( 'NONE',  ( 0.000000000000000000, -0.4610925014493142959, -0.8873520750565775383 ) ) ;
#12790=ORIENTED_EDGE ( 'NONE', *, *, #22086, .F. ) ;
#12791=CARTESIAN_POINT ( 'NONE',  ( 8.999999999999998224, 78.18175027177548486, -85.69488855492920720 ) ) ;
#12793=EDGE_CURVE ( 'NONE', #34589, #18324, #24460, .T. ) ;
#12794=EDGE_CURVE ( 'NONE', #11355, #10144, #40015, .T. ) ;
#12796=ORIENTED_EDGE ( 'NONE', *, *, #37251, .T. ) ;
#12798=DIRECTION ( 'NONE',  ( -1.000000000000000000, 0.000000000000000000, 0.000000000000000000 ) ) ;
#12805=CIRCLE ( 'NONE', #6514, 120.5010000000000190 ) ;
#12810=CARTESIAN_POINT ( 'NONE',  ( 17.99999999999999645, 94.83915810436401728, 59.94836581341619564 ) ) ;
#12812=DIRECTION ( 'NONE',  ( -1.000000000000000000, 0.000000000000000000, 0.000000000000000000 ) ) ;
#12814=AXIS2_PLACEMENT_3D ( 'NONE', #8571, #21930, #4211 ) ;
#12815=CARTESIAN_POINT ( 'NONE',  ( 17.99999999999999645, 0.000000000000000000, 0.000000000000000000 ) ) ;
#12816=AXIS2_PLACEMENT_3D ( 'NONE', #42192, #35451, #42415 ) ;
#12817=CARTESIAN_POINT ( 'NONE',  ( 0.000000000000000000, 88.56657216608614647, 68.87840567545953263 ) ) ;
#12818=ORIENTED_EDGE ( 'NONE', *, *, #19851, .T. ) ;
#12819=CARTESIAN_POINT ( 'NONE',  ( 9.000000000000001776, -107.1354928292866759, -44.47455650398174498 ) ) ;
#12823=CARTESIAN_POINT ( 'NONE',  ( 17.99999999999999645, -95.38615066513943930, -59.07414607872924250 ) ) ;
#12826=ORIENTED_EDGE ( 'NONE', *, *, #12425, .F. ) ;
#12839=CIRCLE ( 'NONE', #26785, 59.00000000000000000 ) ;
#12840=DIRECTION ( 'NONE',  ( 0.000000000000000000, 0.000000000000000000, 1.000000000000000000 ) ) ;
#12843=LINE ( 'NONE', #26153, #15098 ) ;
#12844=ORIENTED_EDGE ( 'NONE', *, *, #18769, .T. ) ;
#12846=DIRECTION ( 'NONE',  ( 0.000000000000000000, 0.000000000000000000, 1.000000000000000000 ) ) ;
#12849=AXIS2_PLACEMENT_3D ( 'NONE', #39208, #12215, #22919 ) ;
#12851=CARTESIAN_POINT ( 'NONE',  ( 17.99999999999999645, -31.17727234463771424, 111.7317219465818852 ) ) ;
#12852=ORIENTED_EDGE ( 'NONE', *, *, #35086, .F. ) ;
#12855=EDGE_CURVE ( 'NONE', #22539, #25336, #38632, .T. ) ;
#12857=DIRECTION ( 'NONE',  ( 0.000000000000000000, -0.05322217484218560307, 0.9985826956767616114 ) ) ;
#12859=CIRCLE ( 'NONE', #39973, 59.00000000000000711 ) ;
#12860=ORIENTED_EDGE ( 'NONE', *, *, #26210, .F. ) ;
#12861=CARTESIAN_POINT ( 'NONE',  ( 8.999999999999998224, 94.52951811191651643, -67.23221107124801676 ) ) ;
#12863=ORIENTED_EDGE ( 'NONE', *, *, #2238, .F. ) ;
#12867=CARTESIAN_POINT ( 'NONE',  ( 17.99999999999999645, 0.5156212287279957618, 112.1962860721878172 ) ) ;
#12868=DIRECTION ( 'NONE',  ( 1.000000000000000000, 0.000000000000000000, 0.000000000000000000 ) ) ;
#12870=ORIENTED_EDGE ( 'NONE', *, *, #2587, .T. ) ;
#12872=ORIENTED_EDGE ( 'NONE', *, *, #18939, .T. ) ;
#12873=CIRCLE ( 'NONE', #14982, 120.5010000000000332 ) ;
#12874=FACE_OUTER_BOUND ( 'NONE', #30093, .T. ) ;
#12877=DIRECTION ( 'NONE',  ( 1.000000000000000000, 0.000000000000000000, 0.000000000000000000 ) ) ;
#12878=CIRCLE ( 'NONE', #15663, 116.0000000000000000 ) ;
#12894=CARTESIAN_POINT ( 'NONE',  ( 0.000000000000000000, 0.000000000000000000, 0.000000000000000000 ) ) ;
#12895=ADVANCED_FACE ( 'NONE', ( #12002 ), #38791, .F. ) ;
#12897=ORIENTED_EDGE ( 'NONE', *, *, #15831, .T. ) ;
#12903=CIRCLE ( 'NONE', #338, 59.00000000000000000 ) ;
#12907=VERTEX_POINT ( 'NONE', #18570 ) ;
#12911=AXIS2_PLACEMENT_3D ( 'NONE', #77, #290, #13446 ) ;
#12912=ORIENTED_EDGE ( 'NONE', *, *, #33282, .F. ) ;
#12913=FACE_OUTER_BOUND ( 'NONE', #41, .T. ) ;
#12916=DIRECTION ( 'NONE',  ( -1.000000000000000000, 0.000000000000000000, -0.000000000000000000 ) ) ;
#12917=DIRECTION ( 'NONE',  ( 0.000000000000000000, 0.000000000000000000, -1.000000000000000000 ) ) ;
#12921=LINE ( 'NONE', #9408, #40086 ) ;
#12922=CIRCLE ( 'NONE', #25502, 59.00000000000000711 ) ;
#12924=DIRECTION ( 'NONE',  ( 1.000000000000000000, 0.000000000000000000, 0.000000000000000000 ) ) ;
#12925=CIRCLE ( 'NONE', #37284, 116.0000000000000000 ) ;
#12927=CARTESIAN_POINT ( 'NONE',  ( 17.99999999999999645, 34.74871106919619024, 106.6808302961373158 ) ) ;
#12929=EDGE_LOOP ( 'NONE', ( #22386, #20886, #38682, #12169 ) ) ;
#12930=AXIS2_PLACEMENT_3D ( 'NONE', #37768, #34936, #5046 ) ;
#12932=EDGE_CURVE ( 'NONE', #16471, #27833, #15721, .T. ) ;
#12934=CIRCLE ( 'NONE', #18550, 120.5010000000000190 ) ;
#12935=FACE_OUTER_BOUND ( 'NONE', #22332, .T. ) ;
#12938=DIRECTION ( 'NONE',  ( 0.000000000000000000, 0.000000000000000000, 1.000000000000000000 ) ) ;
#12939=VERTEX_POINT ( 'NONE', #22050 ) ;
#12940=AXIS2_PLACEMENT_3D ( 'NONE', #20002, #20218, #279 ) ;
#12941=DIRECTION ( 'NONE',  ( 0.000000000000000000, 0.000000000000000000, 1.000000000000000000 ) ) ;
#12945=EDGE_LOOP ( 'NONE', ( #22197, #9627, #42341, #32984 ) ) ;
#12948=CARTESIAN_POINT ( 'NONE',  ( 17.99999999999999645, -30.01658535635190361, -108.1077105353201233 ) ) ;
#12949=CARTESIAN_POINT ( 'NONE',  ( 0.000000000000000000, 64.58410930313523579, 101.7319213743684685 ) ) ;
#12950=CARTESIAN_POINT ( 'NONE',  ( 0.000000000000000000, 0.000000000000000000, 0.000000000000000000 ) ) ;
#12955=ORIENTED_EDGE ( 'NONE', *, *, #758, .F. ) ;
#12957=CYLINDRICAL_SURFACE ( 'NONE', #42308, 116.0000000000000000 ) ;
#12959=CARTESIAN_POINT ( 'NONE',  ( 0.000000000000000000, 83.58328028049660929, 80.43528614701352808 ) ) ;
#12960=CARTESIAN_POINT ( 'NONE',  ( 17.99999999999999645, 109.4038418350910433, -50.51029986767441926 ) ) ;
#12965=CIRCLE ( 'NONE', #20679, 120.5010000000000332 ) ;
#12966=CARTESIAN_POINT ( 'NONE',  ( 17.99999999999999645, 78.75547124681369837, 91.20343606297029737 ) ) ;
#12968=EDGE_CURVE ( 'NONE', #38008, #22806, #42052, .T. ) ;
#12969=VERTEX_POINT ( 'NONE', #4786 ) ;
#12970=AXIS2_PLACEMENT_3D ( 'NONE', #5080, #18672, #19075 ) ;
#12971=CYLINDRICAL_SURFACE ( 'NONE', #2025, 58.99999999999999289 ) ;
#12974=VECTOR ( 'NONE', #3343, 1000.000000000000000 ) ;
#12976=ORIENTED_EDGE ( 'NONE', *, *, #34228, .F. ) ;
#12980=ORIENTED_EDGE ( 'NONE', *, *, #2820, .F. ) ;
#12981=CYLINDRICAL_SURFACE ( 'NONE', #766, 59.00000000000000000 ) ;
#12986=CARTESIAN_POINT ( 'NONE',  ( 17.99999999999999645, 103.4151313792879421, -61.85306461934305844 ) ) ;
#12987=CARTESIAN_POINT ( 'NONE',  ( 17.99999999999999645, -84.09610293794118263, 74.27057253242982426 ) ) ;
#12989=DIRECTION ( 'NONE',  ( 1.000000000000000000, -0.000000000000000000, -0.000000000000000000 ) ) ;
#12990=ORIENTED_EDGE ( 'NONE', *, *, #6027, .F. ) ;
#12992=CARTESIAN_POINT ( 'NONE',  ( 17.99999999999999645, -15.21076497709792008, 119.5371223922154797 ) ) ;
#12993=EDGE_CURVE ( 'NONE', #39732, #41661, #36566, .T. ) ;
#12995=EDGE_CURVE ( 'NONE', #28903, #31744, #42141, .T. ) ;
#12998=CIRCLE ( 'NONE', #29743, 59.00000000000000000 ) ;
#12999=ORIENTED_EDGE ( 'NONE', *, *, #16121, .F. ) ;
#13002=AXIS2_PLACEMENT_3D ( 'NONE', #27047, #155, #40315 ) ;
#13006=ORIENTED_EDGE ( 'NONE', *, *, #38335, .F. ) ;
#13016=CYLINDRICAL_SURFACE ( 'NONE', #20819, 116.0000000000000000 ) ;
#13020=CARTESIAN_POINT ( 'NONE',  ( 0.000000000000000000, 103.5682682299982673, 43.14958040911701431 ) ) ;
#13022=EDGE_LOOP ( 'NONE', ( #5357, #33640, #30252, #17903 ) ) ;
#13024=DIRECTION ( 'NONE',  ( 0.000000000000000000, 0.000000000000000000, 1.000000000000000000 ) ) ;
#13030=EDGE_CURVE ( 'NONE', #31004, #21207, #8031, .T. ) ;
#13031=DIRECTION ( 'NONE',  ( 0.000000000000000000, 0.000000000000000000, 1.000000000000000000 ) ) ;
#13034=VECTOR ( 'NONE', #18888, 1000.000000000000000 ) ;
#13036=EDGE_LOOP ( 'NONE', ( #42920, #27363, #28515, #10383 ) ) ;
#13037=VERTEX_POINT ( 'NONE', #29638 ) ;
#13039=DIRECTION ( 'NONE',  ( 1.000000000000000000, 0.000000000000000000, 0.000000000000000000 ) ) ;
#13041=AXIS2_PLACEMENT_3D ( 'NONE', #16381, #7127, #2602 ) ;
#13042=FACE_OUTER_BOUND ( 'NONE', #11752, .T. ) ;
#13050=FACE_OUTER_BOUND ( 'NONE', #41764, .T. ) ;
#13051=CARTESIAN_POINT ( 'NONE',  ( 17.99999999999999645, 0.000000000000000000, 0.000000000000000000 ) ) ;
#13052=AXIS2_PLACEMENT_3D ( 'NONE', #14766, #14983, #17834 ) ;
#13054=EDGE_CURVE ( 'NONE', #21840, #9577, #19896, .T. ) ;
#13055=DIRECTION ( 'NONE',  ( -1.000000000000000000, -0.000000000000000000, -0.000000000000000000 ) ) ;
#13060=EDGE_CURVE ( 'NONE', #1786, #39040, #41433, .T. ) ;
#13061=DIRECTION ( 'NONE',  ( 1.000000000000000000, 0.000000000000000000, 0.000000000000000000 ) ) ;
#13070=VERTEX_POINT ( 'NONE', #12631 ) ;
#13072=CARTESIAN_POINT ( 'NONE',  ( 9.000000000000001776, -5.492704054967489924, 115.8698847939556202 ) ) ;
#13073=AXIS2_PLACEMENT_3D ( 'NONE', #36867, #11142, #25708 ) ;
#13076=CARTESIAN_POINT ( 'NONE',  ( 17.99999999999999645, 0.000000000000000000, 0.000000000000000000 ) ) ;
#13078=CARTESIAN_POINT ( 'NONE',  ( 0.000000000000000000, 0.000000000000000000, 0.000000000000000000 ) ) ;
#13081=EDGE_LOOP ( 'NONE', ( #11018, #1309, #23240, #38075 ) ) ;
#13090=CARTESIAN_POINT ( 'NONE',  ( 0.000000000000000000, -3.996885678772176043, -120.4346956066682424 ) ) ;
#13093=CARTESIAN_POINT ( 'NONE',  ( 0.000000000000000000, 111.7974656912331426, -9.465682155094398809 ) ) ;
#13095=DIRECTION ( 'NONE',  ( 0.000000000000000000, 0.8747630845319623871, -0.4845508703326482647 ) ) ;
#13097=ORIENTED_EDGE ( 'NONE', *, *, #8092, .T. ) ;
#13098=AXIS2_PLACEMENT_3D ( 'NONE', #23804, #37929, #7833 ) ;
#13099=LINE ( 'NONE', #26400, #2818 ) ;
#13100=AXIS2_PLACEMENT_3D ( 'NONE', #4051, #14572, #20920 ) ;
#13101=ORIENTED_EDGE ( 'NONE', *, *, #21305, .T. ) ;
#13105=CARTESIAN_POINT ( 'NONE',  ( 17.99999999999999645, 0.000000000000000000, 0.000000000000000000 ) ) ;
#13107=LINE ( 'NONE', #23151, #2966 ) ;
#13108=AXIS2_PLACEMENT_3D ( 'NONE', #13179, #9236, #12741 ) ;
#13111=CARTESIAN_POINT ( 'NONE',  ( 17.99999999999999645, 0.5156212287294736907, -112.1962860721878315 ) ) ;
#13119=EDGE_CURVE ( 'NONE', #22718, #21350, #9124, .T. ) ;
#13120=DIRECTION ( 'NONE',  ( -1.000000000000000000, 0.000000000000000000, -0.000000000000000000 ) ) ;
#13121=AXIS2_PLACEMENT_3D ( 'NONE', #19474, #19049, #42338 ) ;
#13123=FACE_OUTER_BOUND ( 'NONE', #42144, .T. ) ;
#13126=VECTOR ( 'NONE', #41132, 1000.000000000000000 ) ;
#13127=EDGE_LOOP ( 'NONE', ( #24755, #29755, #26260, #28673 ) ) ;
#13129=DIRECTION ( 'NONE',  ( 0.000000000000000000, 0.3140767120219494779, -0.9493976084683810601 ) ) ;
#13131=CIRCLE ( 'NONE', #20100, 59.00000000000000711 ) ;
#13135=DIRECTION ( 'NONE',  ( -1.000000000000000000, 0.000000000000000000, 0.000000000000000000 ) ) ;
#13136=ORIENTED_EDGE ( 'NONE', *, *, #21825, .F. ) ;
#13139=ORIENTED_EDGE ( 'NONE', *, *, #34277, .T. ) ;
#13142=ORIENTED_EDGE ( 'NONE', *, *, #2625, .T. ) ;
#13146=ORIENTED_EDGE ( 'NONE', *, *, #33609, .T. ) ;
#13148=DIRECTION ( 'NONE',  ( -1.000000000000000000, -0.000000000000000000, -0.000000000000000000 ) ) ;
#13153=DIRECTION ( 'NONE',  ( -1.000000000000000000, -0.000000000000000000, -0.000000000000000000 ) ) ;
#13155=EDGE_CURVE ( 'NONE', #23465, #20981, #35179, .T. ) ;
#13159=EDGE_LOOP ( 'NONE', ( #10998, #41970, #23044, #24480 ) ) ;
#13160=CARTESIAN_POINT ( 'NONE',  ( 17.99999999999999645, -45.89132998248120288, 102.3829004574628385 ) ) ;
#13162=VERTEX_POINT ( 'NONE', #42487 ) ;
#13171=DIRECTION ( 'NONE',  ( -1.000000000000000000, -0.000000000000000000, -0.000000000000000000 ) ) ;
#13174=CARTESIAN_POINT ( 'NONE',  ( 17.99999999999999645, 115.6826031496112392, 8.575274253897841703 ) ) ;
#13175=ORIENTED_EDGE ( 'NONE', *, *, #15891, .F. ) ;
#13176=CARTESIAN_POINT ( 'NONE',  ( 17.99999999999999645, 0.000000000000000000, 0.000000000000000000 ) ) ;
#13179=CARTESIAN_POINT ( 'NONE',  ( 0.000000000000000000, -57.40245293794601622, -96.40140491896693220 ) ) ;
#13181=CIRCLE ( 'NONE', #25083, 120.5010000000000190 ) ;
#13183=CARTESIAN_POINT ( 'NONE',  ( 0.000000000000000000, -35.78484819117709748, 110.3423972910431701 ) ) ;
#13186=CARTESIAN_POINT ( 'NONE',  ( 9.000000000000001776, -63.55543939553828636, 97.03971415477303708 ) ) ;
#13187=ORIENTED_EDGE ( 'NONE', *, *, #23162, .T. ) ;
#13190=EDGE_CURVE ( 'NONE', #17417, #5363, #32892, .T. ) ;
#13195=VERTEX_POINT ( 'NONE', #36368 ) ;
#13196=EDGE_CURVE ( 'NONE', #17370, #19286, #1005, .T. ) ;
#13197=CARTESIAN_POINT ( 'NONE',  ( 17.99999999999999645, 78.18175027177430536, 85.69488855493025881 ) ) ;
#13206=DIRECTION ( 'NONE',  ( 0.000000000000000000, -0.4132121857683668242, -0.9106347728549183396 ) ) ;
#13215=ORIENTED_EDGE ( 'NONE', *, *, #11040, .F. ) ;
#13219=EDGE_CURVE ( 'NONE', #2641, #14947, #33781, .T. ) ;
#13223=EDGE_CURVE ( 'NONE', #40725, #25529, #27019, .T. ) ;
#13224=CARTESIAN_POINT ( 'NONE',  ( 0.000000000000000000, -91.65951123222436081, -71.09524597798180423 ) ) ;
#13232=DIRECTION ( 'NONE',  ( -1.000000000000000000, -0.000000000000000000, -0.000000000000000000 ) ) ;
#13233=LINE ( 'NONE', #6872, #3797 ) ;
#13236=DIRECTION ( 'NONE',  ( 0.000000000000000000, 0.000000000000000000, 1.000000000000000000 ) ) ;
#13237=CARTESIAN_POINT ( 'NONE',  ( 0.000000000000000000, -103.4151313792866489, -61.85306461934516875 ) ) ;
#13240=ORIENTED_EDGE ( 'NONE', *, *, #1645, .T. ) ;
#13244=EDGE_CURVE ( 'NONE', #32792, #36933, #34494, .T. ) ;
#13245=CARTESIAN_POINT ( 'NONE',  ( 0.000000000000000000, 95.38615066513983720, 59.07414607872858170 ) ) ;
#13249=ORIENTED_EDGE ( 'NONE', *, *, #7384, .F. ) ;
#13252=DIRECTION ( 'NONE',  ( 0.000000000000000000, 0.6783118362696123338, 0.7347741508630707408 ) ) ;
#13258=CARTESIAN_POINT ( 'NONE',  ( 0.000000000000000000, -105.3681574666261298, -38.54638589714993202 ) ) ;
#13261=DIRECTION ( 'NONE',  ( -1.000000000000000000, 0.000000000000000000, 0.000000000000000000 ) ) ;
#13263=CARTESIAN_POINT ( 'NONE',  ( 0.000000000000000000, 69.90696807222487053, 98.15042952503540619 ) ) ;
#13264=ORIENTED_EDGE ( 'NONE', *, *, #8389, .F. ) ;
#13269=AXIS2_PLACEMENT_3D ( 'NONE', #27721, #10916, #4114 ) ;
#13270=AXIS2_PLACEMENT_3D ( 'NONE', #31786, #1874, #15237 ) ;
#13271=ORIENTED_EDGE ( 'NONE', *, *, #36954, .T. ) ;
#13274=LINE ( 'NONE', #17427, #17885 ) ;
#13275=ORIENTED_EDGE ( 'NONE', *, *, #5733, .F. ) ;
#13278=AXIS2_PLACEMENT_3D ( 'NONE', #14194, #37515, #37290 ) ;
#13280=ORIENTED_EDGE ( 'NONE', *, *, #23057, .F. ) ;
#13281=ORIENTED_EDGE ( 'NONE', *, *, #29366, .T. ) ;
#13283=LINE ( 'NONE', #26372, #38880 ) ;
#13284=CARTESIAN_POINT ( 'NONE',  ( 0.000000000000000000, 0.000000000000000000, 0.000000000000000000 ) ) ;
#13286=ORIENTED_EDGE ( 'NONE', *, *, #40493, .F. ) ;
#13287=DIRECTION ( 'NONE',  ( -1.000000000000000000, 0.000000000000000000, 0.000000000000000000 ) ) ;
#13289=CARTESIAN_POINT ( 'NONE',  ( 17.99999999999999645, -16.77566611177856615, 119.3275660838941832 ) ) ;
#13292=VERTEX_POINT ( 'NONE', #17436 ) ;
#13294=DIRECTION ( 'NONE',  ( -1.000000000000000000, 0.000000000000000000, 0.000000000000000000 ) ) ;
#13295=ADVANCED_FACE ( 'NONE', ( #16993 ), #24413, .F. ) ;
#13296=DIRECTION ( 'NONE',  ( 1.000000000000000000, 0.000000000000000000, 0.000000000000000000 ) ) ;
#13297=EDGE_CURVE ( 'NONE', #21728, #3675, #36604, .T. ) ;
#13298=ADVANCED_FACE ( 'NONE', ( #350 ), #23968, .F. ) ;
#13299=VERTEX_POINT ( 'NONE', #10859 ) ;
#13301=EDGE_CURVE ( 'NONE', #42436, #37254, #26883, .T. ) ;
#13303=FACE_OUTER_BOUND ( 'NONE', #12420, .T. ) ;
#13307=CARTESIAN_POINT ( 'NONE',  ( 17.99999999999999645, 62.45178862086345362, -93.20969140437443912 ) ) ;
#13308=VECTOR ( 'NONE', #31323, 1000.000000000000000 ) ;
#13310=AXIS2_PLACEMENT_3D ( 'NONE', #32069, #12021, #29026 ) ;
#13317=CYLINDRICAL_SURFACE ( 'NONE', #32212, 120.5010000000000190 ) ;
#13320=DIRECTION ( 'NONE',  ( 0.000000000000000000, 0.000000000000000000, 1.000000000000000000 ) ) ;
#13321=DIRECTION ( 'NONE',  ( -1.000000000000000000, -0.000000000000000000, -0.000000000000000000 ) ) ;
#13323=CYLINDRICAL_SURFACE ( 'NONE', #10712, 120.5010000000000190 ) ;
#13329=AXIS2_PLACEMENT_3D ( 'NONE', #7758, #18073, #38495 ) ;
#13331=VECTOR ( 'NONE', #19326, 1000.000000000000000 ) ;
#13333=VECTOR ( 'NONE', #17391, 1000.000000000000000 ) ;
#13334=EDGE_LOOP ( 'NONE', ( #32222, #12561, #4183, #922 ) ) ;
#13335=CARTESIAN_POINT ( 'NONE',  ( 9.000000000000001776, -112.8457601792513714, -26.86697618949492039 ) ) ;
#13336=DIRECTION ( 'NONE',  ( -1.000000000000000000, 0.000000000000000000, -0.000000000000000000 ) ) ;
#13339=CARTESIAN_POINT ( 'NONE',  ( 0.000000000000000000, 0.000000000000000000, 0.000000000000000000 ) ) ;
#13340=DIRECTION ( 'NONE',  ( 1.000000000000000000, 0.000000000000000000, 0.000000000000000000 ) ) ;
#13341=CIRCLE ( 'NONE', #19611, 120.5010000000000190 ) ;
#13343=LINE ( 'NONE', #36644, #24539 ) ;
#13344=DIRECTION ( 'NONE',  ( -1.000000000000000000, -0.000000000000000000, 0.000000000000000000 ) ) ;
#13346=EDGE_CURVE ( 'NONE', #5841, #9004, #16427, .T. ) ;
#13352=ORIENTED_EDGE ( 'NONE', *, *, #7547, .T. ) ;
#13355=ORIENTED_EDGE ( 'NONE', *, *, #20049, .F. ) ;
#13356=FACE_OUTER_BOUND ( 'NONE', #39749, .T. ) ;
#13357=DIRECTION ( 'NONE',  ( -1.000000000000000000, -0.000000000000000000, -0.000000000000000000 ) ) ;
#13358=DIRECTION ( 'NONE',  ( -1.000000000000000000, 0.000000000000000000, 0.000000000000000000 ) ) ;
#13361=CARTESIAN_POINT ( 'NONE',  ( 0.000000000000000000, 107.1354928292869744, 44.47455650398100602 ) ) ;
#13363=DIRECTION ( 'NONE',  ( 1.000000000000000000, 0.000000000000000000, 0.000000000000000000 ) ) ;
#13364=EDGE_CURVE ( 'NONE', #12448, #17417, #12934, .T. ) ;
#13368=ORIENTED_EDGE ( 'NONE', *, *, #31392, .F. ) ;
#13373=DIRECTION ( 'NONE',  ( 1.000000000000000000, 0.000000000000000000, 0.000000000000000000 ) ) ;
#13374=CARTESIAN_POINT ( 'NONE',  ( 17.99999999999999645, -118.8387007424472159, 19.94628303336445185 ) ) ;
#13380=VERTEX_POINT ( 'NONE', #17871 ) ;
#13381=ORIENTED_EDGE ( 'NONE', *, *, #7547, .F. ) ;
#13385=DIRECTION ( 'NONE',  ( -1.000000000000000000, 0.000000000000000000, -0.000000000000000000 ) ) ;
#13386=ORIENTED_EDGE ( 'NONE', *, *, #32240, .F. ) ;
#13394=VECTOR ( 'NONE', #3025, 1000.000000000000000 ) ;
#13397=ORIENTED_EDGE ( 'NONE', *, *, #38291, .F. ) ;
#13398=DIRECTION ( 'NONE',  ( -1.000000000000000000, 0.000000000000000000, 0.000000000000000000 ) ) ;
#13400=CYLINDRICAL_SURFACE ( 'NONE', #22575, 59.00000000000000000 ) ;
#13401=EDGE_LOOP ( 'NONE', ( #22537, #15078, #31499, #18823 ) ) ;
#13403=ORIENTED_EDGE ( 'NONE', *, *, #42519, .F. ) ;
#13406=FACE_OUTER_BOUND ( 'NONE', #22238, .T. ) ;
#13409=ADVANCED_FACE ( 'NONE', ( #1235 ), #4947, .F. ) ;
#13410=DIRECTION ( 'NONE',  ( -1.000000000000000000, 0.000000000000000000, -0.000000000000000000 ) ) ;
#13412=VERTEX_POINT ( 'NONE', #18096 ) ;
#13414=EDGE_CURVE ( 'NONE', #4007, #36553, #11292, .T. ) ;
#13415=DIRECTION ( 'NONE',  ( 0.000000000000000000, 0.000000000000000000, -1.000000000000000000 ) ) ;
#13416=DIRECTION ( 'NONE',  ( -1.000000000000000000, -0.000000000000000000, -0.000000000000000000 ) ) ;
#13418=ORIENTED_EDGE ( 'NONE', *, *, #7629, .F. ) ;
#13422=VECTOR ( 'NONE', #23354, 1000.000000000000000 ) ;
#13424=AXIS2_PLACEMENT_3D ( 'NONE', #3513, #36910, #30170 ) ;
#13436=EDGE_CURVE ( 'NONE', #31605, #4616, #7497, .T. ) ;
#13439=CARTESIAN_POINT ( 'NONE',  ( 17.99999999999999645, -114.6488492393081913, 37.09625815499973100 ) ) ;
#13440=ORIENTED_EDGE ( 'NONE', *, *, #42069, .F. ) ;
#13442=VERTEX_POINT ( 'NONE', #31066 ) ;
#13443=CYLINDRICAL_SURFACE ( 'NONE', #31876, 59.00000000000000000 ) ;
#13446=DIRECTION ( 'NONE',  ( 0.000000000000000000, 0.000000000000000000, 1.000000000000000000 ) ) ;
#13450=EDGE_CURVE ( 'NONE', #5730, #16033, #372, .T. ) ;
#13452=CIRCLE ( 'NONE', #29454, 116.0000000000000000 ) ;
#13453=DIRECTION ( 'NONE',  ( 0.000000000000000000, -0.7164567402983067490, -0.6976315211349933820 ) ) ;
#13458=AXIS2_PLACEMENT_3D ( 'NONE', #10433, #30724, #40511 ) ;
#13460=CARTESIAN_POINT ( 'NONE',  ( 0.000000000000000000, 0.000000000000000000, 0.000000000000000000 ) ) ;
#13463=ORIENTED_EDGE ( 'NONE', *, *, #12200, .F. ) ;
#13464=LINE ( 'NONE', #21498, #15008 ) ;
#13468=CARTESIAN_POINT ( 'NONE',  ( 0.000000000000000000, 67.32409792376505209, 89.75376489259387824 ) ) ;
#13469=DIRECTION ( 'NONE',  ( -1.000000000000000000, -0.000000000000000000, 0.000000000000000000 ) ) ;
#13470=LINE ( 'NONE', #42884, #25569 ) ;
#13475=DIRECTION ( 'NONE',  ( -1.000000000000000000, 0.000000000000000000, 0.000000000000000000 ) ) ;
#13478=ORIENTED_EDGE ( 'NONE', *, *, #23591, .F. ) ;
#13480=ORIENTED_EDGE ( 'NONE', *, *, #27106, .T. ) ;
#13484=VERTEX_POINT ( 'NONE', #37805 ) ;
#13485=EDGE_CURVE ( 'NONE', #21478, #27228, #17160, .T. ) ;
#13489=DIRECTION ( 'NONE',  ( -1.000000000000000000, -0.000000000000000000, -0.000000000000000000 ) ) ;
#13493=CARTESIAN_POINT ( 'NONE',  ( 0.000000000000000000, 0.000000000000000000, 0.000000000000000000 ) ) ;
#13496=CARTESIAN_POINT ( 'NONE',  ( 0.000000000000000000, 112.5220807139884016, 28.19186676675879255 ) ) ;
#13498=DIRECTION ( 'NONE',  ( 1.000000000000000000, 0.000000000000000000, 0.000000000000000000 ) ) ;
#13499=VERTEX_POINT ( 'NONE', #30644 ) ;
#13500=FACE_OUTER_BOUND ( 'NONE', #29526, .T. ) ;
#13504=ORIENTED_EDGE ( 'NONE', *, *, #17362, .T. ) ;
#13505=CARTESIAN_POINT ( 'NONE',  ( 17.99999999999999645, -73.78980555658671392, 95.26571049921967926 ) ) ;
#13506=AXIS2_PLACEMENT_3D ( 'NONE', #42369, #12089, #38667 ) ;
#13507=DIRECTION ( 'NONE',  ( 0.000000000000000000, 6.115635305138573842E-15, -1.000000000000000000 ) ) ;
#13508=CIRCLE ( 'NONE', #20529, 116.0000000000000000 ) ;
#13510=VERTEX_POINT ( 'NONE', #36946 ) ;
#13513=ORIENTED_EDGE ( 'NONE', *, *, #4926, .F. ) ;
#13519=EDGE_CURVE ( 'NONE', #10297, #40092, #37159, .T. ) ;
#13520=DIRECTION ( 'NONE',  ( 0.000000000000000000, 0.6783118362696123338, 0.7347741508630707408 ) ) ;
#13521=DIRECTION ( 'NONE',  ( 0.000000000000000000, -0.8477344278896649099, -0.5304209081197521769 ) ) ;
#13522=ORIENTED_EDGE ( 'NONE', *, *, #3431, .F. ) ;
#13523=CARTESIAN_POINT ( 'NONE',  ( 17.99999999999999645, 29.02167576844250618, -108.3790330702166926 ) ) ;
#13524=ORIENTED_EDGE ( 'NONE', *, *, #19420, .T. ) ;
#13525=AXIS2_PLACEMENT_3D ( 'NONE', #38935, #5137, #18930 ) ;
#13526=DIRECTION ( 'NONE',  ( -1.000000000000000000, 0.000000000000000000, 0.000000000000000000 ) ) ;
#13532=CIRCLE ( 'NONE', #19126, 116.0000000000000000 ) ;
#13535=EDGE_CURVE ( 'NONE', #30056, #6492, #39368, .T. ) ;
#13536=EDGE_CURVE ( 'NONE', #42855, #22705, #7333, .T. ) ;
#13537=VERTEX_POINT ( 'NONE', #40631 ) ;
#13540=ADVANCED_FACE ( 'NONE', ( #34973 ), #15575, .F. ) ;
#13542=VECTOR ( 'NONE', #31618, 1000.000000000000000 ) ;
#13543=DIRECTION ( 'NONE',  ( 0.000000000000000000, 0.000000000000000000, 1.000000000000000000 ) ) ;
#13544=DIRECTION ( 'NONE',  ( -1.000000000000000000, 0.000000000000000000, -0.000000000000000000 ) ) ;
#13545=ORIENTED_EDGE ( 'NONE', *, *, #10059, .T. ) ;
#13546=CARTESIAN_POINT ( 'NONE',  ( 0.000000000000000000, 0.000000000000000000, 0.000000000000000000 ) ) ;
#13547=DIRECTION ( 'NONE',  ( -1.000000000000000000, -0.000000000000000000, -0.000000000000000000 ) ) ;
#13552=AXIS2_PLACEMENT_3D ( 'NONE', #3852, #14597, #10213 ) ;
#13554=ORIENTED_EDGE ( 'NONE', *, *, #18087, .T. ) ;
#13555=CYLINDRICAL_SURFACE ( 'NONE', #25946, 120.5010000000000190 ) ;
#13556=DIRECTION ( 'NONE',  ( -1.000000000000000000, -0.000000000000000000, 0.000000000000000000 ) ) ;
#13561=AXIS2_PLACEMENT_3D ( 'NONE', #38181, #25558, #38388 ) ;
#13567=ORIENTED_EDGE ( 'NONE', *, *, #29074, .T. ) ;
#13568=FACE_OUTER_BOUND ( 'NONE', #5859, .T. ) ;
#13569=ADVANCED_FACE ( 'NONE', ( #5305 ), #8358, .F. ) ;
#13570=VECTOR ( 'NONE', #8470, 1000.000000000000000 ) ;
#13572=DIRECTION ( 'NONE',  ( 0.000000000000000000, 0.000000000000000000, 1.000000000000000000 ) ) ;
#13574=DIRECTION ( 'NONE',  ( -1.000000000000000000, -0.000000000000000000, -0.000000000000000000 ) ) ;
#13577=DIRECTION ( 'NONE',  ( -1.000000000000000000, -0.000000000000000000, -0.000000000000000000 ) ) ;
#13581=ORIENTED_EDGE ( 'NONE', *, *, #21276, .T. ) ;
#13588=ORIENTED_EDGE ( 'NONE', *, *, #19959, .F. ) ;
#13590=EDGE_CURVE ( 'NONE', #38310, #25529, #21389, .T. ) ;
#13591=EDGE_CURVE ( 'NONE', #32317, #23529, #39400, .T. ) ;
#13593=AXIS2_PLACEMENT_3D ( 'NONE', #27455, #31164, #1254 ) ;
#13595=ADVANCED_FACE ( 'NONE', ( #15370 ), #34765, .F. ) ;
#13596=AXIS2_PLACEMENT_3D ( 'NONE', #1171, #27829, #14736 ) ;
#13598=DIRECTION ( 'NONE',  ( 1.000000000000000000, 0.000000000000000000, 0.000000000000000000 ) ) ;
#13602=AXIS2_PLACEMENT_3D ( 'NONE', #14748, #28052, #41310 ) ;
#13605=ORIENTED_EDGE ( 'NONE', *, *, #11338, .F. ) ;
#13610=DIRECTION ( 'NONE',  ( 1.000000000000000000, 0.000000000000000000, 0.000000000000000000 ) ) ;
#13615=DIRECTION ( 'NONE',  ( 0.000000000000000000, 0.000000000000000000, 1.000000000000000000 ) ) ;
#13616=AXIS2_PLACEMENT_3D ( 'NONE', #18674, #15373, #11437 ) ;
#13617=ORIENTED_EDGE ( 'NONE', *, *, #6080, .T. ) ;
#13618=CARTESIAN_POINT ( 'NONE',  ( 0.000000000000000000, -34.03109950475806045, 115.5957406979048727 ) ) ;
#13624=ADVANCED_FACE ( 'NONE', ( #1586 ), #21721, .F. ) ;
#13625=AXIS2_PLACEMENT_3D ( 'NONE', #10386, #23724, #4858 ) ;
#13626=ORIENTED_EDGE ( 'NONE', *, *, #5351, .T. ) ;
#13632=AXIS2_PLACEMENT_3D ( 'NONE', #5780, #20636, #33907 ) ;
#13633=DIRECTION ( 'NONE',  ( 0.000000000000000000, 0.000000000000000000, 1.000000000000000000 ) ) ;
#13634=VERTEX_POINT ( 'NONE', #41510 ) ;
#13635=FACE_OUTER_BOUND ( 'NONE', #1180, .T. ) ;
#13637=CIRCLE ( 'NONE', #40780, 58.99999999999999289 ) ;
#13638=DIRECTION ( 'NONE',  ( 0.000000000000000000, -0.9574220383620080099, 0.2886919473396124536 ) ) ;
#13639=ORIENTED_EDGE ( 'NONE', *, *, #12258, .F. ) ;
#13644=ORIENTED_EDGE ( 'NONE', *, *, #14381, .T. ) ;
#13645=EDGE_CURVE ( 'NONE', #14175, #20513, #16462, .T. ) ;
#13649=AXIS2_PLACEMENT_3D ( 'NONE', #5565, #28922, #28071 ) ;
#13651=FACE_OUTER_BOUND ( 'NONE', #29287, .T. ) ;
#13653=EDGE_CURVE ( 'NONE', #7056, #38476, #17194, .T. ) ;
#13654=CIRCLE ( 'NONE', #40074, 59.00000000000000000 ) ;
#13655=ORIENTED_EDGE ( 'NONE', *, *, #11974, .T. ) ;
#13656=DIRECTION ( 'NONE',  ( -1.000000000000000000, 0.000000000000000000, 0.000000000000000000 ) ) ;
#13657=ORIENTED_EDGE ( 'NONE', *, *, #15199, .F. ) ;
#13659=CIRCLE ( 'NONE', #12288, 116.0000000000000000 ) ;
#13662=ADVANCED_FACE ( 'NONE', ( #10358 ), #11024, .F. ) ;
#13664=ORIENTED_EDGE ( 'NONE', *, *, #15710, .F. ) ;
#13665=VERTEX_POINT ( 'NONE', #26947 ) ;
#13668=CARTESIAN_POINT ( 'NONE',  ( 8.999999999999998224, -104.0201923570379137, 51.34003878071028026 ) ) ;
#13673=FACE_OUTER_BOUND ( 'NONE', #9031, .T. ) ;
#13680=CARTESIAN_POINT ( 'NONE',  ( 8.999999999999998224, 59.47573314508733944, 99.59235496188628645 ) ) ;
#13683=AXIS2_PLACEMENT_3D ( 'NONE', #30531, #41168, #11318 ) ;
#13684=ORIENTED_EDGE ( 'NONE', *, *, #32982, .F. ) ;
#13685=DIRECTION ( 'NONE',  ( 0.000000000000000000, 0.000000000000000000, 1.000000000000000000 ) ) ;
#13686=CIRCLE ( 'NONE', #33838, 58.99999999999999289 ) ;
#13689=CARTESIAN_POINT ( 'NONE',  ( 0.000000000000000000, 0.000000000000000000, 0.000000000000000000 ) ) ;
#13690=DIRECTION ( 'NONE',  ( 1.000000000000000000, 0.000000000000000000, 0.000000000000000000 ) ) ;
#13697=EDGE_CURVE ( 'NONE', #22079, #21461, #16934, .T. ) ;
#13698=DIRECTION ( 'NONE',  ( 1.000000000000000000, -0.000000000000000000, -0.000000000000000000 ) ) ;
#13699=AXIS2_PLACEMENT_3D ( 'NONE', #17721, #30992, #31435 ) ;
#13702=VERTEX_POINT ( 'NONE', #10791 ) ;
#13703=DIRECTION ( 'NONE',  ( -1.000000000000000000, 0.000000000000000000, 0.000000000000000000 ) ) ;
#13706=CYLINDRICAL_SURFACE ( 'NONE', #21652, 59.00000000000000000 ) ;
#13707=EDGE_CURVE ( 'NONE', #14373, #40885, #27824, .T. ) ;
#13708=ORIENTED_EDGE ( 'NONE', *, *, #17174, .F. ) ;
#13710=VERTEX_POINT ( 'NONE', #30655 ) ;
#13711=DIRECTION ( 'NONE',  ( -1.000000000000000000, -0.000000000000000000, 0.000000000000000000 ) ) ;
#13713=CARTESIAN_POINT ( 'NONE',  ( 0.000000000000000000, 12.43843445475317822, 111.5058645182329968 ) ) ;
#13718=CIRCLE ( 'NONE', #42231, 58.99999999999998579 ) ;
#13720=CIRCLE ( 'NONE', #24898, 120.5010000000000474 ) ;
#13723=VECTOR ( 'NONE', #8630, 1000.000000000000000 ) ;
#13726=VERTEX_POINT ( 'NONE', #11231 ) ;
#13727=LINE ( 'NONE', #13505, #24844 ) ;
#13728=CYLINDRICAL_SURFACE ( 'NONE', #11336, 59.00000000000000000 ) ;
#13729=AXIS2_PLACEMENT_3D ( 'NONE', #42641, #22424, #6227 ) ;
#13730=ORIENTED_EDGE ( 'NONE', *, *, #14202, .T. ) ;
#13732=DIRECTION ( 'NONE',  ( -1.000000000000000000, -0.000000000000000000, -0.000000000000000000 ) ) ;
#13733=ORIENTED_EDGE ( 'NONE', *, *, #7219, .T. ) ;
#13735=ADVANCED_FACE ( 'NONE', ( #519 ), #30437, .F. ) ;
#13736=ORIENTED_EDGE ( 'NONE', *, *, #23973, .T. ) ;
#13742=LINE ( 'NONE', #34417, #21992 ) ;
#13745=DIRECTION ( 'NONE',  ( 0.000000000000000000, 0.000000000000000000, 1.000000000000000000 ) ) ;
#13746=CARTESIAN_POINT ( 'NONE',  ( 0.000000000000000000, 107.5680526044915410, 31.89649718262280231 ) ) ;
#13749=CARTESIAN_POINT ( 'NONE',  ( 0.000000000000000000, 63.55543939553896848, -97.03971415477259654 ) ) ;
#13758=VERTEX_POINT ( 'NONE', #3561 ) ;
#13765=CARTESIAN_POINT ( 'NONE',  ( 0.000000000000000000, 0.000000000000000000, 0.000000000000000000 ) ) ;
#13766=DIRECTION ( 'NONE',  ( 0.000000000000000000, 0.000000000000000000, 1.000000000000000000 ) ) ;
#13767=ADVANCED_FACE ( 'NONE', ( #277 ), #18454, .F. ) ;
#13770=CYLINDRICAL_SURFACE ( 'NONE', #9790, 120.5010000000000190 ) ;
#13774=CARTESIAN_POINT ( 'NONE',  ( 0.000000000000000000, -40.37724737309996215, -104.6802291180871265 ) ) ;
#13775=CARTESIAN_POINT ( 'NONE',  ( 0.000000000000000000, 0.000000000000000000, 0.000000000000000000 ) ) ;
#13777=CIRCLE ( 'NONE', #5381, 116.0000000000000000 ) ;
#13778=CYLINDRICAL_SURFACE ( 'NONE', #2907, 120.5010000000000190 ) ;
#13780=EDGE_LOOP ( 'NONE', ( #18418, #2473, #14084, #36482 ) ) ;
#13781=CARTESIAN_POINT ( 'NONE',  ( 9.000000000000001776, 25.18647942089895153, -113.2326863338525271 ) ) ;
#13786=LINE ( 'NONE', #21209, #28138 ) ;
#13787=VERTEX_POINT ( 'NONE', #21733 ) ;
#13788=AXIS2_PLACEMENT_3D ( 'NONE', #25268, #32203, #25898 ) ;
#13790=VECTOR ( 'NONE', #34793, 1000.000000000000000 ) ;
#13791=EDGE_CURVE ( 'NONE', #24778, #32443, #31510, .T. ) ;
#13793=ORIENTED_EDGE ( 'NONE', *, *, #29946, .F. ) ;
#13802=DIRECTION ( 'NONE',  ( 0.000000000000000000, 0.000000000000000000, 1.000000000000000000 ) ) ;
#13804=DIRECTION ( 'NONE',  ( 0.000000000000000000, 0.000000000000000000, -1.000000000000000000 ) ) ;
#13811=ORIENTED_EDGE ( 'NONE', *, *, #32788, .F. ) ;
#13815=ORIENTED_EDGE ( 'NONE', *, *, #8445, .T. ) ;
#13820=AXIS2_PLACEMENT_3D ( 'NONE', #17501, #27083, #10482 ) ;
#13821=EDGE_CURVE ( 'NONE', #6418, #28542, #38726, .T. ) ;
#13824=FACE_OUTER_BOUND ( 'NONE', #40727, .T. ) ;
#13831=CARTESIAN_POINT ( 'NONE',  ( 9.000000000000001776, -113.8630351447207119, 22.16324045874372572 ) ) ;
#13832=CARTESIAN_POINT ( 'NONE',  ( 17.99999999999999645, 84.62908780824989208, -85.78116633471202590 ) ) ;
#13834=CYLINDRICAL_SURFACE ( 'NONE', #23566, 59.00000000000000000 ) ;
#13836=ORIENTED_EDGE ( 'NONE', *, *, #33121, .T. ) ;
#13837=CYLINDRICAL_SURFACE ( 'NONE', #4689, 120.5010000000000190 ) ;
#13839=CARTESIAN_POINT ( 'NONE',  ( 17.99999999999999645, 119.8996782608631406, -12.02323392193236629 ) ) ;
#13840=ORIENTED_EDGE ( 'NONE', *, *, #9099, .T. ) ;
#13841=DIRECTION ( 'NONE',  ( 0.000000000000000000, 0.05322217484217877520, -0.9985826956767620555 ) ) ;
#13842=VERTEX_POINT ( 'NONE', #14951 ) ;
#13846=CIRCLE ( 'NONE', #28456, 58.99999999999999289 ) ;
#13848=AXIS2_PLACEMENT_3D ( 'NONE', #10255, #6971, #7183 ) ;
#13849=EDGE_CURVE ( 'NONE', #13442, #42855, #28254, .T. ) ;
#13854=ADVANCED_FACE ( 'NONE', ( #41950 ), #41519, .F. ) ;
#13859=CARTESIAN_POINT ( 'NONE',  ( 17.99999999999999645, 71.21168426767107462, 86.70160608319346807 ) ) ;
#13860=CARTESIAN_POINT ( 'NONE',  ( 0.000000000000000000, 0.000000000000000000, 0.000000000000000000 ) ) ;
#13861=CARTESIAN_POINT ( 'NONE',  ( 9.000000000000001776, -114.8812324315174038, -16.07179003769264369 ) ) ;
#13862=ORIENTED_EDGE ( 'NONE', *, *, #21843, .F. ) ;
#13863=CARTESIAN_POINT ( 'NONE',  ( 0.000000000000000000, -29.86146780999875716, -112.0905559814581665 ) ) ;
#13871=VERTEX_POINT ( 'NONE', #35414 ) ;
#13873=DIRECTION ( 'NONE',  ( 0.000000000000000000, 0.000000000000000000, 1.000000000000000000 ) ) ;
#13875=FACE_OUTER_BOUND ( 'NONE', #21794, .T. ) ;
#13876=EDGE_CURVE ( 'NONE', #9442, #28845, #32508, .T. ) ;
#13877=CIRCLE ( 'NONE', #20875, 59.00000000000000000 ) ;
#13880=ORIENTED_EDGE ( 'NONE', *, *, #42114, .F. ) ;
#13883=DIRECTION ( 'NONE',  ( 0.000000000000000000, -0.8477344278896649099, -0.5304209081197521769 ) ) ;
#13884=ORIENTED_EDGE ( 'NONE', *, *, #35729, .F. ) ;
#13885=ORIENTED_EDGE ( 'NONE', *, *, #21887, .T. ) ;
#13887=CARTESIAN_POINT ( 'NONE',  ( 17.99999999999999645, -46.83041522348427321, -101.9567785075606139 ) ) ;
#13890=ORIENTED_EDGE ( 'NONE', *, *, #25378, .F. ) ;
#13894=DIRECTION ( 'NONE',  ( 0.000000000000000000, 0.9714298932647106311, -0.2373266998711118791 ) ) ;
#13905=CARTESIAN_POINT ( 'NONE',  ( 0.000000000000000000, -117.9424311864587480, -24.69967462999156282 ) ) ;
#13909=EDGE_CURVE ( 'NONE', #11189, #33175, #33190, .T. ) ;
#13911=DIRECTION ( 'NONE',  ( 0.000000000000000000, 0.000000000000000000, 1.000000000000000000 ) ) ;
#13912=LINE ( 'NONE', #4038, #12254 ) ;
#13914=DIRECTION ( 'NONE',  ( -1.000000000000000000, -0.000000000000000000, -0.000000000000000000 ) ) ;
#13915=VERTEX_POINT ( 'NONE', #14732 ) ;
#13917=ORIENTED_EDGE ( 'NONE', *, *, #18446, .F. ) ;
#13924=CARTESIAN_POINT ( 'NONE',  ( 0.000000000000000000, 0.000000000000000000, 0.000000000000000000 ) ) ;
#13926=CARTESIAN_POINT ( 'NONE',  ( 0.000000000000000000, 41.62036691425679180, -113.0850832732710529 ) ) ;
#13927=EDGE_LOOP ( 'NONE', ( #38627, #37270, #25739, #29730 ) ) ;
#13930=CARTESIAN_POINT ( 'NONE',  ( 0.000000000000000000, 0.000000000000000000, 0.000000000000000000 ) ) ;
#13931=AXIS2_PLACEMENT_3D ( 'NONE', #38917, #16244, #15820 ) ;
#13934=DIRECTION ( 'NONE',  ( 0.000000000000000000, 0.000000000000000000, 1.000000000000000000 ) ) ;
#13935=ORIENTED_EDGE ( 'NONE', *, *, #685, .T. ) ;
#13937=CIRCLE ( 'NONE', #17443, 120.5010000000000474 ) ;
#13942=LINE ( 'NONE', #7361, #9937 ) ;
#13945=EDGE_CURVE ( 'NONE', #24349, #39974, #8812, .T. ) ;
#13947=EDGE_LOOP ( 'NONE', ( #37921, #13175, #12897, #4626 ) ) ;
#13949=ORIENTED_EDGE ( 'NONE', *, *, #9584, .F. ) ;
#13951=CARTESIAN_POINT ( 'NONE',  ( 17.99999999999999645, 51.98489025774451733, -108.7109110710156159 ) ) ;
#13954=DIRECTION ( 'NONE',  ( 0.000000000000000000, -0.9911528310040084166, 0.1327255272837126743 ) ) ;
#13955=VERTEX_POINT ( 'NONE', #9220 ) ;
#13957=DIRECTION ( 'NONE',  ( 0.000000000000000000, 1.787647243040506224E-14, -1.000000000000000000 ) ) ;
#13958=EDGE_CURVE ( 'NONE', #15836, #287, #18618, .T. ) ;
#13959=ORIENTED_EDGE ( 'NONE', *, *, #32860, .T. ) ;
#13962=ADVANCED_FACE ( 'NONE', ( #33211 ), #5939, .F. ) ;
#13966=CARTESIAN_POINT ( 'NONE',  ( 17.99999999999999645, -57.40245293794732362, 96.40140491896615060 ) ) ;
#13967=CARTESIAN_POINT ( 'NONE',  ( 8.999999999999998224, -69.72480978690109055, 92.70626138605992139 ) ) ;
#13968=FACE_OUTER_BOUND ( 'NONE', #40907, .T. ) ;
#13974=DIRECTION ( 'NONE',  ( -1.000000000000000000, -0.000000000000000000, -0.000000000000000000 ) ) ;
#13975=AXIS2_PLACEMENT_3D ( 'NONE', #3659, #40097, #19450 ) ;
#13976=CARTESIAN_POINT ( 'NONE',  ( 0.000000000000000000, -71.21168426767047777, -86.70160608319397966 ) ) ;
#13977=ADVANCED_FACE ( 'NONE', ( #43016 ), #19087, .F. ) ;
#13981=DIRECTION ( 'NONE',  ( 1.000000000000000000, 0.000000000000000000, 0.000000000000000000 ) ) ;
#13982=ORIENTED_EDGE ( 'NONE', *, *, #22086, .T. ) ;
#13984=CYLINDRICAL_SURFACE ( 'NONE', #6240, 120.5010000000000190 ) ;
#13985=AXIS2_PLACEMENT_3D ( 'NONE', #3302, #36466, #40988 ) ;
#13990=DIRECTION ( 'NONE',  ( 1.000000000000000000, -0.000000000000000000, 0.000000000000000000 ) ) ;
#13993=ORIENTED_EDGE ( 'NONE', *, *, #41711, .F. ) ;
#13996=FACE_OUTER_BOUND ( 'NONE', #9470, .T. ) ;
#13997=ORIENTED_EDGE ( 'NONE', *, *, #24195, .F. ) ;
#13998=DIRECTION ( 'NONE',  ( 0.000000000000000000, 0.000000000000000000, 1.000000000000000000 ) ) ;
#13999=CARTESIAN_POINT ( 'NONE',  ( 17.99999999999999645, 114.8812324315175033, 16.07179003769187986 ) ) ;
#14002=EDGE_CURVE ( 'NONE', #39508, #41141, #10911, .T. ) ;
#14004=EDGE_LOOP ( 'NONE', ( #24206, #40583, #22569, #23313 ) ) ;
#14005=CARTESIAN_POINT ( 'NONE',  ( 17.99999999999999645, 120.2856157092986678, 7.201503623197233139 ) ) ;
#14008=CIRCLE ( 'NONE', #22780, 59.00000000000000000 ) ;
#14010=CARTESIAN_POINT ( 'NONE',  ( 0.000000000000000000, -78.18175027177490222, 85.69488855492974722 ) ) ;
#14012=CARTESIAN_POINT ( 'NONE',  ( 0.000000000000000000, 100.8494052988179561, -65.95368414178808791 ) ) ;
#14015=CARTESIAN_POINT ( 'NONE',  ( 17.99999999999999645, -110.3490479609630910, 38.71798610214488434 ) ) ;
#14018=ORIENTED_EDGE ( 'NONE', *, *, #27198, .F. ) ;
#14022=DIRECTION ( 'NONE',  ( -1.000000000000000000, 0.000000000000000000, 0.000000000000000000 ) ) ;
#14029=AXIS2_PLACEMENT_3D ( 'NONE', #3222, #9793, #13745 ) ;
#14032=DIRECTION ( 'NONE',  ( -1.000000000000000000, -0.000000000000000000, -0.000000000000000000 ) ) ;
#14037=VERTEX_POINT ( 'NONE', #42582 ) ;
#14044=CARTESIAN_POINT ( 'NONE',  ( 17.99999999999999645, -94.52951811191513798, -67.23221107124996365 ) ) ;
#14046=DIRECTION ( 'NONE',  ( 1.000000000000000000, -0.000000000000000000, -0.000000000000000000 ) ) ;
#14048=AXIS2_PLACEMENT_3D ( 'NONE', #6201, #35649, #12130 ) ;
#14051=VECTOR ( 'NONE', #16958, 1000.000000000000000 ) ;
#14053=CARTESIAN_POINT ( 'NONE',  ( 17.99999999999999645, -111.8797445107944100, -8.437727291343872338 ) ) ;
#14055=VECTOR ( 'NONE', #6780, 1000.000000000000000 ) ;
#14057=ORIENTED_EDGE ( 'NONE', *, *, #2892, .F. ) ;
#14060=EDGE_LOOP ( 'NONE', ( #31950, #24151, #15977, #37331 ) ) ;
#14063=ORIENTED_EDGE ( 'NONE', *, *, #10055, .F. ) ;
#14066=ADVANCED_FACE ( 'NONE', ( #3943 ), #17329, .F. ) ;
#14068=DIRECTION ( 'NONE',  ( 0.000000000000000000, -0.9911528310040057521, -0.1327255272837325473 ) ) ;
#14069=DIRECTION ( 'NONE',  ( -1.000000000000000000, 0.000000000000000000, 0.000000000000000000 ) ) ;
#14071=ORIENTED_EDGE ( 'NONE', *, *, #26825, .T. ) ;
#14073=CARTESIAN_POINT ( 'NONE',  ( 17.99999999999999645, 119.7318547011703629, -13.59315897125608430 ) ) ;
#14084=ORIENTED_EDGE ( 'NONE', *, *, #8389, .T. ) ;
#14086=DIRECTION ( 'NONE',  ( 1.000000000000000000, 0.000000000000000000, 0.000000000000000000 ) ) ;
#14087=ADVANCED_FACE ( 'NONE', ( #37121 ), #4163, .F. ) ;
#14090=EDGE_CURVE ( 'NONE', #27124, #22079, #23478, .T. ) ;
#14091=CIRCLE ( 'NONE', #802, 120.5010000000000474 ) ;
#14092=CARTESIAN_POINT ( 'NONE',  ( 17.99999999999999645, 112.8457601792519256, -26.86697618949260402 ) ) ;
#14096=VECTOR ( 'NONE', #10057, 1000.000000000000000 ) ;
#14098=LINE ( 'NONE', #17386, #17285 ) ;
#14099=LINE ( 'NONE', #37402, #38640 ) ;
#14100=VERTEX_POINT ( 'NONE', #33855 ) ;
#14102=LINE ( 'NONE', #10374, #31455 ) ;
#14103=CARTESIAN_POINT ( 'NONE',  ( 17.99999999999999645, -114.8812324315176312, 16.07179003769107339 ) ) ;
#14105=ORIENTED_EDGE ( 'NONE', *, *, #40000, .T. ) ;
#14106=CYLINDRICAL_SURFACE ( 'NONE', #5503, 59.00000000000000000 ) ;
#14109=DIRECTION ( 'NONE',  ( 0.000000000000000000, 0.000000000000000000, 1.000000000000000000 ) ) ;
#14111=ORIENTED_EDGE ( 'NONE', *, *, #26225, .T. ) ;
#14114=DIRECTION ( 'NONE',  ( -1.000000000000000000, -0.000000000000000000, -0.000000000000000000 ) ) ;
#14118=VECTOR ( 'NONE', #18155, 1000.000000000000000 ) ;
#14119=DIRECTION ( 'NONE',  ( -1.000000000000000000, 0.000000000000000000, 0.000000000000000000 ) ) ;
#14120=ORIENTED_EDGE ( 'NONE', *, *, #16228, .T. ) ;
#14121=LINE ( 'NONE', #24161, #7693 ) ;
#14122=ORIENTED_EDGE ( 'NONE', *, *, #19929, .F. ) ;
#14123=AXIS2_PLACEMENT_3D ( 'NONE', #33194, #34058, #17514 ) ;
#14124=CYLINDRICAL_SURFACE ( 'NONE', #19074, 116.0000000000000000 ) ;
#14125=DIRECTION ( 'NONE',  ( 1.000000000000000000, 0.000000000000000000, 0.000000000000000000 ) ) ;
#14127=DIRECTION ( 'NONE',  ( 0.000000000000000000, -0.4132121857683850874, 0.9106347728549100129 ) ) ;
#14129=DIRECTION ( 'NONE',  ( 0.000000000000000000, 0.9714298932647106311, -0.2373266998711118791 ) ) ;
#14134=DIRECTION ( 'NONE',  ( -1.000000000000000000, 0.000000000000000000, 0.000000000000000000 ) ) ;
#14140=ADVANCED_FACE ( 'NONE', ( #13824 ), #33426, .F. ) ;
#14147=CARTESIAN_POINT ( 'NONE',  ( 17.99999999999999645, 109.4038418350903470, 50.51029986767587587 ) ) ;
#14148=DIRECTION ( 'NONE',  ( 1.000000000000000000, -0.000000000000000000, -0.000000000000000000 ) ) ;
#14149=ORIENTED_EDGE ( 'NONE', *, *, #28857, .T. ) ;
#14152=CYLINDRICAL_SURFACE ( 'NONE', #7705, 59.00000000000000000 ) ;
#14154=LINE ( 'NONE', #31368, #12496 ) ;
#14155=VECTOR ( 'NONE', #34012, 1000.000000000000000 ) ;
#14157=EDGE_CURVE ( 'NONE', #5703, #12547, #436, .T. ) ;
#14170=DIRECTION ( 'NONE',  ( 0.000000000000000000, -0.7865515558026354714, -0.6175246149462008116 ) ) ;
#14171=LINE ( 'NONE', #26013, #25567 ) ;
#14172=ORIENTED_EDGE ( 'NONE', *, *, #30681, .F. ) ;
#14175=VERTEX_POINT ( 'NONE', #30168 ) ;
#14183=ADVANCED_FACE ( 'NONE', ( #1112 ), #10306, .F. ) ;
#14186=CARTESIAN_POINT ( 'NONE',  ( 9.000000000000001776, 0.6819280456844267757, -115.9979955608738607 ) ) ;
#14187=LINE ( 'NONE', #30553, #23570 ) ;
#14190=CIRCLE ( 'NONE', #24674, 59.00000000000000711 ) ;
#14191=DIRECTION ( 'NONE',  ( 0.000000000000000000, 0.7164567402983116340, 0.6976315211349882750 ) ) ;
#14193=LINE ( 'NONE', #13335, #6493 ) ;
#14194=CARTESIAN_POINT ( 'NONE',  ( 17.99999999999999645, 0.000000000000000000, 0.000000000000000000 ) ) ;
#14195=EDGE_CURVE ( 'NONE', #7227, #18461, #40384, .T. ) ;
#14196=AXIS2_PLACEMENT_3D ( 'NONE', #9610, #35989, #9378 ) ;
#14202=EDGE_CURVE ( 'NONE', #2350, #37579, #38113, .T. ) ;
#14203=CARTESIAN_POINT ( 'NONE',  ( 17.99999999999999645, 0.000000000000000000, 0.000000000000000000 ) ) ;
#14206=CARTESIAN_POINT ( 'NONE',  ( 0.000000000000000000, 51.98489025774302519, 108.7109110710163549 ) ) ;
#14214=LINE ( 'NONE', #17509, #8053 ) ;
#14229=DIRECTION ( 'NONE',  ( -1.000000000000000000, -0.000000000000000000, -0.000000000000000000 ) ) ;
#14231=DIRECTION ( 'NONE',  ( -1.000000000000000000, 0.000000000000000000, -0.000000000000000000 ) ) ;
#14233=DIRECTION ( 'NONE',  ( 0.000000000000000000, 0.000000000000000000, 1.000000000000000000 ) ) ;
#14238=CARTESIAN_POINT ( 'NONE',  ( 17.99999999999999645, 0.000000000000000000, 0.000000000000000000 ) ) ;
#14241=DIRECTION ( 'NONE',  ( -1.000000000000000000, -0.000000000000000000, -0.000000000000000000 ) ) ;
#14243=ORIENTED_EDGE ( 'NONE', *, *, #5799, .F. ) ;
#14245=EDGE_LOOP ( 'NONE', ( #9087, #26061, #6884, #1240 ) ) ;
#14254=DIRECTION ( 'NONE',  ( 1.000000000000000000, 0.000000000000000000, 0.000000000000000000 ) ) ;
#14256=CARTESIAN_POINT ( 'NONE',  ( 17.99999999999999645, 0.000000000000000000, 0.000000000000000000 ) ) ;
#14259=CARTESIAN_POINT ( 'NONE',  ( -10.00000000000000000, 0.000000000000000000, 0.000000000000000000 ) ) ;
#14262=EDGE_LOOP ( 'NONE', ( #35236, #7407, #40307, #26642 ) ) ;
#14266=EDGE_LOOP ( 'NONE', ( #6271, #11229, #24422, #33733 ) ) ;
#14267=AXIS2_PLACEMENT_3D ( 'NONE', #31450, #14670, #8095 ) ;
#14275=CIRCLE ( 'NONE', #33775, 116.0000000000000000 ) ;
#14278=VECTOR ( 'NONE', #29314, 1000.000000000000000 ) ;
#14285=AXIS2_PLACEMENT_3D ( 'NONE', #11459, #24795, #25025 ) ;
#14286=EDGE_LOOP ( 'NONE', ( #15240, #6254, #3977, #7752 ) ) ;
#14292=ADVANCED_FACE ( 'NONE', ( #21244 ), #7883, .F. ) ;
#14293=ORIENTED_EDGE ( 'NONE', *, *, #3912, .T. ) ;
#14298=EDGE_CURVE ( 'NONE', #31074, #32443, #24934, .T. ) ;
#14300=CIRCLE ( 'NONE', #1026, 59.00000000000000000 ) ;
#14303=EDGE_CURVE ( 'NONE', #13702, #11934, #25603, .T. ) ;
#14305=DIRECTION ( 'NONE',  ( 0.000000000000000000, 0.000000000000000000, 1.000000000000000000 ) ) ;
#14306=VECTOR ( 'NONE', #1359, 1000.000000000000000 ) ;
#14307=FACE_OUTER_BOUND ( 'NONE', #15263, .T. ) ;
#14311=ORIENTED_EDGE ( 'NONE', *, *, #10418, .T. ) ;
#14318=AXIS2_PLACEMENT_3D ( 'NONE', #36919, #23661, #32791 ) ;
#14322=EDGE_CURVE ( 'NONE', #21257, #29613, #25365, .T. ) ;
#14325=ADVANCED_FACE ( 'NONE', ( #5042 ), #22103, .F. ) ;
#14326=EDGE_CURVE ( 'NONE', #40263, #1932, #16534, .T. ) ;
#14328=ORIENTED_EDGE ( 'NONE', *, *, #1659, .F. ) ;
#14329=VERTEX_POINT ( 'NONE', #41695 ) ;
#14331=CARTESIAN_POINT ( 'NONE',  ( 17.99999999999999645, -2.418575551220017328, -120.4767259403369053 ) ) ;
#14332=DIRECTION ( 'NONE',  ( 0.000000000000000000, 0.000000000000000000, 1.000000000000000000 ) ) ;
#14337=AXIS2_PLACEMENT_3D ( 'NONE', #14671, #11384, #8096 ) ;
#14344=CARTESIAN_POINT ( 'NONE',  ( 17.99999999999999645, 34.03109950475885626, -115.5957406979046596 ) ) ;
#14345=CIRCLE ( 'NONE', #17859, 58.99999999999999289 ) ;
#14351=EDGE_CURVE ( 'NONE', #6315, #18244, #38206, .T. ) ;
#14352=ORIENTED_EDGE ( 'NONE', *, *, #33507, .F. ) ;
#14355=DIRECTION ( 'NONE',  ( -1.000000000000000000, 0.000000000000000000, 0.000000000000000000 ) ) ;
#14359=CARTESIAN_POINT ( 'NONE',  ( 17.99999999999999645, 0.000000000000000000, 0.000000000000000000 ) ) ;
#14360=EDGE_LOOP ( 'NONE', ( #8583, #42875, #8069, #24738 ) ) ;
#14367=CIRCLE ( 'NONE', #24862, 59.00000000000000000 ) ;
#14370=VECTOR ( 'NONE', #3122, 1000.000000000000000 ) ;
#14373=VERTEX_POINT ( 'NONE', #21679 ) ;
#14377=EDGE_CURVE ( 'NONE', #36486, #42699, #11835, .T. ) ;
#14381=EDGE_CURVE ( 'NONE', #16155, #25554, #26265, .T. ) ;
#14388=CIRCLE ( 'NONE', #38736, 116.0000000000000000 ) ;
#14390=DIRECTION ( 'NONE',  ( -1.000000000000000000, -0.000000000000000000, -0.000000000000000000 ) ) ;
#14393=DIRECTION ( 'NONE',  ( 0.000000000000000000, -0.5528000653611833126, -0.8333139190825216147 ) ) ;
#14394=CARTESIAN_POINT ( 'NONE',  ( 0.000000000000000000, 0.000000000000000000, 0.000000000000000000 ) ) ;
#14396=CARTESIAN_POINT ( 'NONE',  ( 0.000000000000000000, 0.000000000000000000, 0.000000000000000000 ) ) ;
#14398=EDGE_CURVE ( 'NONE', #8366, #28381, #25584, .T. ) ;
#14404=CIRCLE ( 'NONE', #23475, 59.00000000000000000 ) ;
#14405=AXIS2_PLACEMENT_3D ( 'NONE', #20425, #23481, #13873 ) ;
#14408=CARTESIAN_POINT ( 'NONE',  ( 17.99999999999999645, 73.51007459736548810, -89.73443560133290475 ) ) ;
#14410=CARTESIAN_POINT ( 'NONE',  ( 17.99999999999999645, -119.0898412705473532, -18.38751498043852806 ) ) ;
#14412=CARTESIAN_POINT ( 'NONE',  ( 0.000000000000000000, 41.60679253225764285, 108.2814610871947423 ) ) ;
#14419=DIRECTION ( 'NONE',  ( 1.000000000000000000, 0.000000000000000000, 0.000000000000000000 ) ) ;
#14420=ORIENTED_EDGE ( 'NONE', *, *, #5313, .T. ) ;
#14421=LINE ( 'NONE', #27731, #5705 ) ;
#14423=AXIS2_PLACEMENT_3D ( 'NONE', #16270, #26303, #41397 ) ;
#14426=VERTEX_POINT ( 'NONE', #42733 ) ;
#14427=LINE ( 'NONE', #423, #26040 ) ;
#14428=VERTEX_POINT ( 'NONE', #5888 ) ;
#14429=FACE_OUTER_BOUND ( 'NONE', #3633, .T. ) ;
#14434=CARTESIAN_POINT ( 'NONE',  ( 17.99999999999999645, -45.89132998247981732, -102.3829004574634496 ) ) ;
#14435=EDGE_CURVE ( 'NONE', #22146, #19271, #9560, .T. ) ;
#14436=DIRECTION ( 'NONE',  ( 1.000000000000000000, 0.000000000000000000, 0.000000000000000000 ) ) ;
#14440=AXIS2_PLACEMENT_3D ( 'NONE', #39046, #22523, #19245 ) ;
#14442=DIRECTION ( 'NONE',  ( 0.000000000000000000, -1.246648735278247733E-14, -1.000000000000000000 ) ) ;
#14443=FACE_OUTER_BOUND ( 'NONE', #41889, .T. ) ;
#14444=CIRCLE ( 'NONE', #12323, 59.00000000000000000 ) ;
#14450=AXIS2_PLACEMENT_3D ( 'NONE', #29892, #10219, #39224 ) ;
#14455=CARTESIAN_POINT ( 'NONE',  ( 0.000000000000000000, 108.8880088604282008, -39.99251838045848473 ) ) ;
#14456=AXIS2_PLACEMENT_3D ( 'NONE', #36940, #40206, #47 ) ;
#14457=EDGE_CURVE ( 'NONE', #5006, #6315, #20752, .T. ) ;
#14463=CARTESIAN_POINT ( 'NONE',  ( -10.00000000000000000, 0.000000000000000000, 0.000000000000000000 ) ) ;
#14465=CIRCLE ( 'NONE', #42971, 120.5010000000000190 ) ;
#14468=CIRCLE ( 'NONE', #30497, 120.5010000000000332 ) ;
#14475=AXIS2_PLACEMENT_3D ( 'NONE', #18301, #21793, #35041 ) ;
#14480=DIRECTION ( 'NONE',  ( -1.000000000000000000, 0.000000000000000000, 0.000000000000000000 ) ) ;
#14482=DIRECTION ( 'NONE',  ( -1.000000000000000000, -0.000000000000000000, -0.000000000000000000 ) ) ;
#14484=ORIENTED_EDGE ( 'NONE', *, *, #1041, .T. ) ;
#14486=DIRECTION ( 'NONE',  ( 0.000000000000000000, 0.000000000000000000, 1.000000000000000000 ) ) ;
#14489=FACE_OUTER_BOUND ( 'NONE', #7839, .T. ) ;
#14490=EDGE_CURVE ( 'NONE', #30129, #38244, #2554, .T. ) ;
#14493=VERTEX_POINT ( 'NONE', #25787 ) ;
#14494=LINE ( 'NONE', #28653, #21774 ) ;
#14498=DIRECTION ( 'NONE',  ( -1.000000000000000000, 0.000000000000000000, -0.000000000000000000 ) ) ;
#14500=CYLINDRICAL_SURFACE ( 'NONE', #29005, 116.0000000000000000 ) ;
#14502=CIRCLE ( 'NONE', #1228, 59.00000000000002132 ) ;
#14503=ORIENTED_EDGE ( 'NONE', *, *, #25789, .F. ) ;
#14505=AXIS2_PLACEMENT_3D ( 'NONE', #9827, #36217, #32741 ) ;
#14507=LINE ( 'NONE', #18442, #21982 ) ;
#14508=ADVANCED_FACE ( 'NONE', ( #15538 ), #28834, .F. ) ;
#14512=VERTEX_POINT ( 'NONE', #8966 ) ;
#14516=VECTOR ( 'NONE', #29398, 1000.000000000000000 ) ;
#14517=ORIENTED_EDGE ( 'NONE', *, *, #6996, .T. ) ;
#14518=CARTESIAN_POINT ( 'NONE',  ( -10.00000000000000000, 0.000000000000000000, 0.000000000000000000 ) ) ;
#14520=DIRECTION ( 'NONE',  ( -1.000000000000000000, -0.000000000000000000, -0.000000000000000000 ) ) ;
#14522=ORIENTED_EDGE ( 'NONE', *, *, #34277, .F. ) ;
#14526=EDGE_CURVE ( 'NONE', #31565, #20200, #8160, .T. ) ;
#14528=ADVANCED_FACE ( 'NONE', ( #32298 ), #29262, .F. ) ;
#14530=DIRECTION ( 'NONE',  ( -1.000000000000000000, -0.000000000000000000, -0.000000000000000000 ) ) ;
#14532=ORIENTED_EDGE ( 'NONE', *, *, #16170, .T. ) ;
#14534=CARTESIAN_POINT ( 'NONE',  ( 17.99999999999999645, 0.000000000000000000, 0.000000000000000000 ) ) ;
#14538=AXIS2_PLACEMENT_3D ( 'NONE', #36024, #32131, #12082 ) ;
#14539=CIRCLE ( 'NONE', #27076, 116.0000000000000000 ) ;
#14544=CARTESIAN_POINT ( 'NONE',  ( 0.000000000000000000, -82.63181128086789329, 81.41243003646944487 ) ) ;
#14546=EDGE_CURVE ( 'NONE', #21330, #28092, #32516, .T. ) ;
#14549=VERTEX_POINT ( 'NONE', #13926 ) ;
#14553=EDGE_CURVE ( 'NONE', #22175, #10037, #40705, .T. ) ;
#14555=DIRECTION ( 'NONE',  ( 1.000000000000000000, 0.000000000000000000, 0.000000000000000000 ) ) ;
#14559=DIRECTION ( 'NONE',  ( 1.000000000000000000, 0.000000000000000000, 0.000000000000000000 ) ) ;
#14560=ADVANCED_FACE ( 'NONE', ( #41356 ), #34388, .F. ) ;
#14563=CARTESIAN_POINT ( 'NONE',  ( 8.999999999999998224, 59.47573314508868236, -99.59235496188547643 ) ) ;
#14564=CIRCLE ( 'NONE', #42391, 120.5010000000000332 ) ;
#14567=AXIS2_PLACEMENT_3D ( 'NONE', #18899, #39309, #12533 ) ;
#14568=CARTESIAN_POINT ( 'NONE',  ( 8.999999999999998224, 82.63181128086732485, 81.41243003647002752 ) ) ;
#14569=VERTEX_POINT ( 'NONE', #21585 ) ;
#14571=ORIENTED_EDGE ( 'NONE', *, *, #10667, .F. ) ;
#14572=DIRECTION ( 'NONE',  ( 1.000000000000000000, 0.000000000000000000, 0.000000000000000000 ) ) ;
#14576=DIRECTION ( 'NONE',  ( 0.000000000000000000, 0.000000000000000000, 1.000000000000000000 ) ) ;
#14577=ORIENTED_EDGE ( 'NONE', *, *, #28483, .T. ) ;
#14580=DIRECTION ( 'NONE',  ( 0.000000000000000000, 0.000000000000000000, 1.000000000000000000 ) ) ;
#14581=DIRECTION ( 'NONE',  ( -1.000000000000000000, 0.000000000000000000, 0.000000000000000000 ) ) ;
#14585=ORIENTED_EDGE ( 'NONE', *, *, #32103, .T. ) ;
#14586=DIRECTION ( 'NONE',  ( 0.000000000000000000, 0.3641605752528167539, 0.9313361774523405412 ) ) ;
#14588=CYLINDRICAL_SURFACE ( 'NONE', #39081, 59.00000000000000000 ) ;
#14595=AXIS2_PLACEMENT_3D ( 'NONE', #40294, #23763, #20717 ) ;
#14597=DIRECTION ( 'NONE',  ( 0.000000000000000000, 0.000000000000000000, 1.000000000000000000 ) ) ;
#14599=ORIENTED_EDGE ( 'NONE', *, *, #20848, .T. ) ;
#14603=DIRECTION ( 'NONE',  ( 1.000000000000000000, 0.000000000000000000, 0.000000000000000000 ) ) ;
#14606=DIRECTION ( 'NONE',  ( -1.000000000000000000, 0.000000000000000000, 0.000000000000000000 ) ) ;
#14607=DIRECTION ( 'NONE',  ( 1.000000000000000000, 0.000000000000000000, 0.000000000000000000 ) ) ;
#14612=EDGE_CURVE ( 'NONE', #16671, #6774, #18682, .T. ) ;
#14613=CYLINDRICAL_SURFACE ( 'NONE', #40562, 59.00000000000001421 ) ;
#14617=VERTEX_POINT ( 'NONE', #7994 ) ;
#14618=DIRECTION ( 'NONE',  ( 0.000000000000000000, 0.000000000000000000, 1.000000000000000000 ) ) ;
#14619=DIRECTION ( 'NONE',  ( 1.000000000000000000, 0.000000000000000000, 0.000000000000000000 ) ) ;
#14620=CARTESIAN_POINT ( 'NONE',  ( 0.000000000000000000, 61.59243992711459015, 93.77976230226062171 ) ) ;
#14624=VECTOR ( 'NONE', #33495, 1000.000000000000000 ) ;
#14627=VECTOR ( 'NONE', #42537, 1000.000000000000000 ) ;
#14630=CARTESIAN_POINT ( 'NONE',  ( 0.000000000000000000, 0.000000000000000000, 0.000000000000000000 ) ) ;
#14634=EDGE_CURVE ( 'NONE', #17487, #41070, #6775, .T. ) ;
#14635=DIRECTION ( 'NONE',  ( -1.000000000000000000, 0.000000000000000000, -0.000000000000000000 ) ) ;
#14638=CARTESIAN_POINT ( 'NONE',  ( 0.000000000000000000, -109.4038418350907023, 50.51029986767514401 ) ) ;
#14642=CARTESIAN_POINT ( 'NONE',  ( 17.99999999999999645, 117.9424311864592312, -24.69967462998914698 ) ) ;
#14646=ORIENTED_EDGE ( 'NONE', *, *, #6662, .T. ) ;
#14647=CARTESIAN_POINT ( 'NONE',  ( 17.99999999999999645, -112.1427988504408120, 3.502162136923045566 ) ) ;
#14649=DIRECTION ( 'NONE',  ( 1.000000000000000000, 0.000000000000000000, -0.000000000000000000 ) ) ;
#14651=VERTEX_POINT ( 'NONE', #37453 ) ;
#14652=DIRECTION ( 'NONE',  ( 0.000000000000000000, 0.8183027759081702435, -0.5747874102144051589 ) ) ;
#14656=CIRCLE ( 'NONE', #20237, 59.00000000000000711 ) ;
#14657=DIRECTION ( 'NONE',  ( 0.000000000000000000, 0.000000000000000000, 1.000000000000000000 ) ) ;
#14658=DIRECTION ( 'NONE',  ( -1.000000000000000000, 0.000000000000000000, -0.000000000000000000 ) ) ;
#14659=EDGE_LOOP ( 'NONE', ( #3412, #34790, #21364, #26270 ) ) ;
#14663=CARTESIAN_POINT ( 'NONE',  ( 17.99999999999999645, -93.26762629039376407, -76.29967815892449323 ) ) ;
#14665=ORIENTED_EDGE ( 'NONE', *, *, #3431, .T. ) ;
#14667=CYLINDRICAL_SURFACE ( 'NONE', #18399, 120.5010000000000190 ) ;
#14670=DIRECTION ( 'NONE',  ( -1.000000000000000000, -0.000000000000000000, -0.000000000000000000 ) ) ;
#14671=CARTESIAN_POINT ( 'NONE',  ( 0.000000000000000000, -51.27532863109303918, -99.79535634195178773 ) ) ;
#14674=CYLINDRICAL_SURFACE ( 'NONE', #19928, 120.5010000000000190 ) ;
#14677=CIRCLE ( 'NONE', #40415, 120.5010000000000190 ) ;
#14680=DIRECTION ( 'NONE',  ( 0.000000000000000000, 0.9968120070307504577, -0.07978610555307970309 ) ) ;
#14682=EDGE_CURVE ( 'NONE', #14651, #1613, #17295, .T. ) ;
#14683=AXIS2_PLACEMENT_3D ( 'NONE', #27724, #21852, #18578 ) ;
#14685=DIRECTION ( 'NONE',  ( 0.000000000000000000, 0.000000000000000000, 1.000000000000000000 ) ) ;
#14689=ORIENTED_EDGE ( 'NONE', *, *, #17846, .T. ) ;
#14691=DIRECTION ( 'NONE',  ( 0.000000000000000000, 0.8183027759081701324, -0.5747874102144052699 ) ) ;
#14692=VERTEX_POINT ( 'NONE', #12153 ) ;
#14695=EDGE_LOOP ( 'NONE', ( #27651, #26561, #39131, #23138 ) ) ;
#14698=ADVANCED_FACE ( 'NONE', ( #38311 ), #29168, .F. ) ;
#14705=DIRECTION ( 'NONE',  ( -1.000000000000000000, -0.000000000000000000, -0.000000000000000000 ) ) ;
#14707=CARTESIAN_POINT ( 'NONE',  ( 0.000000000000000000, 29.36437154451999376, 116.8684075565137164 ) ) ;
#14708=ORIENTED_EDGE ( 'NONE', *, *, #25467, .T. ) ;
#14712=AXIS2_PLACEMENT_3D ( 'NONE', #9085, #39173, #22440 ) ;
#14715=CIRCLE ( 'NONE', #2809, 58.99999999999999289 ) ;
#14716=CARTESIAN_POINT ( 'NONE',  ( 17.99999999999999645, 6.854627147200274884, -115.7972974066012881 ) ) ;
#14717=CYLINDRICAL_SURFACE ( 'NONE', #26993, 58.99999999999998579 ) ;
#14718=AXIS2_PLACEMENT_3D ( 'NONE', #20714, #28545, #21802 ) ;
#14720=ADVANCED_FACE ( 'NONE', ( #22421 ), #8431, .F. ) ;
#14721=DIRECTION ( 'NONE',  ( -1.000000000000000000, 0.000000000000000000, 0.000000000000000000 ) ) ;
#14722=ORIENTED_EDGE ( 'NONE', *, *, #18791, .F. ) ;
#14728=VERTEX_POINT ( 'NONE', #1656 ) ;
#14730=ORIENTED_EDGE ( 'NONE', *, *, #14002, .F. ) ;
#14732=CARTESIAN_POINT ( 'NONE',  ( 0.000000000000000000, 0.000000000000000000, 130.0000000000000000 ) ) ;
#14735=EDGE_CURVE ( 'NONE', #39353, #32376, #32566, .T. ) ;
#14736=DIRECTION ( 'NONE',  ( 0.000000000000000000, 0.000000000000000000, 1.000000000000000000 ) ) ;
#14737=VECTOR ( 'NONE', #2688, 1000.000000000000000 ) ;
#14738=ORIENTED_EDGE ( 'NONE', *, *, #42848, .T. ) ;
#14740=VERTEX_POINT ( 'NONE', #38738 ) ;
#14741=DIRECTION ( 'NONE',  ( 1.000000000000000000, 0.000000000000000000, 0.000000000000000000 ) ) ;
#14743=CARTESIAN_POINT ( 'NONE',  ( 0.000000000000000000, -100.6739960869721102, 49.52796165323228195 ) ) ;
#14745=EDGE_CURVE ( 'NONE', #17370, #28827, #29787, .T. ) ;
#14746=DIRECTION ( 'NONE',  ( 0.000000000000000000, -0.9213119778704165208, 0.3888241754733123834 ) ) ;
#14748=CARTESIAN_POINT ( 'NONE',  ( 17.99999999999999645, 88.56657216608614647, 68.87840567545953263 ) ) ;
#14749=VERTEX_POINT ( 'NONE', #12373 ) ;
#14750=ORIENTED_EDGE ( 'NONE', *, *, #25812, .F. ) ;
#14751=FACE_OUTER_BOUND ( 'NONE', #4477, .T. ) ;
#14752=FACE_OUTER_BOUND ( 'NONE', #29544, .T. ) ;
#14753=ADVANCED_FACE ( 'NONE', ( #34830 ), #8863, .F. ) ;
#14754=CIRCLE ( 'NONE', #39088, 116.0000000000000000 ) ;
#14758=EDGE_CURVE ( 'NONE', #11646, #17236, #8197, .T. ) ;
#14760=DIRECTION ( 'NONE',  ( 0.000000000000000000, 0.000000000000000000, 1.000000000000000000 ) ) ;
#14761=DIRECTION ( 'NONE',  ( 1.000000000000000000, 0.000000000000000000, 0.000000000000000000 ) ) ;
#14762=DIRECTION ( 'NONE',  ( 1.000000000000000000, 0.000000000000000000, 0.000000000000000000 ) ) ;
#14763=VERTEX_POINT ( 'NONE', #35673 ) ;
#14766=CARTESIAN_POINT ( 'NONE',  ( 17.99999999999999645, -107.5680526044921947, 31.89649718262059608 ) ) ;
#14767=DIRECTION ( 'NONE',  ( 1.000000000000000000, 0.000000000000000000, 0.000000000000000000 ) ) ;
#14771=ORIENTED_EDGE ( 'NONE', *, *, #4982, .F. ) ;
#14772=PRESENTATION_STYLE_ASSIGNMENT (( #1421 ) ) ;
#14779=ADVANCED_FACE ( 'NONE', ( #31564 ), #32413, .F. ) ;
#14780=DIRECTION ( 'NONE',  ( 1.000000000000000000, -0.000000000000000000, 0.000000000000000000 ) ) ;
#14781=ORIENTED_EDGE ( 'NONE', *, *, #22481, .F. ) ;
#14783=CIRCLE ( 'NONE', #16171, 59.00000000000001421 ) ;
#14784=ORIENTED_EDGE ( 'NONE', *, *, #26874, .F. ) ;
#14789=DIRECTION ( 'NONE',  ( 1.000000000000000000, 0.000000000000000000, 0.000000000000000000 ) ) ;
#14790=EDGE_CURVE ( 'NONE', #13665, #22361, #38146, .T. ) ;
#14792=DIRECTION ( 'NONE',  ( -1.000000000000000000, -0.000000000000000000, -0.000000000000000000 ) ) ;
#14794=DIRECTION ( 'NONE',  ( 0.000000000000000000, -0.6783118362696222148, 0.7347741508630615259 ) ) ;
#14795=DIRECTION ( 'NONE',  ( 0.000000000000000000, 0.000000000000000000, 1.000000000000000000 ) ) ;
#14798=CARTESIAN_POINT ( 'NONE',  ( 17.99999999999999645, 63.24564713401931471, -102.5693868539688651 ) ) ;
#14801=EDGE_CURVE ( 'NONE', #20222, #32977, #10269, .T. ) ;
#14804=VECTOR ( 'NONE', #20563, 1000.000000000000000 ) ;
#14811=CARTESIAN_POINT ( 'NONE',  ( 0.000000000000000000, -25.18647942089817349, 113.2326863338526977 ) ) ;
#14813=CARTESIAN_POINT ( 'NONE',  ( 17.99999999999999645, 0.000000000000000000, 0.000000000000000000 ) ) ;
#14814=ORIENTED_EDGE ( 'NONE', *, *, #31274, .T. ) ;
#14815=DIRECTION ( 'NONE',  ( 0.000000000000000000, 0.000000000000000000, 1.000000000000000000 ) ) ;
#14819=DIRECTION ( 'NONE',  ( 0.000000000000000000, 0.2113826236296182937, 0.9774033898178680069 ) ) ;
#14820=DIRECTION ( 'NONE',  ( 0.000000000000000000, 0.000000000000000000, 1.000000000000000000 ) ) ;
#14823=DIRECTION ( 'NONE',  ( -1.000000000000000000, 0.000000000000000000, 0.000000000000000000 ) ) ;
#14825=ADVANCED_FACE ( 'NONE', ( #31790 ), #1877, .F. ) ;
#14827=CARTESIAN_POINT ( 'NONE',  ( 17.99999999999999645, 29.86146781000101669, -112.0905559814575696 ) ) ;
#14831=DIRECTION ( 'NONE',  ( 0.000000000000000000, -0.6783118362696075598, -0.7347741508630751817 ) ) ;
#14833=DIRECTION ( 'NONE',  ( -1.000000000000000000, 0.000000000000000000, 0.000000000000000000 ) ) ;
#14836=AXIS2_PLACEMENT_3D ( 'NONE', #4029, #3382, #30245 ) ;
#14841=EDGE_CURVE ( 'NONE', #3472, #34324, #16282, .T. ) ;
#14842=ORIENTED_EDGE ( 'NONE', *, *, #40197, .F. ) ;
#14847=DIRECTION ( 'NONE',  ( 0.000000000000000000, 0.1062934856473589651, 0.9943348002101377592 ) ) ;
#14855=VERTEX_POINT ( 'NONE', #35879 ) ;
#14857=CARTESIAN_POINT ( 'NONE',  ( 9.000000000000001776, -11.65176648920959757, -115.4133282497343487 ) ) ;
#14859=ORIENTED_EDGE ( 'NONE', *, *, #39407, .T. ) ;
#14865=LINE ( 'NONE', #28165, #35538 ) ;
#14866=CARTESIAN_POINT ( 'NONE',  ( 17.99999999999999645, 0.000000000000000000, 0.000000000000000000 ) ) ;
#14867=ORIENTED_EDGE ( 'NONE', *, *, #17366, .T. ) ;
#14868=AXIS2_PLACEMENT_3D ( 'NONE', #28963, #12593, #25910 ) ;
#14870=CARTESIAN_POINT ( 'NONE',  ( 17.99999999999999645, 0.000000000000000000, 130.0000000000000000 ) ) ;
#14873=CIRCLE ( 'NONE', #10674, 116.0000000000000000 ) ;
#14877=VERTEX_POINT ( 'NONE', #10135 ) ;
#14878=DIRECTION ( 'NONE',  ( -1.000000000000000000, -0.000000000000000000, -0.000000000000000000 ) ) ;
#14879=EDGE_CURVE ( 'NONE', #31728, #22071, #3568, .T. ) ;
#14881=EDGE_CURVE ( 'NONE', #30882, #11023, #11708, .T. ) ;
#14882=LINE ( 'NONE', #33834, #15908 ) ;
#14886=ORIENTED_EDGE ( 'NONE', *, *, #12995, .F. ) ;
#14888=DIRECTION ( 'NONE',  ( 0.000000000000000000, 0.9213119778704139673, -0.3888241754733182676 ) ) ;
#14890=ORIENTED_EDGE ( 'NONE', *, *, #22139, .F. ) ;
#14901=ORIENTED_EDGE ( 'NONE', *, *, #40228, .T. ) ;
#14903=VERTEX_POINT ( 'NONE', #6010 ) ;
#14904=DIRECTION ( 'NONE',  ( 0.000000000000000000, 0.8993121301712202476, -0.4373073204588531770 ) ) ;
#14905=VECTOR ( 'NONE', #28989, 1000.000000000000000 ) ;
#14908=EDGE_CURVE ( 'NONE', #30500, #32325, #32632, .T. ) ;
#14909=FACE_OUTER_BOUND ( 'NONE', #8045, .T. ) ;
#14910=CARTESIAN_POINT ( 'NONE',  ( 17.99999999999999645, -95.31344542257777164, 66.11616384574416827 ) ) ;
#14918=VECTOR ( 'NONE', #32558, 1000.000000000000000 ) ;
#14921=AXIS2_PLACEMENT_3D ( 'NONE', #22836, #36086, #5986 ) ;
#14925=ORIENTED_EDGE ( 'NONE', *, *, #25713, .F. ) ;
#14930=CARTESIAN_POINT ( 'NONE',  ( -10.00000000000000000, 0.000000000000000000, 0.000000000000000000 ) ) ;
#14931=EDGE_CURVE ( 'NONE', #42055, #8238, #26363, .T. ) ;
#14934=DIRECTION ( 'NONE',  ( 0.000000000000000000, -0.8183027759081623609, -0.5747874102144165942 ) ) ;
#14935=ORIENTED_EDGE ( 'NONE', *, *, #18891, .T. ) ;
#14938=CARTESIAN_POINT ( 'NONE',  ( 17.99999999999999645, 0.000000000000000000, 0.000000000000000000 ) ) ;
#14939=VECTOR ( 'NONE', #9057, 1000.000000000000000 ) ;
#14940=EDGE_LOOP ( 'NONE', ( #36467, #3586, #28027, #19294 ) ) ;
#14941=DIRECTION ( 'NONE',  ( -1.000000000000000000, 0.000000000000000000, 0.000000000000000000 ) ) ;
#14942=DIRECTION ( 'NONE',  ( -1.000000000000000000, -0.000000000000000000, 0.000000000000000000 ) ) ;
#14944=ORIENTED_EDGE ( 'NONE', *, *, #17864, .F. ) ;
#14947=VERTEX_POINT ( 'NONE', #2920 ) ;
#14949=ADVANCED_FACE ( 'NONE', ( #16512 ), #13016, .F. ) ;
#14951=CARTESIAN_POINT ( 'NONE',  ( 17.99999999999999645, -25.18647942089668490, -113.2326863338530245 ) ) ;
#14956=ORIENTED_EDGE ( 'NONE', *, *, #8861, .F. ) ;
#14958=VERTEX_POINT ( 'NONE', #20008 ) ;
#14963=ORIENTED_EDGE ( 'NONE', *, *, #10055, .T. ) ;
#14964=EDGE_CURVE ( 'NONE', #9297, #16728, #33277, .T. ) ;
#14966=DIRECTION ( 'NONE',  ( 1.000000000000000000, 0.000000000000000000, 0.000000000000000000 ) ) ;
#14970=ORIENTED_EDGE ( 'NONE', *, *, #28876, .F. ) ;
#14971=DIRECTION ( 'NONE',  ( -1.000000000000000000, 0.000000000000000000, 0.000000000000000000 ) ) ;
#14977=DIRECTION ( 'NONE',  ( 0.000000000000000000, 0.9996456111234524045, 0.02662052143777833904 ) ) ;
#14982=AXIS2_PLACEMENT_3D ( 'NONE', #12733, #9228, #25841 ) ;
#14983=DIRECTION ( 'NONE',  ( -1.000000000000000000, -0.000000000000000000, 0.000000000000000000 ) ) ;
#14984=AXIS2_PLACEMENT_3D ( 'NONE', #25736, #35705, #2955 ) ;
#14985=ADVANCED_FACE ( 'NONE', ( #4672 ), #40875, .F. ) ;
#14999=DIRECTION ( 'NONE',  ( -1.000000000000000000, 0.000000000000000000, 0.000000000000000000 ) ) ;
#15001=ORIENTED_EDGE ( 'NONE', *, *, #4411, .T. ) ;
#15002=DIRECTION ( 'NONE',  ( -1.000000000000000000, -0.000000000000000000, -0.000000000000000000 ) ) ;
#15003=DIRECTION ( 'NONE',  ( -1.000000000000000000, 0.000000000000000000, 0.000000000000000000 ) ) ;
#15006=EDGE_CURVE ( 'NONE', #14549, #9049, #13131, .T. ) ;
#15007=CARTESIAN_POINT ( 'NONE',  ( 17.99999999999999645, 0.000000000000000000, 0.000000000000000000 ) ) ;
#15008=VECTOR ( 'NONE', #33712, 1000.000000000000000 ) ;
#15010=DIRECTION ( 'NONE',  ( -1.000000000000000000, -0.000000000000000000, -0.000000000000000000 ) ) ;
#15011=VERTEX_POINT ( 'NONE', #27605 ) ;
#15015=DIRECTION ( 'NONE',  ( 0.000000000000000000, 0.000000000000000000, 1.000000000000000000 ) ) ;
#15016=ORIENTED_EDGE ( 'NONE', *, *, #36911, .T. ) ;
#15022=CARTESIAN_POINT ( 'NONE',  ( 0.000000000000000000, 115.5737863835462349, 9.934782381634081005 ) ) ;
#15025=CARTESIAN_POINT ( 'NONE',  ( 17.99999999999999645, 120.4984140710909202, 0.7894348306988416830 ) ) ;
#15031=ORIENTED_EDGE ( 'NONE', *, *, #15620, .F. ) ;
#15035=CARTESIAN_POINT ( 'NONE',  ( 17.99999999999999645, 0.000000000000000000, 0.000000000000000000 ) ) ;
#15036=VECTOR ( 'NONE', #33252, 1000.000000000000000 ) ;
#15037=CYLINDRICAL_SURFACE ( 'NONE', #30516, 58.99999999999998579 ) ;
#15038=DIRECTION ( 'NONE',  ( 0.000000000000000000, 0.000000000000000000, 1.000000000000000000 ) ) ;
#15039=AXIS2_PLACEMENT_3D ( 'NONE', #20242, #36772, #3799 ) ;
#15046=FACE_OUTER_BOUND ( 'NONE', #42703, .T. ) ;
#15047=LINE ( 'NONE', #2115, #41499 ) ;
#15048=CIRCLE ( 'NONE', #36607, 58.99999999999999289 ) ;
#15050=ORIENTED_EDGE ( 'NONE', *, *, #4062, .F. ) ;
#15055=DIRECTION ( 'NONE',  ( 1.000000000000000000, 0.000000000000000000, 0.000000000000000000 ) ) ;
#15062=ORIENTED_EDGE ( 'NONE', *, *, #16383, .F. ) ;
#15064=CARTESIAN_POINT ( 'NONE',  ( 0.000000000000000000, 0.000000000000000000, 0.000000000000000000 ) ) ;
#15066=DIRECTION ( 'NONE',  ( 1.000000000000000000, 0.000000000000000000, 0.000000000000000000 ) ) ;
#15067=ORIENTED_EDGE ( 'NONE', *, *, #3043, .T. ) ;
#15068=AXIS2_PLACEMENT_3D ( 'NONE', #37892, #8244, #22014 ) ;
#15073=EDGE_LOOP ( 'NONE', ( #15502, #22963, #21427, #28057 ) ) ;
#15078=ORIENTED_EDGE ( 'NONE', *, *, #6428, .F. ) ;
#15081=DIRECTION ( 'NONE',  ( 1.000000000000000000, 0.000000000000000000, 0.000000000000000000 ) ) ;
#15082=CARTESIAN_POINT ( 'NONE',  ( 0.000000000000000000, 0.000000000000000000, 0.000000000000000000 ) ) ;
#15084=AXIS2_PLACEMENT_3D ( 'NONE', #20824, #37561, #34077 ) ;
#15085=CARTESIAN_POINT ( 'NONE',  ( 17.99999999999999645, 84.62908780824989208, -85.78116633471202590 ) ) ;
#15096=CARTESIAN_POINT ( 'NONE',  ( -10.00000000000000000, 0.000000000000000000, 0.000000000000000000 ) ) ;
#15098=VECTOR ( 'NONE', #29008, 1000.000000000000000 ) ;
#15100=CYLINDRICAL_SURFACE ( 'NONE', #22516, 120.5010000000000190 ) ;
#15101=VECTOR ( 'NONE', #33567, 1000.000000000000000 ) ;
#15106=EDGE_CURVE ( 'NONE', #7888, #42671, #17383, .T. ) ;
#15109=ORIENTED_EDGE ( 'NONE', *, *, #23805, .T. ) ;
#15111=DIRECTION ( 'NONE',  ( 0.000000000000000000, -0.2631025642275283127, 0.9647678688145140402 ) ) ;
#15113=VECTOR ( 'NONE', #12714, 1000.000000000000000 ) ;
#15115=VERTEX_POINT ( 'NONE', #17595 ) ;
#15122=DIRECTION ( 'NONE',  ( 0.000000000000000000, 0.000000000000000000, 1.000000000000000000 ) ) ;
#15124=ORIENTED_EDGE ( 'NONE', *, *, #39250, .F. ) ;
#15128=CARTESIAN_POINT ( 'NONE',  ( 17.99999999999999645, -80.74349901498459303, 77.90224541347254217 ) ) ;
#15131=EDGE_CURVE ( 'NONE', #9666, #40313, #32603, .T. ) ;
#15133=DIRECTION ( 'NONE',  ( 1.000000000000000000, 0.000000000000000000, 0.000000000000000000 ) ) ;
#15136=DIRECTION ( 'NONE',  ( 0.000000000000000000, 0.000000000000000000, 1.000000000000000000 ) ) ;
#15141=AXIS2_PLACEMENT_3D ( 'NONE', #10521, #33427, #3512 ) ;
#15142=ORIENTED_EDGE ( 'NONE', *, *, #6177, .T. ) ;
#15148=CIRCLE ( 'NONE', #39466, 120.5010000000000332 ) ;
#15152=VECTOR ( 'NONE', #28809, 1000.000000000000000 ) ;
#15154=CIRCLE ( 'NONE', #38189, 116.0000000000000000 ) ;
#15159=ORIENTED_EDGE ( 'NONE', *, *, #21394, .T. ) ;
#15163=DIRECTION ( 'NONE',  ( 0.000000000000000000, 0.000000000000000000, -1.000000000000000000 ) ) ;
#15164=DIRECTION ( 'NONE',  ( 0.000000000000000000, 0.000000000000000000, 1.000000000000000000 ) ) ;
#15165=EDGE_CURVE ( 'NONE', #2401, #5171, #28260, .T. ) ;
#15167=CIRCLE ( 'NONE', #25623, 120.5010000000000616 ) ;
#15171=VECTOR ( 'NONE', #38412, 1000.000000000000000 ) ;
#15175=DIRECTION ( 'NONE',  ( -1.000000000000000000, 0.000000000000000000, 0.000000000000000000 ) ) ;
#15176=DIRECTION ( 'NONE',  ( -1.000000000000000000, 0.000000000000000000, 0.000000000000000000 ) ) ;
#15177=CARTESIAN_POINT ( 'NONE',  ( 0.000000000000000000, -23.21237537461820466, 109.7700237000591414 ) ) ;
#15178=AXIS2_PLACEMENT_3D ( 'NONE', #34996, #31731, #25022 ) ;
#15185=CARTESIAN_POINT ( 'NONE',  ( 17.99999999999999645, -97.19627249181047546, -71.22763238166585609 ) ) ;
#15188=EDGE_CURVE ( 'NONE', #42499, #33862, #6805, .T. ) ;
#15190=FACE_OUTER_BOUND ( 'NONE', #241, .T. ) ;
#15195=ORIENTED_EDGE ( 'NONE', *, *, #13519, .T. ) ;
#15197=FACE_OUTER_BOUND ( 'NONE', #5225, .T. ) ;
#15199=EDGE_CURVE ( 'NONE', #33331, #14549, #31902, .T. ) ;
#15201=CARTESIAN_POINT ( 'NONE',  ( 0.000000000000000000, 112.8457601792515419, 26.86697618949414945 ) ) ;
#15202=ORIENTED_EDGE ( 'NONE', *, *, #5891, .T. ) ;
#15204=ORIENTED_EDGE ( 'NONE', *, *, #10818, .F. ) ;
#15208=CIRCLE ( 'NONE', #24232, 120.5010000000000332 ) ;
#15212=ORIENTED_EDGE ( 'NONE', *, *, #42017, .F. ) ;
#15213=CIRCLE ( 'NONE', #1919, 59.00000000000000711 ) ;
#15215=AXIS2_PLACEMENT_3D ( 'NONE', #18743, #15010, #42435 ) ;
#15223=CARTESIAN_POINT ( 'NONE',  ( 0.000000000000000000, -35.72777019205596361, -106.3569410558020962 ) ) ;
#15227=FACE_OUTER_BOUND ( 'NONE', #36399, .T. ) ;
#15232=DIRECTION ( 'NONE',  ( -1.000000000000000000, -0.000000000000000000, -0.000000000000000000 ) ) ;
#15233=CARTESIAN_POINT ( 'NONE',  ( 17.99999999999999645, 69.90696807222488474, 98.15042952503540619 ) ) ;
#15234=CIRCLE ( 'NONE', #39553, 58.99999999999998579 ) ;
#15237=DIRECTION ( 'NONE',  ( 0.000000000000000000, 0.000000000000000000, 1.000000000000000000 ) ) ;
#15240=ORIENTED_EDGE ( 'NONE', *, *, #3748, .F. ) ;
#15241=CARTESIAN_POINT ( 'NONE',  ( 17.99999999999999645, -56.51398178981757070, -96.92493144647505687 ) ) ;
#15243=ORIENTED_EDGE ( 'NONE', *, *, #3139, .T. ) ;
#15253=ORIENTED_EDGE ( 'NONE', *, *, #33156, .F. ) ;
#15255=EDGE_CURVE ( 'NONE', #8245, #31622, #5538, .T. ) ;
#15257=ORIENTED_EDGE ( 'NONE', *, *, #19674, .F. ) ;
#15262=CARTESIAN_POINT ( 'NONE',  ( 0.000000000000000000, 0.000000000000000000, 0.000000000000000000 ) ) ;
#15263=EDGE_LOOP ( 'NONE', ( #9922, #10584, #17554, #18731 ) ) ;
#15264=DIRECTION ( 'NONE',  ( 1.000000000000000000, 0.000000000000000000, 0.000000000000000000 ) ) ;
#15269=ADVANCED_FACE ( 'NONE', ( #4890 ), #34784, .F. ) ;
#15274=ORIENTED_EDGE ( 'NONE', *, *, #2420, .T. ) ;
#15276=DIRECTION ( 'NONE',  ( -1.000000000000000000, -0.000000000000000000, 0.000000000000000000 ) ) ;
#15279=CYLINDRICAL_SURFACE ( 'NONE', #8532, 116.0000000000000000 ) ;
#15288=ORIENTED_EDGE ( 'NONE', *, *, #24169, .F. ) ;
#15289=CARTESIAN_POINT ( 'NONE',  ( 0.000000000000000000, -51.98489025774233596, -108.7109110710166391 ) ) ;
#15290=DIRECTION ( 'NONE',  ( 0.000000000000000000, 0.000000000000000000, 1.000000000000000000 ) ) ;
#15292=CIRCLE ( 'NONE', #3357, 59.00000000000000711 ) ;
#15293=AXIS2_PLACEMENT_3D ( 'NONE', #43089, #19790, #13453 ) ;
#15294=CARTESIAN_POINT ( 'NONE',  ( 17.99999999999999645, 52.19040376560566585, -99.31985817764127944 ) ) ;
#15295=ORIENTED_EDGE ( 'NONE', *, *, #37195, .F. ) ;
#15298=LINE ( 'NONE', #37720, #7671 ) ;
#15299=AXIS2_PLACEMENT_3D ( 'NONE', #31309, #7730, #31729 ) ;
#15303=CARTESIAN_POINT ( 'NONE',  ( 0.000000000000000000, 0.000000000000000000, 0.000000000000000000 ) ) ;
#15304=ORIENTED_EDGE ( 'NONE', *, *, #27639, .F. ) ;
#15308=ORIENTED_EDGE ( 'NONE', *, *, #36929, .F. ) ;
#15310=ORIENTED_EDGE ( 'NONE', *, *, #28357, .F. ) ;
#15312=ORIENTED_EDGE ( 'NONE', *, *, #10733, .T. ) ;
#15314=DIRECTION ( 'NONE',  ( 0.000000000000000000, 0.000000000000000000, 1.000000000000000000 ) ) ;
#15323=DIRECTION ( 'NONE',  ( -1.000000000000000000, -0.000000000000000000, -0.000000000000000000 ) ) ;
#15325=EDGE_CURVE ( 'NONE', #24215, #7262, #568, .T. ) ;
#15326=FACE_OUTER_BOUND ( 'NONE', #40059, .T. ) ;
#15330=CARTESIAN_POINT ( 'NONE',  ( 17.99999999999999645, 0.000000000000000000, 0.000000000000000000 ) ) ;
#15335=CARTESIAN_POINT ( 'NONE',  ( 17.99999999999999645, 46.83041522348636931, -101.9567785075596618 ) ) ;
#15340=ORIENTED_EDGE ( 'NONE', *, *, #24773, .F. ) ;
#15343=CARTESIAN_POINT ( 'NONE',  ( 0.000000000000000000, -97.19627249181141337, 71.22763238166453448 ) ) ;
#15345=EDGE_LOOP ( 'NONE', ( #17907, #40789, #40434, #18003 ) ) ;
#15346=AXIS2_PLACEMENT_3D ( 'NONE', #14259, #37578, #1783 ) ;
#15347=CARTESIAN_POINT ( 'NONE',  ( 0.000000000000000000, 80.74349901498510462, -77.90224541347200216 ) ) ;
#15348=ORIENTED_EDGE ( 'NONE', *, *, #39810, .F. ) ;
#15354=CARTESIAN_POINT ( 'NONE',  ( 0.000000000000000000, -87.92975456462950490, 69.68953103478128241 ) ) ;
#15358=DIRECTION ( 'NONE',  ( -1.000000000000000000, -0.000000000000000000, -0.000000000000000000 ) ) ;
#15359=LINE ( 'NONE', #35164, #35174 ) ;
#15360=ORIENTED_EDGE ( 'NONE', *, *, #5238, .T. ) ;
#15361=CARTESIAN_POINT ( 'NONE',  ( 0.000000000000000000, 0.000000000000000000, 0.000000000000000000 ) ) ;
#15362=DIRECTION ( 'NONE',  ( 0.000000000000000000, 0.1062934856473656403, -0.9943348002101370930 ) ) ;
#15366=CARTESIAN_POINT ( 'NONE',  ( 0.000000000000000000, -75.03166794516737070, -94.29071961951585479 ) ) ;
#15367=DIRECTION ( 'NONE',  ( -1.000000000000000000, -0.000000000000000000, -0.000000000000000000 ) ) ;
#15368=ORIENTED_EDGE ( 'NONE', *, *, #10818, .T. ) ;
#15370=FACE_OUTER_BOUND ( 'NONE', #31778, .T. ) ;
#15371=AXIS2_PLACEMENT_3D ( 'NONE', #24461, #6168, #19516 ) ;
#15373=DIRECTION ( 'NONE',  ( -1.000000000000000000, -0.000000000000000000, 0.000000000000000000 ) ) ;
#15376=CIRCLE ( 'NONE', #19542, 116.0000000000000000 ) ;
#15377=EDGE_CURVE ( 'NONE', #4507, #29613, #34724, .T. ) ;
#15381=CIRCLE ( 'NONE', #13278, 120.5010000000000190 ) ;
#15391=DIRECTION ( 'NONE',  ( 0.000000000000000000, 0.7525707698561396874, -0.6585113790650372056 ) ) ;
#15392=ORIENTED_EDGE ( 'NONE', *, *, #26345, .F. ) ;
#15394=VERTEX_POINT ( 'NONE', #23428 ) ;
#15395=CARTESIAN_POINT ( 'NONE',  ( 0.000000000000000000, 103.4151313792870610, 61.85306461934443689 ) ) ;
#15396=CYLINDRICAL_SURFACE ( 'NONE', #15178, 59.00000000000000000 ) ;
#15403=DIRECTION ( 'NONE',  ( 0.000000000000000000, 0.9407002666710342353, -0.3392388661180278930 ) ) ;
#15405=AXIS2_PLACEMENT_3D ( 'NONE', #27193, #16748, #3795 ) ;
#15407=DIRECTION ( 'NONE',  ( 1.000000000000000000, 0.000000000000000000, -0.000000000000000000 ) ) ;
#15410=EDGE_CURVE ( 'NONE', #16222, #10174, #27775, .T. ) ;
#15411=CIRCLE ( 'NONE', #10477, 58.99999999999999289 ) ;
#15413=CARTESIAN_POINT ( 'NONE',  ( 17.99999999999999645, 0.000000000000000000, 0.000000000000000000 ) ) ;
#15414=VECTOR ( 'NONE', #24253, 1000.000000000000000 ) ;
#15418=CARTESIAN_POINT ( 'NONE',  ( 17.99999999999999645, 0.000000000000000000, 0.000000000000000000 ) ) ;
#15419=CARTESIAN_POINT ( 'NONE',  ( 17.99999999999999645, -34.74871106919551522, -106.6808302961375148 ) ) ;
#15421=CARTESIAN_POINT ( 'NONE',  ( 17.99999999999999645, -115.6826031496111398, -8.575274253898639287 ) ) ;
#15426=CIRCLE ( 'NONE', #9804, 59.00000000000000000 ) ;
#15428=EDGE_CURVE ( 'NONE', #39201, #20639, #12449, .T. ) ;
#15430=VERTEX_POINT ( 'NONE', #36689 ) ;
#15434=CYLINDRICAL_SURFACE ( 'NONE', #16369, 59.00000000000000000 ) ;
#15438=DIRECTION ( 'NONE',  ( 0.000000000000000000, 0.000000000000000000, 1.000000000000000000 ) ) ;
#15439=DIRECTION ( 'NONE',  ( -1.000000000000000000, -0.000000000000000000, -0.000000000000000000 ) ) ;
#15443=DIRECTION ( 'NONE',  ( 1.000000000000000000, 0.000000000000000000, 0.000000000000000000 ) ) ;
#15446=ORIENTED_EDGE ( 'NONE', *, *, #13219, .F. ) ;
#15448=DIRECTION ( 'NONE',  ( 0.000000000000000000, 0.4610925014493266194, -0.8873520750565710991 ) ) ;
#15449=CARTESIAN_POINT ( 'NONE',  ( 17.99999999999999645, 17.33727698085324320, -110.8498592715971967 ) ) ;
#15450=ORIENTED_EDGE ( 'NONE', *, *, #39763, .F. ) ;
#15456=ORIENTED_EDGE ( 'NONE', *, *, #37195, .T. ) ;
#15457=DIRECTION ( 'NONE',  ( 1.000000000000000000, 0.000000000000000000, 0.000000000000000000 ) ) ;
#15458=CARTESIAN_POINT ( 'NONE',  ( 17.99999999999999645, -105.3681574666266414, 38.54638589714855357 ) ) ;
#15459=CIRCLE ( 'NONE', #21050, 59.00000000000000000 ) ;
#15460=DIRECTION ( 'NONE',  ( 0.000000000000000000, 0.000000000000000000, 1.000000000000000000 ) ) ;
#15461=CARTESIAN_POINT ( 'NONE',  ( 17.99999999999999645, -11.41303419184897017, -111.6154788735837116 ) ) ;
#15462=EDGE_LOOP ( 'NONE', ( #35155, #13418, #7472, #10528 ) ) ;
#15463=CARTESIAN_POINT ( 'NONE',  ( 17.99999999999999645, -100.6739960869721102, 49.52796165323228195 ) ) ;
#15467=CARTESIAN_POINT ( 'NONE',  ( 17.99999999999999645, 84.77518783075095143, 73.49448960231384831 ) ) ;
#15468=CIRCLE ( 'NONE', #5676, 120.5010000000000190 ) ;
#15470=VECTOR ( 'NONE', #9078, 1000.000000000000000 ) ;
#15472=ORIENTED_EDGE ( 'NONE', *, *, #10444, .F. ) ;
#15473=CARTESIAN_POINT ( 'NONE',  ( 0.000000000000000000, -97.97378550988267421, 62.10585602713726416 ) ) ;
#15474=ORIENTED_EDGE ( 'NONE', *, *, #37560, .F. ) ;
#15476=CARTESIAN_POINT ( 'NONE',  ( 17.99999999999999645, 29.02167576844106023, 108.3790330702170621 ) ) ;
#15477=CARTESIAN_POINT ( 'NONE',  ( 9.000000000000001776, 47.31079789947484926, 105.9135893174952656 ) ) ;
#15479=VERTEX_POINT ( 'NONE', #25845 ) ;
#15488=ORIENTED_EDGE ( 'NONE', *, *, #25061, .F. ) ;
#15491=ORIENTED_EDGE ( 'NONE', *, *, #15687, .F. ) ;
#15495=DIRECTION ( 'NONE',  ( 0.000000000000000000, 0.000000000000000000, 1.000000000000000000 ) ) ;
#15500=CARTESIAN_POINT ( 'NONE',  ( 0.000000000000000000, 104.2166695095712470, 60.49278301857841456 ) ) ;
#15502=ORIENTED_EDGE ( 'NONE', *, *, #42715, .F. ) ;
#15504=CYLINDRICAL_SURFACE ( 'NONE', #20847, 59.00000000000000000 ) ;
#15507=LINE ( 'NONE', #28801, #14118 ) ;
#15508=ORIENTED_EDGE ( 'NONE', *, *, #21505, .F. ) ;
#15509=EDGE_CURVE ( 'NONE', #5216, #33264, #22223, .T. ) ;
#15510=ORIENTED_EDGE ( 'NONE', *, *, #26099, .T. ) ;
#15512=ORIENTED_EDGE ( 'NONE', *, *, #27711, .T. ) ;
#15514=CARTESIAN_POINT ( 'NONE',  ( 8.999999999999998224, -82.63181128086679905, -81.41243003647058174 ) ) ;
#15521=AXIS2_PLACEMENT_3D ( 'NONE', #27328, #889, #4382 ) ;
#15523=VERTEX_POINT ( 'NONE', #36704 ) ;
#15524=DIRECTION ( 'NONE',  ( -1.000000000000000000, 0.000000000000000000, 0.000000000000000000 ) ) ;
#15526=EDGE_CURVE ( 'NONE', #34978, #13537, #39542, .T. ) ;
#15531=CIRCLE ( 'NONE', #21123, 59.00000000000000000 ) ;
#15538=FACE_OUTER_BOUND ( 'NONE', #5992, .T. ) ;
#15539=EDGE_CURVE ( 'NONE', #29797, #13292, #14539, .T. ) ;
#15540=DIRECTION ( 'NONE',  ( 0.000000000000000000, 0.8183027759081662467, 0.5747874102144109321 ) ) ;
#15542=FACE_OUTER_BOUND ( 'NONE', #16873, .T. ) ;
#15543=AXIS2_PLACEMENT_3D ( 'NONE', #19397, #32665, #16313 ) ;
#15548=CARTESIAN_POINT ( 'NONE',  ( 17.99999999999999645, 0.000000000000000000, 0.000000000000000000 ) ) ;
#15549=EDGE_LOOP ( 'NONE', ( #4957, #9077, #42495, #8442 ) ) ;
#15550=DIRECTION ( 'NONE',  ( 1.000000000000000000, -0.000000000000000000, -0.000000000000000000 ) ) ;
#15552=VERTEX_POINT ( 'NONE', #43035 ) ;
#15562=ORIENTED_EDGE ( 'NONE', *, *, #15717, .T. ) ;
#15565=DIRECTION ( 'NONE',  ( 0.000000000000000000, -0.7164567402983210709, 0.6976315211349786161 ) ) ;
#15567=DIRECTION ( 'NONE',  ( -1.000000000000000000, 0.000000000000000000, 0.000000000000000000 ) ) ;
#15569=DIRECTION ( 'NONE',  ( 1.000000000000000000, 0.000000000000000000, 0.000000000000000000 ) ) ;
#15571=ADVANCED_FACE ( 'NONE', ( #40183 ), #19525, .F. ) ;
#15572=ORIENTED_EDGE ( 'NONE', *, *, #18574, .F. ) ;
#15575=CYLINDRICAL_SURFACE ( 'NONE', #40803, 59.00000000000000000 ) ;
#15577=CYLINDRICAL_SURFACE ( 'NONE', #27561, 116.0000000000000000 ) ;
#15578=LINE ( 'NONE', #5309, #28674 ) ;
#15582=EDGE_CURVE ( 'NONE', #41485, #36227, #20127, .T. ) ;
#15583=AXIS2_PLACEMENT_3D ( 'NONE', #33957, #40916, #11274 ) ;
#15584=ORIENTED_EDGE ( 'NONE', *, *, #40000, .F. ) ;
#15585=ORIENTED_EDGE ( 'NONE', *, *, #23264, .T. ) ;
#15587=CARTESIAN_POINT ( 'NONE',  ( 0.000000000000000000, -51.98489025774377126, 108.7109110710159854 ) ) ;
#15588=DIRECTION ( 'NONE',  ( -1.000000000000000000, 0.000000000000000000, 0.000000000000000000 ) ) ;
#15589=DIRECTION ( 'NONE',  ( -1.000000000000000000, -0.000000000000000000, -0.000000000000000000 ) ) ;
#15590=ORIENTED_EDGE ( 'NONE', *, *, #10115, .T. ) ;
#15598=ORIENTED_EDGE ( 'NONE', *, *, #41616, .F. ) ;
#15602=EDGE_CURVE ( 'NONE', #42205, #2052, #19437, .T. ) ;
#15603=ORIENTED_EDGE ( 'NONE', *, *, #2076, .T. ) ;
#15604=DIRECTION ( 'NONE',  ( 0.000000000000000000, 0.000000000000000000, 1.000000000000000000 ) ) ;
#15605=VERTEX_POINT ( 'NONE', #29976 ) ;
#15607=VERTEX_POINT ( 'NONE', #33441 ) ;
#15610=CARTESIAN_POINT ( 'NONE',  ( 17.99999999999999645, -12.43843445475238063, -111.5058645182330963 ) ) ;
#15612=AXIS2_PLACEMENT_3D ( 'NONE', #15625, #19131, #41787 ) ;
#15614=DIRECTION ( 'NONE',  ( 0.000000000000000000, 0.9574220383620062336, -0.2886919473396182267 ) ) ;
#15617=ORIENTED_EDGE ( 'NONE', *, *, #23393, .F. ) ;
#15620=EDGE_CURVE ( 'NONE', #41781, #39732, #32586, .T. ) ;
#15625=CARTESIAN_POINT ( 'NONE',  ( 0.000000000000000000, 0.000000000000000000, 0.000000000000000000 ) ) ;
#15628=AXIS2_PLACEMENT_3D ( 'NONE', #40975, #33367, #17032 ) ;
#15629=DIRECTION ( 'NONE',  ( -1.000000000000000000, -0.000000000000000000, -0.000000000000000000 ) ) ;
#15632=VERTEX_POINT ( 'NONE', #23021 ) ;
#15633=CYLINDRICAL_SURFACE ( 'NONE', #40963, 59.00000000000000000 ) ;
#15635=DIRECTION ( 'NONE',  ( 0.000000000000000000, 0.000000000000000000, 1.000000000000000000 ) ) ;
#15638=CARTESIAN_POINT ( 'NONE',  ( 0.000000000000000000, -0.6819280456836842585, 115.9979955608738607 ) ) ;
#15641=ORIENTED_EDGE ( 'NONE', *, *, #30745, .T. ) ;
#15644=DIRECTION ( 'NONE',  ( -1.000000000000000000, -0.000000000000000000, -0.000000000000000000 ) ) ;
#15645=CARTESIAN_POINT ( 'NONE',  ( 17.99999999999999645, -95.38615066514023511, 59.07414607872794932 ) ) ;
#15651=CYLINDRICAL_SURFACE ( 'NONE', #7467, 59.00000000000000000 ) ;
#15657=CARTESIAN_POINT ( 'NONE',  ( 0.000000000000000000, 0.000000000000000000, 0.000000000000000000 ) ) ;
#15658=EDGE_CURVE ( 'NONE', #189, #32209, #33649, .T. ) ;
#15660=EDGE_CURVE ( 'NONE', #36933, #7190, #4178, .T. ) ;
#15663=AXIS2_PLACEMENT_3D ( 'NONE', #1482, #1699, #22041 ) ;
#15666=AXIS2_PLACEMENT_3D ( 'NONE', #8003, #18099, #7575 ) ;
#15667=ORIENTED_EDGE ( 'NONE', *, *, #19902, .F. ) ;
#15669=DIRECTION ( 'NONE',  ( 0.000000000000000000, 0.000000000000000000, 1.000000000000000000 ) ) ;
#15673=FACE_OUTER_BOUND ( 'NONE', #12342, .T. ) ;
#15675=FACE_OUTER_BOUND ( 'NONE', #40640, .T. ) ;
#15676=CIRCLE ( 'NONE', #33078, 116.0000000000000000 ) ;
#15677=EDGE_LOOP ( 'NONE', ( #4840, #39964, #2283, #30672 ) ) ;
#15679=DIRECTION ( 'NONE',  ( -1.000000000000000000, -0.000000000000000000, 0.000000000000000000 ) ) ;
#15681=ORIENTED_EDGE ( 'NONE', *, *, #26928, .T. ) ;
#15682=LINE ( 'NONE', #38555, #14905 ) ;
#15687=EDGE_CURVE ( 'NONE', #13955, #7485, #35340, .T. ) ;
#15691=CARTESIAN_POINT ( 'NONE',  ( 0.000000000000000000, -37.07968990261405651, -109.9140418541961282 ) ) ;
#15692=ORIENTED_EDGE ( 'NONE', *, *, #5673, .T. ) ;
#15696=VECTOR ( 'NONE', #4013, 1000.000000000000000 ) ;
#15697=ORIENTED_EDGE ( 'NONE', *, *, #30087, .T. ) ;
#15700=DIRECTION ( 'NONE',  ( 0.000000000000000000, 0.7525707698561353576, 0.6585113790650422017 ) ) ;
#15701=CARTESIAN_POINT ( 'NONE',  ( 0.000000000000000000, -113.8630351447204134, -22.16324045874526405 ) ) ;
#15702=ORIENTED_EDGE ( 'NONE', *, *, #4930, .T. ) ;
#15705=AXIS2_PLACEMENT_3D ( 'NONE', #41938, #12086, #34975 ) ;
#15706=ORIENTED_EDGE ( 'NONE', *, *, #6177, .F. ) ;
#15710=EDGE_CURVE ( 'NONE', #23276, #13537, #19372, .T. ) ;
#15711=CARTESIAN_POINT ( 'NONE',  ( 17.99999999999999645, 109.3506818544110217, 38.70953859161051014 ) ) ;
#15712=ADVANCED_FACE ( 'NONE', ( #901 ), #13837, .F. ) ;
#15713=EDGE_CURVE ( 'NONE', #41781, #19147, #34657, .T. ) ;
#15717=EDGE_CURVE ( 'NONE', #37692, #3781, #11665, .T. ) ;
#15721=CIRCLE ( 'NONE', #17823, 59.00000000000000000 ) ;
#15722=CYLINDRICAL_SURFACE ( 'NONE', #13310, 59.00000000000000000 ) ;
#15724=DIRECTION ( 'NONE',  ( -1.000000000000000000, 0.000000000000000000, -0.000000000000000000 ) ) ;
#15725=ADVANCED_FACE ( 'NONE', ( #7684 ), #17999, .F. ) ;
#15727=ORIENTED_EDGE ( 'NONE', *, *, #11342, .T. ) ;
#15728=DIRECTION ( 'NONE',  ( 0.000000000000000000, 0.000000000000000000, 1.000000000000000000 ) ) ;
#15730=DIRECTION ( 'NONE',  ( -1.000000000000000000, 0.000000000000000000, 0.000000000000000000 ) ) ;
#15732=DIRECTION ( 'NONE',  ( 1.000000000000000000, 0.000000000000000000, 0.000000000000000000 ) ) ;
#15733=DIRECTION ( 'NONE',  ( 0.000000000000000000, 0.000000000000000000, 1.000000000000000000 ) ) ;
#15736=AXIS2_PLACEMENT_3D ( 'NONE', #35801, #5929, #36239 ) ;
#15737=ORIENTED_EDGE ( 'NONE', *, *, #17797, .F. ) ;
#15738=CYLINDRICAL_SURFACE ( 'NONE', #31048, 59.00000000000000000 ) ;
#15740=AXIS2_PLACEMENT_3D ( 'NONE', #39135, #6620, #36081 ) ;
#15744=AXIS2_PLACEMENT_3D ( 'NONE', #39920, #36226, #9837 ) ;
#15745=CIRCLE ( 'NONE', #1760, 59.00000000000000000 ) ;
#15748=AXIS2_PLACEMENT_3D ( 'NONE', #23733, #14125, #11271 ) ;
#15749=CARTESIAN_POINT ( 'NONE',  ( 0.000000000000000000, 45.89132998248050654, 102.3829004574631512 ) ) ;
#15751=CARTESIAN_POINT ( 'NONE',  ( 17.99999999999999645, 110.0562500189198829, 49.07252625220148445 ) ) ;
#15752=DIRECTION ( 'NONE',  ( -1.000000000000000000, -0.000000000000000000, -0.000000000000000000 ) ) ;
#15753=AXIS2_PLACEMENT_3D ( 'NONE', #18207, #1348, #31036 ) ;
#15754=ORIENTED_EDGE ( 'NONE', *, *, #1152, .F. ) ;
#15759=DIRECTION ( 'NONE',  ( -1.000000000000000000, 0.000000000000000000, 0.000000000000000000 ) ) ;
#15763=ORIENTED_EDGE ( 'NONE', *, *, #5348, .T. ) ;
#15765=CARTESIAN_POINT ( 'NONE',  ( 17.99999999999999645, 0.000000000000000000, 0.000000000000000000 ) ) ;
#15767=ORIENTED_EDGE ( 'NONE', *, *, #36954, .F. ) ;
#15770=CIRCLE ( 'NONE', #26194, 58.99999999999999289 ) ;
#15773=EDGE_CURVE ( 'NONE', #33862, #13871, #10972, .T. ) ;
#15774=DIRECTION ( 'NONE',  ( 0.000000000000000000, 0.000000000000000000, 1.000000000000000000 ) ) ;
#15777=DIRECTION ( 'NONE',  ( 0.000000000000000000, -0.9407002666710296834, -0.3392388661180402165 ) ) ;
#15783=DIRECTION ( 'NONE',  ( 0.000000000000000000, 0.000000000000000000, 1.000000000000000000 ) ) ;
#15788=ORIENTED_EDGE ( 'NONE', *, *, #5477, .T. ) ;
#15789=DIRECTION ( 'NONE',  ( 0.000000000000000000, 0.9968120070307497915, 0.07978610555308651708 ) ) ;
#15795=VERTEX_POINT ( 'NONE', #8979 ) ;
#15798=VECTOR ( 'NONE', #2212, 1000.000000000000000 ) ;
#15799=CYLINDRICAL_SURFACE ( 'NONE', #41402, 120.5010000000000190 ) ;
#15800=AXIS2_PLACEMENT_3D ( 'NONE', #13746, #4091, #13957 ) ;
#15803=CIRCLE ( 'NONE', #40145, 59.00000000000000000 ) ;
#15804=DIRECTION ( 'NONE',  ( 0.000000000000000000, 0.4132121857683728749, 0.9106347728549155640 ) ) ;
#15805=ORIENTED_EDGE ( 'NONE', *, *, #42461, .T. ) ;
#15807=ORIENTED_EDGE ( 'NONE', *, *, #40703, .F. ) ;
#15811=DIRECTION ( 'NONE',  ( -1.000000000000000000, -0.000000000000000000, -0.000000000000000000 ) ) ;
#15813=DIRECTION ( 'NONE',  ( 0.000000000000000000, -0.8747630845319657178, 0.4845508703326421029 ) ) ;
#15814=VERTEX_POINT ( 'NONE', #24974 ) ;
#15820=DIRECTION ( 'NONE',  ( 0.000000000000000000, 0.4132121857683791477, -0.9106347728549126774 ) ) ;
#15822=CIRCLE ( 'NONE', #25014, 120.5010000000000190 ) ;
#15824=ORIENTED_EDGE ( 'NONE', *, *, #14351, .T. ) ;
#15831=EDGE_CURVE ( 'NONE', #39546, #6952, #24961, .T. ) ;
#15832=CIRCLE ( 'NONE', #26971, 59.00000000000000000 ) ;
#15834=CARTESIAN_POINT ( 'NONE',  ( 17.99999999999999645, 0.000000000000000000, 0.000000000000000000 ) ) ;
#15836=VERTEX_POINT ( 'NONE', #28848 ) ;
#15840=CYLINDRICAL_SURFACE ( 'NONE', #12816, 116.0000000000000000 ) ;
#15844=DIRECTION ( 'NONE',  ( -1.000000000000000000, -0.000000000000000000, -0.000000000000000000 ) ) ;
#15849=EDGE_CURVE ( 'NONE', #23547, #14512, #38638, .T. ) ;
#15851=CIRCLE ( 'NONE', #33849, 59.00000000000000000 ) ;
#15857=CARTESIAN_POINT ( 'NONE',  ( 0.000000000000000000, 0.000000000000000000, 0.000000000000000000 ) ) ;
#15861=VERTEX_POINT ( 'NONE', #31911 ) ;
#15862=CARTESIAN_POINT ( 'NONE',  ( 17.99999999999999645, 112.1427988504407551, 3.502162136923788083 ) ) ;
#15864=DIRECTION ( 'NONE',  ( -1.000000000000000000, 0.000000000000000000, -0.000000000000000000 ) ) ;
#15865=CIRCLE ( 'NONE', #38139, 120.5010000000000190 ) ;
#15866=DIRECTION ( 'NONE',  ( 1.000000000000000000, 0.000000000000000000, 0.000000000000000000 ) ) ;
#15867=CARTESIAN_POINT ( 'NONE',  ( 17.99999999999999645, 15.21076497709711184, 119.5371223922155792 ) ) ;
#15869=CARTESIAN_POINT ( 'NONE',  ( 0.000000000000000000, -108.8880088604273766, -39.99251838046071583 ) ) ;
#15872=DIRECTION ( 'NONE',  ( -1.000000000000000000, -0.000000000000000000, 0.000000000000000000 ) ) ;
#15873=AXIS2_PLACEMENT_3D ( 'NONE', #2192, #11853, #42116 ) ;
#15876=AXIS2_PLACEMENT_3D ( 'NONE', #15241, #41799, #8636 ) ;
#15877=AXIS2_PLACEMENT_3D ( 'NONE', #4901, #38273, #28056 ) ;
#15882=EDGE_CURVE ( 'NONE', #7958, #7274, #8875, .T. ) ;
#15889=DIRECTION ( 'NONE',  ( 0.000000000000000000, -0.5963673585385078635, 0.8027116379309587879 ) ) ;
#15891=EDGE_CURVE ( 'NONE', #39546, #7856, #5696, .T. ) ;
#15899=DIRECTION ( 'NONE',  ( -1.000000000000000000, -0.000000000000000000, 0.000000000000000000 ) ) ;
#15901=AXIS2_PLACEMENT_3D ( 'NONE', #8588, #21950, #5332 ) ;
#15902=CARTESIAN_POINT ( 'NONE',  ( 0.000000000000000000, -17.77780072541623113, -114.6296200873377842 ) ) ;
#15903=ORIENTED_EDGE ( 'NONE', *, *, #27935, .T. ) ;
#15905=AXIS2_PLACEMENT_3D ( 'NONE', #24479, #7633, #11147 ) ;
#15906=CARTESIAN_POINT ( 'NONE',  ( 9.000000000000001776, 42.87700105098753056, -107.7847984684000551 ) ) ;
#15908=VECTOR ( 'NONE', #34705, 1000.000000000000000 ) ;
#15912=ORIENTED_EDGE ( 'NONE', *, *, #13244, .F. ) ;
#15918=ORIENTED_EDGE ( 'NONE', *, *, #38694, .T. ) ;
#15919=DIRECTION ( 'NONE',  ( 1.000000000000000000, 0.000000000000000000, 0.000000000000000000 ) ) ;
#15920=DIRECTION ( 'NONE',  ( 0.000000000000000000, 0.2113826236296184047, 0.9774033898178678959 ) ) ;
#15921=DIRECTION ( 'NONE',  ( 1.000000000000000000, 0.000000000000000000, 0.000000000000000000 ) ) ;
#15923=LINE ( 'NONE', #9566, #7246 ) ;
#15925=EDGE_CURVE ( 'NONE', #7262, #27181, #21477, .T. ) ;
#15928=FACE_OUTER_BOUND ( 'NONE', #37494, .T. ) ;
#15931=AXIS2_PLACEMENT_3D ( 'NONE', #15347, #15133, #18850 ) ;
#15936=AXIS2_PLACEMENT_3D ( 'NONE', #9711, #26512, #39787 ) ;
#15938=EDGE_LOOP ( 'NONE', ( #23174, #20713, #18805, #18131 ) ) ;
#15939=AXIS2_PLACEMENT_3D ( 'NONE', #709, #40424, #7263 ) ;
#15942=FACE_OUTER_BOUND ( 'NONE', #33044, .T. ) ;
#15943=LINE ( 'NONE', #29236, #31130 ) ;
#15948=CARTESIAN_POINT ( 'NONE',  ( 0.000000000000000000, -80.74349901498355564, -77.90224541347362219 ) ) ;
#15951=CARTESIAN_POINT ( 'NONE',  ( 17.99999999999999645, 112.5220807139887853, -28.19186676675730752 ) ) ;
#15953=CARTESIAN_POINT ( 'NONE',  ( 17.99999999999999645, 67.32409792376505209, 89.75376489259387824 ) ) ;
#15956=FACE_OUTER_BOUND ( 'NONE', #21914, .T. ) ;
#15960=VECTOR ( 'NONE', #31628, 1000.000000000000000 ) ;
#15968=CIRCLE ( 'NONE', #6866, 59.00000000000001421 ) ;
#15969=DIRECTION ( 'NONE',  ( 0.000000000000000000, 0.000000000000000000, 1.000000000000000000 ) ) ;
#15971=DIRECTION ( 'NONE',  ( 0.000000000000000000, 0.000000000000000000, 1.000000000000000000 ) ) ;
#15972=CARTESIAN_POINT ( 'NONE',  ( 0.000000000000000000, 0.000000000000000000, 0.000000000000000000 ) ) ;
#15976=CARTESIAN_POINT ( 'NONE',  ( 0.000000000000000000, -66.49630760163542220, -90.36876423296052963 ) ) ;
#15977=ORIENTED_EDGE ( 'NONE', *, *, #27198, .T. ) ;
#15979=CARTESIAN_POINT ( 'NONE',  ( 17.99999999999999645, -47.58001226230465619, -110.7096808509488284 ) ) ;
#15980=ORIENTED_EDGE ( 'NONE', *, *, #32583, .F. ) ;
#15984=DIRECTION ( 'NONE',  ( 0.000000000000000000, -0.05322217484218560307, 0.9985826956767616114 ) ) ;
#15992=DIRECTION ( 'NONE',  ( 1.000000000000000000, 0.000000000000000000, 0.000000000000000000 ) ) ;
#15993=AXIS2_PLACEMENT_3D ( 'NONE', #3306, #23862, #26471 ) ;
#15997=LINE ( 'NONE', #42563, #8170 ) ;
#15998=CARTESIAN_POINT ( 'NONE',  ( 17.99999999999999645, -114.8812324315174038, -16.07179003769265080 ) ) ;
#15999=DIRECTION ( 'NONE',  ( -1.000000000000000000, -0.000000000000000000, -0.000000000000000000 ) ) ;
#16000=CARTESIAN_POINT ( 'NONE',  ( 17.99999999999999645, -61.59243992711522964, 93.77976230226020959 ) ) ;
#16004=CYLINDRICAL_SURFACE ( 'NONE', #17841, 120.5010000000000190 ) ;
#16007=EDGE_CURVE ( 'NONE', #9120, #9695, #36004, .T. ) ;
#16013=ORIENTED_EDGE ( 'NONE', *, *, #11175, .T. ) ;
#16014=ORIENTED_EDGE ( 'NONE', *, *, #27431, .F. ) ;
#16016=CARTESIAN_POINT ( 'NONE',  ( 0.000000000000000000, -107.2703412112697094, 32.88383143828427535 ) ) ;
#16017=AXIS2_PLACEMENT_3D ( 'NONE', #17348, #30625, #37361 ) ;
#16018=VECTOR ( 'NONE', #957, 1000.000000000000000 ) ;
#16022=DIRECTION ( 'NONE',  ( -1.000000000000000000, -0.000000000000000000, -0.000000000000000000 ) ) ;
#16025=ORIENTED_EDGE ( 'NONE', *, *, #36626, .T. ) ;
#16030=DIRECTION ( 'NONE',  ( 0.000000000000000000, 3.198947698072485022E-14, -1.000000000000000000 ) ) ;
#16031=VERTEX_POINT ( 'NONE', #16853 ) ;
#16033=VERTEX_POINT ( 'NONE', #19683 ) ;
#16036=CARTESIAN_POINT ( 'NONE',  ( 0.000000000000000000, 91.51415974874592507, 64.91094698989330425 ) ) ;
#16039=ORIENTED_EDGE ( 'NONE', *, *, #35981, .F. ) ;
#16040=DIRECTION ( 'NONE',  ( 1.000000000000000000, 0.000000000000000000, 0.000000000000000000 ) ) ;
#16042=DIRECTION ( 'NONE',  ( -1.000000000000000000, -0.000000000000000000, 0.000000000000000000 ) ) ;
#16043=ORIENTED_EDGE ( 'NONE', *, *, #31312, .F. ) ;
#16046=CIRCLE ( 'NONE', #20960, 59.00000000000000000 ) ;
#16047=CIRCLE ( 'NONE', #37597, 59.00000000000000711 ) ;
#16049=LINE ( 'NONE', #29555, #35986 ) ;
#16051=ORIENTED_EDGE ( 'NONE', *, *, #10027, .F. ) ;
#16053=ORIENTED_EDGE ( 'NONE', *, *, #10369, .T. ) ;
#16055=CARTESIAN_POINT ( 'NONE',  ( 8.999999999999998224, 91.65951123222482977, 71.09524597798119316 ) ) ;
#16058=DIRECTION ( 'NONE',  ( 0.000000000000000000, 0.1062934856473589651, 0.9943348002101377592 ) ) ;
#16064=DIRECTION ( 'NONE',  ( 1.000000000000000000, -0.000000000000000000, -0.000000000000000000 ) ) ;
#16069=EDGE_CURVE ( 'NONE', #21133, #27409, #7459, .T. ) ;
#16070=ORIENTED_EDGE ( 'NONE', *, *, #33144, .T. ) ;
#16073=CIRCLE ( 'NONE', #8388, 116.0000000000000000 ) ;
#16081=ORIENTED_EDGE ( 'NONE', *, *, #32483, .F. ) ;
#16082=DIRECTION ( 'NONE',  ( 0.000000000000000000, -0.1590634960190788760, 0.9872683547213435551 ) ) ;
#16085=DIRECTION ( 'NONE',  ( 0.000000000000000000, 0.000000000000000000, 1.000000000000000000 ) ) ;
#16086=ORIENTED_EDGE ( 'NONE', *, *, #17738, .T. ) ;
#16092=EDGE_LOOP ( 'NONE', ( #37684, #16436, #36258, #8637 ) ) ;
#16093=CARTESIAN_POINT ( 'NONE',  ( 17.99999999999999645, -112.1702510623870239, -2.471285140323770335 ) ) ;
#16094=EDGE_CURVE ( 'NONE', #41377, #6181, #38846, .T. ) ;
#16095=DIRECTION ( 'NONE',  ( -1.000000000000000000, -0.000000000000000000, -0.000000000000000000 ) ) ;
#16097=DIRECTION ( 'NONE',  ( -1.000000000000000000, 0.000000000000000000, 0.000000000000000000 ) ) ;
#16098=AXIS2_PLACEMENT_3D ( 'NONE', #22090, #32285, #35747 ) ;
#16101=AXIS2_PLACEMENT_3D ( 'NONE', #39185, #2947, #42032 ) ;
#16105=AXIS2_PLACEMENT_3D ( 'NONE', #24150, #10821, #30464 ) ;
#16106=DIRECTION ( 'NONE',  ( 0.000000000000000000, 0.000000000000000000, 1.000000000000000000 ) ) ;
#16107=CARTESIAN_POINT ( 'NONE',  ( 17.99999999999999645, 118.8387007424473580, -19.94628303336373065 ) ) ;
#16111=ORIENTED_EDGE ( 'NONE', *, *, #19051, .F. ) ;
#16113=FACE_OUTER_BOUND ( 'NONE', #894, .T. ) ;
#16116=DIRECTION ( 'NONE',  ( -1.000000000000000000, -0.000000000000000000, 0.000000000000000000 ) ) ;
#16117=ORIENTED_EDGE ( 'NONE', *, *, #21705, .T. ) ;
#16121=EDGE_CURVE ( 'NONE', #4402, #39721, #30777, .T. ) ;
#16122=ORIENTED_EDGE ( 'NONE', *, *, #27351, .F. ) ;
#16126=CARTESIAN_POINT ( 'NONE',  ( 8.999999999999998224, 115.9387338813861419, 3.769613505536451026 ) ) ;
#16128=DIRECTION ( 'NONE',  ( -1.000000000000000000, -0.000000000000000000, -0.000000000000000000 ) ) ;
#16130=CARTESIAN_POINT ( 'NONE',  ( 0.000000000000000000, -114.6488492393077081, -37.09625815500128709 ) ) ;
#16132=LINE ( 'NONE', #10203, #11766 ) ;
#16144=AXIS2_PLACEMENT_3D ( 'NONE', #7488, #37375, #493 ) ;
#16148=CARTESIAN_POINT ( 'NONE',  ( 0.000000000000000000, 98.69720329640956891, 60.94966826379944536 ) ) ;
#16149=CARTESIAN_POINT ( 'NONE',  ( 0.000000000000000000, 108.8880088604276608, 39.99251838045997687 ) ) ;
#16151=DIRECTION ( 'NONE',  ( -1.000000000000000000, -0.000000000000000000, -0.000000000000000000 ) ) ;
#16152=ORIENTED_EDGE ( 'NONE', *, *, #21157, .T. ) ;
#16154=DIRECTION ( 'NONE',  ( 0.000000000000000000, 0.000000000000000000, 1.000000000000000000 ) ) ;
#16155=VERTEX_POINT ( 'NONE', #34458 ) ;
#16156=DIRECTION ( 'NONE',  ( -1.000000000000000000, -0.000000000000000000, 0.000000000000000000 ) ) ;
#16159=ADVANCED_FACE ( 'NONE', ( #17289 ), #4568, .F. ) ;
#16164=EDGE_CURVE ( 'NONE', #6044, #1782, #39521, .T. ) ;
#16165=AXIS2_PLACEMENT_3D ( 'NONE', #38125, #14603, #31812 ) ;
#16166=ORIENTED_EDGE ( 'NONE', *, *, #42085, .F. ) ;
#16170=EDGE_CURVE ( 'NONE', #31963, #21287, #27049, .T. ) ;
#16171=AXIS2_PLACEMENT_3D ( 'NONE', #33019, #29994, #22606 ) ;
#16174=ADVANCED_FACE ( 'NONE', ( #4128 ), #20998, .F. ) ;
#16175=DIRECTION ( 'NONE',  ( -1.000000000000000000, 0.000000000000000000, -0.000000000000000000 ) ) ;
#16176=DIRECTION ( 'NONE',  ( 0.000000000000000000, 0.000000000000000000, 1.000000000000000000 ) ) ;
#16178=ORIENTED_EDGE ( 'NONE', *, *, #11244, .T. ) ;
#16180=DIRECTION ( 'NONE',  ( 1.000000000000000000, 0.000000000000000000, 0.000000000000000000 ) ) ;
#16183=DIRECTION ( 'NONE',  ( 1.000000000000000000, 0.000000000000000000, 0.000000000000000000 ) ) ;
#16188=VERTEX_POINT ( 'NONE', #636 ) ;
#16189=DIRECTION ( 'NONE',  ( -1.000000000000000000, 0.000000000000000000, 0.000000000000000000 ) ) ;
#16191=ADVANCED_FACE ( 'NONE', ( #7421 ), #34042, .F. ) ;
#16193=ORIENTED_EDGE ( 'NONE', *, *, #27421, .F. ) ;
#16198=CIRCLE ( 'NONE', #99, 59.00000000000001421 ) ;
#16203=CARTESIAN_POINT ( 'NONE',  ( -10.00000000000000000, 0.000000000000000000, 0.000000000000000000 ) ) ;
#16205=DIRECTION ( 'NONE',  ( -1.000000000000000000, -0.000000000000000000, 0.000000000000000000 ) ) ;
#16206=DIRECTION ( 'NONE',  ( -1.000000000000000000, 0.000000000000000000, -0.000000000000000000 ) ) ;
#16208=ORIENTED_EDGE ( 'NONE', *, *, #9698, .F. ) ;
#16211=VERTEX_POINT ( 'NONE', #40560 ) ;
#16214=VERTEX_POINT ( 'NONE', #14206 ) ;
#16219=AXIS2_PLACEMENT_3D ( 'NONE', #35700, #36138, #22665 ) ;
#16221=AXIS2_PLACEMENT_3D ( 'NONE', #21249, #41250, #11396 ) ;
#16222=VERTEX_POINT ( 'NONE', #37526 ) ;
#16223=DIRECTION ( 'NONE',  ( 1.000000000000000000, 0.000000000000000000, 0.000000000000000000 ) ) ;
#16227=LINE ( 'NONE', #19513, #30311 ) ;
#16228=EDGE_CURVE ( 'NONE', #6410, #821, #33599, .T. ) ;
#16230=CYLINDRICAL_SURFACE ( 'NONE', #13269, 59.00000000000000000 ) ;
#16231=EDGE_LOOP ( 'NONE', ( #26276, #422, #19519, #9425 ) ) ;
#16232=CARTESIAN_POINT ( 'NONE',  ( 0.000000000000000000, 0.000000000000000000, 0.000000000000000000 ) ) ;
#16236=DIRECTION ( 'NONE',  ( 0.000000000000000000, -0.4610925014493144625, -0.8873520750565775383 ) ) ;
#16237=CARTESIAN_POINT ( 'NONE',  ( 0.000000000000000000, 93.26762629039527042, -76.29967815892260319 ) ) ;
#16240=CARTESIAN_POINT ( 'NONE',  ( 0.000000000000000000, 0.000000000000000000, 0.000000000000000000 ) ) ;
#16241=ORIENTED_EDGE ( 'NONE', *, *, #18892, .T. ) ;
#16242=CARTESIAN_POINT ( 'NONE',  ( 17.99999999999999645, 0.000000000000000000, 0.000000000000000000 ) ) ;
#16244=DIRECTION ( 'NONE',  ( 1.000000000000000000, 0.000000000000000000, 0.000000000000000000 ) ) ;
#16245=EDGE_LOOP ( 'NONE', ( #39533, #4424, #19124, #40822 ) ) ;
#16248=DIRECTION ( 'NONE',  ( 1.000000000000000000, 0.000000000000000000, 0.000000000000000000 ) ) ;
#16250=EDGE_CURVE ( 'NONE', #29621, #31163, #18368, .T. ) ;
#16251=EDGE_LOOP ( 'NONE', ( #28222, #27180, #27648, #1935 ) ) ;
#16255=CIRCLE ( 'NONE', #42705, 116.0000000000000000 ) ;
#16259=ADVANCED_FACE ( 'NONE', ( #28596 ), #1725, .F. ) ;
#16260=CARTESIAN_POINT ( 'NONE',  ( 0.000000000000000000, 99.97660604679964536, 67.26937820704921478 ) ) ;
#16262=DIRECTION ( 'NONE',  ( -1.000000000000000000, 0.000000000000000000, -0.000000000000000000 ) ) ;
#16263=EDGE_LOOP ( 'NONE', ( #23410, #41937, #25983, #13146 ) ) ;
#16264=AXIS2_PLACEMENT_3D ( 'NONE', #39234, #22948, #39456 ) ;
#16266=DIRECTION ( 'NONE',  ( 1.000000000000000000, 0.000000000000000000, 0.000000000000000000 ) ) ;
#16270=CARTESIAN_POINT ( 'NONE',  ( 0.000000000000000000, 6.486220790509957368, -112.0098273076986715 ) ) ;
#16273=CARTESIAN_POINT ( 'NONE',  ( 0.000000000000000000, -117.6086855750632765, -26.24286718912224003 ) ) ;
#16274=CYLINDRICAL_SURFACE ( 'NONE', #42233, 116.0000000000000000 ) ;
#16281=ORIENTED_EDGE ( 'NONE', *, *, #4490, .T. ) ;
#16282=LINE ( 'NONE', #39365, #36729 ) ;
#16283=VERTEX_POINT ( 'NONE', #22066 ) ;
#16284=DIRECTION ( 'NONE',  ( 1.000000000000000000, 0.000000000000000000, 0.000000000000000000 ) ) ;
#16285=DIRECTION ( 'NONE',  ( 1.000000000000000000, -0.000000000000000000, -0.000000000000000000 ) ) ;
#16287=ORIENTED_EDGE ( 'NONE', *, *, #14322, .T. ) ;
#16289=DIRECTION ( 'NONE',  ( 0.000000000000000000, 0.000000000000000000, 1.000000000000000000 ) ) ;
#16291=AXIS2_PLACEMENT_3D ( 'NONE', #23948, #13055, #20254 ) ;
#16292=CARTESIAN_POINT ( 'NONE',  ( 0.000000000000000000, 0.000000000000000000, 0.000000000000000000 ) ) ;
#16297=CIRCLE ( 'NONE', #33680, 59.00000000000000000 ) ;
#16298=DIRECTION ( 'NONE',  ( 0.000000000000000000, 0.000000000000000000, 1.000000000000000000 ) ) ;
#16299=ORIENTED_EDGE ( 'NONE', *, *, #6856, .F. ) ;
#16302=CARTESIAN_POINT ( 'NONE',  ( 0.000000000000000000, 29.02167576844250618, -108.3790330702166926 ) ) ;
#16307=CARTESIAN_POINT ( 'NONE',  ( 0.000000000000000000, 112.5120133921107737, 43.14554256761054063 ) ) ;
#16308=ORIENTED_EDGE ( 'NONE', *, *, #35830, .F. ) ;
#16310=EDGE_CURVE ( 'NONE', #39322, #34186, #10302, .T. ) ;
#16313=DIRECTION ( 'NONE',  ( 0.000000000000000000, 0.000000000000000000, 1.000000000000000000 ) ) ;
#16315=ADVANCED_FACE ( 'NONE', ( #31430 ), #5221, .F. ) ;
#16317=DIRECTION ( 'NONE',  ( 1.000000000000000000, 0.000000000000000000, 0.000000000000000000 ) ) ;
#16318=ORIENTED_EDGE ( 'NONE', *, *, #21810, .F. ) ;
#16327=VECTOR ( 'NONE', #27037, 1000.000000000000000 ) ;
#16330=DIRECTION ( 'NONE',  ( -1.000000000000000000, -0.000000000000000000, 0.000000000000000000 ) ) ;
#16332=CARTESIAN_POINT ( 'NONE',  ( 17.99999999999999645, -111.9370513079666409, -44.61600100275288838 ) ) ;
#16339=CIRCLE ( 'NONE', #27453, 58.99999999999999289 ) ;
#16341=CARTESIAN_POINT ( 'NONE',  ( 0.000000000000000000, 35.72777019205667415, 106.3569410558018404 ) ) ;
#16345=ORIENTED_EDGE ( 'NONE', *, *, #25056, .T. ) ;
#16353=CARTESIAN_POINT ( 'NONE',  ( 0.000000000000000000, 6.486220790508443912, 112.0098273076987567 ) ) ;
#16355=DIRECTION ( 'NONE',  ( -1.000000000000000000, 0.000000000000000000, 0.000000000000000000 ) ) ;
#16356=CIRCLE ( 'NONE', #19862, 116.0000000000000000 ) ;
#16358=AXIS2_PLACEMENT_3D ( 'NONE', #15463, #15264, #18967 ) ;
#16359=VERTEX_POINT ( 'NONE', #27955 ) ;
#16360=CARTESIAN_POINT ( 'NONE',  ( 17.99999999999999645, 109.4038418350903470, 50.51029986767587587 ) ) ;
#16362=AXIS2_PLACEMENT_3D ( 'NONE', #12655, #16596, #39226 ) ;
#16363=EDGE_LOOP ( 'NONE', ( #38122, #30804, #10876, #33386 ) ) ;
#16365=DIRECTION ( 'NONE',  ( -1.000000000000000000, -0.000000000000000000, -0.000000000000000000 ) ) ;
#16366=ADVANCED_FACE ( 'NONE', ( #18160 ), #28159, .F. ) ;
#16367=ORIENTED_EDGE ( 'NONE', *, *, #13436, .F. ) ;
#16368=LINE ( 'NONE', #29674, #37813 ) ;
#16369=AXIS2_PLACEMENT_3D ( 'NONE', #25888, #9060, #35460 ) ;
#16370=ADVANCED_FACE ( 'NONE', ( #5013 ), #10408, .F. ) ;
#16371=DIRECTION ( 'NONE',  ( 0.000000000000000000, -0.1590634960190789038, 0.9872683547213435551 ) ) ;
#16376=VERTEX_POINT ( 'NONE', #23743 ) ;
#16381=CARTESIAN_POINT ( 'NONE',  ( 0.000000000000000000, -110.3490479609633752, 20.28201389785361641 ) ) ;
#16382=CARTESIAN_POINT ( 'NONE',  ( 17.99999999999999645, 68.61497464550731706, -99.05794392877534449 ) ) ;
#16383=EDGE_CURVE ( 'NONE', #10188, #37671, #41629, .T. ) ;
#16386=CIRCLE ( 'NONE', #9415, 58.99999999999999289 ) ;
#16388=VERTEX_POINT ( 'NONE', #14344 ) ;
#16390=CARTESIAN_POINT ( 'NONE',  ( 17.99999999999999645, 0.000000000000000000, 0.000000000000000000 ) ) ;
#16391=DIRECTION ( 'NONE',  ( 1.000000000000000000, 0.000000000000000000, 0.000000000000000000 ) ) ;
#16393=EDGE_CURVE ( 'NONE', #34831, #14549, #571, .T. ) ;
#16394=VERTEX_POINT ( 'NONE', #33737 ) ;
#16398=AXIS2_PLACEMENT_3D ( 'NONE', #30058, #16979, #40042 ) ;
#16403=AXIS2_PLACEMENT_3D ( 'NONE', #9286, #6014, #1883 ) ;
#16408=CARTESIAN_POINT ( 'NONE',  ( 17.99999999999999645, 6.854627147198713466, 115.7972974066013734 ) ) ;
#16410=DIRECTION ( 'NONE',  ( 0.000000000000000000, -0.5963673585385078635, 0.8027116379309587879 ) ) ;
#16414=AXIS2_PLACEMENT_3D ( 'NONE', #13160, #6362, #19287 ) ;
#16416=ADVANCED_FACE ( 'NONE', ( #7776 ), #7120, .F. ) ;
#16417=AXIS2_PLACEMENT_3D ( 'NONE', #21564, #31543, #41561 ) ;
#16419=CARTESIAN_POINT ( 'NONE',  ( 0.000000000000000000, 115.6826031496112392, 8.575274253897841703 ) ) ;
#16421=AXIS2_PLACEMENT_3D ( 'NONE', #37956, #34697, #4354 ) ;
#16423=CIRCLE ( 'NONE', #23407, 59.00000000000000000 ) ;
#16427=CIRCLE ( 'NONE', #31745, 59.00000000000000711 ) ;
#16428=DIRECTION ( 'NONE',  ( 1.000000000000000000, 0.000000000000000000, 0.000000000000000000 ) ) ;
#16431=VECTOR ( 'NONE', #37393, 1000.000000000000000 ) ;
#16435=CIRCLE ( 'NONE', #42868, 59.00000000000000711 ) ;
#16436=ORIENTED_EDGE ( 'NONE', *, *, #27985, .T. ) ;
#16438=ORIENTED_EDGE ( 'NONE', *, *, #34743, .F. ) ;
#16442=EDGE_CURVE ( 'NONE', #18211, #41769, #27216, .T. ) ;
#16444=DIRECTION ( 'NONE',  ( 1.000000000000000000, -0.000000000000000000, -0.000000000000000000 ) ) ;
#16447=DIRECTION ( 'NONE',  ( 0.000000000000000000, 0.9911528310040066403, 0.1327255272837255529 ) ) ;
#16449=DIRECTION ( 'NONE',  ( -1.000000000000000000, -0.000000000000000000, 0.000000000000000000 ) ) ;
#16459=CARTESIAN_POINT ( 'NONE',  ( 17.99999999999999645, 109.1131968883995000, 26.12628443612074847 ) ) ;
#16461=ORIENTED_EDGE ( 'NONE', *, *, #16829, .T. ) ;
#16462=CIRCLE ( 'NONE', #42204, 116.0000000000000000 ) ;
#16469=CIRCLE ( 'NONE', #33131, 59.00000000000000000 ) ;
#16470=CIRCLE ( 'NONE', #36633, 59.00000000000000000 ) ;
#16471=VERTEX_POINT ( 'NONE', #21351 ) ;
#16472=DIRECTION ( 'NONE',  ( 0.000000000000000000, -0.6382441836448261574, 0.7698339834299011697 ) ) ;
#16474=EDGE_CURVE ( 'NONE', #31337, #40745, #34604, .T. ) ;
#16475=ORIENTED_EDGE ( 'NONE', *, *, #301, .T. ) ;
#16477=EDGE_CURVE ( 'NONE', #27385, #1786, #18086, .T. ) ;
#16482=CARTESIAN_POINT ( 'NONE',  ( 17.99999999999999645, 80.74349901498408144, 77.90224541347306797 ) ) ;
#16486=DIRECTION ( 'NONE',  ( 0.000000000000000000, 0.000000000000000000, 1.000000000000000000 ) ) ;
#16489=CARTESIAN_POINT ( 'NONE',  ( 0.000000000000000000, -110.1579703617967567, 21.29539948940213634 ) ) ;
#16490=CIRCLE ( 'NONE', #37348, 120.5010000000000332 ) ;
#16492=VECTOR ( 'NONE', #382, 1000.000000000000000 ) ;
#16494=AXIS2_PLACEMENT_3D ( 'NONE', #17376, #37171, #16724 ) ;
#16496=AXIS2_PLACEMENT_3D ( 'NONE', #2023, #28886, #38254 ) ;
#16499=CARTESIAN_POINT ( 'NONE',  ( 0.000000000000000000, 109.3506818544110217, 38.70953859161051014 ) ) ;
#16502=ADVANCED_FACE ( 'NONE', ( #42206 ), #15633, .F. ) ;
#16505=EDGE_CURVE ( 'NONE', #252, #10316, #2070, .T. ) ;
#16508=EDGE_CURVE ( 'NONE', #42137, #1326, #39556, .T. ) ;
#16509=AXIS2_PLACEMENT_3D ( 'NONE', #43145, #13294, #26592 ) ;
#16512=FACE_OUTER_BOUND ( 'NONE', #11620, .T. ) ;
#16514=CARTESIAN_POINT ( 'NONE',  ( 17.99999999999999645, 0.000000000000000000, 0.000000000000000000 ) ) ;
#16515=DIRECTION ( 'NONE',  ( 0.000000000000000000, 0.3641605752528230266, -0.9313361774523380987 ) ) ;
#16518=CARTESIAN_POINT ( 'NONE',  ( 0.000000000000000000, -104.2166695095708349, -60.49278301857916063 ) ) ;
#16519=DIRECTION ( 'NONE',  ( 1.000000000000000000, -0.000000000000000000, -0.000000000000000000 ) ) ;
#16520=FACE_OUTER_BOUND ( 'NONE', #26963, .T. ) ;
#16522=ORIENTED_EDGE ( 'NONE', *, *, #31324, .F. ) ;
#16525=CIRCLE ( 'NONE', #35997, 116.0000000000000000 ) ;
#16527=AXIS2_PLACEMENT_3D ( 'NONE', #39946, #40166, #6165 ) ;
#16528=CARTESIAN_POINT ( 'NONE',  ( 9.000000000000001776, -115.9387338813861277, -3.769613505537241949 ) ) ;
#16529=VERTEX_POINT ( 'NONE', #31556 ) ;
#16532=DIRECTION ( 'NONE',  ( 0.000000000000000000, 0.000000000000000000, 1.000000000000000000 ) ) ;
#16534=CIRCLE ( 'NONE', #26980, 120.5010000000000332 ) ;
#16536=EDGE_CURVE ( 'NONE', #27165, #8980, #22218, .T. ) ;
#16538=CARTESIAN_POINT ( 'NONE',  ( 17.99999999999999645, 0.000000000000000000, 0.000000000000000000 ) ) ;
#16539=CARTESIAN_POINT ( 'NONE',  ( 17.99999999999999645, -109.4038418350900059, -50.51029986767660773 ) ) ;
#16542=AXIS2_PLACEMENT_3D ( 'NONE', #11155, #21213, #24484 ) ;
#16543=ORIENTED_EDGE ( 'NONE', *, *, #2752, .T. ) ;
#16545=DIRECTION ( 'NONE',  ( 0.000000000000000000, 0.7865515558026396903, 0.6175246149461955936 ) ) ;
#16546=CIRCLE ( 'NONE', #5367, 59.00000000000001421 ) ;
#16554=ORIENTED_EDGE ( 'NONE', *, *, #7738, .F. ) ;
#16561=EDGE_CURVE ( 'NONE', #2432, #37344, #5142, .T. ) ;
#16565=EDGE_CURVE ( 'NONE', #37962, #28053, #20816, .T. ) ;
#16567=VERTEX_POINT ( 'NONE', #28732 ) ;
#16573=AXIS2_PLACEMENT_3D ( 'NONE', #19784, #33048, #42218 ) ;
#16574=DIRECTION ( 'NONE',  ( 1.000000000000000000, 0.000000000000000000, 0.000000000000000000 ) ) ;
#16577=VERTEX_POINT ( 'NONE', #35462 ) ;
#16578=CYLINDRICAL_SURFACE ( 'NONE', #38379, 116.0000000000000000 ) ;
#16579=EDGE_CURVE ( 'NONE', #11572, #24177, #36793, .T. ) ;
#16583=ORIENTED_EDGE ( 'NONE', *, *, #14351, .F. ) ;
#16584=EDGE_CURVE ( 'NONE', #27244, #4304, #18504, .T. ) ;
#16585=CYLINDRICAL_SURFACE ( 'NONE', #16509, 59.00000000000000000 ) ;
#16589=ORIENTED_EDGE ( 'NONE', *, *, #12479, .F. ) ;
#16591=ORIENTED_EDGE ( 'NONE', *, *, #4100, .T. ) ;
#16596=DIRECTION ( 'NONE',  ( 1.000000000000000000, 0.000000000000000000, 0.000000000000000000 ) ) ;
#16599=EDGE_LOOP ( 'NONE', ( #16672, #28839, #5720, #37028 ) ) ;
#16600=VECTOR ( 'NONE', #22960, 1000.000000000000000 ) ;
#16604=CIRCLE ( 'NONE', #19374, 58.99999999999998579 ) ;
#16609=LINE ( 'NONE', #29902, #30175 ) ;
#16611=DIRECTION ( 'NONE',  ( 0.000000000000000000, -1.152562038276115876E-14, -1.000000000000000000 ) ) ;
#16613=CARTESIAN_POINT ( 'NONE',  ( 17.99999999999999645, -78.75547124681429523, 91.20343606296975736 ) ) ;
#16618=EDGE_CURVE ( 'NONE', #16033, #13299, #18734, .T. ) ;
#16620=DIRECTION ( 'NONE',  ( 0.000000000000000000, 0.9407002666710319039, 0.3392388661180341658 ) ) ;
#16621=FACE_OUTER_BOUND ( 'NONE', #5746, .T. ) ;
#16627=EDGE_CURVE ( 'NONE', #36886, #21959, #1946, .T. ) ;
#16628=VECTOR ( 'NONE', #7335, 1000.000000000000000 ) ;
#16633=CARTESIAN_POINT ( 'NONE',  ( 17.99999999999999645, 54.09091620264857880, -102.6166301549512525 ) ) ;
#16644=CARTESIAN_POINT ( 'NONE',  ( 17.99999999999999645, 0.000000000000000000, 0.000000000000000000 ) ) ;
#16646=ORIENTED_EDGE ( 'NONE', *, *, #21960, .T. ) ;
#16647=LINE ( 'NONE', #29934, #14055 ) ;
#16649=DIRECTION ( 'NONE',  ( 1.000000000000000000, 0.000000000000000000, 0.000000000000000000 ) ) ;
#16652=CARTESIAN_POINT ( 'NONE',  ( 0.000000000000000000, 114.1157422997283248, 20.82300072952973480 ) ) ;
#16653=EDGE_CURVE ( 'NONE', #36927, #10297, #11042, .T. ) ;
#16654=DIRECTION ( 'NONE',  ( -1.000000000000000000, -0.000000000000000000, -0.000000000000000000 ) ) ;
#16658=CARTESIAN_POINT ( 'NONE',  ( 0.000000000000000000, 15.21076497709875852, -119.5371223922153519 ) ) ;
#16659=CARTESIAN_POINT ( 'NONE',  ( 0.000000000000000000, 75.03166794516801019, 94.29071961951534320 ) ) ;
#16660=AXIS2_PLACEMENT_3D ( 'NONE', #17811, #31519, #31087 ) ;
#16661=VERTEX_POINT ( 'NONE', #6216 ) ;
#16667=DIRECTION ( 'NONE',  ( 0.000000000000000000, 0.000000000000000000, 1.000000000000000000 ) ) ;
#16671=VERTEX_POINT ( 'NONE', #64 ) ;
#16672=ORIENTED_EDGE ( 'NONE', *, *, #39181, .F. ) ;
#16674=CARTESIAN_POINT ( 'NONE',  ( 17.99999999999999645, -100.6739960869721102, 49.52796165323228195 ) ) ;
#16676=CARTESIAN_POINT ( 'NONE',  ( 17.99999999999999645, -72.00556975657760006, 86.04342158279364128 ) ) ;
#16677=EDGE_CURVE ( 'NONE', #566, #18966, #34722, .T. ) ;
#16678=CARTESIAN_POINT ( 'NONE',  ( 17.99999999999999645, -30.01658535635337444, 108.1077105353196970 ) ) ;
#16679=VERTEX_POINT ( 'NONE', #16273 ) ;
#16682=CARTESIAN_POINT ( 'NONE',  ( 9.000000000000001776, 113.8630351447208824, -22.16324045874292636 ) ) ;
#16683=DIRECTION ( 'NONE',  ( -1.000000000000000000, -0.000000000000000000, 0.000000000000000000 ) ) ;
#16685=AXIS2_PLACEMENT_3D ( 'NONE', #18267, #14971, #18059 ) ;
#16687=LINE ( 'NONE', #23660, #30529 ) ;
#16689=ORIENTED_EDGE ( 'NONE', *, *, #12641, .F. ) ;
#16691=ORIENTED_EDGE ( 'NONE', *, *, #7648, .T. ) ;
#16693=DIRECTION ( 'NONE',  ( 0.000000000000000000, -0.9213119778704086382, -0.3888241754733307021 ) ) ;
#16695=DIRECTION ( 'NONE',  ( 1.000000000000000000, 0.000000000000000000, 0.000000000000000000 ) ) ;
#16696=ORIENTED_EDGE ( 'NONE', *, *, #17408, .F. ) ;
#16699=CARTESIAN_POINT ( 'NONE',  ( 0.000000000000000000, -111.9370513079672520, 44.61600100275137493 ) ) ;
#16700=ORIENTED_EDGE ( 'NONE', *, *, #3878, .T. ) ;
#16702=EDGE_LOOP ( 'NONE', ( #29126, #7811, #9758, #33442 ) ) ;
#16706=DIRECTION ( 'NONE',  ( 1.000000000000000000, -0.000000000000000000, -0.000000000000000000 ) ) ;
#16707=DIRECTION ( 'NONE',  ( 0.000000000000000000, 0.000000000000000000, 1.000000000000000000 ) ) ;
#16710=CARTESIAN_POINT ( 'NONE',  ( 0.000000000000000000, 0.000000000000000000, 0.000000000000000000 ) ) ;
#16714=CIRCLE ( 'NONE', #10420, 59.00000000000002132 ) ;
#16718=VERTEX_POINT ( 'NONE', #39995 ) ;
#16720=EDGE_CURVE ( 'NONE', #10939, #22195, #32622, .T. ) ;
#16724=DIRECTION ( 'NONE',  ( 0.000000000000000000, 0.000000000000000000, 1.000000000000000000 ) ) ;
#16728=VERTEX_POINT ( 'NONE', #16499 ) ;
#16730=VERTEX_POINT ( 'NONE', #23056 ) ;
#16733=DIRECTION ( 'NONE',  ( 1.000000000000000000, 0.000000000000000000, 0.000000000000000000 ) ) ;
#16735=ORIENTED_EDGE ( 'NONE', *, *, #36548, .F. ) ;
#16739=LINE ( 'NONE', #12590, #5505 ) ;
#16740=AXIS2_PLACEMENT_3D ( 'NONE', #22578, #35820, #8582 ) ;
#16741=CARTESIAN_POINT ( 'NONE',  ( 17.99999999999999645, -24.22031524825905890, -109.5520369638039710 ) ) ;
#16745=VECTOR ( 'NONE', #20556, 1000.000000000000000 ) ;
#16746=DIRECTION ( 'NONE',  ( 0.000000000000000000, 0.000000000000000000, 1.000000000000000000 ) ) ;
#16748=DIRECTION ( 'NONE',  ( -1.000000000000000000, -0.000000000000000000, -0.000000000000000000 ) ) ;
#16751=CYLINDRICAL_SURFACE ( 'NONE', #34460, 58.99999999999999289 ) ;
#16754=FACE_OUTER_BOUND ( 'NONE', #41549, .T. ) ;
#16757=EDGE_CURVE ( 'NONE', #30050, #34978, #17191, .T. ) ;
#16759=EDGE_CURVE ( 'NONE', #20222, #2394, #41526, .T. ) ;
#16765=CARTESIAN_POINT ( 'NONE',  ( 0.000000000000000000, 0.000000000000000000, 0.000000000000000000 ) ) ;
#16766=CYLINDRICAL_SURFACE ( 'NONE', #375, 59.00000000000000000 ) ;
#16768=CARTESIAN_POINT ( 'NONE',  ( -10.00000000000000000, 0.000000000000000000, 0.000000000000000000 ) ) ;
#16770=DIRECTION ( 'NONE',  ( 0.000000000000000000, 0.000000000000000000, 1.000000000000000000 ) ) ;
#16771=EDGE_LOOP ( 'NONE', ( #33350, #15204, #19256, #25798 ) ) ;
#16773=CIRCLE ( 'NONE', #29991, 58.99999999999998579 ) ;
#16776=AXIS2_PLACEMENT_3D ( 'NONE', #1732, #41006, #4573 ) ;
#16781=DIRECTION ( 'NONE',  ( -1.000000000000000000, -0.000000000000000000, 0.000000000000000000 ) ) ;
#16783=ORIENTED_EDGE ( 'NONE', *, *, #18111, .T. ) ;
#16788=LINE ( 'NONE', #10422, #39454 ) ;
#16790=FACE_OUTER_BOUND ( 'NONE', #7041, .T. ) ;
#16791=ORIENTED_EDGE ( 'NONE', *, *, #2285, .F. ) ;
#16803=CIRCLE ( 'NONE', #39720, 59.00000000000000711 ) ;
#16817=EDGE_CURVE ( 'NONE', #7190, #20690, #11599, .T. ) ;
#16818=VERTEX_POINT ( 'NONE', #16984 ) ;
#16821=DIRECTION ( 'NONE',  ( -1.000000000000000000, 0.000000000000000000, 0.000000000000000000 ) ) ;
#16824=EDGE_CURVE ( 'NONE', #3775, #8700, #26568, .T. ) ;
#16825=CARTESIAN_POINT ( 'NONE',  ( 0.000000000000000000, -112.5120133921110295, 43.14554256760978745 ) ) ;
#16829=EDGE_CURVE ( 'NONE', #32698, #37380, #8089, .T. ) ;
#16833=VECTOR ( 'NONE', #1419, 1000.000000000000000 ) ;
#16835=LINE ( 'NONE', #20321, #37332 ) ;
#16838=AXIS2_PLACEMENT_3D ( 'NONE', #29177, #9512, #9288 ) ;
#16839=ORIENTED_EDGE ( 'NONE', *, *, #41036, .T. ) ;
#16841=DIRECTION ( 'NONE',  ( -1.000000000000000000, 0.000000000000000000, -0.000000000000000000 ) ) ;
#16847=DIRECTION ( 'NONE',  ( 0.000000000000000000, 0.7164567402983115230, 0.6976315211349884970 ) ) ;
#16850=CARTESIAN_POINT ( 'NONE',  ( -10.00000000000000000, 0.000000000000000000, 0.000000000000000000 ) ) ;
#16853=CARTESIAN_POINT ( 'NONE',  ( 17.99999999999999645, -120.2856157092987388, 7.201503623196430226 ) ) ;
#16854=ORIENTED_EDGE ( 'NONE', *, *, #4580, .T. ) ;
#16855=CIRCLE ( 'NONE', #22434, 116.0000000000000000 ) ;
#16862=EDGE_CURVE ( 'NONE', #5549, #23636, #38724, .T. ) ;
#16864=ORIENTED_EDGE ( 'NONE', *, *, #6289, .F. ) ;
#16866=CIRCLE ( 'NONE', #11973, 120.5010000000000190 ) ;
#16867=CARTESIAN_POINT ( 'NONE',  ( 17.99999999999999645, 0.000000000000000000, 0.000000000000000000 ) ) ;
#16872=LINE ( 'NONE', #209, #32565 ) ;
#16873=EDGE_LOOP ( 'NONE', ( #6086, #6644, #14243, #39014 ) ) ;
#16874=EDGE_CURVE ( 'NONE', #41968, #7568, #9963, .T. ) ;
#16876=AXIS2_PLACEMENT_3D ( 'NONE', #33458, #17359, #20622 ) ;
#16878=DIRECTION ( 'NONE',  ( 0.000000000000000000, -0.5963673585384914322, -0.8027116379309711114 ) ) ;
#16881=ORIENTED_EDGE ( 'NONE', *, *, #37959, .F. ) ;
#16885=ORIENTED_EDGE ( 'NONE', *, *, #36752, .F. ) ;
#16887=DIRECTION ( 'NONE',  ( 1.000000000000000000, 0.000000000000000000, 0.000000000000000000 ) ) ;
#16889=ORIENTED_EDGE ( 'NONE', *, *, #26192, .T. ) ;
#16891=ORIENTED_EDGE ( 'NONE', *, *, #9634, .T. ) ;
#16905=VECTOR ( 'NONE', #12713, 1000.000000000000000 ) ;
#16907=DIRECTION ( 'NONE',  ( 0.000000000000000000, 0.000000000000000000, 1.000000000000000000 ) ) ;
#16910=ORIENTED_EDGE ( 'NONE', *, *, #4100, .F. ) ;
#16911=DIRECTION ( 'NONE',  ( -1.000000000000000000, 0.000000000000000000, 0.000000000000000000 ) ) ;
#16912=EDGE_CURVE ( 'NONE', #9577, #9442, #13274, .T. ) ;
#16913=VERTEX_POINT ( 'NONE', #20055 ) ;
#16918=CARTESIAN_POINT ( 'NONE',  ( 0.000000000000000000, 84.62908780824871258, 85.78116633471321961 ) ) ;
#16919=CARTESIAN_POINT ( 'NONE',  ( 0.000000000000000000, 0.000000000000000000, 0.000000000000000000 ) ) ;
#16920=ORIENTED_EDGE ( 'NONE', *, *, #5442, .F. ) ;
#16921=DIRECTION ( 'NONE',  ( -1.000000000000000000, -0.000000000000000000, -0.000000000000000000 ) ) ;
#16925=CARTESIAN_POINT ( 'NONE',  ( 0.000000000000000000, -79.94368240339366594, -90.16373242487986772 ) ) ;
#16927=CARTESIAN_POINT ( 'NONE',  ( 0.000000000000000000, 11.41303419185120482, -111.6154788735834700 ) ) ;
#16929=AXIS2_PLACEMENT_3D ( 'NONE', #23767, #37037, #7143 ) ;
#16932=AXIS2_PLACEMENT_3D ( 'NONE', #3924, #30589, #20798 ) ;
#16933=ORIENTED_EDGE ( 'NONE', *, *, #1222, .F. ) ;
#16934=LINE ( 'NONE', #33683, #29017 ) ;
#16938=ORIENTED_EDGE ( 'NONE', *, *, #34577, .F. ) ;
#16939=DIRECTION ( 'NONE',  ( -1.000000000000000000, 0.000000000000000000, 0.000000000000000000 ) ) ;
#16941=EDGE_CURVE ( 'NONE', #24177, #10039, #40487, .T. ) ;
#16942=LINE ( 'NONE', #30225, #20037 ) ;
#16944=DIRECTION ( 'NONE',  ( -1.000000000000000000, 0.000000000000000000, 0.000000000000000000 ) ) ;
#16945=CARTESIAN_POINT ( 'NONE',  ( 17.99999999999999645, 115.9387338813862129, -3.769613505534868736 ) ) ;
#16946=VERTEX_POINT ( 'NONE', #30065 ) ;
#16950=CIRCLE ( 'NONE', #3654, 59.00000000000002132 ) ;
#16951=DIRECTION ( 'NONE',  ( 1.000000000000000000, 0.000000000000000000, 0.000000000000000000 ) ) ;
#16958=DIRECTION ( 'NONE',  ( -1.000000000000000000, 0.000000000000000000, -0.000000000000000000 ) ) ;
#16965=DIRECTION ( 'NONE',  ( -1.000000000000000000, 0.000000000000000000, 0.000000000000000000 ) ) ;
#16969=DIRECTION ( 'NONE',  ( 0.000000000000000000, -0.9714298932647074114, -0.2373266998711251186 ) ) ;
#16972=CARTESIAN_POINT ( 'NONE',  ( 0.000000000000000000, 111.2559044912529345, -32.83479428644565701 ) ) ;
#16978=ADVANCED_FACE ( 'NONE', ( #6904 ), #3614, .F. ) ;
#16979=DIRECTION ( 'NONE',  ( 1.000000000000000000, 0.000000000000000000, 0.000000000000000000 ) ) ;
#16980=ORIENTED_EDGE ( 'NONE', *, *, #28352, .F. ) ;
#16981=AXIS2_PLACEMENT_3D ( 'NONE', #32817, #39139, #5770 ) ;
#16984=CARTESIAN_POINT ( 'NONE',  ( 17.99999999999999645, 116.0452958106484971, -32.46506308663343532 ) ) ;
#16993=FACE_OUTER_BOUND ( 'NONE', #20136, .T. ) ;
#16994=EDGE_CURVE ( 'NONE', #13070, #14175, #11499, .T. ) ;
#16995=EDGE_CURVE ( 'NONE', #21974, #26598, #13686, .T. ) ;
#16999=DIRECTION ( 'NONE',  ( 1.000000000000000000, 0.000000000000000000, 0.000000000000000000 ) ) ;
#17004=ORIENTED_EDGE ( 'NONE', *, *, #4760, .T. ) ;
#17006=CIRCLE ( 'NONE', #13506, 59.00000000000000000 ) ;
#17007=CARTESIAN_POINT ( 'NONE',  ( 17.99999999999999645, 0.000000000000000000, 0.000000000000000000 ) ) ;
#17009=VERTEX_POINT ( 'NONE', #37867 ) ;
#17012=CARTESIAN_POINT ( 'NONE',  ( 0.000000000000000000, 0.000000000000000000, 0.000000000000000000 ) ) ;
#17015=CARTESIAN_POINT ( 'NONE',  ( 17.99999999999999645, 11.65176648921033298, 115.4133282497342918 ) ) ;
#17019=VERTEX_POINT ( 'NONE', #4938 ) ;
#17024=AXIS2_PLACEMENT_3D ( 'NONE', #34596, #27417, #37435 ) ;
#17027=FACE_OUTER_BOUND ( 'NONE', #16251, .T. ) ;
#17028=ORIENTED_EDGE ( 'NONE', *, *, #13958, .T. ) ;
#17032=DIRECTION ( 'NONE',  ( 0.000000000000000000, 0.1590634960190723812, -0.9872683547213445543 ) ) ;
#17034=CIRCLE ( 'NONE', #41369, 120.5010000000000190 ) ;
#17040=DIRECTION ( 'NONE',  ( 0.000000000000000000, 0.1590634960190655534, 0.9872683547213456645 ) ) ;
#17043=EDGE_CURVE ( 'NONE', #16913, #42436, #21579, .T. ) ;
#17044=ORIENTED_EDGE ( 'NONE', *, *, #11977, .T. ) ;
#17049=ORIENTED_EDGE ( 'NONE', *, *, #15509, .T. ) ;
#17058=CARTESIAN_POINT ( 'NONE',  ( 17.99999999999999645, -27.83061035786878890, -117.2431154827800270 ) ) ;
#17060=VECTOR ( 'NONE', #24923, 1000.000000000000000 ) ;
#17063=VECTOR ( 'NONE', #30763, 1000.000000000000000 ) ;
#17064=DIRECTION ( 'NONE',  ( -1.000000000000000000, -0.000000000000000000, -0.000000000000000000 ) ) ;
#17070=LINE ( 'NONE', #19695, #28306 ) ;
#17071=ORIENTED_EDGE ( 'NONE', *, *, #8153, .F. ) ;
#17074=DIRECTION ( 'NONE',  ( 0.000000000000000000, 0.000000000000000000, 1.000000000000000000 ) ) ;
#17075=DIRECTION ( 'NONE',  ( 1.000000000000000000, 0.000000000000000000, 0.000000000000000000 ) ) ;
#17077=EDGE_CURVE ( 'NONE', #28092, #4616, #42201, .T. ) ;
#17079=DIRECTION ( 'NONE',  ( 0.000000000000000000, 0.000000000000000000, 1.000000000000000000 ) ) ;
#17080=ORIENTED_EDGE ( 'NONE', *, *, #40908, .F. ) ;
#17084=ORIENTED_EDGE ( 'NONE', *, *, #30060, .F. ) ;
#17090=AXIS2_PLACEMENT_3D ( 'NONE', #23290, #32858, #19800 ) ;
#17094=VERTEX_POINT ( 'NONE', #37445 ) ;
#17095=CARTESIAN_POINT ( 'NONE',  ( 17.99999999999999645, -75.72520367775142347, 82.78868281115956052 ) ) ;
#17096=AXIS2_PLACEMENT_3D ( 'NONE', #26659, #39925, #33410 ) ;
#17102=VECTOR ( 'NONE', #10371, 1000.000000000000000 ) ;
#17103=ORIENTED_EDGE ( 'NONE', *, *, #18759, .F. ) ;
#17105=ORIENTED_EDGE ( 'NONE', *, *, #7652, .T. ) ;
#17107=CARTESIAN_POINT ( 'NONE',  ( 17.99999999999999645, 87.74575819880170968, 75.87280091124503656 ) ) ;
#17109=DIRECTION ( 'NONE',  ( -1.000000000000000000, 0.000000000000000000, -0.000000000000000000 ) ) ;
#17110=CARTESIAN_POINT ( 'NONE',  ( 17.99999999999999645, -87.92975456462855277, -69.68953103478244770 ) ) ;
#17111=ORIENTED_EDGE ( 'NONE', *, *, #28934, .F. ) ;
#17115=EDGE_CURVE ( 'NONE', #31141, #37671, #31349, .T. ) ;
#17118=ORIENTED_EDGE ( 'NONE', *, *, #20637, .F. ) ;
#17119=EDGE_CURVE ( 'NONE', #34811, #10513, #24181, .T. ) ;
#17121=ORIENTED_EDGE ( 'NONE', *, *, #36626, .F. ) ;
#17124=AXIS2_PLACEMENT_3D ( 'NONE', #7095, #8346, #31488 ) ;
#17128=VERTEX_POINT ( 'NONE', #34605 ) ;
#17136=ORIENTED_EDGE ( 'NONE', *, *, #4045, .T. ) ;
#17137=FACE_OUTER_BOUND ( 'NONE', #28991, .T. ) ;
#17139=CIRCLE ( 'NONE', #32423, 59.00000000000001421 ) ;
#17140=CARTESIAN_POINT ( 'NONE',  ( 17.99999999999999645, 0.000000000000000000, 0.000000000000000000 ) ) ;
#17141=CARTESIAN_POINT ( 'NONE',  ( 17.99999999999999645, 91.51415974874592507, 64.91094698989330425 ) ) ;
#17154=EDGE_CURVE ( 'NONE', #14749, #23147, #19560, .T. ) ;
#17156=ORIENTED_EDGE ( 'NONE', *, *, #19144, .F. ) ;
#17157=CARTESIAN_POINT ( 'NONE',  ( -10.00000000000000000, 0.000000000000000000, 0.000000000000000000 ) ) ;
#17158=ORIENTED_EDGE ( 'NONE', *, *, #23556, .T. ) ;
#17160=CIRCLE ( 'NONE', #27576, 116.0000000000000000 ) ;
#17168=LINE ( 'NONE', #10587, #24969 ) ;
#17172=FACE_OUTER_BOUND ( 'NONE', #22392, .T. ) ;
#17174=EDGE_CURVE ( 'NONE', #10231, #5717, #18612, .T. ) ;
#17177=LINE ( 'NONE', #10382, #42528 ) ;
#17178=ORIENTED_EDGE ( 'NONE', *, *, #40546, .F. ) ;
#17179=VERTEX_POINT ( 'NONE', #12782 ) ;
#17184=DIRECTION ( 'NONE',  ( -1.000000000000000000, -0.000000000000000000, -0.000000000000000000 ) ) ;
#17185=CIRCLE ( 'NONE', #3885, 116.0000000000000000 ) ;
#17189=DIRECTION ( 'NONE',  ( 0.000000000000000000, -0.7525707698561440173, 0.6585113790650324317 ) ) ;
#17191=CIRCLE ( 'NONE', #31082, 59.00000000000000000 ) ;
#17192=EDGE_LOOP ( 'NONE', ( #6761, #30915, #4335, #29895 ) ) ;
#17193=EDGE_CURVE ( 'NONE', #40970, #42489, #30433, .T. ) ;
#17194=CIRCLE ( 'NONE', #11604, 120.5010000000000332 ) ;
#17195=DIRECTION ( 'NONE',  ( -1.000000000000000000, -0.000000000000000000, -0.000000000000000000 ) ) ;
#17198=EDGE_CURVE ( 'NONE', #29037, #2879, #22795, .T. ) ;
#17199=FACE_OUTER_BOUND ( 'NONE', #25525, .T. ) ;
#17204=ORIENTED_EDGE ( 'NONE', *, *, #16757, .T. ) ;
#17207=DIRECTION ( 'NONE',  ( 1.000000000000000000, -0.000000000000000000, -0.000000000000000000 ) ) ;
#17211=DIRECTION ( 'NONE',  ( 1.000000000000000000, -0.000000000000000000, 0.000000000000000000 ) ) ;
#17212=EDGE_CURVE ( 'NONE', #20513, #7249, #26091, .T. ) ;
#17217=DIRECTION ( 'NONE',  ( 1.000000000000000000, 0.000000000000000000, 0.000000000000000000 ) ) ;
#17219=FACE_OUTER_BOUND ( 'NONE', #38559, .T. ) ;
#17221=CIRCLE ( 'NONE', #41560, 59.00000000000001421 ) ;
#17222=DIRECTION ( 'NONE',  ( 0.000000000000000000, 0.000000000000000000, 1.000000000000000000 ) ) ;
#17225=FACE_OUTER_BOUND ( 'NONE', #18773, .T. ) ;
#17229=DIRECTION ( 'NONE',  ( 0.000000000000000000, 0.000000000000000000, 1.000000000000000000 ) ) ;
#17232=CARTESIAN_POINT ( 'NONE',  ( 17.99999999999999645, 57.40245293794799153, -96.40140491896575270 ) ) ;
#17233=ADVANCED_FACE ( 'NONE', ( #25468 ), #2914, .F. ) ;
#17236=VERTEX_POINT ( 'NONE', #2071 ) ;
#17237=AXIS2_PLACEMENT_3D ( 'NONE', #34581, #37843, #28066 ) ;
#17241=ORIENTED_EDGE ( 'NONE', *, *, #18402, .T. ) ;
#17244=AXIS2_PLACEMENT_3D ( 'NONE', #15834, #29779, #26071 ) ;
#17247=CYLINDRICAL_SURFACE ( 'NONE', #13683, 120.5010000000000190 ) ;
#17248=ORIENTED_EDGE ( 'NONE', *, *, #12793, .F. ) ;
#17249=CARTESIAN_POINT ( 'NONE',  ( 8.999999999999998224, -73.51007459736368332, -89.73443560133438268 ) ) ;
#17250=CARTESIAN_POINT ( 'NONE',  ( 0.000000000000000000, 25.18647942089895153, -113.2326863338525271 ) ) ;
#17254=ADVANCED_FACE ( 'NONE', ( #28733 ), #16274, .F. ) ;
#17257=DIRECTION ( 'NONE',  ( 0.000000000000000000, 0.8477344278896686847, 0.5304209081197460707 ) ) ;
#17260=CIRCLE ( 'NONE', #42268, 58.99999999999998579 ) ;
#17262=CARTESIAN_POINT ( 'NONE',  ( -10.00000000000000000, 0.000000000000000000, 0.000000000000000000 ) ) ;
#17266=VERTEX_POINT ( 'NONE', #28939 ) ;
#17267=AXIS2_PLACEMENT_3D ( 'NONE', #18256, #11457, #41754 ) ;
#17271=EDGE_CURVE ( 'NONE', #19094, #12205, #2703, .T. ) ;
#17275=CARTESIAN_POINT ( 'NONE',  ( 8.999999999999998224, -79.18387647320706435, -84.76976882518842160 ) ) ;
#17278=EDGE_CURVE ( 'NONE', #276, #6849, #19139, .T. ) ;
#17282=CARTESIAN_POINT ( 'NONE',  ( 17.99999999999999645, -116.0452958106478434, -32.46506308663576590 ) ) ;
#17284=EDGE_CURVE ( 'NONE', #10707, #8886, #42923, .T. ) ;
#17285=VECTOR ( 'NONE', #10802, 1000.000000000000000 ) ;
#17288=ORIENTED_EDGE ( 'NONE', *, *, #27130, .F. ) ;
#17289=FACE_OUTER_BOUND ( 'NONE', #10855, .T. ) ;
#17290=VERTEX_POINT ( 'NONE', #25892 ) ;
#17294=ORIENTED_EDGE ( 'NONE', *, *, #42125, .T. ) ;
#17295=CIRCLE ( 'NONE', #20064, 59.00000000000000000 ) ;
#17296=LINE ( 'NONE', #9629, #9045 ) ;
#17297=AXIS2_PLACEMENT_3D ( 'NONE', #40455, #36975, #33702 ) ;
#17300=AXIS2_PLACEMENT_3D ( 'NONE', #6382, #29321, #16236 ) ;
#17302=DIRECTION ( 'NONE',  ( 0.000000000000000000, 0.000000000000000000, 1.000000000000000000 ) ) ;
#17303=ORIENTED_EDGE ( 'NONE', *, *, #18599, .F. ) ;
#17307=EDGE_CURVE ( 'NONE', #25294, #26402, #22851, .T. ) ;
#17312=DIRECTION ( 'NONE',  ( -1.000000000000000000, 0.000000000000000000, 0.000000000000000000 ) ) ;
#17317=VERTEX_POINT ( 'NONE', #36307 ) ;
#17324=CIRCLE ( 'NONE', #7492, 58.99999999999999289 ) ;
#17326=VECTOR ( 'NONE', #1649, 1000.000000000000000 ) ;
#17327=AXIS2_PLACEMENT_3D ( 'NONE', #41528, #8172, #11681 ) ;
#17329=CYLINDRICAL_SURFACE ( 'NONE', #17923, 59.00000000000000000 ) ;
#17331=AXIS2_PLACEMENT_3D ( 'NONE', #3022, #16391, #41908 ) ;
#17338=LINE ( 'NONE', #7025, #37459 ) ;
#17346=DIRECTION ( 'NONE',  ( 1.000000000000000000, 0.000000000000000000, 0.000000000000000000 ) ) ;
#17348=CARTESIAN_POINT ( 'NONE',  ( 0.000000000000000000, 0.000000000000000000, -116.0000000000000000 ) ) ;
#17352=DIRECTION ( 'NONE',  ( 0.000000000000000000, 0.000000000000000000, 1.000000000000000000 ) ) ;
#17353=AXIS2_PLACEMENT_3D ( 'NONE', #35153, #1988, #18641 ) ;
#17354=VERTEX_POINT ( 'NONE', #7281 ) ;
#17359=DIRECTION ( 'NONE',  ( -1.000000000000000000, 0.000000000000000000, 0.000000000000000000 ) ) ;
#17361=EDGE_CURVE ( 'NONE', #16661, #33331, #27169, .T. ) ;
#17362=EDGE_CURVE ( 'NONE', #17236, #5841, #5321, .T. ) ;
#17366=EDGE_CURVE ( 'NONE', #18461, #19393, #9489, .T. ) ;
#17370=VERTEX_POINT ( 'NONE', #39789 ) ;
#17374=ORIENTED_EDGE ( 'NONE', *, *, #34123, .F. ) ;
#17376=CARTESIAN_POINT ( 'NONE',  ( 0.000000000000000000, 0.000000000000000000, 0.000000000000000000 ) ) ;
#17381=VECTOR ( 'NONE', #30870, 1000.000000000000000 ) ;
#17383=LINE ( 'NONE', #524, #5422 ) ;
#17384=ORIENTED_EDGE ( 'NONE', *, *, #40493, .T. ) ;
#17385=CARTESIAN_POINT ( 'NONE',  ( 17.99999999999999645, 0.000000000000000000, 0.000000000000000000 ) ) ;
#17386=CARTESIAN_POINT ( 'NONE',  ( 8.999999999999998224, -108.8880088604279166, 39.99251838045924501 ) ) ;
#17388=VERTEX_POINT ( 'NONE', #20641 ) ;
#17389=EDGE_CURVE ( 'NONE', #21931, #3781, #20217, .T. ) ;
#17391=DIRECTION ( 'NONE',  ( -1.000000000000000000, 0.000000000000000000, 0.000000000000000000 ) ) ;
#17394=ORIENTED_EDGE ( 'NONE', *, *, #41649, .T. ) ;
#17400=ORIENTED_EDGE ( 'NONE', *, *, #16584, .T. ) ;
#17401=VERTEX_POINT ( 'NONE', #33476 ) ;
#17404=VECTOR ( 'NONE', #27397, 1000.000000000000000 ) ;
#17406=DIRECTION ( 'NONE',  ( -1.000000000000000000, 0.000000000000000000, 0.000000000000000000 ) ) ;
#17408=EDGE_CURVE ( 'NONE', #23134, #14428, #33878, .T. ) ;
#17409=CARTESIAN_POINT ( 'NONE',  ( 8.999999999999998224, 79.18387647320761857, 84.76976882518788159 ) ) ;
#17413=LINE ( 'NONE', #20684, #8566 ) ;
#17417=VERTEX_POINT ( 'NONE', #10128 ) ;
#17420=CARTESIAN_POINT ( 'NONE',  ( 0.000000000000000000, 0.000000000000000000, 0.000000000000000000 ) ) ;
#17421=ORIENTED_EDGE ( 'NONE', *, *, #23393, .T. ) ;
#17423=AXIS2_PLACEMENT_3D ( 'NONE', #14394, #34221, #11119 ) ;
#17424=EDGE_CURVE ( 'NONE', #4402, #42699, #10910, .T. ) ;
#17425=ORIENTED_EDGE ( 'NONE', *, *, #33726, .T. ) ;
#17427=CARTESIAN_POINT ( 'NONE',  ( 17.99999999999999645, -120.4984140710909344, 0.7894348306980537577 ) ) ;
#17431=ORIENTED_EDGE ( 'NONE', *, *, #39074, .F. ) ;
#17433=ORIENTED_EDGE ( 'NONE', *, *, #40262, .F. ) ;
#17436=CARTESIAN_POINT ( 'NONE',  ( 0.000000000000000000, 48.55277268144325120, 105.3500273609081432 ) ) ;
#17438=DIRECTION ( 'NONE',  ( 0.000000000000000000, 0.000000000000000000, 1.000000000000000000 ) ) ;
#17440=LINE ( 'NONE', #39853, #19165 ) ;
#17441=ORIENTED_EDGE ( 'NONE', *, *, #27133, .T. ) ;
#17442=CARTESIAN_POINT ( 'NONE',  ( 0.000000000000000000, 0.000000000000000000, 0.000000000000000000 ) ) ;
#17443=AXIS2_PLACEMENT_3D ( 'NONE', #35572, #25794, #35766 ) ;
#17445=CARTESIAN_POINT ( 'NONE',  ( 0.000000000000000000, 0.000000000000000000, 0.000000000000000000 ) ) ;
#17446=EDGE_CURVE ( 'NONE', #22368, #26752, #10201, .T. ) ;
#17447=ORIENTED_EDGE ( 'NONE', *, *, #7946, .F. ) ;
#17449=DIRECTION ( 'NONE',  ( 0.000000000000000000, 0.000000000000000000, 1.000000000000000000 ) ) ;
#17453=CARTESIAN_POINT ( 'NONE',  ( 17.99999999999999645, 41.62036691425530677, 113.0850832732715787 ) ) ;
#17459=VERTEX_POINT ( 'NONE', #13224 ) ;
#17464=CIRCLE ( 'NONE', #13985, 120.5010000000000190 ) ;
#17465=CARTESIAN_POINT ( 'NONE',  ( 0.000000000000000000, 80.02407177072956301, 78.64108602299977235 ) ) ;
#17466=CIRCLE ( 'NONE', #29959, 59.00000000000000711 ) ;
#17467=AXIS2_PLACEMENT_3D ( 'NONE', #16644, #17064, #36429 ) ;
#17469=ORIENTED_EDGE ( 'NONE', *, *, #35669, .T. ) ;
#17470=DIRECTION ( 'NONE',  ( 0.000000000000000000, 3.528251137579946599E-15, -1.000000000000000000 ) ) ;
#17471=CARTESIAN_POINT ( 'NONE',  ( 0.000000000000000000, 114.6488492393079639, 37.09625815500055523 ) ) ;
#17479=DIRECTION ( 'NONE',  ( -1.000000000000000000, -0.000000000000000000, -0.000000000000000000 ) ) ;
#17480=CARTESIAN_POINT ( 'NONE',  ( 0.000000000000000000, -120.2856157092986393, -7.201503623198056481 ) ) ;
#17481=LINE ( 'NONE', #9864, #17063 ) ;
#17487=VERTEX_POINT ( 'NONE', #26725 ) ;
#17489=CARTESIAN_POINT ( 'NONE',  ( 17.99999999999999645, -107.2703412112697094, 32.88383143828427535 ) ) ;
#17491=DIRECTION ( 'NONE',  ( 0.000000000000000000, 0.000000000000000000, 1.000000000000000000 ) ) ;
#17495=AXIS2_PLACEMENT_3D ( 'NONE', #21441, #857, #14652 ) ;
#17496=EDGE_CURVE ( 'NONE', #20343, #30860, #15803, .T. ) ;
#17497=DIRECTION ( 'NONE',  ( -1.000000000000000000, -0.000000000000000000, -0.000000000000000000 ) ) ;
#17501=CARTESIAN_POINT ( 'NONE',  ( 17.99999999999999645, 0.000000000000000000, 0.000000000000000000 ) ) ;
#17504=EDGE_LOOP ( 'NONE', ( #24145, #41385, #33874, #4265 ) ) ;
#17505=CARTESIAN_POINT ( 'NONE',  ( 0.000000000000000000, -51.27532863109435368, 99.79535634195110561 ) ) ;
#17507=ORIENTED_EDGE ( 'NONE', *, *, #7961, .T. ) ;
#17508=FACE_OUTER_BOUND ( 'NONE', #3178, .T. ) ;
#17509=CARTESIAN_POINT ( 'NONE',  ( 17.99999999999999645, 119.8996782608631406, -12.02323392193236629 ) ) ;
#17513=CIRCLE ( 'NONE', #23090, 59.00000000000000000 ) ;
#17514=DIRECTION ( 'NONE',  ( 0.000000000000000000, 0.000000000000000000, 1.000000000000000000 ) ) ;
#17516=DIRECTION ( 'NONE',  ( 1.000000000000000000, 0.000000000000000000, 0.000000000000000000 ) ) ;
#17517=EDGE_LOOP ( 'NONE', ( #18300, #33960, #42651, #2193 ) ) ;
#17523=VERTEX_POINT ( 'NONE', #11025 ) ;
#17524=CARTESIAN_POINT ( 'NONE',  ( 17.99999999999999645, -67.32409792376445523, -89.75376489259431878 ) ) ;
#17525=DIRECTION ( 'NONE',  ( 0.000000000000000000, 0.000000000000000000, 1.000000000000000000 ) ) ;
#17534=AXIS2_PLACEMENT_3D ( 'NONE', #603, #42943, #10002 ) ;
#17536=DIRECTION ( 'NONE',  ( 1.000000000000000000, 0.000000000000000000, 0.000000000000000000 ) ) ;
#17547=EDGE_CURVE ( 'NONE', #26216, #40741, #33219, .T. ) ;
#17551=CYLINDRICAL_SURFACE ( 'NONE', #30382, 59.00000000000001421 ) ;
#17552=ORIENTED_EDGE ( 'NONE', *, *, #42508, .F. ) ;
#17553=CARTESIAN_POINT ( 'NONE',  ( 0.000000000000000000, -61.59243992711522964, 93.77976230226020959 ) ) ;
#17554=ORIENTED_EDGE ( 'NONE', *, *, #19103, .T. ) ;
#17560=VECTOR ( 'NONE', #30144, 1000.000000000000000 ) ;
#17567=ORIENTED_EDGE ( 'NONE', *, *, #8153, .T. ) ;
#17570=FACE_OUTER_BOUND ( 'NONE', #31912, .T. ) ;
#17571=DIRECTION ( 'NONE',  ( 0.000000000000000000, 0.000000000000000000, 1.000000000000000000 ) ) ;
#17587=AXIS2_PLACEMENT_3D ( 'NONE', #8019, #35061, #14815 ) ;
#17592=CIRCLE ( 'NONE', #37038, 116.0000000000000000 ) ;
#17594=ORIENTED_EDGE ( 'NONE', *, *, #22311, .F. ) ;
#17595=CARTESIAN_POINT ( 'NONE',  ( 0.000000000000000000, 2.418575551222442055, -120.4767259403368769 ) ) ;
#17596=ORIENTED_EDGE ( 'NONE', *, *, #24683, .T. ) ;
#17597=DIRECTION ( 'NONE',  ( -1.000000000000000000, 0.000000000000000000, 0.000000000000000000 ) ) ;
#17599=DIRECTION ( 'NONE',  ( -1.000000000000000000, -0.000000000000000000, 0.000000000000000000 ) ) ;
#17601=CARTESIAN_POINT ( 'NONE',  ( 17.99999999999999645, 0.000000000000000000, 0.000000000000000000 ) ) ;
#17602=EDGE_CURVE ( 'NONE', #25476, #29070, #12350, .T. ) ;
#17604=CYLINDRICAL_SURFACE ( 'NONE', #22042, 59.00000000000000000 ) ;
#17607=CYLINDRICAL_SURFACE ( 'NONE', #67, 120.5010000000000190 ) ;
#17608=CARTESIAN_POINT ( 'NONE',  ( 17.99999999999999645, 40.37724737310070111, 104.6802291180868565 ) ) ;
#17609=EDGE_CURVE ( 'NONE', #40313, #13499, #42950, .T. ) ;
#17610=DIRECTION ( 'NONE',  ( -1.000000000000000000, 0.000000000000000000, 0.000000000000000000 ) ) ;
#17611=ORIENTED_EDGE ( 'NONE', *, *, #31178, .F. ) ;
#17612=CARTESIAN_POINT ( 'NONE',  ( 0.000000000000000000, -89.07460286905796920, -81.15544420875052367 ) ) ;
#17613=EDGE_LOOP ( 'NONE', ( #36426, #22833, #14944, #16891 ) ) ;
#17615=CARTESIAN_POINT ( 'NONE',  ( 17.99999999999999645, 15.21076497709711184, 119.5371223922155792 ) ) ;
#17623=EDGE_CURVE ( 'NONE', #10231, #2623, #31838, .T. ) ;
#17624=CARTESIAN_POINT ( 'NONE',  ( 9.000000000000001776, 52.88069566989596382, -103.2454939717363516 ) ) ;
#17628=DIRECTION ( 'NONE',  ( 0.000000000000000000, -0.8747630845319658288, 0.4845508703326421585 ) ) ;
#17629=ORIENTED_EDGE ( 'NONE', *, *, #22208, .T. ) ;
#17631=AXIS2_PLACEMENT_3D ( 'NONE', #27100, #13577, #13804 ) ;
#17636=VERTEX_POINT ( 'NONE', #41080 ) ;
#17639=ORIENTED_EDGE ( 'NONE', *, *, #28631, .F. ) ;
#17643=DIRECTION ( 'NONE',  ( 1.000000000000000000, 0.000000000000000000, 0.000000000000000000 ) ) ;
#17648=ORIENTED_EDGE ( 'NONE', *, *, #24612, .F. ) ;
#17651=DIRECTION ( 'NONE',  ( 1.000000000000000000, 0.000000000000000000, 0.000000000000000000 ) ) ;
#17658=ORIENTED_EDGE ( 'NONE', *, *, #12030, .T. ) ;
#17664=DIRECTION ( 'NONE',  ( -1.000000000000000000, 0.000000000000000000, 0.000000000000000000 ) ) ;
#17665=CARTESIAN_POINT ( 'NONE',  ( 17.99999999999999645, 0.000000000000000000, 0.000000000000000000 ) ) ;
#17667=EDGE_CURVE ( 'NONE', #25771, #1782, #17260, .T. ) ;
#17668=CARTESIAN_POINT ( 'NONE',  ( 17.99999999999999645, 0.000000000000000000, 0.000000000000000000 ) ) ;
#17669=VERTEX_POINT ( 'NONE', #15587 ) ;
#17677=ORIENTED_EDGE ( 'NONE', *, *, #32482, .F. ) ;
#17678=LINE ( 'NONE', #31385, #25233 ) ;
#17680=VERTEX_POINT ( 'NONE', #21937 ) ;
#17681=CIRCLE ( 'NONE', #37149, 58.99999999999999289 ) ;
#17684=EDGE_LOOP ( 'NONE', ( #2419, #5486, #42720, #27781 ) ) ;
#17685=CARTESIAN_POINT ( 'NONE',  ( 0.000000000000000000, 57.69704296431184787, 105.7900857083231472 ) ) ;
#17688=LINE ( 'NONE', #1045, #42757 ) ;
#17690=AXIS2_PLACEMENT_3D ( 'NONE', #560, #13914, #7114 ) ;
#17698=CARTESIAN_POINT ( 'NONE',  ( 0.000000000000000000, 0.000000000000000000, 0.000000000000000000 ) ) ;
#17700=ADVANCED_FACE ( 'NONE', ( #5941 ), #18455, .F. ) ;
#17704=AXIS2_PLACEMENT_3D ( 'NONE', #27993, #24518, #15122 ) ;
#17707=CARTESIAN_POINT ( 'NONE',  ( 0.000000000000000000, -98.39501399267926729, -53.91376164787777014 ) ) ;
#17712=ORIENTED_EDGE ( 'NONE', *, *, #18629, .F. ) ;
#17714=ORIENTED_EDGE ( 'NONE', *, *, #18711, .F. ) ;
#17718=AXIS2_PLACEMENT_3D ( 'NONE', #8212, #21343, #7765 ) ;
#17719=ORIENTED_EDGE ( 'NONE', *, *, #22788, .T. ) ;
#17721=CARTESIAN_POINT ( 'NONE',  ( 17.99999999999999645, 0.000000000000000000, 0.000000000000000000 ) ) ;
#17724=DIRECTION ( 'NONE',  ( 0.000000000000000000, 0.000000000000000000, 1.000000000000000000 ) ) ;
#17726=CIRCLE ( 'NONE', #38562, 58.99999999999998579 ) ;
#17727=ORIENTED_EDGE ( 'NONE', *, *, #32163, .T. ) ;
#17729=CARTESIAN_POINT ( 'NONE',  ( 0.000000000000000000, -34.74871106919691499, 106.6808302961370600 ) ) ;
#17730=CYLINDRICAL_SURFACE ( 'NONE', #37784, 116.0000000000000000 ) ;
#17731=AXIS2_PLACEMENT_3D ( 'NONE', #40325, #6744, #20108 ) ;
#17733=ORIENTED_EDGE ( 'NONE', *, *, #4725, .F. ) ;
#17736=AXIS2_PLACEMENT_3D ( 'NONE', #22690, #29642, #35522 ) ;
#17738=EDGE_CURVE ( 'NONE', #27890, #42312, #5316, .T. ) ;
#17740=LINE ( 'NONE', #31010, #42742 ) ;
#17743=CARTESIAN_POINT ( 'NONE',  ( 17.99999999999999645, -103.1672962317654338, 44.09967643725834563 ) ) ;
#17744=ORIENTED_EDGE ( 'NONE', *, *, #19821, .F. ) ;
#17751=DIRECTION ( 'NONE',  ( -1.000000000000000000, -0.000000000000000000, -0.000000000000000000 ) ) ;
#17761=ORIENTED_EDGE ( 'NONE', *, *, #15131, .F. ) ;
#17762=CARTESIAN_POINT ( 'NONE',  ( 17.99999999999999645, 41.33768078145502756, 104.3046912715542902 ) ) ;
#17763=CIRCLE ( 'NONE', #42088, 120.5010000000000190 ) ;
#17766=ORIENTED_EDGE ( 'NONE', *, *, #32004, .T. ) ;
#17767=CARTESIAN_POINT ( 'NONE',  ( 17.99999999999999645, 0.000000000000000000, 0.000000000000000000 ) ) ;
#17771=ORIENTED_EDGE ( 'NONE', *, *, #8944, .T. ) ;
#17778=ORIENTED_EDGE ( 'NONE', *, *, #3400, .F. ) ;
#17779=DIRECTION ( 'NONE',  ( 0.000000000000000000, 0.000000000000000000, 1.000000000000000000 ) ) ;
#17781=VERTEX_POINT ( 'NONE', #28479 ) ;
#17784=DIRECTION ( 'NONE',  ( 0.000000000000000000, 0.000000000000000000, 1.000000000000000000 ) ) ;
#17786=DIRECTION ( 'NONE',  ( 1.000000000000000000, 0.000000000000000000, 0.000000000000000000 ) ) ;
#17787=VECTOR ( 'NONE', #2300, 1000.000000000000000 ) ;
#17791=VECTOR ( 'NONE', #40759, 1000.000000000000000 ) ;
#17794=ADVANCED_FACE ( 'NONE', ( #38676 ), #42379, .F. ) ;
#17797=EDGE_CURVE ( 'NONE', #12185, #30056, #35415, .T. ) ;
#17798=VECTOR ( 'NONE', #27000, 1000.000000000000000 ) ;
#17803=DIRECTION ( 'NONE',  ( -1.000000000000000000, -0.000000000000000000, -0.000000000000000000 ) ) ;
#17805=DIRECTION ( 'NONE',  ( 0.000000000000000000, 0.1590634960190654978, 0.9872683547213455535 ) ) ;
#17807=AXIS2_PLACEMENT_3D ( 'NONE', #28028, #27816, #11658 ) ;
#17808=VERTEX_POINT ( 'NONE', #12523 ) ;
#17811=CARTESIAN_POINT ( 'NONE',  ( 17.99999999999999645, -101.1249659627859216, 48.60055280209385842 ) ) ;
#17813=DIRECTION ( 'NONE',  ( 0.000000000000000000, 0.9996456111234526265, -0.02662052143777151811 ) ) ;
#17814=CIRCLE ( 'NONE', #32409, 116.0000000000000000 ) ;
#17817=VERTEX_POINT ( 'NONE', #22571 ) ;
#17818=DIRECTION ( 'NONE',  ( 0.000000000000000000, 0.000000000000000000, 1.000000000000000000 ) ) ;
#17819=CIRCLE ( 'NONE', #21990, 58.99999999999998579 ) ;
#17821=EDGE_CURVE ( 'NONE', #42455, #2432, #464, .T. ) ;
#17822=ORIENTED_EDGE ( 'NONE', *, *, #14745, .T. ) ;
#17823=AXIS2_PLACEMENT_3D ( 'NONE', #21420, #11790, #8694 ) ;
#17831=CIRCLE ( 'NONE', #33099, 58.99999999999999289 ) ;
#17832=ORIENTED_EDGE ( 'NONE', *, *, #26088, .F. ) ;
#17834=DIRECTION ( 'NONE',  ( 0.000000000000000000, 0.000000000000000000, 1.000000000000000000 ) ) ;
#17836=CARTESIAN_POINT ( 'NONE',  ( 17.99999999999999645, -120.4984140710909202, -0.7894348306996294973 ) ) ;
#17841=AXIS2_PLACEMENT_3D ( 'NONE', #9005, #2646, #2424 ) ;
#17843=DIRECTION ( 'NONE',  ( -1.000000000000000000, -0.000000000000000000, -0.000000000000000000 ) ) ;
#17844=ADVANCED_FACE ( 'NONE', ( #36250 ), #32779, .F. ) ;
#17846=EDGE_CURVE ( 'NONE', #18385, #2814, #9522, .T. ) ;
#17847=LINE ( 'NONE', #14563, #22604 ) ;
#17848=VECTOR ( 'NONE', #11265, 1000.000000000000000 ) ;
#17849=EDGE_LOOP ( 'NONE', ( #39220, #38448, #8234, #36383 ) ) ;
#17850=ADVANCED_FACE ( 'NONE', ( #3067 ), #10077, .F. ) ;
#17852=VECTOR ( 'NONE', #42759, 1000.000000000000000 ) ;
#17855=ORIENTED_EDGE ( 'NONE', *, *, #2745, .T. ) ;
#17859=AXIS2_PLACEMENT_3D ( 'NONE', #979, #14559, #33953 ) ;
#17864=EDGE_CURVE ( 'NONE', #30173, #2012, #30385, .T. ) ;
#17869=ORIENTED_EDGE ( 'NONE', *, *, #4223, .T. ) ;
#17870=CARTESIAN_POINT ( 'NONE',  ( 17.99999999999999645, -112.5120133921110295, 43.14554256760978745 ) ) ;
#17871=CARTESIAN_POINT ( 'NONE',  ( 0.000000000000000000, -68.61497464550662073, 99.05794392877581345 ) ) ;
#17874=DIRECTION ( 'NONE',  ( 0.000000000000000000, 0.2113826236296183214, 0.9774033898178677848 ) ) ;
#17876=CARTESIAN_POINT ( 'NONE',  ( 17.99999999999999645, 106.5605152861910909, -56.26142179985714620 ) ) ;
#17878=DIRECTION ( 'NONE',  ( -1.000000000000000000, -0.000000000000000000, 0.000000000000000000 ) ) ;
#17881=LINE ( 'NONE', #18531, #38492 ) ;
#17884=VECTOR ( 'NONE', #2581, 1000.000000000000000 ) ;
#17885=VECTOR ( 'NONE', #6695, 1000.000000000000000 ) ;
#17886=DIRECTION ( 'NONE',  ( -1.000000000000000000, -0.000000000000000000, -0.000000000000000000 ) ) ;
#17888=DIRECTION ( 'NONE',  ( -1.000000000000000000, 0.000000000000000000, -0.000000000000000000 ) ) ;
#17895=AXIS2_PLACEMENT_3D ( 'NONE', #6702, #20065, #29636 ) ;
#17898=DIRECTION ( 'NONE',  ( 1.000000000000000000, 0.000000000000000000, 0.000000000000000000 ) ) ;
#17899=ORIENTED_EDGE ( 'NONE', *, *, #20185, .F. ) ;
#17902=AXIS2_PLACEMENT_3D ( 'NONE', #41814, #18106, #31370 ) ;
#17903=ORIENTED_EDGE ( 'NONE', *, *, #4733, .T. ) ;
#17907=ORIENTED_EDGE ( 'NONE', *, *, #25867, .T. ) ;
#17909=EDGE_CURVE ( 'NONE', #22945, #32325, #35305, .T. ) ;
#17913=EDGE_CURVE ( 'NONE', #11528, #20639, #1192, .T. ) ;
#17917=ORIENTED_EDGE ( 'NONE', *, *, #1603, .F. ) ;
#17921=EDGE_CURVE ( 'NONE', #39845, #14958, #14468, .T. ) ;
#17922=VECTOR ( 'NONE', #11728, 1000.000000000000000 ) ;
#17923=AXIS2_PLACEMENT_3D ( 'NONE', #7668, #27325, #24071 ) ;
#17927=DIRECTION ( 'NONE',  ( 0.000000000000000000, 0.000000000000000000, 1.000000000000000000 ) ) ;
#17929=DIRECTION ( 'NONE',  ( 0.000000000000000000, -0.3641605752528102036, -0.9313361774523430947 ) ) ;
#17930=ORIENTED_EDGE ( 'NONE', *, *, #4893, .F. ) ;
#17933=AXIS2_PLACEMENT_3D ( 'NONE', #28166, #5657, #38592 ) ;
#17934=ORIENTED_EDGE ( 'NONE', *, *, #13958, .F. ) ;
#17938=VERTEX_POINT ( 'NONE', #2860 ) ;
#17940=CARTESIAN_POINT ( 'NONE',  ( 17.99999999999999645, 37.07968990261480968, 109.9140418541958724 ) ) ;
#17942=ORIENTED_EDGE ( 'NONE', *, *, #32431, .T. ) ;
#17943=CARTESIAN_POINT ( 'NONE',  ( -10.00000000000000000, 0.000000000000000000, 0.000000000000000000 ) ) ;
#17945=FACE_OUTER_BOUND ( 'NONE', #2036, .T. ) ;
#17947=FACE_OUTER_BOUND ( 'NONE', #3693, .T. ) ;
#17948=CARTESIAN_POINT ( 'NONE',  ( 17.99999999999999645, 104.2166695095712470, 60.49278301857841456 ) ) ;
#17952=CYLINDRICAL_SURFACE ( 'NONE', #19242, 120.5010000000000190 ) ;
#17957=LINE ( 'NONE', #2164, #1106 ) ;
#17958=ORIENTED_EDGE ( 'NONE', *, *, #8266, .T. ) ;
#17959=FACE_OUTER_BOUND ( 'NONE', #4790, .T. ) ;
#17963=EDGE_LOOP ( 'NONE', ( #7202, #11912, #31365, #24997 ) ) ;
#17965=AXIS2_PLACEMENT_3D ( 'NONE', #34804, #30527, #7966 ) ;
#17968=ORIENTED_EDGE ( 'NONE', *, *, #19133, .F. ) ;
#17969=CARTESIAN_POINT ( 'NONE',  ( -10.00000000000000000, 0.000000000000000000, 0.000000000000000000 ) ) ;
#17970=DIRECTION ( 'NONE',  ( 1.000000000000000000, 0.000000000000000000, 0.000000000000000000 ) ) ;
#17972=DIRECTION ( 'NONE',  ( -1.000000000000000000, 0.000000000000000000, 0.000000000000000000 ) ) ;
#17974=ADVANCED_FACE ( 'NONE', ( #32986 ), #29742, .F. ) ;
#17975=DIRECTION ( 'NONE',  ( -1.000000000000000000, 0.000000000000000000, 0.000000000000000000 ) ) ;
#17979=DIRECTION ( 'NONE',  ( 0.000000000000000000, 0.000000000000000000, 1.000000000000000000 ) ) ;
#17981=CARTESIAN_POINT ( 'NONE',  ( 17.99999999999999645, -64.58410930313591791, 101.7319213743680422 ) ) ;
#17985=AXIS2_PLACEMENT_3D ( 'NONE', #20587, #17751, #887 ) ;
#17993=AXIS2_PLACEMENT_3D ( 'NONE', #8819, #18906, #28906 ) ;
#17994=ORIENTED_EDGE ( 'NONE', *, *, #37018, .T. ) ;
#17996=DIRECTION ( 'NONE',  ( 0.000000000000000000, 0.000000000000000000, 1.000000000000000000 ) ) ;
#17997=DIRECTION ( 'NONE',  ( 1.000000000000000000, 0.000000000000000000, 0.000000000000000000 ) ) ;
#17998=ORIENTED_EDGE ( 'NONE', *, *, #14090, .T. ) ;
#17999=CYLINDRICAL_SURFACE ( 'NONE', #38818, 59.00000000000000000 ) ;
#18001=ADVANCED_FACE ( 'NONE', ( #36908 ), #3298, .F. ) ;
#18002=EDGE_CURVE ( 'NONE', #9695, #39040, #42301, .T. ) ;
#18003=ORIENTED_EDGE ( 'NONE', *, *, #15687, .T. ) ;
#18004=DIRECTION ( 'NONE',  ( 0.000000000000000000, -0.9407002666710364558, 0.3392388661180213427 ) ) ;
#18006=VERTEX_POINT ( 'NONE', #40593 ) ;
#18007=EDGE_CURVE ( 'NONE', #30050, #23276, #24072, .T. ) ;
#18008=DIRECTION ( 'NONE',  ( 0.000000000000000000, 0.000000000000000000, 1.000000000000000000 ) ) ;
#18010=CARTESIAN_POINT ( 'NONE',  ( 0.000000000000000000, 0.000000000000000000, 0.000000000000000000 ) ) ;
#18012=DIRECTION ( 'NONE',  ( 0.000000000000000000, 0.000000000000000000, 1.000000000000000000 ) ) ;
#18014=ORIENTED_EDGE ( 'NONE', *, *, #20397, .T. ) ;
#18017=CIRCLE ( 'NONE', #15901, 59.00000000000001421 ) ;
#18021=CARTESIAN_POINT ( 'NONE',  ( 17.99999999999999645, 17.33727698085173330, 110.8498592715974098 ) ) ;
#18028=ORIENTED_EDGE ( 'NONE', *, *, #7152, .T. ) ;
#18033=EDGE_LOOP ( 'NONE', ( #33969, #21323, #2251, #9834 ) ) ;
#18035=EDGE_CURVE ( 'NONE', #7030, #11794, #27992, .T. ) ;
#18043=VERTEX_POINT ( 'NONE', #24303 ) ;
#18045=ORIENTED_EDGE ( 'NONE', *, *, #1593, .T. ) ;
#18048=DIRECTION ( 'NONE',  ( 1.000000000000000000, 0.000000000000000000, 0.000000000000000000 ) ) ;
#18050=ORIENTED_EDGE ( 'NONE', *, *, #18007, .T. ) ;
#18051=ORIENTED_EDGE ( 'NONE', *, *, #24425, .T. ) ;
#18052=CARTESIAN_POINT ( 'NONE',  ( 0.000000000000000000, -94.83915810436360516, -59.94836581341685644 ) ) ;
#18055=CIRCLE ( 'NONE', #25697, 59.00000000000002132 ) ;
#18058=EDGE_LOOP ( 'NONE', ( #8612, #477, #7075, #42944 ) ) ;
#18059=DIRECTION ( 'NONE',  ( 0.000000000000000000, 0.000000000000000000, 1.000000000000000000 ) ) ;
#18062=EDGE_CURVE ( 'NONE', #30860, #13871, #31023, .T. ) ;
#18063=CARTESIAN_POINT ( 'NONE',  ( 0.000000000000000000, 106.6051926090976991, -45.73109345704713036 ) ) ;
#18066=DIRECTION ( 'NONE',  ( -1.000000000000000000, -0.000000000000000000, -0.000000000000000000 ) ) ;
#18071=DIRECTION ( 'NONE',  ( 0.000000000000000000, -0.8747630845319559478, -0.4845508703326599775 ) ) ;
#18072=ORIENTED_EDGE ( 'NONE', *, *, #24701, .F. ) ;
#18073=DIRECTION ( 'NONE',  ( -1.000000000000000000, 0.000000000000000000, 0.000000000000000000 ) ) ;
#18074=ADVANCED_FACE ( 'NONE', ( #34727 ), #34076, .F. ) ;
#18075=VERTEX_POINT ( 'NONE', #24726 ) ;
#18082=CIRCLE ( 'NONE', #36134, 59.00000000000001421 ) ;
#18084=ADVANCED_FACE ( 'NONE', ( #18194 ), #37559, .F. ) ;
#18086=LINE ( 'NONE', #31348, #34004 ) ;
#18087=EDGE_CURVE ( 'NONE', #7056, #38197, #34496, .T. ) ;
#18091=DIRECTION ( 'NONE',  ( 1.000000000000000000, 0.000000000000000000, 0.000000000000000000 ) ) ;
#18092=ORIENTED_EDGE ( 'NONE', *, *, #18007, .F. ) ;
#18096=CARTESIAN_POINT ( 'NONE',  ( 17.99999999999999645, -16.77566611177701006, -119.3275660838943963 ) ) ;
#18099=DIRECTION ( 'NONE',  ( 1.000000000000000000, 0.000000000000000000, 0.000000000000000000 ) ) ;
#18105=EDGE_CURVE ( 'NONE', #7775, #10843, #31869, .T. ) ;
#18106=DIRECTION ( 'NONE',  ( -1.000000000000000000, -0.000000000000000000, -0.000000000000000000 ) ) ;
#18109=DIRECTION ( 'NONE',  ( 0.000000000000000000, 0.000000000000000000, -1.000000000000000000 ) ) ;
#18111=EDGE_CURVE ( 'NONE', #24063, #33745, #15208, .T. ) ;
#18112=EDGE_CURVE ( 'NONE', #5268, #6410, #26294, .T. ) ;
#18118=ORIENTED_EDGE ( 'NONE', *, *, #6428, .T. ) ;
#18122=DIRECTION ( 'NONE',  ( 0.000000000000000000, 0.000000000000000000, 1.000000000000000000 ) ) ;
#18124=VERTEX_POINT ( 'NONE', #40817 ) ;
#18125=CARTESIAN_POINT ( 'NONE',  ( 0.000000000000000000, 103.5682682299988500, -43.14958040911561454 ) ) ;
#18129=CARTESIAN_POINT ( 'NONE',  ( 17.99999999999999645, -80.02407177072905142, -78.64108602300026973 ) ) ;
#18131=ORIENTED_EDGE ( 'NONE', *, *, #8110, .T. ) ;
#18145=CARTESIAN_POINT ( 'NONE',  ( 0.000000000000000000, -84.09610293794118263, 74.27057253242982426 ) ) ;
#18148=VERTEX_POINT ( 'NONE', #7669 ) ;
#18155=DIRECTION ( 'NONE',  ( -1.000000000000000000, -0.000000000000000000, 0.000000000000000000 ) ) ;
#18160=FACE_OUTER_BOUND ( 'NONE', #30021, .T. ) ;
#18161=ORIENTED_EDGE ( 'NONE', *, *, #15410, .T. ) ;
#18162=EDGE_CURVE ( 'NONE', #18006, #12660, #7458, .T. ) ;
#18164=CIRCLE ( 'NONE', #34115, 116.0000000000000000 ) ;
#18166=DIRECTION ( 'NONE',  ( -1.000000000000000000, -0.000000000000000000, 0.000000000000000000 ) ) ;
#18172=CARTESIAN_POINT ( 'NONE',  ( 17.99999999999999645, 114.1157422997285806, -20.82300072952825332 ) ) ;
#18174=DIRECTION ( 'NONE',  ( 0.000000000000000000, 0.000000000000000000, 1.000000000000000000 ) ) ;
#18176=EDGE_CURVE ( 'NONE', #7568, #41800, #23537, .T. ) ;
#18178=CARTESIAN_POINT ( 'NONE',  ( 0.000000000000000000, -11.41303419185048185, 111.6154788735835410 ) ) ;
#18181=FACE_OUTER_BOUND ( 'NONE', #6202, .T. ) ;
#18183=VERTEX_POINT ( 'NONE', #35360 ) ;
#18184=DIRECTION ( 'NONE',  ( 1.000000000000000000, 0.000000000000000000, 0.000000000000000000 ) ) ;
#18185=CARTESIAN_POINT ( 'NONE',  ( 17.99999999999999645, 61.59243992711459015, 93.77976230226062171 ) ) ;
#18186=DIRECTION ( 'NONE',  ( 0.000000000000000000, 0.9996456111234524045, 0.02662052143777824190 ) ) ;
#18187=ORIENTED_EDGE ( 'NONE', *, *, #33060, .T. ) ;
#18192=CIRCLE ( 'NONE', #3471, 116.0000000000000000 ) ;
#18194=FACE_OUTER_BOUND ( 'NONE', #4143, .T. ) ;
#18195=CIRCLE ( 'NONE', #40418, 59.00000000000000711 ) ;
#18199=ORIENTED_EDGE ( 'NONE', *, *, #2, .T. ) ;
#18201=ORIENTED_EDGE ( 'NONE', *, *, #35565, .T. ) ;
#18203=CARTESIAN_POINT ( 'NONE',  ( 0.000000000000000000, -107.2703412112692689, -32.88383143828572486 ) ) ;
#18205=DIRECTION ( 'NONE',  ( -1.000000000000000000, 0.000000000000000000, -0.000000000000000000 ) ) ;
#18206=ADVANCED_FACE ( 'NONE', ( #5890 ), #2179, .F. ) ;
#18207=CARTESIAN_POINT ( 'NONE',  ( 17.99999999999999645, 0.000000000000000000, 0.000000000000000000 ) ) ;
#18209=DIRECTION ( 'NONE',  ( 0.000000000000000000, -0.5076658003388468954, 0.8615540813938020737 ) ) ;
#18211=VERTEX_POINT ( 'NONE', #25163 ) ;
#18212=DIRECTION ( 'NONE',  ( 1.000000000000000000, 0.000000000000000000, 0.000000000000000000 ) ) ;
#18215=ORIENTED_EDGE ( 'NONE', *, *, #27419, .F. ) ;
#18216=CARTESIAN_POINT ( 'NONE',  ( 0.000000000000000000, 0.000000000000000000, 0.000000000000000000 ) ) ;
#18219=ORIENTED_EDGE ( 'NONE', *, *, #19467, .T. ) ;
#18222=ORIENTED_EDGE ( 'NONE', *, *, #40965, .T. ) ;
#18227=EDGE_CURVE ( 'NONE', #24053, #25660, #40895, .T. ) ;
#18235=ORIENTED_EDGE ( 'NONE', *, *, #7526, .T. ) ;
#18236=DIRECTION ( 'NONE',  ( -1.000000000000000000, -0.000000000000000000, 0.000000000000000000 ) ) ;
#18243=EDGE_CURVE ( 'NONE', #30242, #17459, #21680, .T. ) ;
#18244=VERTEX_POINT ( 'NONE', #11836 ) ;
#18245=ORIENTED_EDGE ( 'NONE', *, *, #35031, .F. ) ;
#18246=CARTESIAN_POINT ( 'NONE',  ( 0.000000000000000000, 71.21168426767221149, -86.70160608319253015 ) ) ;
#18247=DIRECTION ( 'NONE',  ( 0.000000000000000000, 0.3641605752528168094, 0.9313361774523405412 ) ) ;
#18248=CARTESIAN_POINT ( 'NONE',  ( 0.000000000000000000, 0.000000000000000000, 0.000000000000000000 ) ) ;
#18249=LINE ( 'NONE', #8168, #22614 ) ;
#18254=DIRECTION ( 'NONE',  ( -1.000000000000000000, -0.000000000000000000, -0.000000000000000000 ) ) ;
#18255=VECTOR ( 'NONE', #2050, 1000.000000000000000 ) ;
#18256=CARTESIAN_POINT ( 'NONE',  ( 17.99999999999999645, 80.02407177072956301, 78.64108602299977235 ) ) ;
#18263=CARTESIAN_POINT ( 'NONE',  ( 0.000000000000000000, -115.6826031496111398, -8.575274253898639287 ) ) ;
#18264=LINE ( 'NONE', #1615, #22869 ) ;
#18266=ORIENTED_EDGE ( 'NONE', *, *, #17119, .T. ) ;
#18267=CARTESIAN_POINT ( 'NONE',  ( 17.99999999999999645, 0.000000000000000000, 0.000000000000000000 ) ) ;
#18271=EDGE_CURVE ( 'NONE', #13702, #41253, #32300, .T. ) ;
#18272=CARTESIAN_POINT ( 'NONE',  ( 17.99999999999999645, -115.9387338813861277, -3.769613505537241949 ) ) ;
#18274=VERTEX_POINT ( 'NONE', #18405 ) ;
#18275=LINE ( 'NONE', #11705, #6043 ) ;
#18282=ORIENTED_EDGE ( 'NONE', *, *, #32458, .F. ) ;
#18285=CARTESIAN_POINT ( 'NONE',  ( 17.99999999999999645, 0.000000000000000000, 0.000000000000000000 ) ) ;
#18286=AXIS2_PLACEMENT_3D ( 'NONE', #29188, #16095, #16532 ) ;
#18291=CARTESIAN_POINT ( 'NONE',  ( 17.99999999999999645, -112.1427988504407551, -3.502162136924565239 ) ) ;
#18292=EDGE_CURVE ( 'NONE', #17669, #13070, #10266, .T. ) ;
#18296=CARTESIAN_POINT ( 'NONE',  ( 0.000000000000000000, -52.19040376560500505, 99.31985817764160629 ) ) ;
#18300=ORIENTED_EDGE ( 'NONE', *, *, #39289, .F. ) ;
#18301=CARTESIAN_POINT ( 'NONE',  ( 0.000000000000000000, 0.000000000000000000, 0.000000000000000000 ) ) ;
#18303=CARTESIAN_POINT ( 'NONE',  ( 0.000000000000000000, -108.8684555192045025, -27.12806418649726936 ) ) ;
#18306=ORIENTED_EDGE ( 'NONE', *, *, #38986, .T. ) ;
#18311=CIRCLE ( 'NONE', #21803, 116.0000000000000000 ) ;
#18313=AXIS2_PLACEMENT_3D ( 'NONE', #26866, #13574, #42991 ) ;
#18315=ORIENTED_EDGE ( 'NONE', *, *, #36779, .T. ) ;
#18319=EDGE_CURVE ( 'NONE', #34259, #42455, #38619, .T. ) ;
#18321=DIRECTION ( 'NONE',  ( -1.000000000000000000, 0.000000000000000000, 0.000000000000000000 ) ) ;
#18322=ORIENTED_EDGE ( 'NONE', *, *, #18111, .F. ) ;
#18324=VERTEX_POINT ( 'NONE', #34935 ) ;
#18328=DIRECTION ( 'NONE',  ( -1.000000000000000000, -0.000000000000000000, -0.000000000000000000 ) ) ;
#18329=EDGE_CURVE ( 'NONE', #1575, #33606, #17324, .T. ) ;
#18330=DIRECTION ( 'NONE',  ( -1.000000000000000000, 0.000000000000000000, 0.000000000000000000 ) ) ;
#18332=CARTESIAN_POINT ( 'NONE',  ( 0.000000000000000000, 0.000000000000000000, 0.000000000000000000 ) ) ;
#18334=DIRECTION ( 'NONE',  ( 0.000000000000000000, 0.000000000000000000, 1.000000000000000000 ) ) ;
#18335=VERTEX_POINT ( 'NONE', #9172 ) ;
#18337=CARTESIAN_POINT ( 'NONE',  ( 17.99999999999999645, -116.4607004671426438, -30.94182036827323756 ) ) ;
#18340=DIRECTION ( 'NONE',  ( 0.000000000000000000, 0.5528000653611888637, 0.8333139190825180620 ) ) ;
#18348=ADVANCED_FACE ( 'NONE', ( #2381 ), #22104, .F. ) ;
#18349=ADVANCED_FACE ( 'NONE', ( #16621 ), #22734, .F. ) ;
#18350=AXIS2_PLACEMENT_3D ( 'NONE', #41372, #11521, #18109 ) ;
#18357=CARTESIAN_POINT ( 'NONE',  ( 17.99999999999999645, 0.000000000000000000, 0.000000000000000000 ) ) ;
#18358=ORIENTED_EDGE ( 'NONE', *, *, #29118, .F. ) ;
#18366=DIRECTION ( 'NONE',  ( 0.000000000000000000, 0.000000000000000000, -1.000000000000000000 ) ) ;
#18368=LINE ( 'NONE', #15085, #28427 ) ;
#18371=VECTOR ( 'NONE', #29406, 1000.000000000000000 ) ;
#18372=ORIENTED_EDGE ( 'NONE', *, *, #41538, .T. ) ;
#18375=CARTESIAN_POINT ( 'NONE',  ( 9.000000000000001776, -42.87700105098682002, 107.7847984684003393 ) ) ;
#18379=CARTESIAN_POINT ( 'NONE',  ( 17.99999999999999645, 101.1249659627849269, 48.60055280209592610 ) ) ;
#18383=CIRCLE ( 'NONE', #866, 59.00000000000000000 ) ;
#18384=CARTESIAN_POINT ( 'NONE',  ( 0.000000000000000000, 5.492704054968225336, -115.8698847939555776 ) ) ;
#18385=VERTEX_POINT ( 'NONE', #3014 ) ;
#18386=DIRECTION ( 'NONE',  ( -1.000000000000000000, 0.000000000000000000, -0.000000000000000000 ) ) ;
#18387=DIRECTION ( 'NONE',  ( 0.000000000000000000, 0.000000000000000000, 1.000000000000000000 ) ) ;
#18393=CARTESIAN_POINT ( 'NONE',  ( 0.000000000000000000, 34.74871106919619024, 106.6808302961373158 ) ) ;
#18398=EDGE_CURVE ( 'NONE', #11164, #7056, #34001, .T. ) ;
#18399=AXIS2_PLACEMENT_3D ( 'NONE', #11826, #8311, #34707 ) ;
#18402=EDGE_CURVE ( 'NONE', #14428, #30604, #26837, .T. ) ;
#18403=AXIS2_PLACEMENT_3D ( 'NONE', #26991, #36346, #39828 ) ;
#18404=DIRECTION ( 'NONE',  ( 0.000000000000000000, 0.2631025642275217069, -0.9647678688145158166 ) ) ;
#18405=CARTESIAN_POINT ( 'NONE',  ( 0.000000000000000000, -57.69704296431110890, -105.7900857083235451 ) ) ;
#18408=DIRECTION ( 'NONE',  ( 1.000000000000000000, 0.000000000000000000, 0.000000000000000000 ) ) ;
#18411=VERTEX_POINT ( 'NONE', #3243 ) ;
#18413=AXIS2_PLACEMENT_3D ( 'NONE', #39190, #35920, #29409 ) ;
#18414=DIRECTION ( 'NONE',  ( 1.000000000000000000, 0.000000000000000000, 0.000000000000000000 ) ) ;
#18416=CARTESIAN_POINT ( 'NONE',  ( 0.000000000000000000, -78.75547124681308730, -91.20343606297076633 ) ) ;
#18418=ORIENTED_EDGE ( 'NONE', *, *, #34346, .F. ) ;
#18420=ORIENTED_EDGE ( 'NONE', *, *, #19171, .T. ) ;
#18424=AXIS2_PLACEMENT_3D ( 'NONE', #21292, #11225, #24558 ) ;
#18425=ORIENTED_EDGE ( 'NONE', *, *, #34945, .F. ) ;
#18436=FACE_OUTER_BOUND ( 'NONE', #19927, .T. ) ;
#18441=ORIENTED_EDGE ( 'NONE', *, *, #2420, .F. ) ;
#18442=CARTESIAN_POINT ( 'NONE',  ( 9.000000000000001776, -47.31079789947416003, -105.9135893174955783 ) ) ;
#18444=DIRECTION ( 'NONE',  ( 0.000000000000000000, -0.9213119778704166318, 0.3888241754733122724 ) ) ;
#18445=ORIENTED_EDGE ( 'NONE', *, *, #19895, .F. ) ;
#18446=EDGE_CURVE ( 'NONE', #1856, #10231, #10022, .T. ) ;
#18447=ADVANCED_FACE ( 'NONE', ( #3462 ), #36201, .F. ) ;
#18450=EDGE_CURVE ( 'NONE', #17523, #29749, #20782, .T. ) ;
#18452=VECTOR ( 'NONE', #39360, 1000.000000000000000 ) ;
#18454=CYLINDRICAL_SURFACE ( 'NONE', #24874, 59.00000000000000711 ) ;
#18455=CYLINDRICAL_SURFACE ( 'NONE', #26972, 59.00000000000000000 ) ;
#18459=ADVANCED_FACE ( 'NONE', ( #10248 ), #23594, .F. ) ;
#18460=FACE_OUTER_BOUND ( 'NONE', #17504, .T. ) ;
#18461=VERTEX_POINT ( 'NONE', #30329 ) ;
#18464=CARTESIAN_POINT ( 'NONE',  ( 0.000000000000000000, 119.0898412705474385, 18.38751498043774646 ) ) ;
#18467=DIRECTION ( 'NONE',  ( 1.000000000000000000, 0.000000000000000000, 0.000000000000000000 ) ) ;
#18470=ORIENTED_EDGE ( 'NONE', *, *, #13190, .T. ) ;
#18473=DIRECTION ( 'NONE',  ( 1.000000000000000000, 0.000000000000000000, 0.000000000000000000 ) ) ;
#18475=ORIENTED_EDGE ( 'NONE', *, *, #19288, .T. ) ;
#18476=DIRECTION ( 'NONE',  ( 0.000000000000000000, 0.2113826236296182937, 0.9774033898178680069 ) ) ;
#18483=CARTESIAN_POINT ( 'NONE',  ( 0.000000000000000000, 89.07460286905850921, 81.15544420874989839 ) ) ;
#18487=DIRECTION ( 'NONE',  ( -1.000000000000000000, -0.000000000000000000, -0.000000000000000000 ) ) ;
#18488=AXIS2_PLACEMENT_3D ( 'NONE', #28992, #35924, #5832 ) ;
#18490=ORIENTED_EDGE ( 'NONE', *, *, #6426, .T. ) ;
#18491=DIRECTION ( 'NONE',  ( 1.000000000000000000, 0.000000000000000000, 0.000000000000000000 ) ) ;
#18493=CIRCLE ( 'NONE', #15666, 59.00000000000001421 ) ;
#18494=DIRECTION ( 'NONE',  ( -1.000000000000000000, -0.000000000000000000, -0.000000000000000000 ) ) ;
#18495=CARTESIAN_POINT ( 'NONE',  ( 9.000000000000001776, -115.9750404417043939, -2.406240749598616446 ) ) ;
#18497=LINE ( 'NONE', #2696, #14939 ) ;
#18499=ADVANCED_FACE ( 'NONE', ( #6111 ), #1283, .F. ) ;
#18503=EDGE_LOOP ( 'NONE', ( #41517, #4899, #23439, #11811 ) ) ;
#18504=LINE ( 'NONE', #18937, #17326 ) ;
#18510=DIRECTION ( 'NONE',  ( 0.000000000000000000, 1.246648735278247733E-14, -1.000000000000000000 ) ) ;
#18511=AXIS2_PLACEMENT_3D ( 'NONE', #32542, #41721, #25609 ) ;
#18512=EDGE_CURVE ( 'NONE', #566, #27409, #22184, .T. ) ;
#18514=DIRECTION ( 'NONE',  ( -1.000000000000000000, -0.000000000000000000, -0.000000000000000000 ) ) ;
#18515=ORIENTED_EDGE ( 'NONE', *, *, #4189, .T. ) ;
#18517=AXIS2_PLACEMENT_3D ( 'NONE', #18999, #25120, #15700 ) ;
#18518=EDGE_CURVE ( 'NONE', #33403, #11059, #6115, .T. ) ;
#18524=DIRECTION ( 'NONE',  ( 1.000000000000000000, 0.000000000000000000, 0.000000000000000000 ) ) ;
#18526=DIRECTION ( 'NONE',  ( 0.000000000000000000, 0.9574220383620062336, -0.2886919473396183933 ) ) ;
#18527=CIRCLE ( 'NONE', #36541, 120.5010000000000190 ) ;
#18528=CARTESIAN_POINT ( 'NONE',  ( 17.99999999999999645, -47.31079789947556691, 105.9135893174949530 ) ) ;
#18531=CARTESIAN_POINT ( 'NONE',  ( 17.99999999999999645, 110.0562500189198829, 49.07252625220148445 ) ) ;
#18532=CARTESIAN_POINT ( 'NONE',  ( 0.000000000000000000, 0.000000000000000000, 0.000000000000000000 ) ) ;
#18536=EDGE_CURVE ( 'NONE', #15632, #10000, #30533, .T. ) ;
#18538=CARTESIAN_POINT ( 'NONE',  ( 17.99999999999999645, 111.2559044912524939, 32.83479428644713494 ) ) ;
#18540=CARTESIAN_POINT ( 'NONE',  ( 0.000000000000000000, 110.0562500189198829, 49.07252625220149156 ) ) ;
#18544=DIRECTION ( 'NONE',  ( -1.000000000000000000, -0.000000000000000000, 0.000000000000000000 ) ) ;
#18545=CIRCLE ( 'NONE', #11566, 59.00000000000000000 ) ;
#18549=VERTEX_POINT ( 'NONE', #17480 ) ;
#18550=AXIS2_PLACEMENT_3D ( 'NONE', #11951, #24849, #5380 ) ;
#18551=DIRECTION ( 'NONE',  ( 1.000000000000000000, 0.000000000000000000, 0.000000000000000000 ) ) ;
#18559=LINE ( 'NONE', #41400, #13570 ) ;
#18565=EDGE_CURVE ( 'NONE', #33336, #42002, #11735, .T. ) ;
#18566=ORIENTED_EDGE ( 'NONE', *, *, #5423, .T. ) ;
#18570=CARTESIAN_POINT ( 'NONE',  ( 17.99999999999999645, 110.8621702203448649, 34.14058016547577523 ) ) ;
#18574=EDGE_CURVE ( 'NONE', #41141, #29185, #14187, .T. ) ;
#18575=AXIS2_PLACEMENT_3D ( 'NONE', #24639, #11965, #24868 ) ;
#18577=VECTOR ( 'NONE', #23783, 1000.000000000000000 ) ;
#18578=DIRECTION ( 'NONE',  ( 0.000000000000000000, -0.6783118362696222148, 0.7347741508630615259 ) ) ;
#18579=VECTOR ( 'NONE', #13703, 1000.000000000000000 ) ;
#18580=VERTEX_POINT ( 'NONE', #40758 ) ;
#18586=DIRECTION ( 'NONE',  ( 1.000000000000000000, 0.000000000000000000, -0.000000000000000000 ) ) ;
#18587=DIRECTION ( 'NONE',  ( 1.000000000000000000, 0.000000000000000000, 0.000000000000000000 ) ) ;
#18588=AXIS2_PLACEMENT_3D ( 'NONE', #12310, #25638, #29107 ) ;
#18591=ORIENTED_EDGE ( 'NONE', *, *, #22872, .F. ) ;
#18592=AXIS2_PLACEMENT_3D ( 'NONE', #20285, #10870, #10646 ) ;
#18594=DIRECTION ( 'NONE',  ( -1.000000000000000000, 0.000000000000000000, -0.000000000000000000 ) ) ;
#18595=EDGE_LOOP ( 'NONE', ( #11156, #39786, #39658, #16345 ) ) ;
#18596=CYLINDRICAL_SURFACE ( 'NONE', #19572, 120.5010000000000190 ) ;
#18597=CARTESIAN_POINT ( 'NONE',  ( 17.99999999999999645, -101.1403355683142422, -56.80345518653591341 ) ) ;
#18598=EDGE_CURVE ( 'NONE', #37525, #40004, #14502, .T. ) ;
#18599=EDGE_CURVE ( 'NONE', #30629, #22504, #27045, .T. ) ;
#18601=FACE_OUTER_BOUND ( 'NONE', #4848, .T. ) ;
#18609=AXIS2_PLACEMENT_3D ( 'NONE', #16203, #37487, #20304 ) ;
#18610=CARTESIAN_POINT ( 'NONE',  ( 0.000000000000000000, 0.000000000000000000, 0.000000000000000000 ) ) ;
#18612=CIRCLE ( 'NONE', #12315, 120.5010000000000332 ) ;
#18615=DIRECTION ( 'NONE',  ( 0.000000000000000000, 0.000000000000000000, 1.000000000000000000 ) ) ;
#18617=ORIENTED_EDGE ( 'NONE', *, *, #19068, .F. ) ;
#18618=CIRCLE ( 'NONE', #3922, 59.00000000000000000 ) ;
#18625=CIRCLE ( 'NONE', #17902, 116.0000000000000000 ) ;
#18626=EDGE_CURVE ( 'NONE', #22539, #13634, #12414, .T. ) ;
#18629=EDGE_CURVE ( 'NONE', #8703, #2020, #7400, .T. ) ;
#18630=AXIS2_PLACEMENT_3D ( 'NONE', #16489, #29795, #33468 ) ;
#18635=ORIENTED_EDGE ( 'NONE', *, *, #657, .F. ) ;
#18636=FACE_OUTER_BOUND ( 'NONE', #3119, .T. ) ;
#18638=ORIENTED_EDGE ( 'NONE', *, *, #22846, .T. ) ;
#18640=AXIS2_PLACEMENT_3D ( 'NONE', #15645, #36317, #32002 ) ;
#18641=DIRECTION ( 'NONE',  ( 0.000000000000000000, -0.8477344278896651319, -0.5304209081197519549 ) ) ;
#18643=ORIENTED_EDGE ( 'NONE', *, *, #12541, .T. ) ;
#18647=ORIENTED_EDGE ( 'NONE', *, *, #42765, .T. ) ;
#18655=CIRCLE ( 'NONE', #13729, 120.5010000000000190 ) ;
#18657=EDGE_CURVE ( 'NONE', #26205, #36343, #38201, .T. ) ;
#18658=EDGE_CURVE ( 'NONE', #12090, #36312, #12001, .T. ) ;
#18659=DIRECTION ( 'NONE',  ( -1.000000000000000000, 0.000000000000000000, -0.000000000000000000 ) ) ;
#18664=AXIS2_PLACEMENT_3D ( 'NONE', #41559, #18487, #8404 ) ;
#18666=CARTESIAN_POINT ( 'NONE',  ( 0.000000000000000000, 110.1579703617966430, 21.29539948940285043 ) ) ;
#18667=CARTESIAN_POINT ( 'NONE',  ( 17.99999999999999645, 0.000000000000000000, 0.000000000000000000 ) ) ;
#18672=DIRECTION ( 'NONE',  ( -1.000000000000000000, 0.000000000000000000, 0.000000000000000000 ) ) ;
#18673=ORIENTED_EDGE ( 'NONE', *, *, #22259, .F. ) ;
#18674=CARTESIAN_POINT ( 'NONE',  ( 17.99999999999999645, -66.49630760163542220, -90.36876423296052963 ) ) ;
#18682=CIRCLE ( 'NONE', #1198, 59.00000000000000711 ) ;
#18684=VECTOR ( 'NONE', #16519, 1000.000000000000000 ) ;
#18685=ORIENTED_EDGE ( 'NONE', *, *, #32026, .F. ) ;
#18687=DIRECTION ( 'NONE',  ( 0.000000000000000000, 0.000000000000000000, 1.000000000000000000 ) ) ;
#18688=CARTESIAN_POINT ( 'NONE',  ( 17.99999999999999645, 13.00789606333472470, 115.2683592318615382 ) ) ;
#18690=DIRECTION ( 'NONE',  ( 0.000000000000000000, 0.000000000000000000, 1.000000000000000000 ) ) ;
#18697=APPLICATION_CONTEXT ( 'automotive_design' ) ;
#18704=ORIENTED_EDGE ( 'NONE', *, *, #25722, .F. ) ;
#18706=VERTEX_POINT ( 'NONE', #31409 ) ;
#18709=DIRECTION ( 'NONE',  ( 1.000000000000000000, 0.000000000000000000, 0.000000000000000000 ) ) ;
#18711=EDGE_CURVE ( 'NONE', #5699, #35404, #35518, .T. ) ;
#18718=VECTOR ( 'NONE', #41751, 1000.000000000000000 ) ;
#18719=CARTESIAN_POINT ( 'NONE',  ( 17.99999999999999645, -116.4607004671430417, 30.94182036827165660 ) ) ;
#18723=ORIENTED_EDGE ( 'NONE', *, *, #26843, .T. ) ;
#18725=CARTESIAN_POINT ( 'NONE',  ( 0.000000000000000000, 47.31079789947627745, -105.9135893174946119 ) ) ;
#18726=DIRECTION ( 'NONE',  ( -1.000000000000000000, -0.000000000000000000, -0.000000000000000000 ) ) ;
#18727=CIRCLE ( 'NONE', #42314, 120.5010000000000474 ) ;
#18728=ADVANCED_FACE ( 'NONE', ( #31612 ), #8693, .F. ) ;
#18730=DIRECTION ( 'NONE',  ( 0.000000000000000000, 0.000000000000000000, 1.000000000000000000 ) ) ;
#18731=ORIENTED_EDGE ( 'NONE', *, *, #41616, .T. ) ;
#18732=DIRECTION ( 'NONE',  ( 0.000000000000000000, 0.000000000000000000, 1.000000000000000000 ) ) ;
#18733=ORIENTED_EDGE ( 'NONE', *, *, #42990, .F. ) ;
#18734=LINE ( 'NONE', #31779, #26360 ) ;
#18738=DIRECTION ( 'NONE',  ( -1.000000000000000000, 0.000000000000000000, -0.000000000000000000 ) ) ;
#18741=AXIS2_PLACEMENT_3D ( 'NONE', #41348, #35242, #5370 ) ;
#18742=EDGE_LOOP ( 'NONE', ( #485, #16152, #36293, #8454 ) ) ;
#18743=CARTESIAN_POINT ( 'NONE',  ( 0.000000000000000000, 0.000000000000000000, 0.000000000000000000 ) ) ;
#18746=DIRECTION ( 'NONE',  ( 0.000000000000000000, 0.000000000000000000, 1.000000000000000000 ) ) ;
#18747=DIRECTION ( 'NONE',  ( 1.000000000000000000, 0.000000000000000000, 0.000000000000000000 ) ) ;
#18749=CARTESIAN_POINT ( 'NONE',  ( -10.00000000000000000, 0.000000000000000000, 0.000000000000000000 ) ) ;
#18751=CARTESIAN_POINT ( 'NONE',  ( 0.000000000000000000, 0.000000000000000000, 0.000000000000000000 ) ) ;
#18752=ORIENTED_EDGE ( 'NONE', *, *, #37646, .T. ) ;
#18753=DIRECTION ( 'NONE',  ( 1.000000000000000000, 0.000000000000000000, 0.000000000000000000 ) ) ;
#18756=ORIENTED_EDGE ( 'NONE', *, *, #29533, .T. ) ;
#18758=DIRECTION ( 'NONE',  ( 0.000000000000000000, 0.000000000000000000, 1.000000000000000000 ) ) ;
#18759=EDGE_CURVE ( 'NONE', #17938, #22817, #10334, .T. ) ;
#18760=DIRECTION ( 'NONE',  ( 1.000000000000000000, 0.000000000000000000, 0.000000000000000000 ) ) ;
#18762=VERTEX_POINT ( 'NONE', #22049 ) ;
#18769=EDGE_CURVE ( 'NONE', #19587, #815, #28499, .T. ) ;
#18770=DIRECTION ( 'NONE',  ( 0.000000000000000000, 0.000000000000000000, 1.000000000000000000 ) ) ;
#18773=EDGE_LOOP ( 'NONE', ( #36393, #11102, #25973, #26236 ) ) ;
#18777=ORIENTED_EDGE ( 'NONE', *, *, #19288, .F. ) ;
#18778=CARTESIAN_POINT ( 'NONE',  ( 17.99999999999999645, 23.21237537461745859, 109.7700237000592836 ) ) ;
#18779=LINE ( 'NONE', #32033, #28280 ) ;
#18783=CARTESIAN_POINT ( 'NONE',  ( 17.99999999999999645, 67.32409792376626001, -89.75376489259298296 ) ) ;
#18784=VERTEX_POINT ( 'NONE', #8481 ) ;
#18785=LINE ( 'NONE', #28781, #35815 ) ;
#18787=ORIENTED_EDGE ( 'NONE', *, *, #11076, .F. ) ;
#18790=ORIENTED_EDGE ( 'NONE', *, *, #17278, .F. ) ;
#18791=EDGE_CURVE ( 'NONE', #35178, #42713, #40960, .T. ) ;
#18793=DIRECTION ( 'NONE',  ( -1.000000000000000000, -0.000000000000000000, -0.000000000000000000 ) ) ;
#18796=VECTOR ( 'NONE', #9290, 1000.000000000000000 ) ;
#18801=AXIS2_PLACEMENT_3D ( 'NONE', #27551, #24966, #34291 ) ;
#18802=ORIENTED_EDGE ( 'NONE', *, *, #11753, .F. ) ;
#18804=DIRECTION ( 'NONE',  ( 0.000000000000000000, 0.000000000000000000, 1.000000000000000000 ) ) ;
#18805=ORIENTED_EDGE ( 'NONE', *, *, #30036, .F. ) ;
#18813=DIRECTION ( 'NONE',  ( 0.000000000000000000, 9.408669700213191589E-16, -1.000000000000000000 ) ) ;
#18816=DIRECTION ( 'NONE',  ( 0.000000000000000000, -0.05322217484216513333, -0.9985826956767627216 ) ) ;
#18821=CARTESIAN_POINT ( 'NONE',  ( 17.99999999999999645, 0.000000000000000000, 0.000000000000000000 ) ) ;
#18823=ORIENTED_EDGE ( 'NONE', *, *, #38827, .T. ) ;
#18826=ADVANCED_FACE ( 'NONE', ( #8277 ), #5431, .F. ) ;
#18833=DIRECTION ( 'NONE',  ( 0.000000000000000000, 0.000000000000000000, 1.000000000000000000 ) ) ;
#18834=ORIENTED_EDGE ( 'NONE', *, *, #28108, .F. ) ;
#18837=CARTESIAN_POINT ( 'NONE',  ( 0.000000000000000000, 0.000000000000000000, 0.000000000000000000 ) ) ;
#18845=CARTESIAN_POINT ( 'NONE',  ( 0.000000000000000000, -62.45178862086279992, 93.20969140437486544 ) ) ;
#18846=CIRCLE ( 'NONE', #36185, 59.00000000000000000 ) ;
#18847=DIRECTION ( 'NONE',  ( 0.000000000000000000, 0.000000000000000000, 1.000000000000000000 ) ) ;
#18850=DIRECTION ( 'NONE',  ( 0.000000000000000000, -0.2631025642275088838, -0.9647678688145193693 ) ) ;
#18854=EDGE_CURVE ( 'NONE', #7746, #34978, #34030, .T. ) ;
#18855=ORIENTED_EDGE ( 'NONE', *, *, #17738, .F. ) ;
#18856=DIRECTION ( 'NONE',  ( -1.000000000000000000, 0.000000000000000000, 0.000000000000000000 ) ) ;
#18862=DIRECTION ( 'NONE',  ( 0.000000000000000000, 0.000000000000000000, 1.000000000000000000 ) ) ;
#18863=EDGE_CURVE ( 'NONE', #18183, #9792, #36103, .T. ) ;
#18870=DIRECTION ( 'NONE',  ( -1.000000000000000000, -0.000000000000000000, 0.000000000000000000 ) ) ;
#18871=ORIENTED_EDGE ( 'NONE', *, *, #30788, .F. ) ;
#18873=CARTESIAN_POINT ( 'NONE',  ( 0.000000000000000000, -111.7974656912329436, -9.465682155096647676 ) ) ;
#18874=CIRCLE ( 'NONE', #32067, 59.00000000000002132 ) ;
#18875=ORIENTED_EDGE ( 'NONE', *, *, #9099, .F. ) ;
#18879=AXIS2_PLACEMENT_3D ( 'NONE', #42294, #8715, #28808 ) ;
#18886=ORIENTED_EDGE ( 'NONE', *, *, #38829, .F. ) ;
#18887=CARTESIAN_POINT ( 'NONE',  ( 0.000000000000000000, 0.000000000000000000, 0.000000000000000000 ) ) ;
#18888=DIRECTION ( 'NONE',  ( 1.000000000000000000, -0.000000000000000000, 0.000000000000000000 ) ) ;
#18891=EDGE_CURVE ( 'NONE', #9595, #14740, #33314, .T. ) ;
#18892=EDGE_CURVE ( 'NONE', #22284, #41100, #39587, .T. ) ;
#18894=DIRECTION ( 'NONE',  ( -1.000000000000000000, 0.000000000000000000, 0.000000000000000000 ) ) ;
#18899=CARTESIAN_POINT ( 'NONE',  ( 0.000000000000000000, 95.38615066514064722, -59.07414607872728141 ) ) ;
#18903=ORIENTED_EDGE ( 'NONE', *, *, #8368, .T. ) ;
#18906=DIRECTION ( 'NONE',  ( -1.000000000000000000, 0.000000000000000000, 0.000000000000000000 ) ) ;
#18907=VERTEX_POINT ( 'NONE', #39423 ) ;
#18913=VERTEX_POINT ( 'NONE', #29214 ) ;
#18917=EDGE_CURVE ( 'NONE', #19384, #6563, #13283, .T. ) ;
#18920=DIRECTION ( 'NONE',  ( -1.000000000000000000, 0.000000000000000000, -0.000000000000000000 ) ) ;
#18921=CARTESIAN_POINT ( 'NONE',  ( 0.000000000000000000, 94.52951811191560694, 67.23221107124935259 ) ) ;
#18922=DIRECTION ( 'NONE',  ( -1.000000000000000000, 0.000000000000000000, 0.000000000000000000 ) ) ;
#18923=ORIENTED_EDGE ( 'NONE', *, *, #14745, .F. ) ;
#18925=ORIENTED_EDGE ( 'NONE', *, *, #20258, .F. ) ;
#18930=DIRECTION ( 'NONE',  ( 0.000000000000000000, -1.246648735278247733E-14, -1.000000000000000000 ) ) ;
#18931=CARTESIAN_POINT ( 'NONE',  ( 17.99999999999999645, -94.52951811191606168, 67.23221107124869889 ) ) ;
#18932=ORIENTED_EDGE ( 'NONE', *, *, #25551, .F. ) ;
#18934=FACE_OUTER_BOUND ( 'NONE', #5583, .T. ) ;
#18935=CIRCLE ( 'NONE', #7035, 120.5010000000000332 ) ;
#18937=CARTESIAN_POINT ( 'NONE',  ( 17.99999999999999645, -8.827181066045094227, -120.1772519049560231 ) ) ;
#18938=CARTESIAN_POINT ( 'NONE',  ( 0.000000000000000000, -18.35539002514457252, 110.6858262410709273 ) ) ;
#18939=EDGE_CURVE ( 'NONE', #17680, #35461, #20849, .T. ) ;
#18942=ADVANCED_FACE ( 'NONE', ( #12630 ), #26151, .F. ) ;
#18943=ADVANCED_FACE ( 'NONE', ( #42691 ), #19621, .F. ) ;
#18945=DIRECTION ( 'NONE',  ( 1.000000000000000000, 0.000000000000000000, 0.000000000000000000 ) ) ;
#18947=EDGE_LOOP ( 'NONE', ( #9516, #22274, #26783, #935 ) ) ;
#18949=VERTEX_POINT ( 'NONE', #42912 ) ;
#18956=CARTESIAN_POINT ( 'NONE',  ( 17.99999999999999645, 41.62036691425530677, 113.0850832732715787 ) ) ;
#18959=CYLINDRICAL_SURFACE ( 'NONE', #36158, 59.00000000000000000 ) ;
#18963=CARTESIAN_POINT ( 'NONE',  ( -10.00000000000000000, 0.000000000000000000, 0.000000000000000000 ) ) ;
#18964=DIRECTION ( 'NONE',  ( 0.000000000000000000, 0.000000000000000000, 1.000000000000000000 ) ) ;
#18966=VERTEX_POINT ( 'NONE', #127 ) ;
#18967=DIRECTION ( 'NONE',  ( 0.000000000000000000, 0.8183027759081662467, 0.5747874102144109321 ) ) ;
#18969=DIRECTION ( 'NONE',  ( 0.000000000000000000, -0.2113826236296315608, 0.9774033898178652313 ) ) ;
#18971=CARTESIAN_POINT ( 'NONE',  ( 0.000000000000000000, 107.2703412112699368, -32.88383143828351507 ) ) ;
#18975=FACE_OUTER_BOUND ( 'NONE', #14695, .T. ) ;
#18978=ORIENTED_EDGE ( 'NONE', *, *, #11471, .T. ) ;
#18980=CARTESIAN_POINT ( 'NONE',  ( 17.99999999999999645, 111.2721026680460596, 44.61974821237342326 ) ) ;
#18983=ORIENTED_EDGE ( 'NONE', *, *, #35187, .F. ) ;
#18985=ORIENTED_EDGE ( 'NONE', *, *, #30859, .T. ) ;
#18987=CARTESIAN_POINT ( 'NONE',  ( 17.99999999999999645, 96.25468616236661035, 72.49500943364525085 ) ) ;
#18989=DIRECTION ( 'NONE',  ( 0.000000000000000000, 0.000000000000000000, -1.000000000000000000 ) ) ;
#18994=ORIENTED_EDGE ( 'NONE', *, *, #2610, .F. ) ;
#18999=CARTESIAN_POINT ( 'NONE',  ( 0.000000000000000000, -24.22031524826050841, 109.5520369638036584 ) ) ;
#19001=EDGE_LOOP ( 'NONE', ( #4889, #29601, #20364, #1989 ) ) ;
#19005=ORIENTED_EDGE ( 'NONE', *, *, #16994, .T. ) ;
#19008=AXIS2_PLACEMENT_3D ( 'NONE', #9411, #32330, #42564 ) ;
#19012=ORIENTED_EDGE ( 'NONE', *, *, #15620, .T. ) ;
#19014=VERTEX_POINT ( 'NONE', #41530 ) ;
#19016=CARTESIAN_POINT ( 'NONE',  ( 17.99999999999999645, 56.51398178981825993, 96.92493144647468739 ) ) ;
#19022=ORIENTED_EDGE ( 'NONE', *, *, #40939, .T. ) ;
#19023=CARTESIAN_POINT ( 'NONE',  ( 0.000000000000000000, -112.5120133921104753, -43.14554256761132223 ) ) ;
#19024=ORIENTED_EDGE ( 'NONE', *, *, #3584, .T. ) ;
#19025=DIRECTION ( 'NONE',  ( 0.000000000000000000, -0.9968120070307493474, -0.07978610555309334496 ) ) ;
#19028=DIRECTION ( 'NONE',  ( 0.000000000000000000, -0.8747630845319559478, -0.4845508703326599775 ) ) ;
#19030=CIRCLE ( 'NONE', #23193, 116.0000000000000000 ) ;
#19031=ORIENTED_EDGE ( 'NONE', *, *, #30133, .T. ) ;
#19032=CYLINDRICAL_SURFACE ( 'NONE', #6672, 59.00000000000000000 ) ;
#19036=EDGE_CURVE ( 'NONE', #15115, #17938, #15968, .T. ) ;
#19039=CYLINDRICAL_SURFACE ( 'NONE', #14196, 59.00000000000000000 ) ;
#19040=CARTESIAN_POINT ( 'NONE',  ( 17.99999999999999645, 119.8996782608629985, 12.02323392193397211 ) ) ;
#19042=CIRCLE ( 'NONE', #39877, 59.00000000000000000 ) ;
#19045=CARTESIAN_POINT ( 'NONE',  ( 17.99999999999999645, 0.000000000000000000, 0.000000000000000000 ) ) ;
#19046=DIRECTION ( 'NONE',  ( 0.000000000000000000, -0.9911528310040084166, 0.1327255272837126743 ) ) ;
#19049=DIRECTION ( 'NONE',  ( 1.000000000000000000, 0.000000000000000000, 0.000000000000000000 ) ) ;
#19051=EDGE_CURVE ( 'NONE', #5141, #27385, #37516, .T. ) ;
#19053=DIRECTION ( 'NONE',  ( -1.000000000000000000, -0.000000000000000000, 0.000000000000000000 ) ) ;
#19055=AXIS2_PLACEMENT_3D ( 'NONE', #1038, #21405, #14831 ) ;
#19057=DIRECTION ( 'NONE',  ( 0.000000000000000000, -0.7525707698561306946, -0.6585113790650474197 ) ) ;
#19059=ORIENTED_EDGE ( 'NONE', *, *, #2775, .T. ) ;
#19068=EDGE_CURVE ( 'NONE', #18244, #1564, #18082, .T. ) ;
#19070=CARTESIAN_POINT ( 'NONE',  ( 0.000000000000000000, 0.000000000000000000, 0.000000000000000000 ) ) ;
#19072=DIRECTION ( 'NONE',  ( 0.000000000000000000, 0.000000000000000000, 1.000000000000000000 ) ) ;
#19074=AXIS2_PLACEMENT_3D ( 'NONE', #3810, #17195, #13911 ) ;
#19075=DIRECTION ( 'NONE',  ( 0.000000000000000000, 0.000000000000000000, 1.000000000000000000 ) ) ;
#19077=CARTESIAN_POINT ( 'NONE',  ( -10.00000000000000000, 0.000000000000000000, 0.000000000000000000 ) ) ;
#19078=DIRECTION ( 'NONE',  ( -1.000000000000000000, 0.000000000000000000, -0.000000000000000000 ) ) ;
#19079=EDGE_LOOP ( 'NONE', ( #17241, #8596, #4426, #41976 ) ) ;
#19086=ORIENTED_EDGE ( 'NONE', *, *, #15428, .F. ) ;
#19087=CYLINDRICAL_SURFACE ( 'NONE', #41568, 116.0000000000000000 ) ;
#19088=DIRECTION ( 'NONE',  ( 0.000000000000000000, 0.3641605752528230266, -0.9313361774523382097 ) ) ;
#19090=CYLINDRICAL_SURFACE ( 'NONE', #26819, 116.0000000000000000 ) ;
#19092=EDGE_CURVE ( 'NONE', #3822, #18385, #4892, .T. ) ;
#19093=DIRECTION ( 'NONE',  ( 0.000000000000000000, -0.5528000653611833126, -0.8333139190825217257 ) ) ;
#19094=VERTEX_POINT ( 'NONE', #4227 ) ;
#19096=ORIENTED_EDGE ( 'NONE', *, *, #2501, .T. ) ;
#19098=DIRECTION ( 'NONE',  ( -1.000000000000000000, -0.000000000000000000, -0.000000000000000000 ) ) ;
#19099=EDGE_CURVE ( 'NONE', #1834, #40651, #6182, .T. ) ;
#19100=CARTESIAN_POINT ( 'NONE',  ( 17.99999999999999645, 83.49789599728902090, -86.88263557826680028 ) ) ;
#19101=AXIS2_PLACEMENT_3D ( 'NONE', #38716, #26078, #28928 ) ;
#19103=EDGE_CURVE ( 'NONE', #9794, #26508, #21093, .T. ) ;
#19108=CIRCLE ( 'NONE', #22593, 58.99999999999999289 ) ;
#19109=VERTEX_POINT ( 'NONE', #18464 ) ;
#19110=DIRECTION ( 'NONE',  ( 0.000000000000000000, 0.8993121301712202476, -0.4373073204588531770 ) ) ;
#19111=ORIENTED_EDGE ( 'NONE', *, *, #40881, .T. ) ;
#19114=CARTESIAN_POINT ( 'NONE',  ( 17.99999999999999645, -88.00363688980601751, 82.31555682352626491 ) ) ;
#19119=EDGE_CURVE ( 'NONE', #1487, #5158, #23635, .T. ) ;
#19120=CYLINDRICAL_SURFACE ( 'NONE', #34933, 59.00000000000000000 ) ;
#19123=DIRECTION ( 'NONE',  ( 0.000000000000000000, -2.128711519673234442E-14, -1.000000000000000000 ) ) ;
#19124=ORIENTED_EDGE ( 'NONE', *, *, #18319, .T. ) ;
#19126=AXIS2_PLACEMENT_3D ( 'NONE', #14256, #242, #13615 ) ;
#19131=DIRECTION ( 'NONE',  ( -1.000000000000000000, -0.000000000000000000, -0.000000000000000000 ) ) ;
#19132=CARTESIAN_POINT ( 'NONE',  ( 0.000000000000000000, 0.000000000000000000, 0.000000000000000000 ) ) ;
#19133=EDGE_CURVE ( 'NONE', #21485, #16671, #6914, .T. ) ;
#19136=AXIS2_PLACEMENT_3D ( 'NONE', #2972, #39004, #32259 ) ;
#19139=LINE ( 'NONE', #29158, #4625 ) ;
#19144=EDGE_CURVE ( 'NONE', #1445, #12660, #40992, .T. ) ;
#19147=VERTEX_POINT ( 'NONE', #34560 ) ;
#19151=DIRECTION ( 'NONE',  ( 0.000000000000000000, -0.9407002666710364558, 0.3392388661180213427 ) ) ;
#19153=EDGE_LOOP ( 'NONE', ( #5556, #39010, #33210, #22750 ) ) ;
#19154=CARTESIAN_POINT ( 'NONE',  ( 17.99999999999999645, 0.000000000000000000, 0.000000000000000000 ) ) ;
#19155=CYLINDRICAL_SURFACE ( 'NONE', #42370, 59.00000000000000000 ) ;
#19164=EDGE_LOOP ( 'NONE', ( #19225, #10973, #38895, #11 ) ) ;
#19165=VECTOR ( 'NONE', #30283, 1000.000000000000000 ) ;
#19167=DIRECTION ( 'NONE',  ( 0.000000000000000000, -0.1590634960190789038, 0.9872683547213435551 ) ) ;
#19168=DIRECTION ( 'NONE',  ( -1.000000000000000000, -0.000000000000000000, -0.000000000000000000 ) ) ;
#19171=EDGE_CURVE ( 'NONE', #14175, #9120, #31964, .T. ) ;
#19173=DIRECTION ( 'NONE',  ( 0.000000000000000000, 0.000000000000000000, 1.000000000000000000 ) ) ;
#19174=ADVANCED_FACE ( 'NONE', ( #19308 ), #5540, .F. ) ;
#19180=AXIS2_PLACEMENT_3D ( 'NONE', #715, #3759, #33901 ) ;
#19182=CARTESIAN_POINT ( 'NONE',  ( 0.000000000000000000, 94.83915810436401728, 59.94836581341619564 ) ) ;
#19185=CARTESIAN_POINT ( 'NONE',  ( 17.99999999999999645, 106.5605152861910909, -56.26142179985714620 ) ) ;
#19190=VECTOR ( 'NONE', #18894, 1000.000000000000000 ) ;
#19191=DIRECTION ( 'NONE',  ( 1.000000000000000000, 0.000000000000000000, 0.000000000000000000 ) ) ;
#19192=ORIENTED_EDGE ( 'NONE', *, *, #35251, .F. ) ;
#19197=CIRCLE ( 'NONE', #42832, 120.5010000000000190 ) ;
#19199=DIRECTION ( 'NONE',  ( -1.000000000000000000, -0.000000000000000000, -0.000000000000000000 ) ) ;
#19200=DIRECTION ( 'NONE',  ( 0.000000000000000000, 0.000000000000000000, 1.000000000000000000 ) ) ;
#19203=VERTEX_POINT ( 'NONE', #32154 ) ;
#19207=ORIENTED_EDGE ( 'NONE', *, *, #10225, .F. ) ;
#19213=ORIENTED_EDGE ( 'NONE', *, *, #14735, .T. ) ;
#19215=ORIENTED_EDGE ( 'NONE', *, *, #30000, .T. ) ;
#19216=DIRECTION ( 'NONE',  ( -1.000000000000000000, 0.000000000000000000, 0.000000000000000000 ) ) ;
#19220=CIRCLE ( 'NONE', #3107, 120.5010000000000474 ) ;
#19223=ADVANCED_FACE ( 'NONE', ( #12105 ), #42387, .F. ) ;
#19225=ORIENTED_EDGE ( 'NONE', *, *, #16824, .T. ) ;
#19230=CYLINDRICAL_SURFACE ( 'NONE', #9902, 120.5010000000000190 ) ;
#19232=LINE ( 'NONE', #12663, #4326 ) ;
#19233=CYLINDRICAL_SURFACE ( 'NONE', #20976, 59.00000000000000000 ) ;
#19236=CARTESIAN_POINT ( 'NONE',  ( 17.99999999999999645, -46.83041522348565167, 101.9567785075599744 ) ) ;
#19237=EDGE_CURVE ( 'NONE', #21205, #2350, #8586, .T. ) ;
#19239=ORIENTED_EDGE ( 'NONE', *, *, #34295, .T. ) ;
#19242=AXIS2_PLACEMENT_3D ( 'NONE', #11158, #4810, #17302 ) ;
#19243=AXIS2_PLACEMENT_3D ( 'NONE', #4156, #37761, #20812 ) ;
#19245=DIRECTION ( 'NONE',  ( 0.000000000000000000, 0.000000000000000000, 1.000000000000000000 ) ) ;
#19248=AXIS2_PLACEMENT_3D ( 'NONE', #12787, #26317, #36104 ) ;
#19252=ORIENTED_EDGE ( 'NONE', *, *, #27788, .T. ) ;
#19256=ORIENTED_EDGE ( 'NONE', *, *, #33658, .T. ) ;
#19262=ORIENTED_EDGE ( 'NONE', *, *, #28638, .F. ) ;
#19265=ORIENTED_EDGE ( 'NONE', *, *, #3285, .F. ) ;
#19268=EDGE_CURVE ( 'NONE', #12118, #27792, #13877, .T. ) ;
#19270=DIRECTION ( 'NONE',  ( 0.000000000000000000, 0.9213119778704113028, 0.3888241754733244848 ) ) ;
#19271=VERTEX_POINT ( 'NONE', #15395 ) ;
#19281=CYLINDRICAL_SURFACE ( 'NONE', #37454, 59.00000000000000000 ) ;
#19283=EDGE_CURVE ( 'NONE', #1575, #20648, #8810, .T. ) ;
#19286=VERTEX_POINT ( 'NONE', #22168 ) ;
#19287=DIRECTION ( 'NONE',  ( 0.000000000000000000, 0.000000000000000000, 1.000000000000000000 ) ) ;
#19288=EDGE_CURVE ( 'NONE', #26320, #21350, #43075, .T. ) ;
#19289=CARTESIAN_POINT ( 'NONE',  ( 17.99999999999999645, -118.8387007424469601, -19.94628303336605768 ) ) ;
#19294=ORIENTED_EDGE ( 'NONE', *, *, #28816, .T. ) ;
#19297=AXIS2_PLACEMENT_3D ( 'NONE', #13078, #8923, #22688 ) ;
#19299=DIRECTION ( 'NONE',  ( 0.000000000000000000, -0.5076658003388292428, -0.8615540813938123987 ) ) ;
#19301=AXIS2_PLACEMENT_3D ( 'NONE', #21821, #38763, #15038 ) ;
#19304=CARTESIAN_POINT ( 'NONE',  ( 17.99999999999999645, -119.0898412705475522, 18.38751498043690802 ) ) ;
#19307=ORIENTED_EDGE ( 'NONE', *, *, #10869, .T. ) ;
#19308=FACE_OUTER_BOUND ( 'NONE', #36238, .T. ) ;
#19313=DIRECTION ( 'NONE',  ( -1.000000000000000000, 0.000000000000000000, 0.000000000000000000 ) ) ;
#19315=EDGE_LOOP ( 'NONE', ( #42927, #29381, #778, #24500 ) ) ;
#19317=ORIENTED_EDGE ( 'NONE', *, *, #6080, .F. ) ;
#19318=DIRECTION ( 'NONE',  ( 0.000000000000000000, 0.4610925014493267859, -0.8873520750565710991 ) ) ;
#19322=ORIENTED_EDGE ( 'NONE', *, *, #14682, .F. ) ;
#19326=DIRECTION ( 'NONE',  ( -1.000000000000000000, 0.000000000000000000, -0.000000000000000000 ) ) ;
#19327=ADVANCED_FACE ( 'NONE', ( #12320 ), #22800, .F. ) ;
#19328=VERTEX_POINT ( 'NONE', #2443 ) ;
#19329=DIRECTION ( 'NONE',  ( 0.000000000000000000, 0.9826841245925201918, 0.1852887240871181063 ) ) ;
#19337=DIRECTION ( 'NONE',  ( 0.000000000000000000, 0.000000000000000000, 1.000000000000000000 ) ) ;
#19338=ORIENTED_EDGE ( 'NONE', *, *, #40546, .T. ) ;
#19341=CARTESIAN_POINT ( 'NONE',  ( 0.000000000000000000, 120.3696465864706937, -5.624871700594833435 ) ) ;
#19342=CARTESIAN_POINT ( 'NONE',  ( 17.99999999999999645, 0.000000000000000000, 0.000000000000000000 ) ) ;
#19349=EDGE_CURVE ( 'NONE', #1677, #37721, #6380, .T. ) ;
#19351=CIRCLE ( 'NONE', #38119, 116.0000000000000000 ) ;
#19352=CIRCLE ( 'NONE', #10993, 116.0000000000000000 ) ;
#19353=ORIENTED_EDGE ( 'NONE', *, *, #1222, .T. ) ;
#19355=DIRECTION ( 'NONE',  ( 0.000000000000000000, 0.000000000000000000, 1.000000000000000000 ) ) ;
#19358=DIRECTION ( 'NONE',  ( -1.000000000000000000, 0.000000000000000000, -0.000000000000000000 ) ) ;
#19360=CARTESIAN_POINT ( 'NONE',  ( 17.99999999999999645, -107.5680526044921947, 31.89649718262059608 ) ) ;
#19363=DIRECTION ( 'NONE',  ( 1.000000000000000000, -0.000000000000000000, 0.000000000000000000 ) ) ;
#19370=AXIS2_PLACEMENT_3D ( 'NONE', #16674, #1114, #4835 ) ;
#19371=CARTESIAN_POINT ( 'NONE',  ( 0.000000000000000000, -69.72480978689985420, -92.70626138606085931 ) ) ;
#19372=CIRCLE ( 'NONE', #29785, 59.00000000000000000 ) ;
#19374=AXIS2_PLACEMENT_3D ( 'NONE', #10714, #21016, #27309 ) ;
#19375=AXIS2_PLACEMENT_3D ( 'NONE', #15862, #28537, #4944 ) ;
#19378=VERTEX_POINT ( 'NONE', #33224 ) ;
#19379=DIRECTION ( 'NONE',  ( 0.000000000000000000, -0.3140767120219556952, 0.9493976084683790617 ) ) ;
#19380=DIRECTION ( 'NONE',  ( 0.000000000000000000, 0.000000000000000000, 1.000000000000000000 ) ) ;
#19381=ADVANCED_FACE ( 'NONE', ( #10526 ), #9870, .F. ) ;
#19382=LINE ( 'NONE', #26337, #25191 ) ;
#19384=VERTEX_POINT ( 'NONE', #36915 ) ;
#19386=CARTESIAN_POINT ( 'NONE',  ( 0.000000000000000000, 0.000000000000000000, 0.000000000000000000 ) ) ;
#19388=CYLINDRICAL_SURFACE ( 'NONE', #4131, 120.5010000000000190 ) ;
#19390=DIRECTION ( 'NONE',  ( 0.000000000000000000, 0.000000000000000000, 1.000000000000000000 ) ) ;
#19391=SHAPE_REPRESENTATION ( 'internal spur gear_iso_ISO - Internal spur gear 2M 118T 20PA 18FW ---S118S260OD 1.0AF', ( #13552 ), #9968 ) ;
#19393=VERTEX_POINT ( 'NONE', #26900 ) ;
#19394=DIRECTION ( 'NONE',  ( 1.000000000000000000, 0.000000000000000000, 0.000000000000000000 ) ) ;
#19397=CARTESIAN_POINT ( 'NONE',  ( 17.99999999999999645, 66.49630760163600485, 90.36876423296011751 ) ) ;
#19402=DIRECTION ( 'NONE',  ( 0.000000000000000000, -0.6382441836448261574, 0.7698339834299012807 ) ) ;
#19403=ORIENTED_EDGE ( 'NONE', *, *, #28676, .T. ) ;
#19414=EDGE_CURVE ( 'NONE', #20981, #17808, #30174, .T. ) ;
#19415=DIRECTION ( 'NONE',  ( 1.000000000000000000, 0.000000000000000000, 0.000000000000000000 ) ) ;
#19417=ADVANCED_FACE ( 'NONE', ( #39952 ), #10084, .F. ) ;
#19419=EDGE_CURVE ( 'NONE', #23134, #9900, #26263, .T. ) ;
#19420=EDGE_CURVE ( 'NONE', #26461, #8937, #232, .T. ) ;
#19422=ORIENTED_EDGE ( 'NONE', *, *, #17077, .T. ) ;
#19423=CARTESIAN_POINT ( 'NONE',  ( 0.000000000000000000, -23.10276247328181398, 118.2656051737069021 ) ) ;
#19431=VECTOR ( 'NONE', #10923, 1000.000000000000000 ) ;
#19433=AXIS2_PLACEMENT_3D ( 'NONE', #42273, #25119, #25746 ) ;
#19435=DIRECTION ( 'NONE',  ( -1.000000000000000000, 0.000000000000000000, 0.000000000000000000 ) ) ;
#19436=VERTEX_POINT ( 'NONE', #23015 ) ;
#19437=CIRCLE ( 'NONE', #29859, 116.0000000000000000 ) ;
#19438=CARTESIAN_POINT ( 'NONE',  ( 8.999999999999998224, 111.2559044912524939, 32.83479428644713494 ) ) ;
#19440=CARTESIAN_POINT ( 'NONE',  ( 17.99999999999999645, 97.89532456239497549, 54.81585448086229917 ) ) ;
#19446=DIRECTION ( 'NONE',  ( 0.000000000000000000, 0.000000000000000000, 1.000000000000000000 ) ) ;
#19450=DIRECTION ( 'NONE',  ( 0.000000000000000000, 2.305124076552231752E-14, -1.000000000000000000 ) ) ;
#19452=CARTESIAN_POINT ( 'NONE',  ( 17.99999999999999645, -110.3490479609630910, -20.28201389785511211 ) ) ;
#19467=EDGE_CURVE ( 'NONE', #15523, #36745, #19730, .T. ) ;
#19468=ORIENTED_EDGE ( 'NONE', *, *, #2722, .T. ) ;
#19471=CARTESIAN_POINT ( 'NONE',  ( 0.000000000000000000, 120.2856157092987957, -7.201503623195590009 ) ) ;
#19473=CYLINDRICAL_SURFACE ( 'NONE', #34957, 116.0000000000000000 ) ;
#19474=CARTESIAN_POINT ( 'NONE',  ( 17.99999999999999645, -103.5682682299985515, -43.14958040911633219 ) ) ;
#19479=CARTESIAN_POINT ( 'NONE',  ( 17.99999999999999645, 0.000000000000000000, 0.000000000000000000 ) ) ;
#19487=CIRCLE ( 'NONE', #25086, 120.5010000000000616 ) ;
#19492=FACE_OUTER_BOUND ( 'NONE', #26792, .T. ) ;
#19493=FACE_OUTER_BOUND ( 'NONE', #40884, .T. ) ;
#19495=DIRECTION ( 'NONE',  ( 0.000000000000000000, 0.000000000000000000, 1.000000000000000000 ) ) ;
#19501=CARTESIAN_POINT ( 'NONE',  ( 0.000000000000000000, -116.4607004671426438, -30.94182036827324112 ) ) ;
#19502=ORIENTED_EDGE ( 'NONE', *, *, #8593, .T. ) ;
#19503=DIRECTION ( 'NONE',  ( 0.000000000000000000, 0.000000000000000000, -1.000000000000000000 ) ) ;
#19507=ORIENTED_EDGE ( 'NONE', *, *, #9038, .F. ) ;
#19508=ORIENTED_EDGE ( 'NONE', *, *, #25211, .T. ) ;
#19510=CARTESIAN_POINT ( 'NONE',  ( 0.000000000000000000, 0.000000000000000000, 0.000000000000000000 ) ) ;
#19512=EDGE_CURVE ( 'NONE', #6774, #36535, #19487, .T. ) ;
#19513=CARTESIAN_POINT ( 'NONE',  ( 17.99999999999999645, -88.00363688980601751, 82.31555682352626491 ) ) ;
#19516=DIRECTION ( 'NONE',  ( 0.000000000000000000, -0.5528000653611833126, -0.8333139190825217257 ) ) ;
#19519=ORIENTED_EDGE ( 'NONE', *, *, #1788, .T. ) ;
#19521=LINE ( 'NONE', #22372, #22190 ) ;
#19522=FACE_OUTER_BOUND ( 'NONE', #40283, .T. ) ;
#19523=CARTESIAN_POINT ( 'NONE',  ( 17.99999999999999645, -99.97660604680010010, 67.26937820704857529 ) ) ;
#19524=ORIENTED_EDGE ( 'NONE', *, *, #14377, .F. ) ;
#19525=CYLINDRICAL_SURFACE ( 'NONE', #3334, 59.00000000000000000 ) ;
#19529=ORIENTED_EDGE ( 'NONE', *, *, #5102, .F. ) ;
#19530=FACE_OUTER_BOUND ( 'NONE', #38056, .T. ) ;
#19535=LINE ( 'NONE', #5970, #13331 ) ;
#19542=AXIS2_PLACEMENT_3D ( 'NONE', #21239, #33176, #425 ) ;
#19543=FACE_OUTER_BOUND ( 'NONE', #16263, .T. ) ;
#19549=ADVANCED_FACE ( 'NONE', ( #21481 ), #34941, .F. ) ;
#19551=CARTESIAN_POINT ( 'NONE',  ( 0.000000000000000000, -108.8880088604279166, 39.99251838045924501 ) ) ;
#19554=DIRECTION ( 'NONE',  ( 0.000000000000000000, 0.000000000000000000, 1.000000000000000000 ) ) ;
#19557=AXIS2_PLACEMENT_3D ( 'NONE', #41678, #5466, #1745 ) ;
#19558=ORIENTED_EDGE ( 'NONE', *, *, #32163, .F. ) ;
#19560=LINE ( 'NONE', #6218, #13723 ) ;
#19563=CARTESIAN_POINT ( 'NONE',  ( 17.99999999999999645, 0.000000000000000000, 0.000000000000000000 ) ) ;
#19564=EDGE_CURVE ( 'NONE', #4914, #41377, #34734, .T. ) ;
#19566=ORIENTED_EDGE ( 'NONE', *, *, #38261, .T. ) ;
#19569=CIRCLE ( 'NONE', #28600, 120.5010000000000332 ) ;
#19570=DIRECTION ( 'NONE',  ( 1.000000000000000000, 0.000000000000000000, 0.000000000000000000 ) ) ;
#19571=VECTOR ( 'NONE', #40019, 1000.000000000000000 ) ;
#19572=AXIS2_PLACEMENT_3D ( 'NONE', #5862, #32701, #28393 ) ;
#19574=CARTESIAN_POINT ( 'NONE',  ( 0.000000000000000000, 16.77566611177940104, -119.3275660838940553 ) ) ;
#19579=CYLINDRICAL_SURFACE ( 'NONE', #24353, 120.5010000000000190 ) ;
#19584=DIRECTION ( 'NONE',  ( 1.000000000000000000, 0.000000000000000000, 0.000000000000000000 ) ) ;
#19586=ORIENTED_EDGE ( 'NONE', *, *, #15106, .F. ) ;
#19587=VERTEX_POINT ( 'NONE', #40600 ) ;
#19588=DIRECTION ( 'NONE',  ( 0.000000000000000000, 0.000000000000000000, 1.000000000000000000 ) ) ;
#19589=DIRECTION ( 'NONE',  ( 1.000000000000000000, 0.000000000000000000, 0.000000000000000000 ) ) ;
#19597=ORIENTED_EDGE ( 'NONE', *, *, #36270, .F. ) ;
#19598=CIRCLE ( 'NONE', #31422, 59.00000000000000711 ) ;
#19599=ADVANCED_FACE ( 'NONE', ( #4172 ), #24312, .F. ) ;
#19600=LINE ( 'NONE', #22893, #18371 ) ;
#19602=CIRCLE ( 'NONE', #7007, 116.0000000000000000 ) ;
#19611=AXIS2_PLACEMENT_3D ( 'NONE', #36392, #26815, #10223 ) ;
#19613=CARTESIAN_POINT ( 'NONE',  ( 0.000000000000000000, 0.000000000000000000, 0.000000000000000000 ) ) ;
#19617=DIRECTION ( 'NONE',  ( -1.000000000000000000, 0.000000000000000000, -0.000000000000000000 ) ) ;
#19621=CYLINDRICAL_SURFACE ( 'NONE', #1263, 59.00000000000000000 ) ;
#19629=ADVANCED_FACE ( 'NONE', ( #1557 ), #1120, .F. ) ;
#19632=CIRCLE ( 'NONE', #10536, 120.5010000000000474 ) ;
#19635=DIRECTION ( 'NONE',  ( 0.000000000000000000, 0.000000000000000000, 1.000000000000000000 ) ) ;
#19642=DIRECTION ( 'NONE',  ( 0.000000000000000000, 0.000000000000000000, 1.000000000000000000 ) ) ;
#19646=DIRECTION ( 'NONE',  ( 1.000000000000000000, 0.000000000000000000, 0.000000000000000000 ) ) ;
#19647=DIRECTION ( 'NONE',  ( 0.000000000000000000, 0.000000000000000000, 1.000000000000000000 ) ) ;
#19651=EDGE_LOOP ( 'NONE', ( #19005, #18420, #17384, #690 ) ) ;
#19652=DIRECTION ( 'NONE',  ( -1.000000000000000000, -0.000000000000000000, 0.000000000000000000 ) ) ;
#19655=ORIENTED_EDGE ( 'NONE', *, *, #1519, .T. ) ;
#19657=EDGE_CURVE ( 'NONE', #31940, #20361, #33374, .T. ) ;
#19658=EDGE_CURVE ( 'NONE', #2020, #29479, #29221, .T. ) ;
#19659=CARTESIAN_POINT ( 'NONE',  ( 0.000000000000000000, -105.7179949885870514, 37.57629584241652054 ) ) ;
#19661=DIRECTION ( 'NONE',  ( 1.000000000000000000, 0.000000000000000000, 0.000000000000000000 ) ) ;
#19667=CIRCLE ( 'NONE', #7800, 59.00000000000000711 ) ;
#19669=AXIS2_PLACEMENT_3D ( 'NONE', #18666, #31698, #11651 ) ;
#19670=CARTESIAN_POINT ( 'NONE',  ( 0.000000000000000000, 112.1427988504408404, -3.502162136922268409 ) ) ;
#19673=DIRECTION ( 'NONE',  ( 0.000000000000000000, 0.000000000000000000, 1.000000000000000000 ) ) ;
#19674=EDGE_CURVE ( 'NONE', #16359, #39974, #34782, .T. ) ;
#19677=FACE_OUTER_BOUND ( 'NONE', #25695, .T. ) ;
#19679=ORIENTED_EDGE ( 'NONE', *, *, #18512, .F. ) ;
#19681=CARTESIAN_POINT ( 'NONE',  ( 17.99999999999999645, 104.6166166098452379, -50.11350645393572023 ) ) ;
#19682=VERTEX_POINT ( 'NONE', #15343 ) ;
#19683=CARTESIAN_POINT ( 'NONE',  ( 17.99999999999999645, -31.17727234463623631, -111.7317219465823115 ) ) ;
#19684=ORIENTED_EDGE ( 'NONE', *, *, #29609, .T. ) ;
#19687=ORIENTED_EDGE ( 'NONE', *, *, #11867, .T. ) ;
#19688=DIRECTION ( 'NONE',  ( -1.000000000000000000, 0.000000000000000000, -0.000000000000000000 ) ) ;
#19694=CARTESIAN_POINT ( 'NONE',  ( 0.000000000000000000, 0.000000000000000000, 0.000000000000000000 ) ) ;
#19695=CARTESIAN_POINT ( 'NONE',  ( 17.99999999999999645, -73.78980555658542073, -95.26571049922065981 ) ) ;
#19701=EDGE_CURVE ( 'NONE', #39322, #31605, #31305, .T. ) ;
#19704=EDGE_CURVE ( 'NONE', #22705, #14740, #42424, .T. ) ;
#19705=EDGE_CURVE ( 'NONE', #30314, #6504, #22741, .T. ) ;
#19706=DIRECTION ( 'NONE',  ( 0.000000000000000000, 0.000000000000000000, 1.000000000000000000 ) ) ;
#19707=ORIENTED_EDGE ( 'NONE', *, *, #22592, .T. ) ;
#19710=ORIENTED_EDGE ( 'NONE', *, *, #35905, .T. ) ;
#19711=CARTESIAN_POINT ( 'NONE',  ( 17.99999999999999645, 107.2885202478266251, 54.86040852957351888 ) ) ;
#19723=AXIS2_PLACEMENT_3D ( 'NONE', #28552, #38118, #18758 ) ;
#19724=DIRECTION ( 'NONE',  ( -1.000000000000000000, -0.000000000000000000, -0.000000000000000000 ) ) ;
#19727=EDGE_LOOP ( 'NONE', ( #16053, #30867, #9948, #8224 ) ) ;
#19730=LINE ( 'NONE', #3076, #38260 ) ;
#19731=CIRCLE ( 'NONE', #12064, 120.5010000000000190 ) ;
#19732=CARTESIAN_POINT ( 'NONE',  ( 9.000000000000001776, 109.3506818544115617, -38.70953859160898247 ) ) ;
#19735=CARTESIAN_POINT ( 'NONE',  ( 17.99999999999999645, 0.000000000000000000, 0.000000000000000000 ) ) ;
#19737=VERTEX_POINT ( 'NONE', #22111 ) ;
#19742=CARTESIAN_POINT ( 'NONE',  ( 17.99999999999999645, 78.75547124681369837, 91.20343606297029737 ) ) ;
#19748=CARTESIAN_POINT ( 'NONE',  ( 17.99999999999999645, -41.33768078145432412, -104.3046912715545318 ) ) ;
#19754=EDGE_CURVE ( 'NONE', #8245, #34731, #32715, .T. ) ;
#19755=ADVANCED_FACE ( 'NONE', ( #18636 ), #32523, .F. ) ;
#19756=DIRECTION ( 'NONE',  ( -1.000000000000000000, 0.000000000000000000, -0.000000000000000000 ) ) ;
#19762=EDGE_CURVE ( 'NONE', #6492, #31141, #13937, .T. ) ;
#19764=CARTESIAN_POINT ( 'NONE',  ( 17.99999999999999645, 1.592040838891559450E-14, -130.0000000000000000 ) ) ;
#19765=DIRECTION ( 'NONE',  ( -1.000000000000000000, 0.000000000000000000, 0.000000000000000000 ) ) ;
#19767=CARTESIAN_POINT ( 'NONE',  ( 0.000000000000000000, 0.000000000000000000, 0.000000000000000000 ) ) ;
#19769=EDGE_LOOP ( 'NONE', ( #25904, #34549, #26224, #34894 ) ) ;
#19773=ORIENTED_EDGE ( 'NONE', *, *, #41944, .F. ) ;
#19778=CYLINDRICAL_SURFACE ( 'NONE', #25414, 59.00000000000000000 ) ;
#19781=ORIENTED_EDGE ( 'NONE', *, *, #40787, .T. ) ;
#19782=CARTESIAN_POINT ( 'NONE',  ( 17.99999999999999645, 112.1702510623870097, 2.471285140324554153 ) ) ;
#19784=CARTESIAN_POINT ( 'NONE',  ( -10.00000000000000000, 0.000000000000000000, 0.000000000000000000 ) ) ;
#19785=CARTESIAN_POINT ( 'NONE',  ( 17.99999999999999645, 0.000000000000000000, 0.000000000000000000 ) ) ;
#19790=DIRECTION ( 'NONE',  ( 1.000000000000000000, 0.000000000000000000, 0.000000000000000000 ) ) ;
#19797=DIRECTION ( 'NONE',  ( 1.000000000000000000, -0.000000000000000000, -0.000000000000000000 ) ) ;
#19800=DIRECTION ( 'NONE',  ( 0.000000000000000000, -0.5963673585384914322, -0.8027116379309710004 ) ) ;
#19809=ORIENTED_EDGE ( 'NONE', *, *, #39111, .F. ) ;
#19810=DIRECTION ( 'NONE',  ( 0.000000000000000000, 0.2631025642275218179, -0.9647678688145158166 ) ) ;
#19814=DIRECTION ( 'NONE',  ( 0.000000000000000000, -3.528251137579946599E-15, -1.000000000000000000 ) ) ;
#19819=EDGE_CURVE ( 'NONE', #14877, #6394, #33166, .T. ) ;
#19821=EDGE_CURVE ( 'NONE', #9926, #10843, #11855, .T. ) ;
#19822=LINE ( 'NONE', #8908, #12172 ) ;
#19826=ADVANCED_FACE ( 'NONE', ( #36418 ), #40122, .F. ) ;
#19835=AXIS2_PLACEMENT_3D ( 'NONE', #33477, #7073, #40646 ) ;
#19838=AXIS2_PLACEMENT_3D ( 'NONE', #14620, #15055, #4537 ) ;
#19841=FACE_OUTER_BOUND ( 'NONE', #31850, .T. ) ;
#19842=ORIENTED_EDGE ( 'NONE', *, *, #16759, .T. ) ;
#19845=VECTOR ( 'NONE', #25077, 1000.000000000000000 ) ;
#19851=EDGE_CURVE ( 'NONE', #6394, #8087, #31335, .T. ) ;
#19853=ORIENTED_EDGE ( 'NONE', *, *, #16508, .T. ) ;
#19856=CARTESIAN_POINT ( 'NONE',  ( 17.99999999999999645, 0.000000000000000000, 0.000000000000000000 ) ) ;
#19862=AXIS2_PLACEMENT_3D ( 'NONE', #33938, #18066, #5120 ) ;
#19863=DIRECTION ( 'NONE',  ( 0.000000000000000000, 0.000000000000000000, 1.000000000000000000 ) ) ;
#19864=VECTOR ( 'NONE', #5811, 1000.000000000000000 ) ;
#19865=ORIENTED_EDGE ( 'NONE', *, *, #32657, .F. ) ;
#19872=CARTESIAN_POINT ( 'NONE',  ( 17.99999999999999645, -17.33727698085101565, -110.8498592715975519 ) ) ;
#19873=CIRCLE ( 'NONE', #32387, 120.5010000000000190 ) ;
#19878=AXIS2_PLACEMENT_3D ( 'NONE', #11955, #5592, #22429 ) ;
#19881=ORIENTED_EDGE ( 'NONE', *, *, #4066, .T. ) ;
#19883=EDGE_CURVE ( 'NONE', #22806, #16567, #647, .T. ) ;
#19891=ORIENTED_EDGE ( 'NONE', *, *, #33751, .F. ) ;
#19895=EDGE_CURVE ( 'NONE', #21604, #3997, #21630, .T. ) ;
#19896=CIRCLE ( 'NONE', #4528, 59.00000000000000000 ) ;
#19897=ORIENTED_EDGE ( 'NONE', *, *, #22924, .F. ) ;
#19898=CIRCLE ( 'NONE', #1035, 116.0000000000000000 ) ;
#19899=ADVANCED_FACE ( 'NONE', ( #19677 ), #32944, .F. ) ;
#19902=EDGE_CURVE ( 'NONE', #5158, #8622, #42808, .T. ) ;
#19904=ORIENTED_EDGE ( 'NONE', *, *, #11149, .T. ) ;
#19906=ORIENTED_EDGE ( 'NONE', *, *, #18574, .T. ) ;
#19907=VECTOR ( 'NONE', #26477, 1000.000000000000000 ) ;
#19913=CARTESIAN_POINT ( 'NONE',  ( 0.000000000000000000, -13.00789606333550097, 115.2683592318614672 ) ) ;
#19915=ORIENTED_EDGE ( 'NONE', *, *, #280, .F. ) ;
#19916=FACE_OUTER_BOUND ( 'NONE', #31402, .T. ) ;
#19917=ADVANCED_FACE ( 'NONE', ( #6531 ), #26635, .F. ) ;
#19918=CIRCLE ( 'NONE', #15736, 59.00000000000000711 ) ;
#19920=CIRCLE ( 'NONE', #10839, 59.00000000000000711 ) ;
#19921=CARTESIAN_POINT ( 'NONE',  ( 8.999999999999998224, 106.6051926090976991, -45.73109345704713746 ) ) ;
#19924=CIRCLE ( 'NONE', #3128, 59.00000000000000000 ) ;
#19927=EDGE_LOOP ( 'NONE', ( #38983, #16117, #37323, #670 ) ) ;
#19928=AXIS2_PLACEMENT_3D ( 'NONE', #456, #7663, #24065 ) ;
#19929=EDGE_CURVE ( 'NONE', #18075, #39315, #42355, .T. ) ;
#19933=CARTESIAN_POINT ( 'NONE',  ( 17.99999999999999645, 0.000000000000000000, 0.000000000000000000 ) ) ;
#19936=EDGE_LOOP ( 'NONE', ( #35209, #14577, #23318, #9193 ) ) ;
#19943=DIRECTION ( 'NONE',  ( 0.000000000000000000, -0.8183027759081622499, -0.5747874102144165942 ) ) ;
#19946=FACE_OUTER_BOUND ( 'NONE', #39609, .T. ) ;
#19949=DIRECTION ( 'NONE',  ( 1.000000000000000000, 0.000000000000000000, 0.000000000000000000 ) ) ;
#19950=ORIENTED_EDGE ( 'NONE', *, *, #16250, .T. ) ;
#19952=CARTESIAN_POINT ( 'NONE',  ( 17.99999999999999645, 112.5120133921107737, 43.14554256761054063 ) ) ;
#19953=EDGE_CURVE ( 'NONE', #28718, #32806, #4558, .T. ) ;
#19954=ORIENTED_EDGE ( 'NONE', *, *, #33676, .F. ) ;
#19955=ADVANCED_FACE ( 'NONE', ( #34679 ), #13984, .F. ) ;
#19957=ADVANCED_FACE ( 'NONE', ( #40996 ), #41203, .F. ) ;
#19959=EDGE_CURVE ( 'NONE', #37344, #34259, #32627, .T. ) ;
#19960=CARTESIAN_POINT ( 'NONE',  ( 17.99999999999999645, -108.8684555192048435, 27.12806418649580564 ) ) ;
#19966=AXIS2_PLACEMENT_3D ( 'NONE', #40278, #3825, #4052 ) ;
#19968=AXIS2_PLACEMENT_3D ( 'NONE', #18246, #41300, #1815 ) ;
#19970=ORIENTED_EDGE ( 'NONE', *, *, #40732, .T. ) ;
#19975=VERTEX_POINT ( 'NONE', #37294 ) ;
#19983=ORIENTED_EDGE ( 'NONE', *, *, #26258, .T. ) ;
#19985=ORIENTED_EDGE ( 'NONE', *, *, #5831, .T. ) ;
#19989=EDGE_CURVE ( 'NONE', #31004, #12380, #27948, .T. ) ;
#19990=DIRECTION ( 'NONE',  ( 0.000000000000000000, 0.000000000000000000, 1.000000000000000000 ) ) ;
#19994=CIRCLE ( 'NONE', #26940, 120.5010000000000190 ) ;
#20001=DIRECTION ( 'NONE',  ( 0.000000000000000000, -0.4610925014493325591, 0.8873520750565681015 ) ) ;
#20002=CARTESIAN_POINT ( 'NONE',  ( 0.000000000000000000, 75.72520367775197769, -82.78868281115903471 ) ) ;
#20003=AXIS2_PLACEMENT_3D ( 'NONE', #34832, #21365, #15448 ) ;
#20005=VECTOR ( 'NONE', #27679, 1000.000000000000000 ) ;
#20007=EDGE_LOOP ( 'NONE', ( #40597, #35587, #740, #40144 ) ) ;
#20008=CARTESIAN_POINT ( 'NONE',  ( 0.000000000000000000, 119.0898412705476943, -18.38751498043618682 ) ) ;
#20012=CARTESIAN_POINT ( 'NONE',  ( 0.000000000000000000, -116.0452958106482981, 32.46506308663420270 ) ) ;
#20014=EDGE_CURVE ( 'NONE', #16388, #14749, #43141, .T. ) ;
#20017=ORIENTED_EDGE ( 'NONE', *, *, #24716, .T. ) ;
#20018=CARTESIAN_POINT ( 'NONE',  ( 17.99999999999999645, -84.62908780824929522, 85.78116633471262276 ) ) ;
#20022=CARTESIAN_POINT ( 'NONE',  ( 0.000000000000000000, 0.000000000000000000, 0.000000000000000000 ) ) ;
#20023=ORIENTED_EDGE ( 'NONE', *, *, #38434, .T. ) ;
#20025=DIRECTION ( 'NONE',  ( 0.000000000000000000, 4.445596433350732597E-14, -1.000000000000000000 ) ) ;
#20034=AXIS2_PLACEMENT_3D ( 'NONE', #23854, #31665, #34495 ) ;
#20036=ADVANCED_FACE ( 'NONE', ( #24682 ), #40769, .F. ) ;
#20037=VECTOR ( 'NONE', #288, 1000.000000000000000 ) ;
#20042=CIRCLE ( 'NONE', #33917, 59.00000000000000711 ) ;
#20043=ORIENTED_EDGE ( 'NONE', *, *, #23886, .T. ) ;
#20044=FACE_OUTER_BOUND ( 'NONE', #32136, .T. ) ;
#20049=EDGE_CURVE ( 'NONE', #9442, #10476, #35426, .T. ) ;
#20055=CARTESIAN_POINT ( 'NONE',  ( 17.99999999999999645, 69.90696807222488474, 98.15042952503540619 ) ) ;
#20056=ORIENTED_EDGE ( 'NONE', *, *, #35187, .T. ) ;
#20059=CARTESIAN_POINT ( 'NONE',  ( 17.99999999999999645, -111.1352304691226607, -15.40237066878709449 ) ) ;
#20060=AXIS2_PLACEMENT_3D ( 'NONE', #15749, #42530, #12255 ) ;
#20061=AXIS2_PLACEMENT_3D ( 'NONE', #38858, #21902, #25380 ) ;
#20064=AXIS2_PLACEMENT_3D ( 'NONE', #40495, #14792, #20927 ) ;
#20065=DIRECTION ( 'NONE',  ( 1.000000000000000000, 0.000000000000000000, 0.000000000000000000 ) ) ;
#20068=DIRECTION ( 'NONE',  ( 0.000000000000000000, 0.000000000000000000, 1.000000000000000000 ) ) ;
#20069=VECTOR ( 'NONE', #32415, 1000.000000000000000 ) ;
#20070=DIRECTION ( 'NONE',  ( -1.000000000000000000, -0.000000000000000000, -0.000000000000000000 ) ) ;
#20075=CARTESIAN_POINT ( 'NONE',  ( -10.00000000000000000, 0.000000000000000000, 0.000000000000000000 ) ) ;
#20087=CYLINDRICAL_SURFACE ( 'NONE', #29559, 116.0000000000000000 ) ;
#20095=ORIENTED_EDGE ( 'NONE', *, *, #29330, .T. ) ;
#20096=AXIS2_PLACEMENT_3D ( 'NONE', #7617, #4328, #7175 ) ;
#20100=AXIS2_PLACEMENT_3D ( 'NONE', #7285, #36963, #34129 ) ;
#20108=DIRECTION ( 'NONE',  ( 0.000000000000000000, -0.3641605752528292994, 0.9313361774523356562 ) ) ;
#20119=AXIS2_PLACEMENT_3D ( 'NONE', #39203, #15919, #42486 ) ;
#20120=ADVANCED_FACE ( 'NONE', ( #15928 ), #15504, .F. ) ;
#20121=AXIS2_PLACEMENT_3D ( 'NONE', #8628, #15002, #38509 ) ;
#20122=ORIENTED_EDGE ( 'NONE', *, *, #12191, .T. ) ;
#20124=AXIS2_PLACEMENT_3D ( 'NONE', #16482, #3753, #3110 ) ;
#20127=CIRCLE ( 'NONE', #37491, 116.0000000000000000 ) ;
#20128=ORIENTED_EDGE ( 'NONE', *, *, #10418, .F. ) ;
#20129=DIRECTION ( 'NONE',  ( -1.000000000000000000, 0.000000000000000000, 0.000000000000000000 ) ) ;
#20132=ORIENTED_EDGE ( 'NONE', *, *, #13054, .T. ) ;
#20134=ORIENTED_EDGE ( 'NONE', *, *, #25814, .F. ) ;
#20136=EDGE_LOOP ( 'NONE', ( #5062, #23506, #35947, #19353 ) ) ;
#20139=VERTEX_POINT ( 'NONE', #32477 ) ;
#20144=ORIENTED_EDGE ( 'NONE', *, *, #19701, .F. ) ;
#20149=CYLINDRICAL_SURFACE ( 'NONE', #11339, 120.5010000000000190 ) ;
#20155=ADVANCED_FACE ( 'NONE', ( #8930 ), #31624, .F. ) ;
#20164=ORIENTED_EDGE ( 'NONE', *, *, #29007, .F. ) ;
#20168=CARTESIAN_POINT ( 'NONE',  ( 17.99999999999999645, -51.27532863109303918, -99.79535634195178773 ) ) ;
#20173=DIRECTION ( 'NONE',  ( -1.000000000000000000, 0.000000000000000000, 0.000000000000000000 ) ) ;
#20175=VERTEX_POINT ( 'NONE', #34891 ) ;
#20178=FACE_OUTER_BOUND ( 'NONE', #17613, .T. ) ;
#20181=DIRECTION ( 'NONE',  ( 0.000000000000000000, 0.9574220383620042352, 0.2886919473396248326 ) ) ;
#20182=ORIENTED_EDGE ( 'NONE', *, *, #6550, .F. ) ;
#20183=AXIS2_PLACEMENT_3D ( 'NONE', #1985, #25995, #9385 ) ;
#20185=EDGE_CURVE ( 'NONE', #37133, #4351, #4042, .T. ) ;
#20187=CARTESIAN_POINT ( 'NONE',  ( 17.99999999999999645, 0.000000000000000000, 0.000000000000000000 ) ) ;
#20188=ORIENTED_EDGE ( 'NONE', *, *, #5891, .F. ) ;
#20191=ORIENTED_EDGE ( 'NONE', *, *, #630, .F. ) ;
#20193=ORIENTED_EDGE ( 'NONE', *, *, #11346, .T. ) ;
#20195=ORIENTED_EDGE ( 'NONE', *, *, #8397, .F. ) ;
#20200=VERTEX_POINT ( 'NONE', #5853 ) ;
#20202=ORIENTED_EDGE ( 'NONE', *, *, #11413, .F. ) ;
#20212=EDGE_CURVE ( 'NONE', #9730, #34509, #27099, .T. ) ;
#20214=DIRECTION ( 'NONE',  ( 0.000000000000000000, 0.9213119778704114138, 0.3888241754733244848 ) ) ;
#20216=DIRECTION ( 'NONE',  ( -1.000000000000000000, -0.000000000000000000, -0.000000000000000000 ) ) ;
#20217=LINE ( 'NONE', #33270, #29716 ) ;
#20218=DIRECTION ( 'NONE',  ( -1.000000000000000000, -0.000000000000000000, -0.000000000000000000 ) ) ;
#20221=DIRECTION ( 'NONE',  ( -1.000000000000000000, -0.000000000000000000, -0.000000000000000000 ) ) ;
#20222=VERTEX_POINT ( 'NONE', #20282 ) ;
#20223=FACE_OUTER_BOUND ( 'NONE', #2851, .T. ) ;
#20232=AXIS2_PLACEMENT_3D ( 'NONE', #9945, #12812, #6454 ) ;
#20237=AXIS2_PLACEMENT_3D ( 'NONE', #5700, #22124, #42753 ) ;
#20240=ORIENTED_EDGE ( 'NONE', *, *, #1542, .T. ) ;
#20242=CARTESIAN_POINT ( 'NONE',  ( 0.000000000000000000, 0.000000000000000000, 0.000000000000000000 ) ) ;
#20243=DIRECTION ( 'NONE',  ( 0.000000000000000000, 0.000000000000000000, 1.000000000000000000 ) ) ;
#20245=CARTESIAN_POINT ( 'NONE',  ( 17.99999999999999645, -96.25468616236712194, 72.49500943364458294 ) ) ;
#20247=ORIENTED_EDGE ( 'NONE', *, *, #29007, .T. ) ;
#20251=DIRECTION ( 'NONE',  ( 1.000000000000000000, -0.000000000000000000, 0.000000000000000000 ) ) ;
#20254=DIRECTION ( 'NONE',  ( 0.000000000000000000, 0.000000000000000000, 1.000000000000000000 ) ) ;
#20255=ORIENTED_EDGE ( 'NONE', *, *, #5843, .F. ) ;
#20257=ADVANCED_FACE ( 'NONE', ( #30289 ), #26381, .F. ) ;
#20258=EDGE_CURVE ( 'NONE', #18, #16718, #21573, .T. ) ;
#20259=LINE ( 'NONE', #30263, #17798 ) ;
#20260=ORIENTED_EDGE ( 'NONE', *, *, #33949, .F. ) ;
#20262=VECTOR ( 'NONE', #29523, 1000.000000000000000 ) ;
#20264=EDGE_LOOP ( 'NONE', ( #16122, #17507, #20255, #36764 ) ) ;
#20269=AXIS2_PLACEMENT_3D ( 'NONE', #6114, #13336, #42737 ) ;
#20271=CARTESIAN_POINT ( 'NONE',  ( 0.000000000000000000, -23.21237537461669120, -109.7700237000594541 ) ) ;
#20272=VERTEX_POINT ( 'NONE', #12851 ) ;
#20274=CARTESIAN_POINT ( 'NONE',  ( 17.99999999999999645, -119.7318547011700502, -13.59315897125848238 ) ) ;
#20275=DIRECTION ( 'NONE',  ( 0.000000000000000000, 0.000000000000000000, 1.000000000000000000 ) ) ;
#20278=CYLINDRICAL_SURFACE ( 'NONE', #28861, 120.5010000000000190 ) ;
#20282=CARTESIAN_POINT ( 'NONE',  ( 0.000000000000000000, -64.58410930313456788, -101.7319213743688664 ) ) ;
#20283=ORIENTED_EDGE ( 'NONE', *, *, #17623, .T. ) ;
#20285=CARTESIAN_POINT ( 'NONE',  ( 17.99999999999999645, 29.02167576844106023, 108.3790330702170621 ) ) ;
#20286=DIRECTION ( 'NONE',  ( -1.000000000000000000, -0.000000000000000000, 0.000000000000000000 ) ) ;
#20288=VECTOR ( 'NONE', #32663, 1000.000000000000000 ) ;
#20289=CARTESIAN_POINT ( 'NONE',  ( 17.99999999999999645, 120.3696465864706227, 5.624871700596478341 ) ) ;
#20290=ORIENTED_EDGE ( 'NONE', *, *, #27078, .F. ) ;
#20292=CIRCLE ( 'NONE', #2806, 116.0000000000000000 ) ;
#20293=ORIENTED_EDGE ( 'NONE', *, *, #37718, .F. ) ;
#20296=VECTOR ( 'NONE', #41272, 1000.000000000000000 ) ;
#20303=FACE_OUTER_BOUND ( 'NONE', #22918, .T. ) ;
#20304=DIRECTION ( 'NONE',  ( 0.000000000000000000, 0.000000000000000000, 1.000000000000000000 ) ) ;
#20307=CARTESIAN_POINT ( 'NONE',  ( 17.99999999999999645, 0.000000000000000000, 0.000000000000000000 ) ) ;
#20309=DIRECTION ( 'NONE',  ( -1.000000000000000000, 0.000000000000000000, -0.000000000000000000 ) ) ;
#20315=VERTEX_POINT ( 'NONE', #26588 ) ;
#20319=EDGE_CURVE ( 'NONE', #22974, #6539, #16132, .T. ) ;
#20320=AXIS2_PLACEMENT_3D ( 'NONE', #28508, #14761, #28709 ) ;
#20321=CARTESIAN_POINT ( 'NONE',  ( 8.999999999999998224, 115.6826031496112392, 8.575274253897841703 ) ) ;
#20324=DIRECTION ( 'NONE',  ( 0.000000000000000000, 0.000000000000000000, 1.000000000000000000 ) ) ;
#20326=ORIENTED_EDGE ( 'NONE', *, *, #40197, .T. ) ;
#20327=FACE_BOUND ( 'NONE', #23997, .T. ) ;
#20328=DIRECTION ( 'NONE',  ( -1.000000000000000000, -0.000000000000000000, -0.000000000000000000 ) ) ;
#20332=LINE ( 'NONE', #415, #35408 ) ;
#20333=CIRCLE ( 'NONE', #31459, 59.00000000000000711 ) ;
#20334=ORIENTED_EDGE ( 'NONE', *, *, #37251, .F. ) ;
#20335=FACE_OUTER_BOUND ( 'NONE', #9189, .T. ) ;
#20336=DIRECTION ( 'NONE',  ( 0.000000000000000000, 0.000000000000000000, 1.000000000000000000 ) ) ;
#20339=ORIENTED_EDGE ( 'NONE', *, *, #42519, .T. ) ;
#20340=ORIENTED_EDGE ( 'NONE', *, *, #18398, .F. ) ;
#20343=VERTEX_POINT ( 'NONE', #23552 ) ;
#20346=CARTESIAN_POINT ( 'NONE',  ( 0.000000000000000000, -111.1352304691226607, -15.40237066878709449 ) ) ;
#20347=ORIENTED_EDGE ( 'NONE', *, *, #4541, .F. ) ;
#20349=AXIS2_PLACEMENT_3D ( 'NONE', #10337, #913, #3744 ) ;
#20356=FACE_OUTER_BOUND ( 'NONE', #29475, .T. ) ;
#20358=ORIENTED_EDGE ( 'NONE', *, *, #4888, .T. ) ;
#20361=VERTEX_POINT ( 'NONE', #6074 ) ;
#20363=DIRECTION ( 'NONE',  ( 1.000000000000000000, 0.000000000000000000, 0.000000000000000000 ) ) ;
#20364=ORIENTED_EDGE ( 'NONE', *, *, #22670, .F. ) ;
#20372=DIRECTION ( 'NONE',  ( 0.000000000000000000, 0.000000000000000000, 1.000000000000000000 ) ) ;
#20373=DIRECTION ( 'NONE',  ( -1.000000000000000000, -0.000000000000000000, 0.000000000000000000 ) ) ;
#20381=ORIENTED_EDGE ( 'NONE', *, *, #34059, .F. ) ;
#20385=ORIENTED_EDGE ( 'NONE', *, *, #28256, .T. ) ;
#20386=CARTESIAN_POINT ( 'NONE',  ( 17.99999999999999645, -24.22031524826050841, 109.5520369638036584 ) ) ;
#20387=ORIENTED_EDGE ( 'NONE', *, *, #20014, .T. ) ;
#20388=CARTESIAN_POINT ( 'NONE',  ( 0.000000000000000000, 0.000000000000000000, 0.000000000000000000 ) ) ;
#20390=ADVANCED_FACE ( 'NONE', ( #24204 ), #33983, .F. ) ;
#20394=EDGE_LOOP ( 'NONE', ( #41022, #41518, #16367, #20144 ) ) ;
#20396=ORIENTED_EDGE ( 'NONE', *, *, #34512, .F. ) ;
#20397=EDGE_CURVE ( 'NONE', #11355, #23147, #14564, .T. ) ;
#20400=CARTESIAN_POINT ( 'NONE',  ( 0.000000000000000000, -13.00789606333398218, -115.2683592318616235 ) ) ;
#20402=ORIENTED_EDGE ( 'NONE', *, *, #4930, .F. ) ;
#20407=ORIENTED_EDGE ( 'NONE', *, *, #8340, .T. ) ;
#20408=CARTESIAN_POINT ( 'NONE',  ( 17.99999999999999645, 82.63181128086846172, -81.41243003646886223 ) ) ;
#20412=DIRECTION ( 'NONE',  ( 0.000000000000000000, -0.8747630845319559478, -0.4845508703326597000 ) ) ;
#20414=CIRCLE ( 'NONE', #23897, 59.00000000000000711 ) ;
#20416=CARTESIAN_POINT ( 'NONE',  ( 17.99999999999999645, 0.000000000000000000, 0.000000000000000000 ) ) ;
#20417=EDGE_LOOP ( 'NONE', ( #33492, #29920, #31347, #30960 ) ) ;
#20425=CARTESIAN_POINT ( 'NONE',  ( 17.99999999999999645, 0.000000000000000000, 0.000000000000000000 ) ) ;
#20427=EDGE_CURVE ( 'NONE', #19378, #6343, #6209, .T. ) ;
#20429=EDGE_LOOP ( 'NONE', ( #26946, #37347, #30651, #14689 ) ) ;
#20430=DIRECTION ( 'NONE',  ( -1.000000000000000000, -0.000000000000000000, -0.000000000000000000 ) ) ;
#20433=CARTESIAN_POINT ( 'NONE',  ( 0.000000000000000000, 23.85344185397197947, 113.5209818126991621 ) ) ;
#20439=AXIS2_PLACEMENT_3D ( 'NONE', #7816, #5186, #25303 ) ;
#20440=CYLINDRICAL_SURFACE ( 'NONE', #6917, 120.5010000000000190 ) ;
#20441=CYLINDRICAL_SURFACE ( 'NONE', #3385, 59.00000000000000000 ) ;
#20450=EDGE_LOOP ( 'NONE', ( #43118, #28414, #23646, #32321 ) ) ;
#20451=CARTESIAN_POINT ( 'NONE',  ( 17.99999999999999645, 120.2856157092987957, -7.201503623195590009 ) ) ;
#20453=AXIS2_PLACEMENT_3D ( 'NONE', #164, #3658, #17257 ) ;
#20456=PRODUCT_DEFINITION_CONTEXT ( 'detailed design', #7795, 'design' ) ;
#20459=DIRECTION ( 'NONE',  ( 1.000000000000000000, 0.000000000000000000, 0.000000000000000000 ) ) ;
#20460=EDGE_CURVE ( 'NONE', #34731, #37525, #14154, .T. ) ;
#20463=DIRECTION ( 'NONE',  ( -1.000000000000000000, -0.000000000000000000, -0.000000000000000000 ) ) ;
#20464=DIRECTION ( 'NONE',  ( -1.000000000000000000, -0.000000000000000000, 0.000000000000000000 ) ) ;
#20466=FACE_OUTER_BOUND ( 'NONE', #26412, .T. ) ;
#20474=CARTESIAN_POINT ( 'NONE',  ( 17.99999999999999645, 41.62036691425679180, -113.0850832732710529 ) ) ;
#20475=ADVANCED_FACE ( 'NONE', ( #21152 ), #1450, .F. ) ;
#20479=DIRECTION ( 'NONE',  ( 1.000000000000000000, 0.000000000000000000, 0.000000000000000000 ) ) ;
#20483=ORIENTED_EDGE ( 'NONE', *, *, #25551, .T. ) ;
#20484=CIRCLE ( 'NONE', #194, 59.00000000000001421 ) ;
#20487=DIRECTION ( 'NONE',  ( -1.000000000000000000, -0.000000000000000000, -0.000000000000000000 ) ) ;
#20488=ORIENTED_EDGE ( 'NONE', *, *, #5591, .F. ) ;
#20489=CARTESIAN_POINT ( 'NONE',  ( 17.99999999999999645, -105.3681574666266414, 38.54638589714855357 ) ) ;
#20490=ORIENTED_EDGE ( 'NONE', *, *, #13196, .T. ) ;
#20492=VECTOR ( 'NONE', #39121, 1000.000000000000000 ) ;
#20494=CYLINDRICAL_SURFACE ( 'NONE', #616, 116.0000000000000000 ) ;
#20495=EDGE_LOOP ( 'NONE', ( #32434, #35745, #16933, #34188 ) ) ;
#20496=ADVANCED_FACE ( 'NONE', ( #37031 ), #20494, .F. ) ;
#20498=EDGE_CURVE ( 'NONE', #2185, #29068, #39614, .T. ) ;
#20503=ORIENTED_EDGE ( 'NONE', *, *, #13219, .T. ) ;
#20505=ORIENTED_EDGE ( 'NONE', *, *, #8448, .F. ) ;
#20513=VERTEX_POINT ( 'NONE', #18528 ) ;
#20519=ORIENTED_EDGE ( 'NONE', *, *, #12188, .T. ) ;
#20520=DIRECTION ( 'NONE',  ( 0.000000000000000000, 0.000000000000000000, 1.000000000000000000 ) ) ;
#20521=CARTESIAN_POINT ( 'NONE',  ( 0.000000000000000000, 21.55123232222630492, -118.5581519187670096 ) ) ;
#20522=CIRCLE ( 'NONE', #26075, 116.0000000000000000 ) ;
#20526=CIRCLE ( 'NONE', #28174, 120.5010000000000332 ) ;
#20529=AXIS2_PLACEMENT_3D ( 'NONE', #28825, #32085, #22094 ) ;
#20533=ORIENTED_EDGE ( 'NONE', *, *, #26092, .T. ) ;
#20534=CARTESIAN_POINT ( 'NONE',  ( 17.99999999999999645, -107.2703412112692689, -32.88383143828572486 ) ) ;
#20535=CYLINDRICAL_SURFACE ( 'NONE', #20965, 116.0000000000000000 ) ;
#20541=AXIS2_PLACEMENT_3D ( 'NONE', #4594, #11383, #37757 ) ;
#20543=ORIENTED_EDGE ( 'NONE', *, *, #32909, .T. ) ;
#20549=CARTESIAN_POINT ( 'NONE',  ( 0.000000000000000000, 0.000000000000000000, 0.000000000000000000 ) ) ;
#20550=EDGE_LOOP ( 'NONE', ( #856, #37221, #3221, #29725 ) ) ;
#20553=CARTESIAN_POINT ( 'NONE',  ( 17.99999999999999645, -17.33727698085246871, 110.8498592715972961 ) ) ;
#20554=ORIENTED_EDGE ( 'NONE', *, *, #7351, .T. ) ;
#20555=AXIS2_PLACEMENT_3D ( 'NONE', #36046, #32780, #19299 ) ;
#20556=DIRECTION ( 'NONE',  ( -1.000000000000000000, -0.000000000000000000, 0.000000000000000000 ) ) ;
#20559=CIRCLE ( 'NONE', #40679, 116.0000000000000000 ) ;
#20561=CARTESIAN_POINT ( 'NONE',  ( 17.99999999999999645, -86.84764344323014029, 76.89919913989720612 ) ) ;
#20563=DIRECTION ( 'NONE',  ( -1.000000000000000000, 0.000000000000000000, 0.000000000000000000 ) ) ;
#20566=DIRECTION ( 'NONE',  ( -1.000000000000000000, -0.000000000000000000, 0.000000000000000000 ) ) ;
#20568=FACE_OUTER_BOUND ( 'NONE', #39477, .T. ) ;
#20576=ORIENTED_EDGE ( 'NONE', *, *, #6280, .T. ) ;
#20577=DIRECTION ( 'NONE',  ( -1.000000000000000000, -0.000000000000000000, -0.000000000000000000 ) ) ;
#20582=CIRCLE ( 'NONE', #42820, 58.99999999999999289 ) ;
#20584=ORIENTED_EDGE ( 'NONE', *, *, #17077, .F. ) ;
#20585=DIRECTION ( 'NONE',  ( 1.000000000000000000, -0.000000000000000000, -0.000000000000000000 ) ) ;
#20586=VECTOR ( 'NONE', #3699, 1000.000000000000000 ) ;
#20587=CARTESIAN_POINT ( 'NONE',  ( -10.00000000000000000, 0.000000000000000000, 0.000000000000000000 ) ) ;
#20590=CIRCLE ( 'NONE', #16403, 59.00000000000000000 ) ;
#20595=CARTESIAN_POINT ( 'NONE',  ( 8.999999999999998224, 101.1403355683153933, -56.80345518653383152 ) ) ;
#20596=ORIENTED_EDGE ( 'NONE', *, *, #5303, .T. ) ;
#20597=DIRECTION ( 'NONE',  ( -1.000000000000000000, -0.000000000000000000, 0.000000000000000000 ) ) ;
#20599=CARTESIAN_POINT ( 'NONE',  ( 17.99999999999999645, 0.000000000000000000, 0.000000000000000000 ) ) ;
#20600=ORIENTED_EDGE ( 'NONE', *, *, #33326, .T. ) ;
#20601=DIRECTION ( 'NONE',  ( 1.000000000000000000, 0.000000000000000000, 0.000000000000000000 ) ) ;
#20603=CARTESIAN_POINT ( 'NONE',  ( 0.000000000000000000, -87.92975456462855277, -69.68953103478244770 ) ) ;
#20605=ORIENTED_EDGE ( 'NONE', *, *, #4244, .F. ) ;
#20606=FACE_OUTER_BOUND ( 'NONE', #36248, .T. ) ;
#20607=EDGE_LOOP ( 'NONE', ( #25508, #8461, #31537, #32490 ) ) ;
#20610=CARTESIAN_POINT ( 'NONE',  ( 0.000000000000000000, -41.33768078145568836, 104.3046912715539918 ) ) ;
#20614=ORIENTED_EDGE ( 'NONE', *, *, #13876, .T. ) ;
#20615=ADVANCED_FACE ( 'NONE', ( #28750 ), #18959, .F. ) ;
#20616=CIRCLE ( 'NONE', #31743, 58.99999999999998579 ) ;
#20620=AXIS2_PLACEMENT_3D ( 'NONE', #33673, #30425, #40426 ) ;
#20622=DIRECTION ( 'NONE',  ( 0.000000000000000000, 0.000000000000000000, 1.000000000000000000 ) ) ;
#20623=CARTESIAN_POINT ( 'NONE',  ( 17.99999999999999645, 0.000000000000000000, 0.000000000000000000 ) ) ;
#20627=CARTESIAN_POINT ( 'NONE',  ( 17.99999999999999645, 10.40101730206529140, -120.0512800434970018 ) ) ;
#20636=DIRECTION ( 'NONE',  ( 1.000000000000000000, 0.000000000000000000, 0.000000000000000000 ) ) ;
#20637=EDGE_CURVE ( 'NONE', #35175, #3463, #27828, .T. ) ;
#20639=VERTEX_POINT ( 'NONE', #42226 ) ;
#20641=CARTESIAN_POINT ( 'NONE',  ( 17.99999999999999645, 117.6086855750638165, -26.24286718911983485 ) ) ;
#20644=DIRECTION ( 'NONE',  ( -1.000000000000000000, 0.000000000000000000, 0.000000000000000000 ) ) ;
#20645=VECTOR ( 'NONE', #4748, 1000.000000000000000 ) ;
#20646=VECTOR ( 'NONE', #201, 1000.000000000000000 ) ;
#20648=VERTEX_POINT ( 'NONE', #12386 ) ;
#20650=ORIENTED_EDGE ( 'NONE', *, *, #19268, .F. ) ;
#20657=CARTESIAN_POINT ( 'NONE',  ( 17.99999999999999645, 116.4607004671432406, -30.94182036827089632 ) ) ;
#20659=VERTEX_POINT ( 'NONE', #41367 ) ;
#20664=CARTESIAN_POINT ( 'NONE',  ( 17.99999999999999645, 0.000000000000000000, 0.000000000000000000 ) ) ;
#20670=CARTESIAN_POINT ( 'NONE',  ( 0.000000000000000000, -115.0622509503831452, -14.72000021165260897 ) ) ;
#20671=VERTEX_POINT ( 'NONE', #15022 ) ;
#20672=EDGE_LOOP ( 'NONE', ( #5446, #35733, #33638, #19086 ) ) ;
#20675=CIRCLE ( 'NONE', #31110, 59.00000000000000711 ) ;
#20679=AXIS2_PLACEMENT_3D ( 'NONE', #31383, #14607, #23995 ) ;
#20681=FACE_OUTER_BOUND ( 'NONE', #459, .T. ) ;
#20682=VECTOR ( 'NONE', #12573, 1000.000000000000000 ) ;
#20684=CARTESIAN_POINT ( 'NONE',  ( 9.000000000000001776, -6.854627147199504833, 115.7972974066013307 ) ) ;
#20685=CARTESIAN_POINT ( 'NONE',  ( 17.99999999999999645, -91.51415974874549875, -64.91094698989387268 ) ) ;
#20686=CIRCLE ( 'NONE', #27645, 120.5010000000000332 ) ;
#20689=CIRCLE ( 'NONE', #1831, 120.5010000000000190 ) ;
#20690=VERTEX_POINT ( 'NONE', #25080 ) ;
#20698=EDGE_CURVE ( 'NONE', #5055, #16388, #4076, .T. ) ;
#20699=CARTESIAN_POINT ( 'NONE',  ( 17.99999999999999645, -71.21168426767167148, 86.70160608319299911 ) ) ;
#20703=DIRECTION ( 'NONE',  ( 0.000000000000000000, 0.000000000000000000, 1.000000000000000000 ) ) ;
#20706=ORIENTED_EDGE ( 'NONE', *, *, #25631, .T. ) ;
#20709=AXIS2_PLACEMENT_3D ( 'NONE', #27438, #36810, #15015 ) ;
#20711=ORIENTED_EDGE ( 'NONE', *, *, #5906, .T. ) ;
#20712=FACE_OUTER_BOUND ( 'NONE', #4919, .T. ) ;
#20713=ORIENTED_EDGE ( 'NONE', *, *, #904, .F. ) ;
#20714=CARTESIAN_POINT ( 'NONE',  ( 17.99999999999999645, 0.000000000000000000, 0.000000000000000000 ) ) ;
#20717=DIRECTION ( 'NONE',  ( 0.000000000000000000, 0.000000000000000000, 1.000000000000000000 ) ) ;
#20719=ADVANCED_FACE ( 'NONE', ( #40014 ), #6441, .F. ) ;
#20720=VERTEX_POINT ( 'NONE', #13237 ) ;
#20722=DIRECTION ( 'NONE',  ( -1.000000000000000000, 0.000000000000000000, 0.000000000000000000 ) ) ;
#20723=CIRCLE ( 'NONE', #3237, 120.5010000000000332 ) ;
#20726=ADVANCED_FACE ( 'NONE', ( #16520 ), #29594, .F. ) ;
#20732=DIRECTION ( 'NONE',  ( -1.000000000000000000, 0.000000000000000000, -0.000000000000000000 ) ) ;
#20733=AXIS2_PLACEMENT_3D ( 'NONE', #21117, #30685, #759 ) ;
#20738=DIRECTION ( 'NONE',  ( 1.000000000000000000, 0.000000000000000000, 0.000000000000000000 ) ) ;
#20743=AXIS2_PLACEMENT_3D ( 'NONE', #39158, #32637, #2712 ) ;
#20744=ORIENTED_EDGE ( 'NONE', *, *, #10562, .T. ) ;
#20747=AXIS2_PLACEMENT_3D ( 'NONE', #37339, #41031, #4378 ) ;
#20750=CYLINDRICAL_SURFACE ( 'NONE', #6521, 120.5010000000000190 ) ;
#20752=CIRCLE ( 'NONE', #31840, 59.00000000000000000 ) ;
#20755=EDGE_CURVE ( 'NONE', #31163, #8980, #9673, .T. ) ;
#20756=ORIENTED_EDGE ( 'NONE', *, *, #10874, .T. ) ;
#20760=ADVANCED_FACE ( 'NONE', ( #6657 ), #19579, .F. ) ;
#20761=CIRCLE ( 'NONE', #26306, 116.0000000000000000 ) ;
#20765=CARTESIAN_POINT ( 'NONE',  ( 8.999999999999998224, -78.18175027177376535, -85.69488855493077040 ) ) ;
#20767=DIRECTION ( 'NONE',  ( 1.000000000000000000, 0.000000000000000000, 0.000000000000000000 ) ) ;
#20769=DIRECTION ( 'NONE',  ( 0.000000000000000000, 0.9574220383620042352, 0.2886919473396248881 ) ) ;
#20770=LINE ( 'NONE', #34029, #23749 ) ;
#20774=CARTESIAN_POINT ( 'NONE',  ( 0.000000000000000000, -114.1529630473446986, -38.59523323561551678 ) ) ;
#20775=ORIENTED_EDGE ( 'NONE', *, *, #29769, .T. ) ;
#20780=DIRECTION ( 'NONE',  ( 1.000000000000000000, -0.000000000000000000, 0.000000000000000000 ) ) ;
#20782=CIRCLE ( 'NONE', #1915, 59.00000000000000711 ) ;
#20784=EDGE_CURVE ( 'NONE', #27172, #18006, #36761, .T. ) ;
#20787=AXIS2_PLACEMENT_3D ( 'NONE', #25475, #38950, #9281 ) ;
#20789=CARTESIAN_POINT ( 'NONE',  ( 17.99999999999999645, 54.09091620264722877, 102.6166301549519488 ) ) ;
#20790=ORIENTED_EDGE ( 'NONE', *, *, #27901, .F. ) ;
#20791=EDGE_CURVE ( 'NONE', #7422, #42093, #16739, .T. ) ;
#20792=CARTESIAN_POINT ( 'NONE',  ( 17.99999999999999645, -41.62036691425604573, 113.0850832732712945 ) ) ;
#20794=ORIENTED_EDGE ( 'NONE', *, *, #5673, .F. ) ;
#20795=FACE_OUTER_BOUND ( 'NONE', #38554, .T. ) ;
#20798=DIRECTION ( 'NONE',  ( 0.000000000000000000, 0.000000000000000000, 1.000000000000000000 ) ) ;
#20799=FACE_OUTER_BOUND ( 'NONE', #14940, .T. ) ;
#20800=EDGE_LOOP ( 'NONE', ( #8755, #20744, #33297, #38854 ) ) ;
#20802=CARTESIAN_POINT ( 'NONE',  ( 0.000000000000000000, 79.94368240339547071, -90.16373242487824768 ) ) ;
#20804=ORIENTED_EDGE ( 'NONE', *, *, #35729, .T. ) ;
#20805=CARTESIAN_POINT ( 'NONE',  ( 17.99999999999999645, 0.000000000000000000, 0.000000000000000000 ) ) ;
#20807=DIRECTION ( 'NONE',  ( 0.000000000000000000, 0.000000000000000000, 1.000000000000000000 ) ) ;
#20809=ORIENTED_EDGE ( 'NONE', *, *, #12562, .F. ) ;
#20812=DIRECTION ( 'NONE',  ( 0.000000000000000000, -0.7525707698561306946, -0.6585113790650474197 ) ) ;
#20816=CIRCLE ( 'NONE', #20121, 116.0000000000000000 ) ;
#20819=AXIS2_PLACEMENT_3D ( 'NONE', #39590, #20221, #36521 ) ;
#20820=CARTESIAN_POINT ( 'NONE',  ( 17.99999999999999645, 0.000000000000000000, 0.000000000000000000 ) ) ;
#20821=DIRECTION ( 'NONE',  ( 1.000000000000000000, 0.000000000000000000, 0.000000000000000000 ) ) ;
#20824=CARTESIAN_POINT ( 'NONE',  ( -10.00000000000000000, 0.000000000000000000, 0.000000000000000000 ) ) ;
#20829=DIRECTION ( 'NONE',  ( 1.000000000000000000, 0.000000000000000000, 0.000000000000000000 ) ) ;
#20831=ADVANCED_FACE ( 'NONE', ( #4237 ), #20440, .F. ) ;
#20834=DIRECTION ( 'NONE',  ( 1.000000000000000000, 0.000000000000000000, 0.000000000000000000 ) ) ;
#20838=DIRECTION ( 'NONE',  ( 0.000000000000000000, -0.9213119778704165208, 0.3888241754733123834 ) ) ;
#20841=ORIENTED_EDGE ( 'NONE', *, *, #9429, .F. ) ;
#20843=EDGE_LOOP ( 'NONE', ( #26612, #36416, #7604, #43038 ) ) ;
#20847=AXIS2_PLACEMENT_3D ( 'NONE', #28383, #25127, #2342 ) ;
#20848=EDGE_CURVE ( 'NONE', #18762, #19436, #10589, .T. ) ;
#20849=CIRCLE ( 'NONE', #20119, 59.00000000000000000 ) ;
#20850=ORIENTED_EDGE ( 'NONE', *, *, #31178, .T. ) ;
#20858=CARTESIAN_POINT ( 'NONE',  ( -10.00000000000000000, 0.000000000000000000, 0.000000000000000000 ) ) ;
#20859=CARTESIAN_POINT ( 'NONE',  ( 0.000000000000000000, 6.854627147198713466, 115.7972974066013734 ) ) ;
#20862=DIRECTION ( 'NONE',  ( 0.000000000000000000, 0.000000000000000000, -1.000000000000000000 ) ) ;
#20865=ORIENTED_EDGE ( 'NONE', *, *, #34848, .F. ) ;
#20866=EDGE_CURVE ( 'NONE', #39191, #14740, #23922, .T. ) ;
#20869=ORIENTED_EDGE ( 'NONE', *, *, #40437, .F. ) ;
#20874=CARTESIAN_POINT ( 'NONE',  ( 17.99999999999999645, -46.12538073176274622, -111.3235835452215952 ) ) ;
#20875=AXIS2_PLACEMENT_3D ( 'NONE', #12739, #42159, #35202 ) ;
#20879=ORIENTED_EDGE ( 'NONE', *, *, #9698, .T. ) ;
#20881=DIRECTION ( 'NONE',  ( 0.000000000000000000, 0.000000000000000000, -1.000000000000000000 ) ) ;
#20884=EDGE_CURVE ( 'NONE', #17388, #30173, #42450, .T. ) ;
#20886=ORIENTED_EDGE ( 'NONE', *, *, #21505, .T. ) ;
#20887=ORIENTED_EDGE ( 'NONE', *, *, #27096, .F. ) ;
#20893=ORIENTED_EDGE ( 'NONE', *, *, #24865, .F. ) ;
#20895=DIRECTION ( 'NONE',  ( -1.000000000000000000, -0.000000000000000000, -0.000000000000000000 ) ) ;
#20897=ORIENTED_EDGE ( 'NONE', *, *, #15428, .T. ) ;
#20898=ORIENTED_EDGE ( 'NONE', *, *, #15849, .F. ) ;
#20901=AXIS2_PLACEMENT_3D ( 'NONE', #26669, #2855, #12941 ) ;
#20902=CARTESIAN_POINT ( 'NONE',  ( 0.000000000000000000, 57.40245293794667703, 96.40140491896650587 ) ) ;
#20904=DIRECTION ( 'NONE',  ( -1.000000000000000000, -0.000000000000000000, 0.000000000000000000 ) ) ;
#20905=VERTEX_POINT ( 'NONE', #11043 ) ;
#20907=CARTESIAN_POINT ( 'NONE',  ( 17.99999999999999645, 31.17727234463848163, -111.7317219465816862 ) ) ;
#20908=ORIENTED_EDGE ( 'NONE', *, *, #7153, .T. ) ;
#20911=DIRECTION ( 'NONE',  ( 0.000000000000000000, 0.000000000000000000, 1.000000000000000000 ) ) ;
#20914=VERTEX_POINT ( 'NONE', #27185 ) ;
#20919=ORIENTED_EDGE ( 'NONE', *, *, #34960, .T. ) ;
#20920=DIRECTION ( 'NONE',  ( 0.000000000000000000, -0.8747630845319560589, -0.4845508703326597000 ) ) ;
#20925=EDGE_CURVE ( 'NONE', #34186, #36059, #30668, .T. ) ;
#20927=DIRECTION ( 'NONE',  ( 0.000000000000000000, 0.000000000000000000, -1.000000000000000000 ) ) ;
#20928=ORIENTED_EDGE ( 'NONE', *, *, #23914, .F. ) ;
#20930=PRESENTATION_STYLE_ASSIGNMENT (( #7571 ) ) ;
#20934=VERTEX_POINT ( 'NONE', #30233 ) ;
#20943=ORIENTED_EDGE ( 'NONE', *, *, #41850, .F. ) ;
#20950=FACE_OUTER_BOUND ( 'NONE', #20607, .T. ) ;
#20952=DIRECTION ( 'NONE',  ( 0.000000000000000000, -0.2631025642275284238, 0.9647678688145140402 ) ) ;
#20954=ORIENTED_EDGE ( 'NONE', *, *, #23518, .F. ) ;
#20956=CYLINDRICAL_SURFACE ( 'NONE', #18609, 116.0000000000000000 ) ;
#20957=ORIENTED_EDGE ( 'NONE', *, *, #12708, .T. ) ;
#20960=AXIS2_PLACEMENT_3D ( 'NONE', #28089, #18091, #38513 ) ;
#20965=AXIS2_PLACEMENT_3D ( 'NONE', #27279, #20328, #40339 ) ;
#20966=DIRECTION ( 'NONE',  ( 1.000000000000000000, -0.000000000000000000, -0.000000000000000000 ) ) ;
#20968=EDGE_CURVE ( 'NONE', #30836, #20999, #33399, .T. ) ;
#20975=CARTESIAN_POINT ( 'NONE',  ( 0.000000000000000000, 0.000000000000000000, 0.000000000000000000 ) ) ;
#20976=AXIS2_PLACEMENT_3D ( 'NONE', #42518, #38399, #18387 ) ;
#20977=CARTESIAN_POINT ( 'NONE',  ( 17.99999999999999645, 0.000000000000000000, 0.000000000000000000 ) ) ;
#20978=EDGE_CURVE ( 'NONE', #34567, #8378, #39640, .T. ) ;
#20979=CARTESIAN_POINT ( 'NONE',  ( 9.000000000000001776, -113.8630351447204134, -22.16324045874526405 ) ) ;
#20980=CARTESIAN_POINT ( 'NONE',  ( -10.00000000000000000, 0.000000000000000000, 0.000000000000000000 ) ) ;
#20981=VERTEX_POINT ( 'NONE', #29736 ) ;
#20982=DIRECTION ( 'NONE',  ( 0.000000000000000000, 0.6783118362696123338, 0.7347741508630706297 ) ) ;
#20983=CIRCLE ( 'NONE', #30727, 120.5010000000000474 ) ;
#20987=DIRECTION ( 'NONE',  ( -1.000000000000000000, -0.000000000000000000, -0.000000000000000000 ) ) ;
#20989=DIRECTION ( 'NONE',  ( -1.000000000000000000, -0.000000000000000000, 0.000000000000000000 ) ) ;
#20996=VECTOR ( 'NONE', #5159, 1000.000000000000000 ) ;
#20998=CYLINDRICAL_SURFACE ( 'NONE', #13820, 120.5010000000000190 ) ;
#20999=VERTEX_POINT ( 'NONE', #7012 ) ;
#21000=CARTESIAN_POINT ( 'NONE',  ( 17.99999999999999645, 0.000000000000000000, 0.000000000000000000 ) ) ;
#21001=ORIENTED_EDGE ( 'NONE', *, *, #15165, .T. ) ;
#21002=DIRECTION ( 'NONE',  ( -1.000000000000000000, -0.000000000000000000, 0.000000000000000000 ) ) ;
#21003=EDGE_CURVE ( 'NONE', #1814, #13510, #40359, .T. ) ;
#21005=ORIENTED_EDGE ( 'NONE', *, *, #717, .F. ) ;
#21014=DIRECTION ( 'NONE',  ( 0.000000000000000000, 0.000000000000000000, 1.000000000000000000 ) ) ;
#21016=DIRECTION ( 'NONE',  ( -1.000000000000000000, -0.000000000000000000, -0.000000000000000000 ) ) ;
#21022=ORIENTED_EDGE ( 'NONE', *, *, #17446, .T. ) ;
#21023=DIRECTION ( 'NONE',  ( -1.000000000000000000, 0.000000000000000000, 0.000000000000000000 ) ) ;
#21025=AXIS2_PLACEMENT_3D ( 'NONE', #698, #16911, #26918 ) ;
#21027=ORIENTED_EDGE ( 'NONE', *, *, #21810, .T. ) ;
#21028=CIRCLE ( 'NONE', #12618, 58.99999999999999289 ) ;
#21032=EDGE_CURVE ( 'NONE', #2829, #4469, #5533, .T. ) ;
#21036=VECTOR ( 'NONE', #19078, 1000.000000000000000 ) ;
#21041=VERTEX_POINT ( 'NONE', #9655 ) ;
#21043=DIRECTION ( 'NONE',  ( -1.000000000000000000, -0.000000000000000000, -0.000000000000000000 ) ) ;
#21045=CARTESIAN_POINT ( 'NONE',  ( 17.99999999999999645, -66.49630760163661591, 90.36876423295966276 ) ) ;
#21048=CARTESIAN_POINT ( 'NONE',  ( 17.99999999999999645, 45.89132998248186368, -102.3829004574625401 ) ) ;
#21050=AXIS2_PLACEMENT_3D ( 'NONE', #10556, #23466, #26711 ) ;
#21054=AXIS2_PLACEMENT_3D ( 'NONE', #42347, #22754, #22127 ) ;
#21058=CYLINDRICAL_SURFACE ( 'NONE', #41165, 59.00000000000000000 ) ;
#21062=AXIS2_PLACEMENT_3D ( 'NONE', #28747, #18753, #16082 ) ;
#21068=VECTOR ( 'NONE', #5978, 1000.000000000000000 ) ;
#21069=CARTESIAN_POINT ( 'NONE',  ( 0.000000000000000000, -41.33768078145432412, -104.3046912715545318 ) ) ;
#21076=DIRECTION ( 'NONE',  ( -1.000000000000000000, -0.000000000000000000, -0.000000000000000000 ) ) ;
#21079=ORIENTED_EDGE ( 'NONE', *, *, #21360, .F. ) ;
#21085=DIRECTION ( 'NONE',  ( 0.000000000000000000, 0.000000000000000000, 1.000000000000000000 ) ) ;
#21087=DIRECTION ( 'NONE',  ( 0.000000000000000000, -0.9968120070307509017, 0.07978610555307326380 ) ) ;
#21089=CARTESIAN_POINT ( 'NONE',  ( 17.99999999999999645, 112.5120133921113563, -43.14554256760899875 ) ) ;
#21093=LINE ( 'NONE', #15185, #39618 ) ;
#21097=DIRECTION ( 'NONE',  ( 1.000000000000000000, 0.000000000000000000, 0.000000000000000000 ) ) ;
#21099=ORIENTED_EDGE ( 'NONE', *, *, #18329, .T. ) ;
#21100=DIRECTION ( 'NONE',  ( -1.000000000000000000, -0.000000000000000000, -0.000000000000000000 ) ) ;
#21101=CYLINDRICAL_SURFACE ( 'NONE', #28404, 59.00000000000000000 ) ;
#21105=ORIENTED_EDGE ( 'NONE', *, *, #43055, .T. ) ;
#21107=LINE ( 'NONE', #41321, #36937 ) ;
#21111=DIRECTION ( 'NONE',  ( -1.000000000000000000, -0.000000000000000000, -0.000000000000000000 ) ) ;
#21112=ADVANCED_FACE ( 'NONE', ( #37115 ), #7223, .F. ) ;
#21116=AXIS2_PLACEMENT_3D ( 'NONE', #12950, #29746, #10078 ) ;
#21117=CARTESIAN_POINT ( 'NONE',  ( 0.000000000000000000, 0.000000000000000000, 0.000000000000000000 ) ) ;
#21119=ORIENTED_EDGE ( 'NONE', *, *, #8506, .T. ) ;
#21123=AXIS2_PLACEMENT_3D ( 'NONE', #25566, #2592, #8952 ) ;
#21124=CARTESIAN_POINT ( 'NONE',  ( 17.99999999999999645, -105.3681574666261298, -38.54638589714993202 ) ) ;
#21125=CYLINDRICAL_SURFACE ( 'NONE', #21352, 59.00000000000000000 ) ;
#21126=EDGE_CURVE ( 'NONE', #10322, #25878, #9417, .T. ) ;
#21130=LINE ( 'NONE', #11496, #4498 ) ;
#21133=VERTEX_POINT ( 'NONE', #11387 ) ;
#21135=CARTESIAN_POINT ( 'NONE',  ( 9.000000000000001776, -35.78484819117565507, -110.3423972910436390 ) ) ;
#21139=ADVANCED_FACE ( 'NONE', ( #24512 ), #14674, .F. ) ;
#21143=DIRECTION ( 'NONE',  ( 0.000000000000000000, 0.8183027759081663577, 0.5747874102144109321 ) ) ;
#21148=DIRECTION ( 'NONE',  ( 1.000000000000000000, 0.000000000000000000, 0.000000000000000000 ) ) ;
#21152=FACE_OUTER_BOUND ( 'NONE', #28621, .T. ) ;
#21156=CYLINDRICAL_SURFACE ( 'NONE', #19723, 59.00000000000000000 ) ;
#21157=EDGE_CURVE ( 'NONE', #18006, #33231, #27572, .T. ) ;
#21159=CYLINDRICAL_SURFACE ( 'NONE', #42883, 116.0000000000000000 ) ;
#21162=ORIENTED_EDGE ( 'NONE', *, *, #23782, .T. ) ;
#21169=ORIENTED_EDGE ( 'NONE', *, *, #33183, .F. ) ;
#21170=CARTESIAN_POINT ( 'NONE',  ( 17.99999999999999645, -57.69704296431255131, 105.7900857083227777 ) ) ;
#21171=DIRECTION ( 'NONE',  ( -1.000000000000000000, -0.000000000000000000, -0.000000000000000000 ) ) ;
#21173=ORIENTED_EDGE ( 'NONE', *, *, #685, .F. ) ;
#21174=DIRECTION ( 'NONE',  ( 0.000000000000000000, -0.5528000653612000770, 0.8333139190825106235 ) ) ;
#21177=ORIENTED_EDGE ( 'NONE', *, *, #23679, .T. ) ;
#21179=DIRECTION ( 'NONE',  ( 0.000000000000000000, -4.441553645588922428E-15, -1.000000000000000000 ) ) ;
#21180=( GEOMETRIC_REPRESENTATION_CONTEXT ( 3 ) GLOBAL_UNCERTAINTY_ASSIGNED_CONTEXT ( ( #7312 ) ) GLOBAL_UNIT_ASSIGNED_CONTEXT ( ( #38714, #28721, #28518 ) ) REPRESENTATION_CONTEXT ( 'NONE', 'WORKASPACE' ) );
#21181=DIRECTION ( 'NONE',  ( -1.000000000000000000, 0.000000000000000000, 0.000000000000000000 ) ) ;
#21184=ORIENTED_EDGE ( 'NONE', *, *, #9584, .T. ) ;
#21190=CARTESIAN_POINT ( 'NONE',  ( 17.99999999999999645, 0.000000000000000000, 0.000000000000000000 ) ) ;
#21193=CYLINDRICAL_SURFACE ( 'NONE', #31389, 120.5010000000000190 ) ;
#21194=ORIENTED_EDGE ( 'NONE', *, *, #16618, .T. ) ;
#21195=DIRECTION ( 'NONE',  ( 0.000000000000000000, 0.000000000000000000, 1.000000000000000000 ) ) ;
#21197=VECTOR ( 'NONE', #33587, 1000.000000000000000 ) ;
#21198=ORIENTED_EDGE ( 'NONE', *, *, #28823, .T. ) ;
#21200=DIRECTION ( 'NONE',  ( 0.000000000000000000, 0.000000000000000000, 1.000000000000000000 ) ) ;
#21201=CYLINDRICAL_SURFACE ( 'NONE', #26300, 120.5010000000000190 ) ;
#21203=CARTESIAN_POINT ( 'NONE',  ( 8.999999999999998224, 79.18387647320879807, -84.76976882518680156 ) ) ;
#21204=FACE_OUTER_BOUND ( 'NONE', #156, .T. ) ;
#21205=VERTEX_POINT ( 'NONE', #10515 ) ;
#21207=VERTEX_POINT ( 'NONE', #665 ) ;
#21208=ADVANCED_FACE ( 'NONE', ( #1107 ), #40587, .F. ) ;
#21209=CARTESIAN_POINT ( 'NONE',  ( 17.99999999999999645, -120.4984140710909202, -0.7894348306996294973 ) ) ;
#21213=DIRECTION ( 'NONE',  ( 1.000000000000000000, 0.000000000000000000, 0.000000000000000000 ) ) ;
#21214=ORIENTED_EDGE ( 'NONE', *, *, #5669, .T. ) ;
#21215=FACE_OUTER_BOUND ( 'NONE', #19001, .T. ) ;
#21216=CARTESIAN_POINT ( 'NONE',  ( -10.00000000000000000, 0.000000000000000000, 0.000000000000000000 ) ) ;
#21217=AXIS2_PLACEMENT_3D ( 'NONE', #43037, #29331, #16693 ) ;
#21223=CARTESIAN_POINT ( 'NONE',  ( 0.000000000000000000, 64.69195966009891663, 96.28577441832274530 ) ) ;
#21224=VECTOR ( 'NONE', #29256, 1000.000000000000000 ) ;
#21226=CARTESIAN_POINT ( 'NONE',  ( 17.99999999999999645, -29.36437154451924059, -116.8684075565139295 ) ) ;
#21227=EDGE_LOOP ( 'NONE', ( #36063, #36824, #35764, #10033 ) ) ;
#21230=AXIS2_PLACEMENT_3D ( 'NONE', #5849, #16128, #22054 ) ;
#21233=FACE_OUTER_BOUND ( 'NONE', #32841, .T. ) ;
#21239=CARTESIAN_POINT ( 'NONE',  ( 0.000000000000000000, 0.000000000000000000, 0.000000000000000000 ) ) ;
#21243=EDGE_CURVE ( 'NONE', #5141, #9900, #25510, .T. ) ;
#21244=FACE_OUTER_BOUND ( 'NONE', #14360, .T. ) ;
#21245=CARTESIAN_POINT ( 'NONE',  ( 17.99999999999999645, -111.2721026680461733, 14.38025178762581469 ) ) ;
#21248=AXIS2_PLACEMENT_3D ( 'NONE', #37308, #23824, #7423 ) ;
#21249=CARTESIAN_POINT ( 'NONE',  ( 17.99999999999999645, -67.32409792376564894, 89.75376489259340929 ) ) ;
#21254=DIRECTION ( 'NONE',  ( -1.000000000000000000, 0.000000000000000000, 0.000000000000000000 ) ) ;
#21255=CARTESIAN_POINT ( 'NONE',  ( 0.000000000000000000, 47.31079789947484926, 105.9135893174952656 ) ) ;
#21256=CIRCLE ( 'NONE', #12199, 59.00000000000000711 ) ;
#21257=VERTEX_POINT ( 'NONE', #42681 ) ;
#21259=FACE_OUTER_BOUND ( 'NONE', #482, .T. ) ;
#21260=CIRCLE ( 'NONE', #26117, 120.5010000000000332 ) ;
#21267=ORIENTED_EDGE ( 'NONE', *, *, #27414, .F. ) ;
#21270=ORIENTED_EDGE ( 'NONE', *, *, #28352, .T. ) ;
#21276=EDGE_CURVE ( 'NONE', #5508, #8087, #25935, .T. ) ;
#21277=VERTEX_POINT ( 'NONE', #35707 ) ;
#21281=CARTESIAN_POINT ( 'NONE',  ( 8.999999999999998224, 95.31344542257821217, -66.11616384574354299 ) ) ;
#21282=CARTESIAN_POINT ( 'NONE',  ( 17.99999999999999645, 0.000000000000000000, 0.000000000000000000 ) ) ;
#21285=AXIS2_PLACEMENT_3D ( 'NONE', #19440, #2580, #39872 ) ;
#21287=VERTEX_POINT ( 'NONE', #39414 ) ;
#21291=AXIS2_PLACEMENT_3D ( 'NONE', #35397, #16206, #35595 ) ;
#21292=CARTESIAN_POINT ( 'NONE',  ( 0.000000000000000000, 0.000000000000000000, 0.000000000000000000 ) ) ;
#21298=EDGE_CURVE ( 'NONE', #25238, #8366, #39362, .T. ) ;
#21299=VERTEX_POINT ( 'NONE', #9551 ) ;
#21300=CARTESIAN_POINT ( 'NONE',  ( 8.999999999999998224, 69.72480978690046527, 92.70626138606036193 ) ) ;
#21305=EDGE_CURVE ( 'NONE', #5822, #23930, #20616, .T. ) ;
#21307=CIRCLE ( 'NONE', #24784, 58.99999999999999289 ) ;
#21308=ORIENTED_EDGE ( 'NONE', *, *, #4301, .T. ) ;
#21313=CYLINDRICAL_SURFACE ( 'NONE', #28424, 59.00000000000000000 ) ;
#21315=DIRECTION ( 'NONE',  ( 0.000000000000000000, 0.9996456111234524045, 0.02662052143777833904 ) ) ;
#21318=DIRECTION ( 'NONE',  ( -1.000000000000000000, -0.000000000000000000, -0.000000000000000000 ) ) ;
#21320=VERTEX_POINT ( 'NONE', #32673 ) ;
#21321=AXIS2_PLACEMENT_3D ( 'NONE', #13930, #17217, #37458 ) ;
#21323=ORIENTED_EDGE ( 'NONE', *, *, #42657, .T. ) ;
#21325=LINE ( 'NONE', #34578, #13308 ) ;
#21327=DIRECTION ( 'NONE',  ( -1.000000000000000000, -0.000000000000000000, -0.000000000000000000 ) ) ;
#21329=EDGE_CURVE ( 'NONE', #31963, #17636, #16423, .T. ) ;
#21330=VERTEX_POINT ( 'NONE', #35511 ) ;
#21333=EDGE_CURVE ( 'NONE', #31625, #21277, #9757, .T. ) ;
#21335=CARTESIAN_POINT ( 'NONE',  ( 17.99999999999999645, -110.3490479609633752, 20.28201389785361641 ) ) ;
#21336=ORIENTED_EDGE ( 'NONE', *, *, #21991, .F. ) ;
#21337=CYLINDRICAL_SURFACE ( 'NONE', #13329, 59.00000000000000000 ) ;
#21343=DIRECTION ( 'NONE',  ( 1.000000000000000000, 0.000000000000000000, 0.000000000000000000 ) ) ;
#21344=ORIENTED_EDGE ( 'NONE', *, *, #34353, .T. ) ;
#21345=AXIS2_PLACEMENT_3D ( 'NONE', #39706, #26864, #39499 ) ;
#21347=ORIENTED_EDGE ( 'NONE', *, *, #43055, .F. ) ;
#21350=VERTEX_POINT ( 'NONE', #36146 ) ;
#21351=CARTESIAN_POINT ( 'NONE',  ( 17.99999999999999645, 94.52951811191560694, 67.23221107124935259 ) ) ;
#21352=AXIS2_PLACEMENT_3D ( 'NONE', #20685, #30692, #11064 ) ;
#21360=EDGE_CURVE ( 'NONE', #39420, #21974, #33806, .T. ) ;
#21363=DIRECTION ( 'NONE',  ( -1.000000000000000000, 0.000000000000000000, -0.000000000000000000 ) ) ;
#21364=ORIENTED_EDGE ( 'NONE', *, *, #19754, .T. ) ;
#21365=DIRECTION ( 'NONE',  ( 1.000000000000000000, 0.000000000000000000, 0.000000000000000000 ) ) ;
#21366=DIRECTION ( 'NONE',  ( -1.000000000000000000, -0.000000000000000000, 0.000000000000000000 ) ) ;
#21368=ORIENTED_EDGE ( 'NONE', *, *, #38246, .F. ) ;
#21371=CARTESIAN_POINT ( 'NONE',  ( 17.99999999999999645, -109.1131968883996848, -26.12628443612003437 ) ) ;
#21374=VERTEX_POINT ( 'NONE', #15691 ) ;
#21375=EDGE_CURVE ( 'NONE', #36059, #25122, #15745, .T. ) ;
#21376=LINE ( 'NONE', #24423, #20005 ) ;
#21377=DIRECTION ( 'NONE',  ( 0.000000000000000000, 0.000000000000000000, -1.000000000000000000 ) ) ;
#21379=CIRCLE ( 'NONE', #15068, 120.5010000000000190 ) ;
#21380=AXIS2_PLACEMENT_3D ( 'NONE', #32494, #42511, #31867 ) ;
#21382=DIRECTION ( 'NONE',  ( 1.000000000000000000, 0.000000000000000000, 0.000000000000000000 ) ) ;
#21383=DIRECTION ( 'NONE',  ( 1.000000000000000000, 0.000000000000000000, 0.000000000000000000 ) ) ;
#21385=CARTESIAN_POINT ( 'NONE',  ( 17.99999999999999645, -92.25992191227339845, -77.51514567967485902 ) ) ;
#21386=ORIENTED_EDGE ( 'NONE', *, *, #15255, .T. ) ;
#21389=CIRCLE ( 'NONE', #35240, 120.5010000000000190 ) ;
#21390=DIRECTION ( 'NONE',  ( 0.000000000000000000, 0.000000000000000000, 1.000000000000000000 ) ) ;
#21391=VECTOR ( 'NONE', #34592, 1000.000000000000000 ) ;
#21392=VECTOR ( 'NONE', #32889, 1000.000000000000000 ) ;
#21394=EDGE_CURVE ( 'NONE', #21299, #41436, #13654, .T. ) ;
#21396=ORIENTED_EDGE ( 'NONE', *, *, #32860, .F. ) ;
#21397=DIRECTION ( 'NONE',  ( 1.000000000000000000, 0.000000000000000000, 0.000000000000000000 ) ) ;
#21404=ORIENTED_EDGE ( 'NONE', *, *, #17667, .F. ) ;
#21405=DIRECTION ( 'NONE',  ( 1.000000000000000000, 0.000000000000000000, 0.000000000000000000 ) ) ;
#21406=CARTESIAN_POINT ( 'NONE',  ( 17.99999999999999645, 53.40478689619876462, -108.0204598100360016 ) ) ;
#21407=DIRECTION ( 'NONE',  ( 0.000000000000000000, -0.3641605752528101481, -0.9313361774523430947 ) ) ;
#21409=ORIENTED_EDGE ( 'NONE', *, *, #12460, .F. ) ;
#21412=AXIS2_PLACEMENT_3D ( 'NONE', #5710, #42560, #12501 ) ;
#21414=AXIS2_PLACEMENT_3D ( 'NONE', #28120, #2108, #5819 ) ;
#21415=AXIS2_PLACEMENT_3D ( 'NONE', #35244, #42428, #25262 ) ;
#21417=AXIS2_PLACEMENT_3D ( 'NONE', #29961, #12522, #36461 ) ;
#21418=DIRECTION ( 'NONE',  ( 0.000000000000000000, 2.587384167558627638E-15, -1.000000000000000000 ) ) ;
#21420=CARTESIAN_POINT ( 'NONE',  ( 17.99999999999999645, 46.83041522348496954, 101.9567785075603155 ) ) ;
#21421=CIRCLE ( 'NONE', #24209, 59.00000000000000711 ) ;
#21422=DIRECTION ( 'NONE',  ( 0.000000000000000000, 0.000000000000000000, 1.000000000000000000 ) ) ;
#21423=ORIENTED_EDGE ( 'NONE', *, *, #42382, .T. ) ;
#21424=CARTESIAN_POINT ( 'NONE',  ( 17.99999999999999645, -29.02167576844178853, 108.3790330702168774 ) ) ;
#21427=ORIENTED_EDGE ( 'NONE', *, *, #1299, .F. ) ;
#21430=VECTOR ( 'NONE', #37634, 1000.000000000000000 ) ;
#21435=AXIS2_PLACEMENT_3D ( 'NONE', #20416, #3348, #10353 ) ;
#21436=EDGE_LOOP ( 'NONE', ( #16583, #20017, #40046, #32258 ) ) ;
#21441=CARTESIAN_POINT ( 'NONE',  ( 17.99999999999999645, 0.000000000000000000, 0.000000000000000000 ) ) ;
#21447=ORIENTED_EDGE ( 'NONE', *, *, #29480, .F. ) ;
#21448=AXIS2_PLACEMENT_3D ( 'NONE', #24781, #41520, #21734 ) ;
#21450=EDGE_CURVE ( 'NONE', #2020, #5449, #42852, .T. ) ;
#21451=AXIS2_PLACEMENT_3D ( 'NONE', #22313, #22732, #42321 ) ;
#21452=AXIS2_PLACEMENT_3D ( 'NONE', #24471, #14419, #38958 ) ;
#21453=DIRECTION ( 'NONE',  ( 0.000000000000000000, 0.000000000000000000, 1.000000000000000000 ) ) ;
#21455=LINE ( 'NONE', #31875, #31548 ) ;
#21457=CARTESIAN_POINT ( 'NONE',  ( 17.99999999999999645, -103.5682682299985515, -43.14958040911633219 ) ) ;
#21461=VERTEX_POINT ( 'NONE', #35143 ) ;
#21473=DIRECTION ( 'NONE',  ( 1.000000000000000000, 0.000000000000000000, 0.000000000000000000 ) ) ;
#21474=CARTESIAN_POINT ( 'NONE',  ( 0.000000000000000000, 0.000000000000000000, 0.000000000000000000 ) ) ;
#21475=AXIS2_PLACEMENT_3D ( 'NONE', #42789, #26463, #3716 ) ;
#21477=CIRCLE ( 'NONE', #12385, 120.5010000000000474 ) ;
#21478=VERTEX_POINT ( 'NONE', #34729 ) ;
#21480=EDGE_LOOP ( 'NONE', ( #1353, #29488, #38525, #40715 ) ) ;
#21481=FACE_OUTER_BOUND ( 'NONE', #39213, .T. ) ;
#21485=VERTEX_POINT ( 'NONE', #7885 ) ;
#21486=CIRCLE ( 'NONE', #13108, 59.00000000000000000 ) ;
#21490=CARTESIAN_POINT ( 'NONE',  ( 17.99999999999999645, 0.000000000000000000, 0.000000000000000000 ) ) ;
#21492=ORIENTED_EDGE ( 'NONE', *, *, #11073, .F. ) ;
#21494=VECTOR ( 'NONE', #4252, 1000.000000000000000 ) ;
#21496=VERTEX_POINT ( 'NONE', #38414 ) ;
#21498=CARTESIAN_POINT ( 'NONE',  ( 8.999999999999998224, 114.1157422997283248, 20.82300072952973480 ) ) ;
#21500=FACE_OUTER_BOUND ( 'NONE', #39897, .T. ) ;
#21505=EDGE_CURVE ( 'NONE', #7227, #30398, #10719, .T. ) ;
#21508=FACE_OUTER_BOUND ( 'NONE', #28281, .T. ) ;
#21509=CARTESIAN_POINT ( 'NONE',  ( 17.99999999999999645, 111.1352304691227744, 15.40237066878635730 ) ) ;
#21512=ORIENTED_EDGE ( 'NONE', *, *, #36895, .F. ) ;
#21513=AXIS2_PLACEMENT_3D ( 'NONE', #30345, #3681, #30572 ) ;
#21514=VECTOR ( 'NONE', #34970, 1000.000000000000000 ) ;
#21517=ORIENTED_EDGE ( 'NONE', *, *, #32955, .T. ) ;
#21518=DIRECTION ( 'NONE',  ( -1.000000000000000000, -0.000000000000000000, -0.000000000000000000 ) ) ;
#21520=DIRECTION ( 'NONE',  ( 1.000000000000000000, 0.000000000000000000, 0.000000000000000000 ) ) ;
#21522=EDGE_LOOP ( 'NONE', ( #380, #40164, #15667, #17930 ) ) ;
#21529=DIRECTION ( 'NONE',  ( 0.000000000000000000, -0.4610925014493326146, 0.8873520750565681015 ) ) ;
#21530=EDGE_CURVE ( 'NONE', #34259, #1680, #32297, .T. ) ;
#21533=ORIENTED_EDGE ( 'NONE', *, *, #17547, .T. ) ;
#21535=CARTESIAN_POINT ( 'NONE',  ( 0.000000000000000000, 0.000000000000000000, 0.000000000000000000 ) ) ;
#21539=CYLINDRICAL_SURFACE ( 'NONE', #25456, 120.5010000000000190 ) ;
#21540=ORIENTED_EDGE ( 'NONE', *, *, #23903, .F. ) ;
#21544=CARTESIAN_POINT ( 'NONE',  ( 9.000000000000001776, -112.5220807139885864, 28.19186676675806424 ) ) ;
#21546=AXIS2_PLACEMENT_3D ( 'NONE', #36051, #6170, #16447 ) ;
#21554=CARTESIAN_POINT ( 'NONE',  ( 17.99999999999999645, 0.000000000000000000, 0.000000000000000000 ) ) ;
#21555=ORIENTED_EDGE ( 'NONE', *, *, #4045, .F. ) ;
#21556=CYLINDRICAL_SURFACE ( 'NONE', #17965, 59.00000000000000000 ) ;
#21560=CYLINDRICAL_SURFACE ( 'NONE', #33239, 59.00000000000000000 ) ;
#21564=CARTESIAN_POINT ( 'NONE',  ( 0.000000000000000000, 41.33768078145502756, 104.3046912715542902 ) ) ;
#21569=CARTESIAN_POINT ( 'NONE',  ( 17.99999999999999645, 31.17727234463695041, 111.7317219465820983 ) ) ;
#21571=AXIS2_PLACEMENT_3D ( 'NONE', #26426, #13556, #42973 ) ;
#21573=CIRCLE ( 'NONE', #1974, 59.00000000000000000 ) ;
#21576=DIRECTION ( 'NONE',  ( 1.000000000000000000, -0.000000000000000000, -0.000000000000000000 ) ) ;
#21579=LINE ( 'NONE', #15233, #33155 ) ;
#21583=EDGE_CURVE ( 'NONE', #14728, #4296, #29264, .T. ) ;
#21584=ORIENTED_EDGE ( 'NONE', *, *, #20848, .F. ) ;
#21585=CARTESIAN_POINT ( 'NONE',  ( 17.99999999999999645, 112.8457601792515419, 26.86697618949414945 ) ) ;
#21591=CARTESIAN_POINT ( 'NONE',  ( 0.000000000000000000, 0.000000000000000000, 0.000000000000000000 ) ) ;
#21595=DIRECTION ( 'NONE',  ( 0.000000000000000000, 0.2631025642275152676, 0.9647678688145175929 ) ) ;
#21598=CIRCLE ( 'NONE', #35455, 120.5010000000000190 ) ;
#21600=CARTESIAN_POINT ( 'NONE',  ( 0.000000000000000000, -110.0562500189201955, 49.07252625220073838 ) ) ;
#21602=ORIENTED_EDGE ( 'NONE', *, *, #8917, .T. ) ;
#21604=VERTEX_POINT ( 'NONE', #35567 ) ;
#21607=DIRECTION ( 'NONE',  ( -1.000000000000000000, 0.000000000000000000, 0.000000000000000000 ) ) ;
#21610=ADVANCED_FACE ( 'NONE', ( #36412 ), #9174, .F. ) ;
#21612=CARTESIAN_POINT ( 'NONE',  ( 0.000000000000000000, 0.000000000000000000, 0.000000000000000000 ) ) ;
#21618=DIRECTION ( 'NONE',  ( -1.000000000000000000, 0.000000000000000000, -0.000000000000000000 ) ) ;
#21621=DIRECTION ( 'NONE',  ( -1.000000000000000000, -0.000000000000000000, -0.000000000000000000 ) ) ;
#21622=EDGE_CURVE ( 'NONE', #4984, #19384, #5823, .T. ) ;
#21623=CARTESIAN_POINT ( 'NONE',  ( 17.99999999999999645, -8.827181066046698277, 120.1772519049559378 ) ) ;
#21630=CIRCLE ( 'NONE', #12527, 59.00000000000000000 ) ;
#21633=CARTESIAN_POINT ( 'NONE',  ( 17.99999999999999645, 41.33768078145642022, -104.3046912715537076 ) ) ;
#21635=ADVANCED_FACE ( 'NONE', ( #13123 ), #19039, .F. ) ;
#21636=DIRECTION ( 'NONE',  ( -1.000000000000000000, 0.000000000000000000, 0.000000000000000000 ) ) ;
#21639=DIRECTION ( 'NONE',  ( -1.000000000000000000, -0.000000000000000000, -0.000000000000000000 ) ) ;
#21642=DIRECTION ( 'NONE',  ( 0.000000000000000000, -0.2631025642275089393, -0.9647678688145192583 ) ) ;
#21644=DIRECTION ( 'NONE',  ( 0.000000000000000000, 0.000000000000000000, 1.000000000000000000 ) ) ;
#21646=ORIENTED_EDGE ( 'NONE', *, *, #8682, .T. ) ;
#21647=DIRECTION ( 'NONE',  ( -1.000000000000000000, 0.000000000000000000, -0.000000000000000000 ) ) ;
#21651=DIRECTION ( 'NONE',  ( 0.000000000000000000, -0.2631025642275283127, 0.9647678688145140402 ) ) ;
#21652=AXIS2_PLACEMENT_3D ( 'NONE', #27010, #40282, #40927 ) ;
#21656=ADVANCED_FACE ( 'NONE', ( #2382 ), #36204, .F. ) ;
#21659=VERTEX_POINT ( 'NONE', #15751 ) ;
#21661=ADVANCED_FACE ( 'NONE', ( #29056 ), #29690, .F. ) ;
#21666=EDGE_CURVE ( 'NONE', #26858, #13842, #35758, .T. ) ;
#21672=DIRECTION ( 'NONE',  ( 1.000000000000000000, 0.000000000000000000, 0.000000000000000000 ) ) ;
#21673=EDGE_CURVE ( 'NONE', #20905, #4984, #42736, .T. ) ;
#21674=EDGE_LOOP ( 'NONE', ( #23811, #31706, #11074, #11398 ) ) ;
#21677=VECTOR ( 'NONE', #13385, 1000.000000000000000 ) ;
#21679=CARTESIAN_POINT ( 'NONE',  ( 17.99999999999999645, -106.6051926090974007, 45.73109345704783379 ) ) ;
#21680=LINE ( 'NONE', #12050, #27705 ) ;
#21681=CIRCLE ( 'NONE', #18879, 116.0000000000000000 ) ;
#21682=CIRCLE ( 'NONE', #36243, 116.0000000000000000 ) ;
#21685=ORIENTED_EDGE ( 'NONE', *, *, #9863, .F. ) ;
#21687=ORIENTED_EDGE ( 'NONE', *, *, #12793, .T. ) ;
#21689=DIRECTION ( 'NONE',  ( 0.000000000000000000, -0.7164567402983210709, 0.6976315211349786161 ) ) ;
#21692=CARTESIAN_POINT ( 'NONE',  ( 0.000000000000000000, -95.31344542257689056, -66.11616384574544725 ) ) ;
#21693=ORIENTED_EDGE ( 'NONE', *, *, #28876, .T. ) ;
#21695=ORIENTED_EDGE ( 'NONE', *, *, #40262, .T. ) ;
#21696=ORIENTED_EDGE ( 'NONE', *, *, #28357, .T. ) ;
#21705=EDGE_CURVE ( 'NONE', #23222, #10037, #42731, .T. ) ;
#21706=ORIENTED_EDGE ( 'NONE', *, *, #40806, .T. ) ;
#21708=ORIENTED_EDGE ( 'NONE', *, *, #41118, .T. ) ;
#21709=DIRECTION ( 'NONE',  ( 1.000000000000000000, 0.000000000000000000, -0.000000000000000000 ) ) ;
#21711=VECTOR ( 'NONE', #29547, 1000.000000000000000 ) ;
#21713=CIRCLE ( 'NONE', #9106, 59.00000000000000000 ) ;
#21715=CARTESIAN_POINT ( 'NONE',  ( 17.99999999999999645, -62.45178862086279992, 93.20969140437486544 ) ) ;
#21716=LINE ( 'NONE', #34760, #8117 ) ;
#21721=CYLINDRICAL_SURFACE ( 'NONE', #9492, 120.5010000000000190 ) ;
#21728=VERTEX_POINT ( 'NONE', #35761 ) ;
#21729=EDGE_CURVE ( 'NONE', #11059, #25754, #10024, .T. ) ;
#21733=CARTESIAN_POINT ( 'NONE',  ( 0.000000000000000000, 48.55277268144470781, -105.3500273609075180 ) ) ;
#21734=DIRECTION ( 'NONE',  ( 0.000000000000000000, 0.000000000000000000, 1.000000000000000000 ) ) ;
#21736=CARTESIAN_POINT ( 'NONE',  ( 17.99999999999999645, 0.000000000000000000, 0.000000000000000000 ) ) ;
#21737=EDGE_CURVE ( 'NONE', #23636, #14855, #19108, .T. ) ;
#21739=DIRECTION ( 'NONE',  ( 0.000000000000000000, 0.5528000653611945259, -0.8333139190825142872 ) ) ;
#21740=ORIENTED_EDGE ( 'NONE', *, *, #11175, .F. ) ;
#21742=CIRCLE ( 'NONE', #40473, 59.00000000000001421 ) ;
#21748=VECTOR ( 'NONE', #7085, 1000.000000000000000 ) ;
#21750=EDGE_LOOP ( 'NONE', ( #31202, #25520, #42629, #18315 ) ) ;
#21751=ORIENTED_EDGE ( 'NONE', *, *, #37208, .F. ) ;
#21756=DIRECTION ( 'NONE',  ( -1.000000000000000000, 0.000000000000000000, 0.000000000000000000 ) ) ;
#21759=ORIENTED_EDGE ( 'NONE', *, *, #1645, .F. ) ;
#21762=CARTESIAN_POINT ( 'NONE',  ( 17.99999999999999645, 0.000000000000000000, 0.000000000000000000 ) ) ;
#21765=CYLINDRICAL_SURFACE ( 'NONE', #17237, 116.0000000000000000 ) ;
#21769=EDGE_CURVE ( 'NONE', #33264, #37125, #29541, .T. ) ;
#21771=CARTESIAN_POINT ( 'NONE',  ( 17.99999999999999645, 0.000000000000000000, 0.000000000000000000 ) ) ;
#21772=ORIENTED_EDGE ( 'NONE', *, *, #18329, .F. ) ;
#21774=VECTOR ( 'NONE', #1362, 1000.000000000000000 ) ;
#21775=DIRECTION ( 'NONE',  ( 0.000000000000000000, -0.8183027759081743513, 0.5747874102143993857 ) ) ;
#21776=CYLINDRICAL_SURFACE ( 'NONE', #31780, 59.00000000000001421 ) ;
#21777=CIRCLE ( 'NONE', #2870, 59.00000000000000711 ) ;
#21780=CARTESIAN_POINT ( 'NONE',  ( 0.000000000000000000, 3.996885678774600326, -120.4346956066681713 ) ) ;
#21783=ADVANCED_FACE ( 'NONE', ( #33379, #20327 ), #3464, .F. ) ;
#21785=CIRCLE ( 'NONE', #8491, 59.00000000000000711 ) ;
#21791=CARTESIAN_POINT ( 'NONE',  ( 0.000000000000000000, -62.45178862086154226, -93.20969140437570388 ) ) ;
#21792=ORIENTED_EDGE ( 'NONE', *, *, #17307, .F. ) ;
#21793=DIRECTION ( 'NONE',  ( 1.000000000000000000, 0.000000000000000000, 0.000000000000000000 ) ) ;
#21794=EDGE_LOOP ( 'NONE', ( #8288, #9208, #3931, #26530 ) ) ;
#21798=CARTESIAN_POINT ( 'NONE',  ( 9.000000000000001776, -19.12429268481633571, -114.4126803693781085 ) ) ;
#21800=CARTESIAN_POINT ( 'NONE',  ( 0.000000000000000000, 78.75547124681492051, -91.20343606296921735 ) ) ;
#21802=DIRECTION ( 'NONE',  ( 0.000000000000000000, 0.8747630845319623871, -0.4845508703326482647 ) ) ;
#21803=AXIS2_PLACEMENT_3D ( 'NONE', #39232, #35968, #19446 ) ;
#21805=AXIS2_PLACEMENT_3D ( 'NONE', #3274, #36661, #7203 ) ;
#21809=VECTOR ( 'NONE', #21857, 1000.000000000000000 ) ;
#21810=EDGE_CURVE ( 'NONE', #11023, #30476, #14193, .T. ) ;
#21813=EDGE_LOOP ( 'NONE', ( #16938, #623, #3287, #35467 ) ) ;
#21814=DIRECTION ( 'NONE',  ( 0.000000000000000000, 0.000000000000000000, 1.000000000000000000 ) ) ;
#21820=DIRECTION ( 'NONE',  ( 0.000000000000000000, -0.5076658003388292428, -0.8615540813938125098 ) ) ;
#21821=CARTESIAN_POINT ( 'NONE',  ( 17.99999999999999645, -23.21237537461669120, -109.7700237000594541 ) ) ;
#21825=EDGE_CURVE ( 'NONE', #214, #29479, #30903, .T. ) ;
#21826=CARTESIAN_POINT ( 'NONE',  ( 0.000000000000000000, -12.43843445475394027, 111.5058645182329116 ) ) ;
#21830=CARTESIAN_POINT ( 'NONE',  ( 0.000000000000000000, 0.000000000000000000, 0.000000000000000000 ) ) ;
#21832=CARTESIAN_POINT ( 'NONE',  ( 9.000000000000001776, 114.1157422997285806, -20.82300072952825332 ) ) ;
#21833=AXIS2_PLACEMENT_3D ( 'NONE', #29617, #12611, #38980 ) ;
#21835=EDGE_CURVE ( 'NONE', #21873, #5856, #12115, .T. ) ;
#21836=ORIENTED_EDGE ( 'NONE', *, *, #11922, .T. ) ;
#21838=AXIS2_PLACEMENT_3D ( 'NONE', #27449, #30519, #23982 ) ;
#21840=VERTEX_POINT ( 'NONE', #10685 ) ;
#21841=VECTOR ( 'NONE', #8516, 1000.000000000000000 ) ;
#21843=EDGE_CURVE ( 'NONE', #29479, #27194, #24022, .T. ) ;
#21848=EDGE_CURVE ( 'NONE', #29862, #26320, #37894, .T. ) ;
#21851=CARTESIAN_POINT ( 'NONE',  ( 0.000000000000000000, -84.62908780824814414, -85.78116633471378805 ) ) ;
#21852=DIRECTION ( 'NONE',  ( 1.000000000000000000, 0.000000000000000000, 0.000000000000000000 ) ) ;
#21857=DIRECTION ( 'NONE',  ( -1.000000000000000000, -0.000000000000000000, 0.000000000000000000 ) ) ;
#21858=FACE_OUTER_BOUND ( 'NONE', #2191, .T. ) ;
#21860=ORIENTED_EDGE ( 'NONE', *, *, #4345, .F. ) ;
#21863=CARTESIAN_POINT ( 'NONE',  ( 0.000000000000000000, 0.000000000000000000, 0.000000000000000000 ) ) ;
#21865=CARTESIAN_POINT ( 'NONE',  ( 17.99999999999999645, 52.19040376560434424, 99.31985817764196156 ) ) ;
#21866=DIRECTION ( 'NONE',  ( -1.000000000000000000, 0.000000000000000000, 0.000000000000000000 ) ) ;
#21867=FACE_OUTER_BOUND ( 'NONE', #10046, .T. ) ;
#21868=CARTESIAN_POINT ( 'NONE',  ( 17.99999999999999645, -92.10690493017105496, 64.06707842432145128 ) ) ;
#21872=CARTESIAN_POINT ( 'NONE',  ( 17.99999999999999645, 107.5680526044919674, -31.89649718262133149 ) ) ;
#21873=VERTEX_POINT ( 'NONE', #27943 ) ;
#21876=CARTESIAN_POINT ( 'NONE',  ( 17.99999999999999645, -34.74871106919551522, -106.6808302961375148 ) ) ;
#21878=ORIENTED_EDGE ( 'NONE', *, *, #5591, .T. ) ;
#21881=VERTEX_POINT ( 'NONE', #21851 ) ;
#21886=DIRECTION ( 'NONE',  ( 1.000000000000000000, 0.000000000000000000, 0.000000000000000000 ) ) ;
#21887=EDGE_CURVE ( 'NONE', #36681, #30521, #34237, .T. ) ;
#21888=EDGE_CURVE ( 'NONE', #21478, #2989, #244, .T. ) ;
#21892=ORIENTED_EDGE ( 'NONE', *, *, #23805, .F. ) ;
#21896=AXIS2_PLACEMENT_3D ( 'NONE', #31828, #36142, #19402 ) ;
#21897=DIRECTION ( 'NONE',  ( 0.000000000000000000, 0.000000000000000000, 1.000000000000000000 ) ) ;
#21898=ORIENTED_EDGE ( 'NONE', *, *, #38877, .F. ) ;
#21902=DIRECTION ( 'NONE',  ( 1.000000000000000000, 0.000000000000000000, 0.000000000000000000 ) ) ;
#21904=AXIS2_PLACEMENT_3D ( 'NONE', #40609, #30, #691 ) ;
#21905=EDGE_LOOP ( 'NONE', ( #38949, #16854, #32207, #36469 ) ) ;
#21910=ORIENTED_EDGE ( 'NONE', *, *, #11676, .T. ) ;
#21912=VECTOR ( 'NONE', #43169, 1000.000000000000000 ) ;
#21914=EDGE_LOOP ( 'NONE', ( #43158, #29064, #2960, #26520 ) ) ;
#21921=LINE ( 'NONE', #42359, #3987 ) ;
#21924=ADVANCED_BREP_SHAPE_REPRESENTATION ( '', ( #28802, #13552 ), #9968 ) ;
#21925=CARTESIAN_POINT ( 'NONE',  ( 17.99999999999999645, 0.000000000000000000, 0.000000000000000000 ) ) ;
#21928=DIRECTION ( 'NONE',  ( 0.000000000000000000, 0.000000000000000000, 1.000000000000000000 ) ) ;
#21930=DIRECTION ( 'NONE',  ( -1.000000000000000000, 0.000000000000000000, 0.000000000000000000 ) ) ;
#21931=VERTEX_POINT ( 'NONE', #34675 ) ;
#21937=CARTESIAN_POINT ( 'NONE',  ( 0.000000000000000000, 88.00363688980546328, 82.31555682352686176 ) ) ;
#21938=DIRECTION ( 'NONE',  ( -1.000000000000000000, 0.000000000000000000, 0.000000000000000000 ) ) ;
#21940=EDGE_CURVE ( 'NONE', #39201, #25078, #16339, .T. ) ;
#21942=DIRECTION ( 'NONE',  ( 0.000000000000000000, 0.000000000000000000, 1.000000000000000000 ) ) ;
#21945=CARTESIAN_POINT ( 'NONE',  ( 0.000000000000000000, 0.000000000000000000, 0.000000000000000000 ) ) ;
#21946=ORIENTED_EDGE ( 'NONE', *, *, #23556, .F. ) ;
#21947=CARTESIAN_POINT ( 'NONE',  ( -10.00000000000000000, 0.000000000000000000, 0.000000000000000000 ) ) ;
#21948=CYLINDRICAL_SURFACE ( 'NONE', #17267, 59.00000000000000000 ) ;
#21949=EDGE_CURVE ( 'NONE', #38496, #3479, #11565, .T. ) ;
#21950=DIRECTION ( 'NONE',  ( 1.000000000000000000, 0.000000000000000000, 0.000000000000000000 ) ) ;
#21953=VERTEX_POINT ( 'NONE', #25123 ) ;
#21954=FACE_OUTER_BOUND ( 'NONE', #7688, .T. ) ;
#21959=VERTEX_POINT ( 'NONE', #8052 ) ;
#21960=EDGE_CURVE ( 'NONE', #35045, #33779, #34447, .T. ) ;
#21963=CARTESIAN_POINT ( 'NONE',  ( 17.99999999999999645, 116.0452958106480708, 32.46506308663498430 ) ) ;
#21964=AXIS2_PLACEMENT_3D ( 'NONE', #33768, #10651, #4515 ) ;
#21965=DIRECTION ( 'NONE',  ( 0.000000000000000000, 0.000000000000000000, 1.000000000000000000 ) ) ;
#21966=ORIENTED_EDGE ( 'NONE', *, *, #4610, .F. ) ;
#21973=CARTESIAN_POINT ( 'NONE',  ( 0.000000000000000000, 37.07968990261480968, 109.9140418541958724 ) ) ;
#21974=VERTEX_POINT ( 'NONE', #35097 ) ;
#21975=AXIS2_PLACEMENT_3D ( 'NONE', #21591, #18524, #40942 ) ;
#21976=ADVANCED_FACE ( 'NONE', ( #12006 ), #28378, .F. ) ;
#21978=DIRECTION ( 'NONE',  ( -1.000000000000000000, 0.000000000000000000, 0.000000000000000000 ) ) ;
#21980=CARTESIAN_POINT ( 'NONE',  ( 0.000000000000000000, -106.5605152861907072, 56.26142179985788516 ) ) ;
#21981=VERTEX_POINT ( 'NONE', #7621 ) ;
#21982=VECTOR ( 'NONE', #38027, 1000.000000000000000 ) ;
#21983=DIRECTION ( 'NONE',  ( -1.000000000000000000, -0.000000000000000000, -0.000000000000000000 ) ) ;
#21986=DIRECTION ( 'NONE',  ( -1.000000000000000000, 0.000000000000000000, 0.000000000000000000 ) ) ;
#21990=AXIS2_PLACEMENT_3D ( 'NONE', #8770, #5285, #35785 ) ;
#21991=EDGE_CURVE ( 'NONE', #17128, #20200, #33723, .T. ) ;
#21992=VECTOR ( 'NONE', #14606, 1000.000000000000000 ) ;
#21993=ORIENTED_EDGE ( 'NONE', *, *, #17846, .F. ) ;
#21996=( NAMED_UNIT ( * ) SI_UNIT ( $, .STERADIAN. ) SOLID_ANGLE_UNIT ( ) );
#22000=CARTESIAN_POINT ( 'NONE',  ( 0.000000000000000000, -35.78484819117565507, -110.3423972910436390 ) ) ;
#22001=VERTEX_POINT ( 'NONE', #14412 ) ;
#22002=DIRECTION ( 'NONE',  ( 0.000000000000000000, 0.000000000000000000, -1.000000000000000000 ) ) ;
#22009=ORIENTED_EDGE ( 'NONE', *, *, #36048, .T. ) ;
#22011=DIRECTION ( 'NONE',  ( -1.000000000000000000, 0.000000000000000000, 0.000000000000000000 ) ) ;
#22014=DIRECTION ( 'NONE',  ( 0.000000000000000000, -0.7865515558026479059, 0.6175246149461850464 ) ) ;
#22020=CYLINDRICAL_SURFACE ( 'NONE', #35564, 120.5010000000000190 ) ;
#22022=CYLINDRICAL_SURFACE ( 'NONE', #3309, 120.5010000000000190 ) ;
#22023=DIRECTION ( 'NONE',  ( -1.000000000000000000, 0.000000000000000000, 0.000000000000000000 ) ) ;
#22026=EDGE_LOOP ( 'NONE', ( #34943, #20240, #39084, #26183 ) ) ;
#22029=EDGE_LOOP ( 'NONE', ( #13708, #13917, #27030, #37733 ) ) ;
#22031=AXIS2_PLACEMENT_3D ( 'NONE', #27365, #4649, #20412 ) ;
#22032=DIRECTION ( 'NONE',  ( 0.000000000000000000, 0.000000000000000000, 1.000000000000000000 ) ) ;
#22033=DIRECTION ( 'NONE',  ( 1.000000000000000000, -0.000000000000000000, -0.000000000000000000 ) ) ;
#22039=CIRCLE ( 'NONE', #40747, 120.5010000000000190 ) ;
#22041=DIRECTION ( 'NONE',  ( 0.000000000000000000, 0.000000000000000000, 1.000000000000000000 ) ) ;
#22042=AXIS2_PLACEMENT_3D ( 'NONE', #30873, #950, #27614 ) ;
#22049=CARTESIAN_POINT ( 'NONE',  ( 0.000000000000000000, 13.00789606333630566, -115.2683592318613819 ) ) ;
#22050=CARTESIAN_POINT ( 'NONE',  ( 0.000000000000000000, -115.9750404417043939, -2.406240749598616446 ) ) ;
#22053=ORIENTED_EDGE ( 'NONE', *, *, #1546, .T. ) ;
#22054=DIRECTION ( 'NONE',  ( 0.000000000000000000, 0.000000000000000000, 1.000000000000000000 ) ) ;
#22060=CARTESIAN_POINT ( 'NONE',  ( 0.000000000000000000, 0.000000000000000000, 0.000000000000000000 ) ) ;
#22061=ORIENTED_EDGE ( 'NONE', *, *, #174, .F. ) ;
#22062=ADVANCED_FACE ( 'NONE', ( #8697 ), #9334, .F. ) ;
#22064=CYLINDRICAL_SURFACE ( 'NONE', #30615, 59.00000000000000000 ) ;
#22066=CARTESIAN_POINT ( 'NONE',  ( 17.99999999999999645, 110.8621702203453339, -34.14058016547420493 ) ) ;
#22068=AXIS2_PLACEMENT_3D ( 'NONE', #10984, #14480, #27789 ) ;
#22070=CYLINDRICAL_SURFACE ( 'NONE', #42750, 59.00000000000000000 ) ;
#22071=VERTEX_POINT ( 'NONE', #19423 ) ;
#22074=FACE_OUTER_BOUND ( 'NONE', #26489, .T. ) ;
#22076=ORIENTED_EDGE ( 'NONE', *, *, #25580, .F. ) ;
#22079=VERTEX_POINT ( 'NONE', #25751 ) ;
#22081=EDGE_CURVE ( 'NONE', #17523, #18784, #35722, .T. ) ;
#22082=ADVANCED_FACE ( 'NONE', ( #8926 ), #42695, .F. ) ;
#22086=EDGE_CURVE ( 'NONE', #10513, #25132, #24711, .T. ) ;
#22087=EDGE_CURVE ( 'NONE', #11411, #14100, #1676, .T. ) ;
#22088=ADVANCED_FACE ( 'NONE', ( #42918 ), #32052, .F. ) ;
#22089=VECTOR ( 'NONE', #14823, 1000.000000000000000 ) ;
#22090=CARTESIAN_POINT ( 'NONE',  ( 17.99999999999999645, 0.000000000000000000, 0.000000000000000000 ) ) ;
#22094=DIRECTION ( 'NONE',  ( 0.000000000000000000, 0.000000000000000000, 1.000000000000000000 ) ) ;
#22096=EDGE_LOOP ( 'NONE', ( #29208, #11694, #36994, #9010 ) ) ;
#22102=VECTOR ( 'NONE', #17664, 1000.000000000000000 ) ;
#22103=CYLINDRICAL_SURFACE ( 'NONE', #10947, 116.0000000000000000 ) ;
#22104=CYLINDRICAL_SURFACE ( 'NONE', #28461, 120.5010000000000190 ) ;
#22111=CARTESIAN_POINT ( 'NONE',  ( 17.99999999999999645, 89.07460286905850921, 81.15544420874991260 ) ) ;
#22119=VERTEX_POINT ( 'NONE', #2564 ) ;
#22121=VECTOR ( 'NONE', #9221, 1000.000000000000000 ) ;
#22122=EDGE_LOOP ( 'NONE', ( #2858, #40024, #24693, #36223 ) ) ;
#22123=VECTOR ( 'NONE', #8321, 1000.000000000000000 ) ;
#22124=DIRECTION ( 'NONE',  ( 1.000000000000000000, 0.000000000000000000, 0.000000000000000000 ) ) ;
#22126=EDGE_LOOP ( 'NONE', ( #25042, #21892, #3405, #655 ) ) ;
#22127=DIRECTION ( 'NONE',  ( 0.000000000000000000, 0.000000000000000000, -1.000000000000000000 ) ) ;
#22131=DIRECTION ( 'NONE',  ( -1.000000000000000000, 0.000000000000000000, -0.000000000000000000 ) ) ;
#22132=AXIS2_PLACEMENT_3D ( 'NONE', #42075, #38179, #29027 ) ;
#22136=EDGE_CURVE ( 'NONE', #16671, #24120, #34409, .T. ) ;
#22139=EDGE_CURVE ( 'NONE', #15632, #16730, #15923, .T. ) ;
#22142=DIRECTION ( 'NONE',  ( -1.000000000000000000, -0.000000000000000000, -0.000000000000000000 ) ) ;
#22143=ORIENTED_EDGE ( 'NONE', *, *, #40490, .T. ) ;
#22144=EDGE_CURVE ( 'NONE', #5524, #41864, #31655, .T. ) ;
#22146=VERTEX_POINT ( 'NONE', #15500 ) ;
#22150=CIRCLE ( 'NONE', #42297, 59.00000000000000000 ) ;
#22151=ORIENTED_EDGE ( 'NONE', *, *, #496, .T. ) ;
#22164=CARTESIAN_POINT ( 'NONE',  ( 17.99999999999999645, -23.21237537461820466, 109.7700237000591414 ) ) ;
#22168=CARTESIAN_POINT ( 'NONE',  ( 17.99999999999999645, 91.65951123222582453, -71.09524597797991419 ) ) ;
#22169=DIRECTION ( 'NONE',  ( 1.000000000000000000, -0.000000000000000000, 0.000000000000000000 ) ) ;
#22172=CARTESIAN_POINT ( 'NONE',  ( 17.99999999999999645, -94.83915810436360516, -59.94836581341685644 ) ) ;
#22175=VERTEX_POINT ( 'NONE', #5639 ) ;
#22176=CARTESIAN_POINT ( 'NONE',  ( 17.99999999999999645, 3.996885678774600326, -120.4346956066681713 ) ) ;
#22179=ORIENTED_EDGE ( 'NONE', *, *, #24683, .F. ) ;
#22181=EDGE_LOOP ( 'NONE', ( #3273, #7353, #10751, #12112 ) ) ;
#22183=CIRCLE ( 'NONE', #29133, 58.99999999999998579 ) ;
#22184=CIRCLE ( 'NONE', #13098, 116.0000000000000000 ) ;
#22186=VERTEX_POINT ( 'NONE', #42056 ) ;
#22187=AXIS2_PLACEMENT_3D ( 'NONE', #6149, #15367, #19495 ) ;
#22189=ADVANCED_FACE ( 'NONE', ( #19841 ), #583, .F. ) ;
#22190=VECTOR ( 'NONE', #32787, 1000.000000000000000 ) ;
#22191=DIRECTION ( 'NONE',  ( 0.000000000000000000, -0.8477344278896755680, 0.5304209081197350795 ) ) ;
#22195=VERTEX_POINT ( 'NONE', #36813 ) ;
#22197=ORIENTED_EDGE ( 'NONE', *, *, #29497, .T. ) ;
#22200=CARTESIAN_POINT ( 'NONE',  ( 0.000000000000000000, 79.18387647320879807, -84.76976882518680156 ) ) ;
#22205=EDGE_LOOP ( 'NONE', ( #16691, #10373, #30989, #33925 ) ) ;
#22206=ADVANCED_FACE ( 'NONE', ( #20712 ), #20278, .F. ) ;
#22208=EDGE_CURVE ( 'NONE', #25826, #6975, #4436, .T. ) ;
#22209=ORIENTED_EDGE ( 'NONE', *, *, #15410, .F. ) ;
#22211=DIRECTION ( 'NONE',  ( 0.000000000000000000, 0.000000000000000000, 1.000000000000000000 ) ) ;
#22218=CIRCLE ( 'NONE', #38882, 116.0000000000000000 ) ;
#22219=ORIENTED_EDGE ( 'NONE', *, *, #9446, .T. ) ;
#22222=VERTEX_POINT ( 'NONE', #136 ) ;
#22223=CIRCLE ( 'NONE', #10340, 120.5010000000000332 ) ;
#22224=CARTESIAN_POINT ( 'NONE',  ( 0.000000000000000000, 23.21237537461889389, -109.7700237000589709 ) ) ;
#22225=AXIS2_PLACEMENT_3D ( 'NONE', #18203, #37992, #21689 ) ;
#22236=CARTESIAN_POINT ( 'NONE',  ( 17.99999999999999645, 0.000000000000000000, 0.000000000000000000 ) ) ;
#22237=ORIENTED_EDGE ( 'NONE', *, *, #18450, .T. ) ;
#22238=EDGE_LOOP ( 'NONE', ( #33932, #23031, #33470, #4943 ) ) ;
#22242=CARTESIAN_POINT ( 'NONE',  ( 17.99999999999999645, 35.54274411428057334, 115.1399337407607959 ) ) ;
#22243=AXIS2_PLACEMENT_3D ( 'NONE', #16850, #9624, #26639 ) ;
#22244=AXIS2_PLACEMENT_3D ( 'NONE', #17707, #37939, #30977 ) ;
#22245=DIRECTION ( 'NONE',  ( 1.000000000000000000, 0.000000000000000000, 0.000000000000000000 ) ) ;
#22246=ADVANCED_FACE ( 'NONE', ( #43138 ), #26791, .F. ) ;
#22247=DIRECTION ( 'NONE',  ( 1.000000000000000000, -0.000000000000000000, -0.000000000000000000 ) ) ;
#22256=ORIENTED_EDGE ( 'NONE', *, *, #19929, .T. ) ;
#22259=EDGE_CURVE ( 'NONE', #36059, #10415, #37242, .T. ) ;
#22262=EDGE_CURVE ( 'NONE', #10364, #19109, #17440, .T. ) ;
#22267=ORIENTED_EDGE ( 'NONE', *, *, #7104, .F. ) ;
#22274=ORIENTED_EDGE ( 'NONE', *, *, #25485, .F. ) ;
#22283=CARTESIAN_POINT ( 'NONE',  ( 0.000000000000000000, 41.60679253225906393, -108.2814610871942165 ) ) ;
#22284=VERTEX_POINT ( 'NONE', #36372 ) ;
#22288=DIRECTION ( 'NONE',  ( 0.000000000000000000, 0.5528000653611945259, -0.8333139190825142872 ) ) ;
#22289=LINE ( 'NONE', #41875, #15152 ) ;
#22290=LINE ( 'NONE', #1520, #42783 ) ;
#22292=ORIENTED_EDGE ( 'NONE', *, *, #5575, .T. ) ;
#22295=DIRECTION ( 'NONE',  ( -1.000000000000000000, -0.000000000000000000, -0.000000000000000000 ) ) ;
#22296=AXIS2_PLACEMENT_3D ( 'NONE', #12753, #39321, #9459 ) ;
#22299=CYLINDRICAL_SURFACE ( 'NONE', #35025, 58.99999999999999289 ) ;
#22300=DIRECTION ( 'NONE',  ( -1.000000000000000000, -0.000000000000000000, -0.000000000000000000 ) ) ;
#22304=EDGE_CURVE ( 'NONE', #4569, #29068, #41409, .T. ) ;
#22309=ADVANCED_FACE ( 'NONE', ( #16790 ), #7354, .F. ) ;
#22311=EDGE_CURVE ( 'NONE', #40032, #25931, #30076, .T. ) ;
#22313=CARTESIAN_POINT ( 'NONE',  ( 0.000000000000000000, 0.000000000000000000, 0.000000000000000000 ) ) ;
#22317=ORIENTED_EDGE ( 'NONE', *, *, #36013, .F. ) ;
#22320=DIRECTION ( 'NONE',  ( 1.000000000000000000, 0.000000000000000000, 0.000000000000000000 ) ) ;
#22321=AXIS2_PLACEMENT_3D ( 'NONE', #3158, #16097, #29396 ) ;
#22322=DIRECTION ( 'NONE',  ( 0.000000000000000000, 0.000000000000000000, 1.000000000000000000 ) ) ;
#22324=ORIENTED_EDGE ( 'NONE', *, *, #8906, .T. ) ;
#22329=ORIENTED_EDGE ( 'NONE', *, *, #6756, .F. ) ;
#22331=ORIENTED_EDGE ( 'NONE', *, *, #24308, .F. ) ;
#22332=EDGE_LOOP ( 'NONE', ( #22209, #23064, #15510, #18515 ) ) ;
#22338=ORIENTED_EDGE ( 'NONE', *, *, #42405, .F. ) ;
#22345=DIRECTION ( 'NONE',  ( -1.000000000000000000, 0.000000000000000000, 0.000000000000000000 ) ) ;
#22349=EDGE_CURVE ( 'NONE', #33209, #35721, #25422, .T. ) ;
#22351=VERTEX_POINT ( 'NONE', #4737 ) ;
#22352=DIRECTION ( 'NONE',  ( -1.000000000000000000, 0.000000000000000000, 0.000000000000000000 ) ) ;
#22354=EDGE_CURVE ( 'NONE', #42436, #5524, #30287, .T. ) ;
#22356=FACE_OUTER_BOUND ( 'NONE', #250, .T. ) ;
#22361=VERTEX_POINT ( 'NONE', #31364 ) ;
#22364=DIRECTION ( 'NONE',  ( 0.000000000000000000, 0.000000000000000000, 1.000000000000000000 ) ) ;
#22365=CARTESIAN_POINT ( 'NONE',  ( 17.99999999999999645, 63.55543939553896848, -97.03971415477259654 ) ) ;
#22366=CARTESIAN_POINT ( 'NONE',  ( 17.99999999999999645, -27.83061035787034498, 117.2431154827796576 ) ) ;
#22367=DIRECTION ( 'NONE',  ( 0.000000000000000000, 0.000000000000000000, 1.000000000000000000 ) ) ;
#22368=VERTEX_POINT ( 'NONE', #41592 ) ;
#22370=ORIENTED_EDGE ( 'NONE', *, *, #15658, .F. ) ;
#22371=DIRECTION ( 'NONE',  ( -1.000000000000000000, -0.000000000000000000, 0.000000000000000000 ) ) ;
#22372=CARTESIAN_POINT ( 'NONE',  ( 17.99999999999999645, -89.07460286905904923, 81.15544420874930154 ) ) ;
#22373=EDGE_CURVE ( 'NONE', #6418, #9950, #26120, .T. ) ;
#22375=EDGE_CURVE ( 'NONE', #10415, #3709, #18493, .T. ) ;
#22377=EDGE_CURVE ( 'NONE', #508, #5301, #24748, .T. ) ;
#22378=EDGE_CURVE ( 'NONE', #32231, #41864, #42797, .T. ) ;
#22379=CYLINDRICAL_SURFACE ( 'NONE', #26857, 120.5010000000000190 ) ;
#22382=ORIENTED_EDGE ( 'NONE', *, *, #12200, .T. ) ;
#22383=AXIS2_PLACEMENT_3D ( 'NONE', #34422, #15276, #11982 ) ;
#22386=ORIENTED_EDGE ( 'NONE', *, *, #14195, .F. ) ;
#22392=EDGE_LOOP ( 'NONE', ( #27402, #32366, #4129, #41057 ) ) ;
#22393=DIRECTION ( 'NONE',  ( 0.000000000000000000, 0.000000000000000000, 1.000000000000000000 ) ) ;
#22399=CARTESIAN_POINT ( 'NONE',  ( 17.99999999999999645, 103.5682682299982673, 43.14958040911701431 ) ) ;
#22400=DIRECTION ( 'NONE',  ( 0.000000000000000000, 0.3140767120219495334, -0.9493976084683810601 ) ) ;
#22401=DIRECTION ( 'NONE',  ( -1.000000000000000000, -0.000000000000000000, -0.000000000000000000 ) ) ;
#22402=ORIENTED_EDGE ( 'NONE', *, *, #40787, .F. ) ;
#22403=CARTESIAN_POINT ( 'NONE',  ( 0.000000000000000000, 101.8011932243948081, 55.61040422519366189 ) ) ;
#22411=AXIS2_PLACEMENT_3D ( 'NONE', #24820, #1206, #40906 ) ;
#22412=VECTOR ( 'NONE', #12916, 1000.000000000000000 ) ;
#22414=DIRECTION ( 'NONE',  ( 0.000000000000000000, 0.000000000000000000, 1.000000000000000000 ) ) ;
#22415=DIRECTION ( 'NONE',  ( 1.000000000000000000, 0.000000000000000000, 0.000000000000000000 ) ) ;
#22418=AXIS2_PLACEMENT_3D ( 'NONE', #32640, #2715, #2090 ) ;
#22420=VERTEX_POINT ( 'NONE', #21800 ) ;
#22421=FACE_OUTER_BOUND ( 'NONE', #24239, .T. ) ;
#22424=DIRECTION ( 'NONE',  ( 1.000000000000000000, 0.000000000000000000, 0.000000000000000000 ) ) ;
#22425=DIRECTION ( 'NONE',  ( 1.000000000000000000, -0.000000000000000000, -0.000000000000000000 ) ) ;
#22427=EDGE_CURVE ( 'NONE', #5856, #35004, #37462, .T. ) ;
#22429=DIRECTION ( 'NONE',  ( 0.000000000000000000, 0.000000000000000000, 1.000000000000000000 ) ) ;
#22431=LINE ( 'NONE', #32210, #6356 ) ;
#22434=AXIS2_PLACEMENT_3D ( 'NONE', #12894, #15752, #2812 ) ;
#22436=EDGE_LOOP ( 'NONE', ( #2859, #39689, #24033, #40188 ) ) ;
#22438=CARTESIAN_POINT ( 'NONE',  ( 17.99999999999999645, 107.2703412112699368, -32.88383143828351507 ) ) ;
#22439=EDGE_CURVE ( 'NONE', #21953, #42630, #4952, .T. ) ;
#22440=DIRECTION ( 'NONE',  ( 0.000000000000000000, -0.5963673585385078635, 0.8027116379309588989 ) ) ;
#22445=CARTESIAN_POINT ( 'NONE',  ( 17.99999999999999645, -119.0898412705475522, 18.38751498043690802 ) ) ;
#22447=CYLINDRICAL_SURFACE ( 'NONE', #6262, 116.0000000000000000 ) ;
#22448=CIRCLE ( 'NONE', #3532, 116.0000000000000000 ) ;
#22450=DIRECTION ( 'NONE',  ( -1.000000000000000000, 0.000000000000000000, 0.000000000000000000 ) ) ;
#22452=DIRECTION ( 'NONE',  ( -1.000000000000000000, 0.000000000000000000, 0.000000000000000000 ) ) ;
#22453=VERTEX_POINT ( 'NONE', #1663 ) ;
#22454=DIRECTION ( 'NONE',  ( -1.000000000000000000, -0.000000000000000000, 0.000000000000000000 ) ) ;
#22457=DIRECTION ( 'NONE',  ( 1.000000000000000000, 0.000000000000000000, 0.000000000000000000 ) ) ;
#22458=DIRECTION ( 'NONE',  ( 0.000000000000000000, 0.000000000000000000, 1.000000000000000000 ) ) ;
#22460=ORIENTED_EDGE ( 'NONE', *, *, #6317, .F. ) ;
#22472=ORIENTED_EDGE ( 'NONE', *, *, #32672, .F. ) ;
#22479=DIRECTION ( 'NONE',  ( -1.000000000000000000, -0.000000000000000000, -0.000000000000000000 ) ) ;
#22480=ORIENTED_EDGE ( 'NONE', *, *, #21835, .F. ) ;
#22481=EDGE_CURVE ( 'NONE', #10354, #6259, #29603, .T. ) ;
#22484=EDGE_LOOP ( 'NONE', ( #9658, #2687, #39104, #36002 ) ) ;
#22488=EDGE_LOOP ( 'NONE', ( #28847, #4207, #3303, #14859 ) ) ;
#22492=EDGE_CURVE ( 'NONE', #3503, #5699, #40684, .T. ) ;
#22496=CARTESIAN_POINT ( 'NONE',  ( 17.99999999999999645, 116.4607004671428570, 30.94182036827244531 ) ) ;
#22498=EDGE_CURVE ( 'NONE', #40092, #21299, #9367, .T. ) ;
#22501=ORIENTED_EDGE ( 'NONE', *, *, #3326, .F. ) ;
#22504=VERTEX_POINT ( 'NONE', #15867 ) ;
#22505=VECTOR ( 'NONE', #16444, 1000.000000000000000 ) ;
#22506=CARTESIAN_POINT ( 'NONE',  ( 0.000000000000000000, -74.56001736500675747, 88.86396238369010803 ) ) ;
#22509=AXIS2_PLACEMENT_3D ( 'NONE', #17665, #23336, #10872 ) ;
#22515=ADVANCED_FACE ( 'NONE', ( #42643 ), #42221, .F. ) ;
#22516=AXIS2_PLACEMENT_3D ( 'NONE', #24704, #18386, #24495 ) ;
#22517=ORIENTED_EDGE ( 'NONE', *, *, #10143, .F. ) ;
#22520=ORIENTED_EDGE ( 'NONE', *, *, #29074, .F. ) ;
#22523=DIRECTION ( 'NONE',  ( -1.000000000000000000, 0.000000000000000000, -0.000000000000000000 ) ) ;
#22528=AXIS2_PLACEMENT_3D ( 'NONE', #18778, #25729, #39187 ) ;
#22533=ORIENTED_EDGE ( 'NONE', *, *, #22262, .T. ) ;
#22536=AXIS2_PLACEMENT_3D ( 'NONE', #2296, #19584, #36328 ) ;
#22537=ORIENTED_EDGE ( 'NONE', *, *, #9519, .T. ) ;
#22539=VERTEX_POINT ( 'NONE', #25903 ) ;
#22543=CYLINDRICAL_SURFACE ( 'NONE', #5562, 116.0000000000000000 ) ;
#22548=CARTESIAN_POINT ( 'NONE',  ( 17.99999999999999645, 0.000000000000000000, 0.000000000000000000 ) ) ;
#22550=DIRECTION ( 'NONE',  ( -1.000000000000000000, 0.000000000000000000, 0.000000000000000000 ) ) ;
#22554=DIRECTION ( 'NONE',  ( 0.000000000000000000, 0.6783118362696172188, -0.7347741508630661889 ) ) ;
#22556=ORIENTED_EDGE ( 'NONE', *, *, #2775, .F. ) ;
#22559=EDGE_CURVE ( 'NONE', #10188, #12185, #28893, .T. ) ;
#22564=ORIENTED_EDGE ( 'NONE', *, *, #3083, .T. ) ;
#22567=AXIS2_PLACEMENT_3D ( 'NONE', #6898, #16317, #29620 ) ;
#22569=ORIENTED_EDGE ( 'NONE', *, *, #2844, .F. ) ;
#22571=CARTESIAN_POINT ( 'NONE',  ( 17.99999999999999645, -111.2559044912522950, -32.83479428644788811 ) ) ;
#22574=DIRECTION ( 'NONE',  ( -1.000000000000000000, 0.000000000000000000, 0.000000000000000000 ) ) ;
#22575=AXIS2_PLACEMENT_3D ( 'NONE', #1076, #855, #10935 ) ;
#22577=EDGE_CURVE ( 'NONE', #33525, #16679, #18527, .T. ) ;
#22578=CARTESIAN_POINT ( 'NONE',  ( 0.000000000000000000, 84.09610293794069946, 74.27057253243037849 ) ) ;
#22583=FACE_OUTER_BOUND ( 'NONE', #21522, .T. ) ;
#22585=DIRECTION ( 'NONE',  ( 0.000000000000000000, 0.000000000000000000, 1.000000000000000000 ) ) ;
#22592=EDGE_CURVE ( 'NONE', #23588, #23398, #20590, .T. ) ;
#22593=AXIS2_PLACEMENT_3D ( 'NONE', #6526, #23371, #3244 ) ;
#22599=ORIENTED_EDGE ( 'NONE', *, *, #23210, .T. ) ;
#22604=VECTOR ( 'NONE', #14780, 1000.000000000000000 ) ;
#22606=DIRECTION ( 'NONE',  ( 0.000000000000000000, 0.000000000000000000, -1.000000000000000000 ) ) ;
#22607=DIRECTION ( 'NONE',  ( -1.000000000000000000, 0.000000000000000000, 0.000000000000000000 ) ) ;
#22608=DIRECTION ( 'NONE',  ( -1.000000000000000000, 0.000000000000000000, 0.000000000000000000 ) ) ;
#22611=VECTOR ( 'NONE', #23441, 1000.000000000000000 ) ;
#22614=VECTOR ( 'NONE', #11027, 1000.000000000000000 ) ;
#22615=CYLINDRICAL_SURFACE ( 'NONE', #35835, 120.5010000000000190 ) ;
#22618=EDGE_CURVE ( 'NONE', #23414, #39824, #30999, .T. ) ;
#22624=CARTESIAN_POINT ( 'NONE',  ( 17.99999999999999645, 0.000000000000000000, 0.000000000000000000 ) ) ;
#22633=VERTEX_POINT ( 'NONE', #42008 ) ;
#22636=LINE ( 'NONE', #6012, #3269 ) ;
#22643=EDGE_CURVE ( 'NONE', #8344, #29115, #19197, .T. ) ;
#22648=ADVANCED_FACE ( 'NONE', ( #26325 ), #33697, .F. ) ;
#22649=DIRECTION ( 'NONE',  ( -1.000000000000000000, -0.000000000000000000, -0.000000000000000000 ) ) ;
#22655=FACE_OUTER_BOUND ( 'NONE', #21674, .T. ) ;
#22662=CARTESIAN_POINT ( 'NONE',  ( 17.99999999999999645, 117.6086855750638165, -26.24286718911983485 ) ) ;
#22663=CIRCLE ( 'NONE', #7982, 120.5010000000000332 ) ;
#22665=DIRECTION ( 'NONE',  ( 0.000000000000000000, 0.000000000000000000, 1.000000000000000000 ) ) ;
#22670=EDGE_CURVE ( 'NONE', #5275, #24485, #36971, .T. ) ;
#22672=EDGE_CURVE ( 'NONE', #16283, #26598, #13233, .T. ) ;
#22682=VECTOR ( 'NONE', #33050, 1000.000000000000000 ) ;
#22684=LINE ( 'NONE', #13072, #21392 ) ;
#22688=DIRECTION ( 'NONE',  ( 0.000000000000000000, 0.000000000000000000, 1.000000000000000000 ) ) ;
#22689=ORIENTED_EDGE ( 'NONE', *, *, #5477, .F. ) ;
#22690=CARTESIAN_POINT ( 'NONE',  ( 17.99999999999999645, 0.000000000000000000, 0.000000000000000000 ) ) ;
#22691=CARTESIAN_POINT ( 'NONE',  ( 17.99999999999999645, -15.21076497709792008, 119.5371223922154797 ) ) ;
#22697=CARTESIAN_POINT ( 'NONE',  ( 0.000000000000000000, 0.000000000000000000, 0.000000000000000000 ) ) ;
#22699=CIRCLE ( 'NONE', #24794, 120.5010000000000332 ) ;
#22701=CIRCLE ( 'NONE', #14337, 59.00000000000000711 ) ;
#22704=VECTOR ( 'NONE', #16116, 1000.000000000000000 ) ;
#22705=VERTEX_POINT ( 'NONE', #23275 ) ;
#22711=LINE ( 'NONE', #29237, #36503 ) ;
#22712=CARTESIAN_POINT ( 'NONE',  ( 0.000000000000000000, 0.000000000000000000, 0.000000000000000000 ) ) ;
#22715=CIRCLE ( 'NONE', #12235, 58.99999999999998579 ) ;
#22718=VERTEX_POINT ( 'NONE', #16945 ) ;
#22730=EDGE_CURVE ( 'NONE', #5856, #14037, #32393, .T. ) ;
#22732=DIRECTION ( 'NONE',  ( 1.000000000000000000, 0.000000000000000000, 0.000000000000000000 ) ) ;
#22734=CYLINDRICAL_SURFACE ( 'NONE', #34687, 59.00000000000000000 ) ;
#22735=EDGE_CURVE ( 'NONE', #25826, #1540, #24076, .T. ) ;
#22736=DIRECTION ( 'NONE',  ( 0.000000000000000000, 0.000000000000000000, 1.000000000000000000 ) ) ;
#22738=CIRCLE ( 'NONE', #28318, 116.0000000000000000 ) ;
#22741=LINE ( 'NONE', #1774, #14627 ) ;
#22742=DIRECTION ( 'NONE',  ( 0.000000000000000000, 0.000000000000000000, 1.000000000000000000 ) ) ;
#22743=ORIENTED_EDGE ( 'NONE', *, *, #14195, .T. ) ;
#22747=DIRECTION ( 'NONE',  ( 1.000000000000000000, 0.000000000000000000, 0.000000000000000000 ) ) ;
#22749=EDGE_CURVE ( 'NONE', #34617, #39340, #7082, .T. ) ;
#22750=ORIENTED_EDGE ( 'NONE', *, *, #32769, .T. ) ;
#22751=DIRECTION ( 'NONE',  ( 1.000000000000000000, 0.000000000000000000, 0.000000000000000000 ) ) ;
#22753=ORIENTED_EDGE ( 'NONE', *, *, #24247, .T. ) ;
#22754=DIRECTION ( 'NONE',  ( -1.000000000000000000, -0.000000000000000000, -0.000000000000000000 ) ) ;
#22756=DIRECTION ( 'NONE',  ( 0.000000000000000000, 0.000000000000000000, 1.000000000000000000 ) ) ;
#22757=VECTOR ( 'NONE', #36839, 1000.000000000000000 ) ;
#22763=CARTESIAN_POINT ( 'NONE',  ( 0.000000000000000000, -30.01658535635337444, 108.1077105353196970 ) ) ;
#22765=DIRECTION ( 'NONE',  ( 0.000000000000000000, 0.3641605752528229711, -0.9313361774523382097 ) ) ;
#22766=CARTESIAN_POINT ( 'NONE',  ( 0.000000000000000000, 115.5737863835463628, -9.934782381632540904 ) ) ;
#22767=DIRECTION ( 'NONE',  ( 0.000000000000000000, 0.000000000000000000, 1.000000000000000000 ) ) ;
#22770=FACE_OUTER_BOUND ( 'NONE', #21436, .T. ) ;
#22777=DIRECTION ( 'NONE',  ( 0.000000000000000000, -0.9826841245925190815, -0.1852887240871243513 ) ) ;
#22778=DIRECTION ( 'NONE',  ( 0.000000000000000000, 0.000000000000000000, 1.000000000000000000 ) ) ;
#22780=AXIS2_PLACEMENT_3D ( 'NONE', #26083, #39573, #16058 ) ;
#22788=EDGE_CURVE ( 'NONE', #40762, #16567, #39594, .T. ) ;
#22790=VECTOR ( 'NONE', #16285, 1000.000000000000000 ) ;
#22792=CIRCLE ( 'NONE', #11631, 120.5010000000000190 ) ;
#22793=CIRCLE ( 'NONE', #39459, 116.0000000000000000 ) ;
#22795=CIRCLE ( 'NONE', #11634, 116.0000000000000000 ) ;
#22796=DIRECTION ( 'NONE',  ( 0.000000000000000000, 0.05322217484217877520, -0.9985826956767620555 ) ) ;
#22799=EDGE_LOOP ( 'NONE', ( #41984, #34612, #22151, #40779 ) ) ;
#22800=CYLINDRICAL_SURFACE ( 'NONE', #24329, 120.5010000000000190 ) ;
#22804=DIRECTION ( 'NONE',  ( -1.000000000000000000, 0.000000000000000000, -0.000000000000000000 ) ) ;
#22806=VERTEX_POINT ( 'NONE', #19574 ) ;
#22807=DIRECTION ( 'NONE',  ( -1.000000000000000000, 0.000000000000000000, 0.000000000000000000 ) ) ;
#22809=DIRECTION ( 'NONE',  ( 1.000000000000000000, 0.000000000000000000, 0.000000000000000000 ) ) ;
#22813=CYLINDRICAL_SURFACE ( 'NONE', #24381, 120.5010000000000190 ) ;
#22815=CIRCLE ( 'NONE', #18664, 116.0000000000000000 ) ;
#22817=VERTEX_POINT ( 'NONE', #36318 ) ;
#22819=CARTESIAN_POINT ( 'NONE',  ( 17.99999999999999645, 0.000000000000000000, 0.000000000000000000 ) ) ;
#22825=AXIS2_PLACEMENT_3D ( 'NONE', #23492, #23707, #37401 ) ;
#22826=DIRECTION ( 'NONE',  ( 1.000000000000000000, 0.000000000000000000, 0.000000000000000000 ) ) ;
#22827=CARTESIAN_POINT ( 'NONE',  ( 17.99999999999999645, 59.07817985939002625, 105.0250430397510968 ) ) ;
#22828=DIRECTION ( 'NONE',  ( 0.000000000000000000, 0.000000000000000000, 1.000000000000000000 ) ) ;
#22830=DIRECTION ( 'NONE',  ( 1.000000000000000000, 0.000000000000000000, 0.000000000000000000 ) ) ;
#22833=ORIENTED_EDGE ( 'NONE', *, *, #23993, .F. ) ;
#22835=VECTOR ( 'NONE', #20585, 1000.000000000000000 ) ;
#22836=CARTESIAN_POINT ( 'NONE',  ( 0.000000000000000000, 111.1352304691227744, 15.40237066878635730 ) ) ;
#22840=DIRECTION ( 'NONE',  ( 0.000000000000000000, 0.000000000000000000, 1.000000000000000000 ) ) ;
#22841=CARTESIAN_POINT ( 'NONE',  ( 0.000000000000000000, 0.000000000000000000, 0.000000000000000000 ) ) ;
#22846=EDGE_CURVE ( 'NONE', #25771, #40772, #14099, .T. ) ;
#22850=EDGE_CURVE ( 'NONE', #24053, #10364, #33067, .T. ) ;
#22851=LINE ( 'NONE', #39150, #41565 ) ;
#22859=CARTESIAN_POINT ( 'NONE',  ( 17.99999999999999645, 0.000000000000000000, 0.000000000000000000 ) ) ;
#22860=VECTOR ( 'NONE', #20597, 1000.000000000000000 ) ;
#22863=ORIENTED_EDGE ( 'NONE', *, *, #27106, .F. ) ;
#22865=VECTOR ( 'NONE', #24517, 1000.000000000000000 ) ;
#22869=VECTOR ( 'NONE', #24581, 1000.000000000000000 ) ;
#22871=ORIENTED_EDGE ( 'NONE', *, *, #37739, .F. ) ;
#22872=EDGE_CURVE ( 'NONE', #32977, #14493, #31717, .T. ) ;
#22874=ADVANCED_FACE ( 'NONE', ( #33924 ), #21539, .F. ) ;
#22876=VECTOR ( 'NONE', #32994, 1000.000000000000000 ) ;
#22878=ADVANCED_FACE ( 'NONE', ( #41091 ), #38055, .F. ) ;
#22881=ORIENTED_EDGE ( 'NONE', *, *, #8850, .T. ) ;
#22883=CARTESIAN_POINT ( 'NONE',  ( 0.000000000000000000, -37.07968990261553444, 109.9140418541956308 ) ) ;
#22885=DIRECTION ( 'NONE',  ( 0.000000000000000000, -4.539683130352864453E-14, -1.000000000000000000 ) ) ;
#22887=CIRCLE ( 'NONE', #33985, 59.00000000000000000 ) ;
#22889=CARTESIAN_POINT ( 'NONE',  ( 0.000000000000000000, -40.13512380274045199, 113.6206972269520179 ) ) ;
#22893=CARTESIAN_POINT ( 'NONE',  ( 17.99999999999999645, 99.97660604679964536, 67.26937820704921478 ) ) ;
#22894=CYLINDRICAL_SURFACE ( 'NONE', #11573, 116.0000000000000000 ) ;
#22898=ORIENTED_EDGE ( 'NONE', *, *, #2741, .F. ) ;
#22900=AXIS2_PLACEMENT_3D ( 'NONE', #779, #993, #34382 ) ;
#22906=CARTESIAN_POINT ( 'NONE',  ( 0.000000000000000000, 103.1672962317657323, -44.09967643725766351 ) ) ;
#22908=CIRCLE ( 'NONE', #27778, 116.0000000000000000 ) ;
#22912=ORIENTED_EDGE ( 'NONE', *, *, #33642, .F. ) ;
#22916=AXIS2_PLACEMENT_3D ( 'NONE', #29348, #5764, #32812 ) ;
#22918=EDGE_LOOP ( 'NONE', ( #20957, #2498, #1303, #24937 ) ) ;
#22919=DIRECTION ( 'NONE',  ( 0.000000000000000000, 0.8183027759081701324, -0.5747874102144052699 ) ) ;
#22923=VERTEX_POINT ( 'NONE', #11687 ) ;
#22924=EDGE_CURVE ( 'NONE', #7516, #34509, #10804, .T. ) ;
#22934=ADVANCED_FACE ( 'NONE', ( #11035 ), #17604, .F. ) ;
#22935=ORIENTED_EDGE ( 'NONE', *, *, #2094, .F. ) ;
#22939=CARTESIAN_POINT ( 'NONE',  ( 0.000000000000000000, 109.3506818544115617, -38.70953859160899668 ) ) ;
#22941=DIRECTION ( 'NONE',  ( -1.000000000000000000, 0.000000000000000000, -0.000000000000000000 ) ) ;
#22945=VERTEX_POINT ( 'NONE', #24363 ) ;
#22946=FACE_OUTER_BOUND ( 'NONE', #11139, .T. ) ;
#22948=DIRECTION ( 'NONE',  ( -1.000000000000000000, -0.000000000000000000, -0.000000000000000000 ) ) ;
#22949=CARTESIAN_POINT ( 'NONE',  ( 0.000000000000000000, -92.25992191227442163, 77.51514567967366531 ) ) ;
#22954=EDGE_LOOP ( 'NONE', ( #12976, #30114, #16910, #4015 ) ) ;
#22959=DIRECTION ( 'NONE',  ( 1.000000000000000000, 0.000000000000000000, 0.000000000000000000 ) ) ;
#22960=DIRECTION ( 'NONE',  ( -1.000000000000000000, 0.000000000000000000, -0.000000000000000000 ) ) ;
#22961=DIRECTION ( 'NONE',  ( -1.000000000000000000, 0.000000000000000000, 0.000000000000000000 ) ) ;
#22962=DIRECTION ( 'NONE',  ( -1.000000000000000000, -0.000000000000000000, -0.000000000000000000 ) ) ;
#22963=ORIENTED_EDGE ( 'NONE', *, *, #20968, .T. ) ;
#22965=DIRECTION ( 'NONE',  ( 0.000000000000000000, 3.528251137579946599E-15, -1.000000000000000000 ) ) ;
#22970=EDGE_CURVE ( 'NONE', #42093, #3574, #17139, .T. ) ;
#22972=ORIENTED_EDGE ( 'NONE', *, *, #33267, .F. ) ;
#22974=VERTEX_POINT ( 'NONE', #34348 ) ;
#22980=LINE ( 'NONE', #36879, #22412 ) ;
#22985=ORIENTED_EDGE ( 'NONE', *, *, #27032, .F. ) ;
#22988=DIRECTION ( 'NONE',  ( 1.000000000000000000, 0.000000000000000000, 0.000000000000000000 ) ) ;
#22990=CARTESIAN_POINT ( 'NONE',  ( 8.999999999999998224, -68.63002662989811142, 93.51962064069482494 ) ) ;
#22991=CARTESIAN_POINT ( 'NONE',  ( 17.99999999999999645, -78.18175027177375114, -85.69488855493077040 ) ) ;
#22996=ORIENTED_EDGE ( 'NONE', *, *, #3461, .F. ) ;
#23004=EDGE_LOOP ( 'NONE', ( #38211, #22501, #41740, #424 ) ) ;
#23015=CARTESIAN_POINT ( 'NONE',  ( 17.99999999999999645, 13.00789606333630566, -115.2683592318613819 ) ) ;
#23021=CARTESIAN_POINT ( 'NONE',  ( 0.000000000000000000, 107.1354928292875996, -44.47455650397954230 ) ) ;
#23023=EDGE_CURVE ( 'NONE', #36227, #39315, #38909, .T. ) ;
#23025=ORIENTED_EDGE ( 'NONE', *, *, #25762, .T. ) ;
#23031=ORIENTED_EDGE ( 'NONE', *, *, #18598, .F. ) ;
#23032=EDGE_CURVE ( 'NONE', #17179, #26181, #3146, .T. ) ;
#23034=ORIENTED_EDGE ( 'NONE', *, *, #26066, .F. ) ;
#23041=CARTESIAN_POINT ( 'NONE',  ( 17.99999999999999645, 0.000000000000000000, 0.000000000000000000 ) ) ;
#23042=EDGE_LOOP ( 'NONE', ( #35548, #11862, #2708, #23905 ) ) ;
#23043=CARTESIAN_POINT ( 'NONE',  ( -10.00000000000000000, 0.000000000000000000, 0.000000000000000000 ) ) ;
#23044=ORIENTED_EDGE ( 'NONE', *, *, #16474, .F. ) ;
#23047=CARTESIAN_POINT ( 'NONE',  ( 17.99999999999999645, 0.000000000000000000, 0.000000000000000000 ) ) ;
#23054=AXIS2_PLACEMENT_3D ( 'NONE', #12241, #15323, #5244 ) ;
#23056=CARTESIAN_POINT ( 'NONE',  ( 17.99999999999999645, 107.1354928292875996, -44.47455650397954230 ) ) ;
#23057=EDGE_CURVE ( 'NONE', #14617, #26000, #27586, .T. ) ;
#23058=DIRECTION ( 'NONE',  ( 1.000000000000000000, 0.000000000000000000, 0.000000000000000000 ) ) ;
#23064=ORIENTED_EDGE ( 'NONE', *, *, #8268, .F. ) ;
#23066=ORIENTED_EDGE ( 'NONE', *, *, #22354, .T. ) ;
#23073=ORIENTED_EDGE ( 'NONE', *, *, #32193, .F. ) ;
#23074=DIRECTION ( 'NONE',  ( 1.000000000000000000, -0.000000000000000000, -0.000000000000000000 ) ) ;
#23075=ADVANCED_FACE ( 'NONE', ( #38474 ), #22379, .F. ) ;
#23076=CARTESIAN_POINT ( 'NONE',  ( 17.99999999999999645, 11.41303419184972689, 111.6154788735836405 ) ) ;
#23078=DIRECTION ( 'NONE',  ( 0.000000000000000000, 0.000000000000000000, 1.000000000000000000 ) ) ;
#23079=ORIENTED_EDGE ( 'NONE', *, *, #17361, .F. ) ;
#23081=CYLINDRICAL_SURFACE ( 'NONE', #31568, 116.0000000000000000 ) ;
#23083=CYLINDRICAL_SURFACE ( 'NONE', #282, 58.99999999999999289 ) ;
#23085=ORIENTED_EDGE ( 'NONE', *, *, #5238, .F. ) ;
#23090=AXIS2_PLACEMENT_3D ( 'NONE', #6742, #33789, #21179 ) ;
#23097=CYLINDRICAL_SURFACE ( 'NONE', #39043, 120.5010000000000190 ) ;
#23100=CYLINDRICAL_SURFACE ( 'NONE', #16219, 116.0000000000000000 ) ;
#23102=AXIS2_PLACEMENT_3D ( 'NONE', #20610, #33885, #38 ) ;
#23109=VECTOR ( 'NONE', #18920, 1000.000000000000000 ) ;
#23110=EDGE_CURVE ( 'NONE', #32554, #23227, #16435, .T. ) ;
#23116=DIRECTION ( 'NONE',  ( 0.000000000000000000, -0.3140767120219556952, 0.9493976084683789507 ) ) ;
#23117=ORIENTED_EDGE ( 'NONE', *, *, #23886, .F. ) ;
#23120=DIRECTION ( 'NONE',  ( -1.000000000000000000, -0.000000000000000000, 0.000000000000000000 ) ) ;
#23123=CARTESIAN_POINT ( 'NONE',  ( 17.99999999999999645, 0.000000000000000000, 0.000000000000000000 ) ) ;
#23130=ORIENTED_EDGE ( 'NONE', *, *, #13821, .T. ) ;
#23131=DIRECTION ( 'NONE',  ( 0.000000000000000000, 0.000000000000000000, 1.000000000000000000 ) ) ;
#23134=VERTEX_POINT ( 'NONE', #29120 ) ;
#23137=DIRECTION ( 'NONE',  ( 0.000000000000000000, 0.000000000000000000, 1.000000000000000000 ) ) ;
#23138=ORIENTED_EDGE ( 'NONE', *, *, #28823, .F. ) ;
#23139=CIRCLE ( 'NONE', #36315, 120.5010000000000190 ) ;
#23142=EDGE_CURVE ( 'NONE', #16188, #36371, #13637, .T. ) ;
#23143=LINE ( 'NONE', #2992, #9358 ) ;
#23145=ORIENTED_EDGE ( 'NONE', *, *, #3528, .T. ) ;
#23147=VERTEX_POINT ( 'NONE', #33438 ) ;
#23148=DIRECTION ( 'NONE',  ( 0.000000000000000000, 0.8747630845319590565, 0.4845508703326540934 ) ) ;
#23149=DIRECTION ( 'NONE',  ( 0.000000000000000000, 0.000000000000000000, 1.000000000000000000 ) ) ;
#23151=CARTESIAN_POINT ( 'NONE',  ( 17.99999999999999645, 64.58410930313661424, -101.7319213743675732 ) ) ;
#23152=CARTESIAN_POINT ( 'NONE',  ( 0.000000000000000000, -56.51398178981889941, 96.92493144647428949 ) ) ;
#23153=DIRECTION ( 'NONE',  ( 1.000000000000000000, 0.000000000000000000, 0.000000000000000000 ) ) ;
#23159=ORIENTED_EDGE ( 'NONE', *, *, #26985, .T. ) ;
#23161=EDGE_CURVE ( 'NONE', #11572, #10180, #28959, .T. ) ;
#23162=EDGE_CURVE ( 'NONE', #39096, #22718, #17831, .T. ) ;
#23170=EDGE_LOOP ( 'NONE', ( #12912, #2953, #30181, #14120 ) ) ;
#23174=ORIENTED_EDGE ( 'NONE', *, *, #11125, .T. ) ;
#23176=CARTESIAN_POINT ( 'NONE',  ( 9.000000000000001776, -13.00789606333398218, -115.2683592318616235 ) ) ;
#23177=ORIENTED_EDGE ( 'NONE', *, *, #3351, .T. ) ;
#23181=CIRCLE ( 'NONE', #28751, 116.0000000000000000 ) ;
#23184=CIRCLE ( 'NONE', #8512, 116.0000000000000000 ) ;
#23193=AXIS2_PLACEMENT_3D ( 'NONE', #35123, #41229, #21014 ) ;
#23194=DIRECTION ( 'NONE',  ( 0.000000000000000000, -0.1062934856473523454, -0.9943348002101385363 ) ) ;
#23195=CYLINDRICAL_SURFACE ( 'NONE', #105, 59.00000000000000000 ) ;
#23197=CARTESIAN_POINT ( 'NONE',  ( -10.00000000000000000, 0.000000000000000000, 0.000000000000000000 ) ) ;
#23202=FACE_OUTER_BOUND ( 'NONE', #32348, .T. ) ;
#23203=CARTESIAN_POINT ( 'NONE',  ( 17.99999999999999645, -110.3490479609630910, -20.28201389785511211 ) ) ;
#23205=EDGE_CURVE ( 'NONE', #34831, #14426, #2431, .T. ) ;
#23210=EDGE_CURVE ( 'NONE', #12319, #15523, #22715, .T. ) ;
#23211=AXIS2_PLACEMENT_3D ( 'NONE', #21826, #18551, #42467 ) ;
#23212=ORIENTED_EDGE ( 'NONE', *, *, #5461, .F. ) ;
#23216=VECTOR ( 'NONE', #6286, 1000.000000000000000 ) ;
#23218=DIRECTION ( 'NONE',  ( 0.000000000000000000, -0.9996456111234522934, -0.02662052143778445915 ) ) ;
#23219=DIRECTION ( 'NONE',  ( 0.000000000000000000, 0.000000000000000000, 1.000000000000000000 ) ) ;
#23222=VERTEX_POINT ( 'NONE', #25 ) ;
#23223=DIRECTION ( 'NONE',  ( -1.000000000000000000, -0.000000000000000000, 0.000000000000000000 ) ) ;
#23224=AXIS2_PLACEMENT_3D ( 'NONE', #27925, #34219, #14618 ) ;
#23226=EDGE_CURVE ( 'NONE', #34279, #29542, #473, .T. ) ;
#23227=VERTEX_POINT ( 'NONE', #26051 ) ;
#23229=FACE_OUTER_BOUND ( 'NONE', #42751, .T. ) ;
#23231=DIRECTION ( 'NONE',  ( 0.000000000000000000, 0.000000000000000000, 1.000000000000000000 ) ) ;
#23234=ORIENTED_EDGE ( 'NONE', *, *, #16757, .F. ) ;
#23235=DIRECTION ( 'NONE',  ( 0.000000000000000000, 0.4132121857683728749, 0.9106347728549155640 ) ) ;
#23238=ORIENTED_EDGE ( 'NONE', *, *, #17821, .F. ) ;
#23239=CARTESIAN_POINT ( 'NONE',  ( 0.000000000000000000, -104.2166695095716591, 60.49278301857773243 ) ) ;
#23240=ORIENTED_EDGE ( 'NONE', *, *, #18402, .F. ) ;
#23243=AXIS2_PLACEMENT_3D ( 'NONE', #34373, #30895, #4709 ) ;
#23245=CARTESIAN_POINT ( 'NONE',  ( 17.99999999999999645, 0.000000000000000000, 0.000000000000000000 ) ) ;
#23246=DIRECTION ( 'NONE',  ( 1.000000000000000000, 0.000000000000000000, 0.000000000000000000 ) ) ;
#23248=ORIENTED_EDGE ( 'NONE', *, *, #31932, .T. ) ;
#23249=CYLINDRICAL_SURFACE ( 'NONE', #24300, 59.00000000000000000 ) ;
#23251=ORIENTED_EDGE ( 'NONE', *, *, #42438, .T. ) ;
#23252=AXIS2_PLACEMENT_3D ( 'NONE', #33728, #3605, #3172 ) ;
#23255=DIRECTION ( 'NONE',  ( 0.000000000000000000, 0.000000000000000000, 1.000000000000000000 ) ) ;
#23256=FACE_OUTER_BOUND ( 'NONE', #9668, .T. ) ;
#23257=ORIENTED_EDGE ( 'NONE', *, *, #20637, .T. ) ;
#23260=ORIENTED_EDGE ( 'NONE', *, *, #2958, .F. ) ;
#23263=CARTESIAN_POINT ( 'NONE',  ( 17.99999999999999645, -15.21076497709635156, -119.5371223922156503 ) ) ;
#23264=EDGE_CURVE ( 'NONE', #23398, #25997, #6178, .T. ) ;
#23266=DIRECTION ( 'NONE',  ( -1.000000000000000000, 0.000000000000000000, 0.000000000000000000 ) ) ;
#23269=VERTEX_POINT ( 'NONE', #12960 ) ;
#23273=ADVANCED_FACE ( 'NONE', ( #39958 ), #36702, .F. ) ;
#23274=CARTESIAN_POINT ( 'NONE',  ( 17.99999999999999645, -56.51398178981757070, -96.92493144647505687 ) ) ;
#23275=CARTESIAN_POINT ( 'NONE',  ( 0.000000000000000000, -107.2885202478269946, 54.86040852957277281 ) ) ;
#23276=VERTEX_POINT ( 'NONE', #39746 ) ;
#23277=DIRECTION ( 'NONE',  ( -1.000000000000000000, 0.000000000000000000, 0.000000000000000000 ) ) ;
#23283=ORIENTED_EDGE ( 'NONE', *, *, #38288, .F. ) ;
#23285=DIRECTION ( 'NONE',  ( 0.000000000000000000, 0.000000000000000000, 1.000000000000000000 ) ) ;
#23290=CARTESIAN_POINT ( 'NONE',  ( 0.000000000000000000, 0.000000000000000000, 0.000000000000000000 ) ) ;
#23291=ADVANCED_FACE ( 'NONE', ( #23229 ), #9877, .F. ) ;
#23292=DIRECTION ( 'NONE',  ( -1.000000000000000000, -0.000000000000000000, 0.000000000000000000 ) ) ;
#23296=CIRCLE ( 'NONE', #37889, 59.00000000000000711 ) ;
#23299=DIRECTION ( 'NONE',  ( 0.000000000000000000, 0.000000000000000000, 1.000000000000000000 ) ) ;
#23301=DIRECTION ( 'NONE',  ( 0.000000000000000000, 0.000000000000000000, 1.000000000000000000 ) ) ;
#23302=DIRECTION ( 'NONE',  ( 0.000000000000000000, 0.000000000000000000, 1.000000000000000000 ) ) ;
#23313=ORIENTED_EDGE ( 'NONE', *, *, #22377, .F. ) ;
#23316=CARTESIAN_POINT ( 'NONE',  ( 17.99999999999999645, 94.52951811191651643, -67.23221107124801676 ) ) ;
#23317=EDGE_CURVE ( 'NONE', #2864, #27244, #35890, .T. ) ;
#23318=ORIENTED_EDGE ( 'NONE', *, *, #41206, .F. ) ;
#23319=EDGE_LOOP ( 'NONE', ( #42182, #9592, #35578, #25273 ) ) ;
#23321=VECTOR ( 'NONE', #4667, 1000.000000000000000 ) ;
#23322=DIRECTION ( 'NONE',  ( -1.000000000000000000, 0.000000000000000000, 0.000000000000000000 ) ) ;
#23327=EDGE_CURVE ( 'NONE', #12380, #17388, #27619, .T. ) ;
#23329=ORIENTED_EDGE ( 'NONE', *, *, #24194, .F. ) ;
#23335=CARTESIAN_POINT ( 'NONE',  ( 0.000000000000000000, -118.8387007424469601, -19.94628303336605768 ) ) ;
#23336=DIRECTION ( 'NONE',  ( -1.000000000000000000, -0.000000000000000000, -0.000000000000000000 ) ) ;
#23337=ORIENTED_EDGE ( 'NONE', *, *, #15713, .F. ) ;
#23338=ORIENTED_EDGE ( 'NONE', *, *, #16874, .T. ) ;
#23339=CARTESIAN_POINT ( 'NONE',  ( -10.00000000000000000, 0.000000000000000000, 0.000000000000000000 ) ) ;
#23343=FACE_OUTER_BOUND ( 'NONE', #23170, .T. ) ;
#23348=LINE ( 'NONE', #29448, #33154 ) ;
#23354=DIRECTION ( 'NONE',  ( 1.000000000000000000, -0.000000000000000000, -0.000000000000000000 ) ) ;
#23362=ORIENTED_EDGE ( 'NONE', *, *, #129, .T. ) ;
#23365=EDGE_CURVE ( 'NONE', #16031, #36814, #12262, .T. ) ;
#23368=EDGE_CURVE ( 'NONE', #37579, #8622, #22738, .T. ) ;
#23371=DIRECTION ( 'NONE',  ( 1.000000000000000000, 0.000000000000000000, 0.000000000000000000 ) ) ;
#23379=DIRECTION ( 'NONE',  ( 0.000000000000000000, 0.000000000000000000, 1.000000000000000000 ) ) ;
#23380=DIRECTION ( 'NONE',  ( -1.000000000000000000, -0.000000000000000000, -0.000000000000000000 ) ) ;
#23391=DIRECTION ( 'NONE',  ( 1.000000000000000000, 0.000000000000000000, 0.000000000000000000 ) ) ;
#23393=EDGE_CURVE ( 'NONE', #39340, #14569, #25522, .T. ) ;
#23395=ADVANCED_FACE ( 'NONE', ( #31475 ), #23869, .F. ) ;
#23396=CYLINDRICAL_SURFACE ( 'NONE', #42133, 59.00000000000000000 ) ;
#23397=FACE_OUTER_BOUND ( 'NONE', #25652, .T. ) ;
#23398=VERTEX_POINT ( 'NONE', #37132 ) ;
#23399=CYLINDRICAL_SURFACE ( 'NONE', #3589, 59.00000000000000000 ) ;
#23403=DIRECTION ( 'NONE',  ( -1.000000000000000000, -0.000000000000000000, -0.000000000000000000 ) ) ;
#23404=CARTESIAN_POINT ( 'NONE',  ( 17.99999999999999645, 0.000000000000000000, 0.000000000000000000 ) ) ;
#23407=AXIS2_PLACEMENT_3D ( 'NONE', #22906, #2754, #18989 ) ;
#23410=ORIENTED_EDGE ( 'NONE', *, *, #5858, .F. ) ;
#23412=CYLINDRICAL_SURFACE ( 'NONE', #38684, 120.5010000000000190 ) ;
#23414=VERTEX_POINT ( 'NONE', #14044 ) ;
#23416=DIRECTION ( 'NONE',  ( -1.000000000000000000, -0.000000000000000000, -0.000000000000000000 ) ) ;
#23423=DIRECTION ( 'NONE',  ( 0.000000000000000000, 0.000000000000000000, 1.000000000000000000 ) ) ;
#23424=DIRECTION ( 'NONE',  ( 0.000000000000000000, -0.8477344278896755680, 0.5304209081197351905 ) ) ;
#23428=CARTESIAN_POINT ( 'NONE',  ( 0.000000000000000000, 104.0201923570375300, 51.34003878071097660 ) ) ;
#23430=CARTESIAN_POINT ( 'NONE',  ( 17.99999999999999645, -59.07817985939071548, 105.0250430397506847 ) ) ;
#23431=DIRECTION ( 'NONE',  ( 0.000000000000000000, 0.000000000000000000, 1.000000000000000000 ) ) ;
#23436=DIRECTION ( 'NONE',  ( 0.000000000000000000, 0.8993121301712174720, 0.4373073204588591723 ) ) ;
#23437=ORIENTED_EDGE ( 'NONE', *, *, #41178, .T. ) ;
#23439=ORIENTED_EDGE ( 'NONE', *, *, #2978, .F. ) ;
#23441=DIRECTION ( 'NONE',  ( 1.000000000000000000, 0.000000000000000000, -0.000000000000000000 ) ) ;
#23442=AXIS2_PLACEMENT_3D ( 'NONE', #18296, #17643, #7988 ) ;
#23445=DIRECTION ( 'NONE',  ( 0.000000000000000000, 0.9826841245925215240, -0.1852887240871114727 ) ) ;
#23448=ORIENTED_EDGE ( 'NONE', *, *, #19512, .F. ) ;
#23449=CARTESIAN_POINT ( 'NONE',  ( 0.000000000000000000, 120.3696465864706227, 5.624871700596487223 ) ) ;
#23451=AXIS2_PLACEMENT_3D ( 'NONE', #30071, #19199, #39636 ) ;
#23453=ADVANCED_FACE ( 'NONE', ( #4176 ), #17551, .F. ) ;
#23456=CARTESIAN_POINT ( 'NONE',  ( 0.000000000000000000, 41.33768078145642022, -104.3046912715537076 ) ) ;
#23465=VERTEX_POINT ( 'NONE', #29649 ) ;
#23466=DIRECTION ( 'NONE',  ( 1.000000000000000000, 0.000000000000000000, 0.000000000000000000 ) ) ;
#23473=VERTEX_POINT ( 'NONE', #32904 ) ;
#23474=VECTOR ( 'NONE', #37257, 1000.000000000000000 ) ;
#23475=AXIS2_PLACEMENT_3D ( 'NONE', #100, #26350, #26548 ) ;
#23478=CIRCLE ( 'NONE', #4627, 116.0000000000000000 ) ;
#23481=DIRECTION ( 'NONE',  ( -1.000000000000000000, -0.000000000000000000, -0.000000000000000000 ) ) ;
#23482=CARTESIAN_POINT ( 'NONE',  ( 0.000000000000000000, 0.000000000000000000, 0.000000000000000000 ) ) ;
#23483=AXIS2_PLACEMENT_3D ( 'NONE', #4279, #13711, #27017 ) ;
#23486=VECTOR ( 'NONE', #5863, 1000.000000000000000 ) ;
#23489=ORIENTED_EDGE ( 'NONE', *, *, #35256, .F. ) ;
#23491=CIRCLE ( 'NONE', #1149, 116.0000000000000000 ) ;
#23492=CARTESIAN_POINT ( 'NONE',  ( 17.99999999999999645, 35.72777019205808813, -106.3569410558013715 ) ) ;
#23497=CARTESIAN_POINT ( 'NONE',  ( -10.00000000000000000, 0.000000000000000000, 0.000000000000000000 ) ) ;
#23498=DIRECTION ( 'NONE',  ( 0.000000000000000000, 0.000000000000000000, 1.000000000000000000 ) ) ;
#23505=DIRECTION ( 'NONE',  ( 0.000000000000000000, -0.6783118362696222148, 0.7347741508630616369 ) ) ;
#23506=ORIENTED_EDGE ( 'NONE', *, *, #72, .F. ) ;
#23511=VECTOR ( 'NONE', #21363, 1000.000000000000000 ) ;
#23512=CARTESIAN_POINT ( 'NONE',  ( -10.00000000000000000, 0.000000000000000000, 0.000000000000000000 ) ) ;
#23513=VECTOR ( 'NONE', #22169, 1000.000000000000000 ) ;
#23515=CARTESIAN_POINT ( 'NONE',  ( 0.000000000000000000, 40.13512380274121938, -113.6206972269517905 ) ) ;
#23517=CARTESIAN_POINT ( 'NONE',  ( 17.99999999999999645, 75.72520367775197769, -82.78868281115903471 ) ) ;
#23518=EDGE_CURVE ( 'NONE', #19147, #41661, #36170, .T. ) ;
#23520=ORIENTED_EDGE ( 'NONE', *, *, #34653, .F. ) ;
#23522=DIRECTION ( 'NONE',  ( -1.000000000000000000, -0.000000000000000000, 0.000000000000000000 ) ) ;
#23524=EDGE_CURVE ( 'NONE', #38496, #3709, #31065, .T. ) ;
#23527=ORIENTED_EDGE ( 'NONE', *, *, #9472, .F. ) ;
#23529=VERTEX_POINT ( 'NONE', #21692 ) ;
#23533=AXIS2_PLACEMENT_3D ( 'NONE', #4442, #41536, #17813 ) ;
#23536=DIRECTION ( 'NONE',  ( -1.000000000000000000, -0.000000000000000000, -0.000000000000000000 ) ) ;
#23537=CIRCLE ( 'NONE', #20060, 59.00000000000000711 ) ;
#23540=ORIENTED_EDGE ( 'NONE', *, *, #39654, .T. ) ;
#23541=DIRECTION ( 'NONE',  ( 0.000000000000000000, 0.4610925014493206242, 0.8873520750565743187 ) ) ;
#23542=CIRCLE ( 'NONE', #41634, 58.99999999999998579 ) ;
#23544=DIRECTION ( 'NONE',  ( -1.000000000000000000, -0.000000000000000000, -0.000000000000000000 ) ) ;
#23546=CARTESIAN_POINT ( 'NONE',  ( 0.000000000000000000, -105.3681574666266414, 38.54638589714855357 ) ) ;
#23547=VERTEX_POINT ( 'NONE', #34946 ) ;
#23548=DIRECTION ( 'NONE',  ( -1.000000000000000000, 0.000000000000000000, -0.000000000000000000 ) ) ;
#23549=ORIENTED_EDGE ( 'NONE', *, *, #18536, .T. ) ;
#23552=CARTESIAN_POINT ( 'NONE',  ( 17.99999999999999645, 99.97660604679964536, 67.26937820704921478 ) ) ;
#23556=EDGE_CURVE ( 'NONE', #39267, #32325, #14388, .T. ) ;
#23559=DIRECTION ( 'NONE',  ( 0.000000000000000000, -0.5528000653612000770, 0.8333139190825106235 ) ) ;
#23561=FACE_OUTER_BOUND ( 'NONE', #22122, .T. ) ;
#23562=EDGE_LOOP ( 'NONE', ( #15392, #8817, #29975, #1635 ) ) ;
#23564=DIRECTION ( 'NONE',  ( -1.000000000000000000, -0.000000000000000000, -0.000000000000000000 ) ) ;
#23566=AXIS2_PLACEMENT_3D ( 'NONE', #6386, #3520, #3311 ) ;
#23568=DIRECTION ( 'NONE',  ( 0.000000000000000000, -9.408669700213191589E-16, -1.000000000000000000 ) ) ;
#23570=VECTOR ( 'NONE', #620, 1000.000000000000000 ) ;
#23572=CARTESIAN_POINT ( 'NONE',  ( 17.99999999999999645, -114.1529630473452386, 38.59523323561398200 ) ) ;
#23575=AXIS2_PLACEMENT_3D ( 'NONE', #27757, #11163, #869 ) ;
#23577=DIRECTION ( 'NONE',  ( 1.000000000000000000, 0.000000000000000000, 0.000000000000000000 ) ) ;
#23578=ADVANCED_FACE ( 'NONE', ( #42496 ), #6490, .F. ) ;
#23583=DIRECTION ( 'NONE',  ( 1.000000000000000000, 0.000000000000000000, 0.000000000000000000 ) ) ;
#23588=VERTEX_POINT ( 'NONE', #14910 ) ;
#23591=EDGE_CURVE ( 'NONE', #8918, #25725, #40091, .T. ) ;
#23594=CYLINDRICAL_SURFACE ( 'NONE', #27738, 120.5010000000000190 ) ;
#23597=AXIS2_PLACEMENT_3D ( 'NONE', #12482, #25373, #38851 ) ;
#23599=DIRECTION ( 'NONE',  ( 1.000000000000000000, 0.000000000000000000, 0.000000000000000000 ) ) ;
#23601=AXIS2_PLACEMENT_3D ( 'NONE', #35935, #32466, #6065 ) ;
#23602=AXIS2_PLACEMENT_3D ( 'NONE', #2913, #12572, #36516 ) ;
#23605=AXIS2_PLACEMENT_3D ( 'NONE', #36944, #499, #33023 ) ;
#23606=DIRECTION ( 'NONE',  ( -1.000000000000000000, 0.000000000000000000, 0.000000000000000000 ) ) ;
#23610=DIRECTION ( 'NONE',  ( -1.000000000000000000, 0.000000000000000000, -0.000000000000000000 ) ) ;
#23615=ORIENTED_EDGE ( 'NONE', *, *, #2727, .F. ) ;
#23621=LINE ( 'NONE', #3268, #17560 ) ;
#23622=DIRECTION ( 'NONE',  ( -1.000000000000000000, 0.000000000000000000, -0.000000000000000000 ) ) ;
#23623=LINE ( 'NONE', #29494, #17852 ) ;
#23625=CARTESIAN_POINT ( 'NONE',  ( -10.00000000000000000, 0.000000000000000000, 0.000000000000000000 ) ) ;
#23626=EDGE_CURVE ( 'NONE', #10198, #27036, #13727, .T. ) ;
#23631=CARTESIAN_POINT ( 'NONE',  ( 17.99999999999999645, 5.492704054968225336, -115.8698847939555776 ) ) ;
#23635=CIRCLE ( 'NONE', #16660, 59.00000000000000711 ) ;
#23636=VERTEX_POINT ( 'NONE', #4073 ) ;
#23641=DIRECTION ( 'NONE',  ( 1.000000000000000000, 0.000000000000000000, 0.000000000000000000 ) ) ;
#23646=ORIENTED_EDGE ( 'NONE', *, *, #2182, .T. ) ;
#23647=DIRECTION ( 'NONE',  ( 0.000000000000000000, 0.000000000000000000, 1.000000000000000000 ) ) ;
#23656=DIRECTION ( 'NONE',  ( -1.000000000000000000, 0.000000000000000000, -0.000000000000000000 ) ) ;
#23660=CARTESIAN_POINT ( 'NONE',  ( 8.999999999999998224, 104.0201923570382405, -51.34003878070954130 ) ) ;
#23661=DIRECTION ( 'NONE',  ( 1.000000000000000000, 0.000000000000000000, 0.000000000000000000 ) ) ;
#23663=CARTESIAN_POINT ( 'NONE',  ( 17.99999999999999645, 0.000000000000000000, 0.000000000000000000 ) ) ;
#23664=ORIENTED_EDGE ( 'NONE', *, *, #25631, .F. ) ;
#23666=CARTESIAN_POINT ( 'NONE',  ( 0.000000000000000000, 91.51415974874679193, -64.91094698989203948 ) ) ;
#23670=ORIENTED_EDGE ( 'NONE', *, *, #32169, .F. ) ;
#23674=ORIENTED_EDGE ( 'NONE', *, *, #5886, .F. ) ;
#23679=EDGE_CURVE ( 'NONE', #41527, #31337, #37337, .T. ) ;
#23684=DIRECTION ( 'NONE',  ( -1.000000000000000000, 0.000000000000000000, -0.000000000000000000 ) ) ;
#23685=ORIENTED_EDGE ( 'NONE', *, *, #26763, .T. ) ;
#23689=DIRECTION ( 'NONE',  ( 0.000000000000000000, 0.000000000000000000, -1.000000000000000000 ) ) ;
#23692=VECTOR ( 'NONE', #23606, 1000.000000000000000 ) ;
#23695=ORIENTED_EDGE ( 'NONE', *, *, #16829, .F. ) ;
#23700=ADVANCED_FACE ( 'NONE', ( #30291 ), #24207, .F. ) ;
#23702=DIRECTION ( 'NONE',  ( 0.000000000000000000, 0.000000000000000000, 1.000000000000000000 ) ) ;
#23704=CARTESIAN_POINT ( 'NONE',  ( 17.99999999999999645, -111.2721026680459602, -14.38025178762732104 ) ) ;
#23706=DIRECTION ( 'NONE',  ( -1.000000000000000000, -0.000000000000000000, 0.000000000000000000 ) ) ;
#23707=DIRECTION ( 'NONE',  ( 1.000000000000000000, 0.000000000000000000, 0.000000000000000000 ) ) ;
#23708=CARTESIAN_POINT ( 'NONE',  ( 9.000000000000001776, 17.77780072541854040, -114.6296200873374147 ) ) ;
#23709=ORIENTED_EDGE ( 'NONE', *, *, #25362, .T. ) ;
#23711=LINE ( 'NONE', #36974, #21748 ) ;
#23714=AXIS2_PLACEMENT_3D ( 'NONE', #39103, #9439, #42155 ) ;
#23716=ORIENTED_EDGE ( 'NONE', *, *, #31312, .T. ) ;
#23720=CARTESIAN_POINT ( 'NONE',  ( 0.000000000000000000, 0.000000000000000000, 0.000000000000000000 ) ) ;
#23721=DIRECTION ( 'NONE',  ( -1.000000000000000000, 0.000000000000000000, -0.000000000000000000 ) ) ;
#23724=DIRECTION ( 'NONE',  ( 1.000000000000000000, 0.000000000000000000, 0.000000000000000000 ) ) ;
#23731=ORIENTED_EDGE ( 'NONE', *, *, #34416, .T. ) ;
#23733=CARTESIAN_POINT ( 'NONE',  ( 17.99999999999999645, -23.21237537461669120, -109.7700237000594541 ) ) ;
#23735=DIRECTION ( 'NONE',  ( 1.000000000000000000, 0.000000000000000000, 0.000000000000000000 ) ) ;
#23738=ORIENTED_EDGE ( 'NONE', *, *, #1659, .T. ) ;
#23740=AXIS2_PLACEMENT_3D ( 'NONE', #5433, #31414, #32049 ) ;
#23743=CARTESIAN_POINT ( 'NONE',  ( 17.99999999999999645, 113.8630351447205697, 22.16324045874448601 ) ) ;
#23747=EDGE_CURVE ( 'NONE', #508, #34279, #40119, .T. ) ;
#23749=VECTOR ( 'NONE', #842, 1000.000000000000000 ) ;
#23750=CYLINDRICAL_SURFACE ( 'NONE', #27886, 59.00000000000000000 ) ;
#23751=ADVANCED_FACE ( 'NONE', ( #29881 ), #40721, .F. ) ;
#23752=ORIENTED_EDGE ( 'NONE', *, *, #2370, .T. ) ;
#23754=ORIENTED_EDGE ( 'NONE', *, *, #34461, .T. ) ;
#23758=ORIENTED_EDGE ( 'NONE', *, *, #612, .T. ) ;
#23760=ORIENTED_EDGE ( 'NONE', *, *, #28656, .T. ) ;
#23763=DIRECTION ( 'NONE',  ( -1.000000000000000000, 0.000000000000000000, 0.000000000000000000 ) ) ;
#23764=ORIENTED_EDGE ( 'NONE', *, *, #6426, .F. ) ;
#23765=ADVANCED_FACE ( 'NONE', ( #3204 ), #16585, .F. ) ;
#23767=CARTESIAN_POINT ( 'NONE',  ( 17.99999999999999645, 0.000000000000000000, 0.000000000000000000 ) ) ;
#23769=VECTOR ( 'NONE', #5613, 1000.000000000000000 ) ;
#23771=ORIENTED_EDGE ( 'NONE', *, *, #33029, .F. ) ;
#23772=DIRECTION ( 'NONE',  ( -1.000000000000000000, -0.000000000000000000, -0.000000000000000000 ) ) ;
#23773=CIRCLE ( 'NONE', #16105, 120.5010000000000190 ) ;
#23774=ORIENTED_EDGE ( 'NONE', *, *, #38620, .F. ) ;
#23777=CIRCLE ( 'NONE', #9104, 58.99999999999999289 ) ;
#23781=CIRCLE ( 'NONE', #2122, 59.00000000000000000 ) ;
#23782=EDGE_CURVE ( 'NONE', #41100, #15795, #39861, .T. ) ;
#23783=DIRECTION ( 'NONE',  ( -1.000000000000000000, 0.000000000000000000, 0.000000000000000000 ) ) ;
#23784=ORIENTED_EDGE ( 'NONE', *, *, #4982, .T. ) ;
#23788=CARTESIAN_POINT ( 'NONE',  ( 17.99999999999999645, 0.000000000000000000, 0.000000000000000000 ) ) ;
#23791=DIRECTION ( 'NONE',  ( -1.000000000000000000, -0.000000000000000000, -0.000000000000000000 ) ) ;
#23796=VERTEX_POINT ( 'NONE', #23335 ) ;
#23803=AXIS2_PLACEMENT_3D ( 'NONE', #18216, #910, #18008 ) ;
#23804=CARTESIAN_POINT ( 'NONE',  ( 17.99999999999999645, 0.000000000000000000, 0.000000000000000000 ) ) ;
#23805=EDGE_CURVE ( 'NONE', #17354, #2165, #21376, .T. ) ;
#23806=CIRCLE ( 'NONE', #22418, 59.00000000000000000 ) ;
#23811=ORIENTED_EDGE ( 'NONE', *, *, #21949, .T. ) ;
#23815=CIRCLE ( 'NONE', #27256, 58.99999999999999289 ) ;
#23818=CARTESIAN_POINT ( 'NONE',  ( 17.99999999999999645, -0.6819280456820884240, -115.9979955608738607 ) ) ;
#23819=CARTESIAN_POINT ( 'NONE',  ( 17.99999999999999645, 114.1157422997283248, 20.82300072952973480 ) ) ;
#23820=ORIENTED_EDGE ( 'NONE', *, *, #10243, .F. ) ;
#23822=ORIENTED_EDGE ( 'NONE', *, *, #14457, .F. ) ;
#23824=DIRECTION ( 'NONE',  ( -1.000000000000000000, 0.000000000000000000, 0.000000000000000000 ) ) ;
#23825=ORIENTED_EDGE ( 'NONE', *, *, #29246, .F. ) ;
#23827=DIRECTION ( 'NONE',  ( 0.000000000000000000, 0.000000000000000000, 1.000000000000000000 ) ) ;
#23831=CARTESIAN_POINT ( 'NONE',  ( 9.000000000000001776, -104.6166166098442147, -50.11350645393781633 ) ) ;
#23833=CARTESIAN_POINT ( 'NONE',  ( 17.99999999999999645, 0.000000000000000000, 0.000000000000000000 ) ) ;
#23835=EDGE_CURVE ( 'NONE', #9577, #33598, #11613, .T. ) ;
#23838=FACE_OUTER_BOUND ( 'NONE', #4794, .T. ) ;
#23840=CIRCLE ( 'NONE', #3565, 59.00000000000000000 ) ;
#23841=DIRECTION ( 'NONE',  ( -1.000000000000000000, -0.000000000000000000, -0.000000000000000000 ) ) ;
#23847=DIRECTION ( 'NONE',  ( 0.000000000000000000, 0.3140767120219495334, -0.9493976084683810601 ) ) ;
#23850=CARTESIAN_POINT ( 'NONE',  ( 17.99999999999999645, 52.19040376560434424, 99.31985817764196156 ) ) ;
#23853=EDGE_LOOP ( 'NONE', ( #18266, #13982, #7521, #40919 ) ) ;
#23854=CARTESIAN_POINT ( 'NONE',  ( 0.000000000000000000, -92.10690493017015967, -64.06707842432270184 ) ) ;
#23855=CARTESIAN_POINT ( 'NONE',  ( 17.99999999999999645, 117.9424311864592312, -24.69967462998914698 ) ) ;
#23858=VECTOR ( 'NONE', #15730, 1000.000000000000000 ) ;
#23859=ORIENTED_EDGE ( 'NONE', *, *, #26345, .T. ) ;
#23861=EDGE_LOOP ( 'NONE', ( #36028, #11143, #14784, #7119 ) ) ;
#23862=DIRECTION ( 'NONE',  ( -1.000000000000000000, -0.000000000000000000, -0.000000000000000000 ) ) ;
#23866=ORIENTED_EDGE ( 'NONE', *, *, #23032, .F. ) ;
#23867=DIRECTION ( 'NONE',  ( 1.000000000000000000, 0.000000000000000000, 0.000000000000000000 ) ) ;
#23869=CYLINDRICAL_SURFACE ( 'NONE', #22068, 59.00000000000000000 ) ;
#23871=ORIENTED_EDGE ( 'NONE', *, *, #24098, .F. ) ;
#23872=DIRECTION ( 'NONE',  ( 0.000000000000000000, 0.7525707698561353576, 0.6585113790650422017 ) ) ;
#23878=ORIENTED_EDGE ( 'NONE', *, *, #35961, .T. ) ;
#23881=DIRECTION ( 'NONE',  ( 1.000000000000000000, 0.000000000000000000, 0.000000000000000000 ) ) ;
#23883=DIRECTION ( 'NONE',  ( 1.000000000000000000, 0.000000000000000000, 0.000000000000000000 ) ) ;
#23886=EDGE_CURVE ( 'NONE', #2740, #24215, #34844, .T. ) ;
#23888=CARTESIAN_POINT ( 'NONE',  ( 17.99999999999999645, -120.3696465864705800, -5.624871700597302571 ) ) ;
#23891=ORIENTED_EDGE ( 'NONE', *, *, #657, .T. ) ;
#23892=DIRECTION ( 'NONE',  ( 1.000000000000000000, 0.000000000000000000, 0.000000000000000000 ) ) ;
#23897=AXIS2_PLACEMENT_3D ( 'NONE', #2551, #39200, #23116 ) ;
#23903=EDGE_CURVE ( 'NONE', #30236, #8713, #18625, .T. ) ;
#23904=AXIS2_PLACEMENT_3D ( 'NONE', #6789, #30793, #868 ) ;
#23905=ORIENTED_EDGE ( 'NONE', *, *, #39250, .T. ) ;
#23906=DIRECTION ( 'NONE',  ( -1.000000000000000000, 0.000000000000000000, -0.000000000000000000 ) ) ;
#23908=CARTESIAN_POINT ( 'NONE',  ( 17.99999999999999645, 84.09610293794069946, 74.27057253243037849 ) ) ;
#23914=EDGE_CURVE ( 'NONE', #23636, #2185, #4290, .T. ) ;
#23918=ORIENTED_EDGE ( 'NONE', *, *, #25156, .F. ) ;
#23920=CARTESIAN_POINT ( 'NONE',  ( 0.000000000000000000, -112.8457601792513714, -26.86697618949492039 ) ) ;
#23921=CIRCLE ( 'NONE', #5079, 59.00000000000000000 ) ;
#23922=LINE ( 'NONE', #13668, #27856 ) ;
#23924=ORIENTED_EDGE ( 'NONE', *, *, #18035, .F. ) ;
#23927=AXIS2_PLACEMENT_3D ( 'NONE', #24637, #37888, #13031 ) ;
#23930=VERTEX_POINT ( 'NONE', #7798 ) ;
#23936=CARTESIAN_POINT ( 'NONE',  ( 9.000000000000001776, 58.30069736313799211, -100.2847380560561419 ) ) ;
#23945=CARTESIAN_POINT ( 'NONE',  ( 17.99999999999999645, 79.18387647320761857, 84.76976882518788159 ) ) ;
#23946=FACE_OUTER_BOUND ( 'NONE', #38183, .T. ) ;
#23948=CARTESIAN_POINT ( 'NONE',  ( 17.99999999999999645, 0.000000000000000000, 0.000000000000000000 ) ) ;
#23951=VERTEX_POINT ( 'NONE', #9293 ) ;
#23955=ORIENTED_EDGE ( 'NONE', *, *, #1246, .T. ) ;
#23963=ORIENTED_EDGE ( 'NONE', *, *, #38291, .T. ) ;
#23965=ORIENTED_EDGE ( 'NONE', *, *, #42184, .F. ) ;
#23967=LINE ( 'NONE', #17870, #33913 ) ;
#23968=CYLINDRICAL_SURFACE ( 'NONE', #2457, 59.00000000000000000 ) ;
#23973=EDGE_CURVE ( 'NONE', #7856, #30129, #5337, .T. ) ;
#23980=DIRECTION ( 'NONE',  ( -1.000000000000000000, 0.000000000000000000, -0.000000000000000000 ) ) ;
#23982=DIRECTION ( 'NONE',  ( 0.000000000000000000, -0.7525707698561440173, 0.6585113790650322096 ) ) ;
#23984=ORIENTED_EDGE ( 'NONE', *, *, #25061, .T. ) ;
#23987=ORIENTED_EDGE ( 'NONE', *, *, #38220, .F. ) ;
#23992=CARTESIAN_POINT ( 'NONE',  ( 17.99999999999999645, 0.000000000000000000, 0.000000000000000000 ) ) ;
#23993=EDGE_CURVE ( 'NONE', #2012, #37721, #33200, .T. ) ;
#23995=DIRECTION ( 'NONE',  ( 0.000000000000000000, -0.6783118362696075598, -0.7347741508630751817 ) ) ;
#23997=EDGE_LOOP ( 'NONE', ( #40547, #23260, #6128, #33450, #35042, #22179, #12723, #30817, #4634, #23871, #28947, #15727, #7522, #29339, #5081, #39758, #40072, #36428, #7247, #29949, #20128, #23820, #15304, #42770, #22863, #25784, #18886, #7386, #24912, #16014, #13381, #34274, #9177, #21447, #28339, #6942, #27965, #8439, #18617, #23145, #27426, #29694, #37252, #936, #41730, #34193, #40579, #6511, #20396, #4780, #12617, #37771, #12852, #23771, #32237, #37066, #25732, #17611, #24138, #38090, #31424, #15754, #30986, #34506, #17156, #17433, #38494, #28074, #115, #23212, #37050, #39832, #33433, #35605, #22480, #38859, #35052, #9280, #40599, #19684, #840, #15488, #20650, #24543, #24410, #35583, #29351, #7691, #38030, #17552, #24528, #12537, #6062, #42807, #42414, #16281, #22267, #12980, #20402, #21344, #19954, #32587, #4250, #15603, #17639, #40410, #10121, #38931, #15212, #8940, #19207, #25438, #13605, #3806, #6303, #39743, #5208, #19192, #40353, #1461, #31532, #41152, #5378, #5851, #13403, #27050, #15253, #42778, #14503, #145, #20188, #42306, #15980, #30838, #27729, #30815, #26618, #42587, #12790, #6154, #37154, #5756, #18245, #28218, #32310, #16299, #38867, #1267, #1083, #35199, #28592, #30520, #4124, #19529, #25549, #20897, #25173, #1384, #12055, #19215, #38381, #27735, #32269, #9479, #33910, #38613, #13513, #29589, #27673, #35952, #7221, #10555, #13136, #12509, #34218, #21696, #16554, #25423, #33142, #14111, #13386, #16208, #38026, #32122, #13006, #38135, #37974, #7136, #22329, #5598, #31756, #15512, #3606, #11828, #11334, #3427, #5498, #40921, #36542, #32895, #36451, #6135, #36906, #6189, #5415, #35534, #7077, #25081, #40254, #33068, #29018, #17394, #29629, #5437, #28398, #22382, #39684, #32247, #27423, #2099, #18685, #13264, #19265, #5406, #34226, #1037, #42048, #10936, #10222, #21751, #14730, #18566, #37789, #33549, #33285, #22053, #12116, #33100, #14750, #21198, #42104, #39036, #27695, #29761, #36446, #40485, #20340, #30592, #34869, #17121, #3895, #30369, #22076, #21347, #12404, #9898, #16308, #4726, #1991, #23085, #19213, #1375, #20605, #5981, #17761, #39052, #29391, #40152, #34603, #25965, #43165, #26135, #10812, #41471, #16166, #38956, #41161, #36996, #15348, #14522, #26010, #29022, #36943, #1371, #36384, #17998, #15124, #36330, #9710, #6982, #1728, #5462, #28731, #2188, #27698, #10745, #13588, #24733, #23337, #17111, #10008, #41026, #41511, #41881, #31898, #13617, #21772, #9282, #1947, #30214, #23234, #20347, #1068, #15805, #16696, #41476, #465, #9477, #27383, #27277, #33119, #29924, #24121, #10051, #8316, #23760, #40943, #24985, #10226, #32560, #4171, #10695, #5516, #5873, #27160, #39696, #35401, #12195, #23918, #1648, #9383, #35130, #4903, #4127, #8961, #24417, #30975, #12716, #10897, #18199, #5621, #14018, #4852, #7597, #20756, #13997, #11816, #182, #38166, #3650, #28885, #36799, #36828, #11526, #17303, #22996, #10075, #27904, #29857, #35315, #2826, #18215, #29467, #16039, #28548, #24094, #38641, #17080, #1938, #9511, #35728, #43097, #8281, #7308, #24707, #14886, #27294, #25230, #23448, #40068, #34875, #18787, #29123, #9457, #16475, #21005, #24415, #5789, #29843, #42158, #15474, #17832, #5173, #25852, #24747, #31635, #14867, #39495, #348, #40134, #42580, #16522, #20164, #28916, #12009, #34358, #34329, #18994, #36914, #3167, #40470, #10800, #35831, #38115, #28121, #27013, #16013, #41574, #10579, #22871, #27870, #26908, #42886, #7343, #18490, #35255, #2620, #32951, #4384, #7367, #14571, #30335, #6151, #21404, #33842, #8300, #2422, #1522, #3714, #10438, #26541, #41916, #11460, #27377, #25326, #33125, #17421, #30712, #33233, #34741, #28278, #25267, #2294, #41959, #1687, #42857, #31378, #6041, #23738, #6371, #42282, #39120, #15067, #3398, #12778, #13215, #32887 ) ) ;
#23999=DIRECTION ( 'NONE',  ( 0.000000000000000000, 0.7164567402983116340, 0.6976315211349882750 ) ) ;
#24002=CIRCLE ( 'NONE', #17024, 59.00000000000001421 ) ;
#24003=DIRECTION ( 'NONE',  ( -1.000000000000000000, -0.000000000000000000, -0.000000000000000000 ) ) ;
#24006=CARTESIAN_POINT ( 'NONE',  ( 0.000000000000000000, 0.000000000000000000, 0.000000000000000000 ) ) ;
#24009=CYLINDRICAL_SURFACE ( 'NONE', #34405, 116.0000000000000000 ) ;
#24011=AXIS2_PLACEMENT_3D ( 'NONE', #7283, #20644, #33915 ) ;
#24013=VERTEX_POINT ( 'NONE', #34467 ) ;
#24017=DIRECTION ( 'NONE',  ( 0.000000000000000000, 0.000000000000000000, 1.000000000000000000 ) ) ;
#24019=CARTESIAN_POINT ( 'NONE',  ( 17.99999999999999645, 0.000000000000000000, 0.000000000000000000 ) ) ;
#24020=CARTESIAN_POINT ( 'NONE',  ( 17.99999999999999645, 104.2166695095720854, -60.49278301857700768 ) ) ;
#24022=LINE ( 'NONE', #17275, #21197 ) ;
#24023=CARTESIAN_POINT ( 'NONE',  ( 17.99999999999999645, 0.000000000000000000, 0.000000000000000000 ) ) ;
#24029=CARTESIAN_POINT ( 'NONE',  ( 17.99999999999999645, -64.58410930313591791, 101.7319213743680422 ) ) ;
#24031=CARTESIAN_POINT ( 'NONE',  ( 17.99999999999999645, 0.000000000000000000, 0.000000000000000000 ) ) ;
#24033=ORIENTED_EDGE ( 'NONE', *, *, #13707, .F. ) ;
#24035=ORIENTED_EDGE ( 'NONE', *, *, #15713, .T. ) ;
#24036=CIRCLE ( 'NONE', #7264, 116.0000000000000000 ) ;
#24040=CIRCLE ( 'NONE', #11508, 116.0000000000000000 ) ;
#24045=EDGE_CURVE ( 'NONE', #32420, #22146, #642, .T. ) ;
#24053=VERTEX_POINT ( 'NONE', #13999 ) ;
#24056=VECTOR ( 'NONE', #19765, 1000.000000000000000 ) ;
#24062=CARTESIAN_POINT ( 'NONE',  ( 0.000000000000000000, 0.000000000000000000, 0.000000000000000000 ) ) ;
#24063=VERTEX_POINT ( 'NONE', #4806 ) ;
#24064=VECTOR ( 'NONE', #38067, 1000.000000000000000 ) ;
#24065=DIRECTION ( 'NONE',  ( 0.000000000000000000, 0.000000000000000000, 1.000000000000000000 ) ) ;
#24067=AXIS2_PLACEMENT_3D ( 'NONE', #8135, #3588, #30244 ) ;
#24071=DIRECTION ( 'NONE',  ( 0.000000000000000000, 0.000000000000000000, 1.000000000000000000 ) ) ;
#24072=LINE ( 'NONE', #17981, #5387 ) ;
#24073=AXIS2_PLACEMENT_3D ( 'NONE', #26563, #30901, #14129 ) ;
#24074=CARTESIAN_POINT ( 'NONE',  ( 17.99999999999999645, 0.000000000000000000, 0.000000000000000000 ) ) ;
#24075=CYLINDRICAL_SURFACE ( 'NONE', #13424, 116.0000000000000000 ) ;
#24076=CIRCLE ( 'NONE', #27547, 116.0000000000000000 ) ;
#24079=ORIENTED_EDGE ( 'NONE', *, *, #32316, .T. ) ;
#24082=CYLINDRICAL_SURFACE ( 'NONE', #27748, 59.00000000000000000 ) ;
#24084=CYLINDRICAL_SURFACE ( 'NONE', #29847, 59.00000000000000000 ) ;
#24086=ORIENTED_EDGE ( 'NONE', *, *, #904, .T. ) ;
#24089=DIRECTION ( 'NONE',  ( 0.000000000000000000, 0.000000000000000000, -1.000000000000000000 ) ) ;
#24091=PLANE ( 'NONE',  #16017 ) ;
#24094=ORIENTED_EDGE ( 'NONE', *, *, #8134, .F. ) ;
#24097=AXIS2_PLACEMENT_3D ( 'NONE', #33828, #30584, #40788 ) ;
#24098=EDGE_CURVE ( 'NONE', #2567, #17290, #8105, .T. ) ;
#24099=EDGE_LOOP ( 'NONE', ( #29033, #2442, #15031, #24035 ) ) ;
#24102=ORIENTED_EDGE ( 'NONE', *, *, #25839, .F. ) ;
#24104=VECTOR ( 'NONE', #11543, 1000.000000000000000 ) ;
#24105=CYLINDRICAL_SURFACE ( 'NONE', #16876, 120.5010000000000190 ) ;
#24106=CARTESIAN_POINT ( 'NONE',  ( 17.99999999999999645, 68.61497464550731706, -99.05794392877534449 ) ) ;
#24107=AXIS2_PLACEMENT_3D ( 'NONE', #22624, #29363, #9491 ) ;
#24108=DIRECTION ( 'NONE',  ( 0.000000000000000000, 0.000000000000000000, 1.000000000000000000 ) ) ;
#24110=ORIENTED_EDGE ( 'NONE', *, *, #29946, .T. ) ;
#24114=ADVANCED_FACE ( 'NONE', ( #27746 ), #7426, .F. ) ;
#24118=EDGE_CURVE ( 'NONE', #26052, #29277, #410, .T. ) ;
#24119=CARTESIAN_POINT ( 'NONE',  ( 9.000000000000001776, 13.00789606333472470, 115.2683592318615382 ) ) ;
#24120=VERTEX_POINT ( 'NONE', #20789 ) ;
#24121=ORIENTED_EDGE ( 'NONE', *, *, #32267, .F. ) ;
#24123=DIRECTION ( 'NONE',  ( 1.000000000000000000, 0.000000000000000000, 0.000000000000000000 ) ) ;
#24125=LINE ( 'NONE', #34126, #16431 ) ;
#24126=CARTESIAN_POINT ( 'NONE',  ( 0.000000000000000000, -111.8797445107944100, -8.437727291343872338 ) ) ;
#24130=ORIENTED_EDGE ( 'NONE', *, *, #27957, .F. ) ;
#24131=ADVANCED_FACE ( 'NONE', ( #37735 ), #7196, .F. ) ;
#24135=AXIS2_PLACEMENT_3D ( 'NONE', #37746, #1315, #24702 ) ;
#24138=ORIENTED_EDGE ( 'NONE', *, *, #9814, .F. ) ;
#24139=CARTESIAN_POINT ( 'NONE',  ( 17.99999999999999645, 0.000000000000000000, 0.000000000000000000 ) ) ;
#24141=AXIS2_PLACEMENT_3D ( 'NONE', #10530, #17997, #31263 ) ;
#24143=ORIENTED_EDGE ( 'NONE', *, *, #42715, .T. ) ;
#24145=ORIENTED_EDGE ( 'NONE', *, *, #32909, .F. ) ;
#24150=CARTESIAN_POINT ( 'NONE',  ( 17.99999999999999645, 0.000000000000000000, 0.000000000000000000 ) ) ;
#24151=ORIENTED_EDGE ( 'NONE', *, *, #40266, .F. ) ;
#24155=CIRCLE ( 'NONE', #28333, 58.99999999999998579 ) ;
#24156=DIRECTION ( 'NONE',  ( 0.000000000000000000, 0.000000000000000000, 1.000000000000000000 ) ) ;
#24157=CIRCLE ( 'NONE', #15800, 59.00000000000000000 ) ;
#24158=DIRECTION ( 'NONE',  ( 1.000000000000000000, -0.000000000000000000, -0.000000000000000000 ) ) ;
#24159=CIRCLE ( 'NONE', #5320, 59.00000000000000711 ) ;
#24161=CARTESIAN_POINT ( 'NONE',  ( 9.000000000000001776, -115.5737863835461496, -9.934782381634844839 ) ) ;
#24164=EDGE_CURVE ( 'NONE', #2864, #21604, #25343, .T. ) ;
#24167=CARTESIAN_POINT ( 'NONE',  ( 17.99999999999999645, -115.5737863835461496, -9.934782381634859050 ) ) ;
#24168=AXIS2_PLACEMENT_3D ( 'NONE', #32968, #28865, #2412 ) ;
#24169=EDGE_CURVE ( 'NONE', #31896, #4351, #2352, .T. ) ;
#24172=AXIS2_PLACEMENT_3D ( 'NONE', #40980, #7832, #10912 ) ;
#24173=ORIENTED_EDGE ( 'NONE', *, *, #18243, .T. ) ;
#24174=EDGE_CURVE ( 'NONE', #29749, #18043, #11813, .T. ) ;
#24177=VERTEX_POINT ( 'NONE', #34909 ) ;
#24181=LINE ( 'NONE', #21135, #434 ) ;
#24189=SURFACE_STYLE_FILL_AREA ( #37233 ) ;
#24190=EDGE_CURVE ( 'NONE', #6476, #20315, #22289, .T. ) ;
#24194=EDGE_CURVE ( 'NONE', #37603, #42396, #24911, .T. ) ;
#24195=EDGE_CURVE ( 'NONE', #5010, #36072, #5366, .T. ) ;
#24197=ORIENTED_EDGE ( 'NONE', *, *, #20755, .F. ) ;
#24199=CIRCLE ( 'NONE', #3230, 58.99999999999999289 ) ;
#24202=AXIS2_PLACEMENT_3D ( 'NONE', #12948, #13, #20372 ) ;
#24204=FACE_OUTER_BOUND ( 'NONE', #11872, .T. ) ;
#24206=ORIENTED_EDGE ( 'NONE', *, *, #25501, .F. ) ;
#24207=CYLINDRICAL_SURFACE ( 'NONE', #9500, 59.00000000000000000 ) ;
#24208=CARTESIAN_POINT ( 'NONE',  ( 0.000000000000000000, -120.4984140710909344, 0.7894348306980505381 ) ) ;
#24209=AXIS2_PLACEMENT_3D ( 'NONE', #2922, #19570, #32843 ) ;
#24210=ORIENTED_EDGE ( 'NONE', *, *, #4999, .F. ) ;
#24211=VECTOR ( 'NONE', #12022, 1000.000000000000000 ) ;
#24215=VERTEX_POINT ( 'NONE', #18597 ) ;
#24218=VECTOR ( 'NONE', #13469, 1000.000000000000000 ) ;
#24219=CARTESIAN_POINT ( 'NONE',  ( 0.000000000000000000, -109.1131968884000258, 26.12628443611856355 ) ) ;
#24226=DIRECTION ( 'NONE',  ( 0.000000000000000000, 0.9911528310040075285, -0.1327255272837188915 ) ) ;
#24227=EDGE_CURVE ( 'NONE', #42671, #4007, #20042, .T. ) ;
#24229=VERTEX_POINT ( 'NONE', #31864 ) ;
#24230=DIRECTION ( 'NONE',  ( 0.000000000000000000, -0.9574220383620081209, 0.2886919473396123981 ) ) ;
#24232=AXIS2_PLACEMENT_3D ( 'NONE', #41467, #17536, #30809 ) ;
#24238=AXIS2_PLACEMENT_3D ( 'NONE', #17608, #30877, #26965 ) ;
#24239=EDGE_LOOP ( 'NONE', ( #8474, #14149, #38515, #21740 ) ) ;
#24245=CARTESIAN_POINT ( 'NONE',  ( 17.99999999999999645, -72.00556975657644898, -86.04342158279462183 ) ) ;
#24247=EDGE_CURVE ( 'NONE', #30236, #18949, #2157, .T. ) ;
#24248=EDGE_CURVE ( 'NONE', #3479, #13442, #4636, .T. ) ;
#24251=ORIENTED_EDGE ( 'NONE', *, *, #25085, .T. ) ;
#24253=DIRECTION ( 'NONE',  ( -1.000000000000000000, -0.000000000000000000, 0.000000000000000000 ) ) ;
#24254=EDGE_CURVE ( 'NONE', #19014, #26640, #1733, .T. ) ;
#24255=ORIENTED_EDGE ( 'NONE', *, *, #41789, .F. ) ;
#24267=AXIS2_PLACEMENT_3D ( 'NONE', #39260, #22747, #36001 ) ;
#24271=CARTESIAN_POINT ( 'NONE',  ( 0.000000000000000000, 109.4038418350910433, -50.51029986767441216 ) ) ;
#24277=LINE ( 'NONE', #28170, #26167 ) ;
#24281=DIRECTION ( 'NONE',  ( 0.000000000000000000, -0.8747630845319658288, 0.4845508703326421585 ) ) ;
#24287=LINE ( 'NONE', #14015, #36444 ) ;
#24292=CARTESIAN_POINT ( 'NONE',  ( 0.000000000000000000, -109.3506818544112917, 38.70953859160975696 ) ) ;
#24294=ORIENTED_EDGE ( 'NONE', *, *, #42296, .T. ) ;
#24295=CARTESIAN_POINT ( 'NONE',  ( 17.99999999999999645, 0.000000000000000000, 0.000000000000000000 ) ) ;
#24297=AXIS2_PLACEMENT_3D ( 'NONE', #12428, #18793, #15495 ) ;
#24300=AXIS2_PLACEMENT_3D ( 'NONE', #30423, #23684, #39566 ) ;
#24301=VECTOR ( 'NONE', #28004, 1000.000000000000000 ) ;
#24302=CARTESIAN_POINT ( 'NONE',  ( 17.99999999999999645, 75.72520367775085504, 82.78868281116005789 ) ) ;
#24303=CARTESIAN_POINT ( 'NONE',  ( 0.000000000000000000, 87.74575819880170968, 75.87280091124503656 ) ) ;
#24306=CYLINDRICAL_SURFACE ( 'NONE', #15084, 116.0000000000000000 ) ;
#24307=DIRECTION ( 'NONE',  ( -1.000000000000000000, 0.000000000000000000, -0.000000000000000000 ) ) ;
#24308=EDGE_CURVE ( 'NONE', #26693, #26169, #1172, .T. ) ;
#24309=ORIENTED_EDGE ( 'NONE', *, *, #8340, .F. ) ;
#24311=ORIENTED_EDGE ( 'NONE', *, *, #13645, .F. ) ;
#24312=CYLINDRICAL_SURFACE ( 'NONE', #41747, 120.5010000000000190 ) ;
#24313=FACE_OUTER_BOUND ( 'NONE', #33168, .T. ) ;
#24314=ORIENTED_EDGE ( 'NONE', *, *, #36863, .T. ) ;
#24315=DIRECTION ( 'NONE',  ( -1.000000000000000000, 0.000000000000000000, 0.000000000000000000 ) ) ;
#24322=CARTESIAN_POINT ( 'NONE',  ( 0.000000000000000000, 0.000000000000000000, 0.000000000000000000 ) ) ;
#24323=ORIENTED_EDGE ( 'NONE', *, *, #18271, .F. ) ;
#24326=LINE ( 'NONE', #30837, #20296 ) ;
#24329=AXIS2_PLACEMENT_3D ( 'NONE', #25646, #5741, #36053 ) ;
#24331=DIRECTION ( 'NONE',  ( -1.000000000000000000, -0.000000000000000000, -0.000000000000000000 ) ) ;
#24336=CARTESIAN_POINT ( 'NONE',  ( 8.999999999999998224, -37.07968990261405651, -109.9140418541961282 ) ) ;
#24337=DIRECTION ( 'NONE',  ( -1.000000000000000000, 0.000000000000000000, 0.000000000000000000 ) ) ;
#24338=DIRECTION ( 'NONE',  ( -1.000000000000000000, -0.000000000000000000, -0.000000000000000000 ) ) ;
#24340=LINE ( 'NONE', #28238, #6839 ) ;
#24341=EDGE_LOOP ( 'NONE', ( #19773, #19687, #42865, #17744 ) ) ;
#24346=VERTEX_POINT ( 'NONE', #30097 ) ;
#24348=ORIENTED_EDGE ( 'NONE', *, *, #18062, .T. ) ;
#24349=VERTEX_POINT ( 'NONE', #150 ) ;
#24353=AXIS2_PLACEMENT_3D ( 'NONE', #10147, #9728, #23498 ) ;
#24354=ADVANCED_FACE ( 'NONE', ( #9788 ), #26810, .F. ) ;
#24357=DIRECTION ( 'NONE',  ( 1.000000000000000000, 0.000000000000000000, -0.000000000000000000 ) ) ;
#24360=DIRECTION ( 'NONE',  ( -1.000000000000000000, 0.000000000000000000, 0.000000000000000000 ) ) ;
#24361=EDGE_CURVE ( 'NONE', #33336, #32964, #27685, .T. ) ;
#24363=CARTESIAN_POINT ( 'NONE',  ( 0.000000000000000000, -119.0898412705475522, 18.38751498043690802 ) ) ;
#24366=DIRECTION ( 'NONE',  ( 0.000000000000000000, -0.8747630845319657178, 0.4845508703326421029 ) ) ;
#24371=CARTESIAN_POINT ( 'NONE',  ( 0.000000000000000000, 37.07968990261625208, -109.9140418541953750 ) ) ;
#24381=AXIS2_PLACEMENT_3D ( 'NONE', #42601, #5964, #2880 ) ;
#24383=LINE ( 'NONE', #550, #21430 ) ;
#24384=CYLINDRICAL_SURFACE ( 'NONE', #3124, 59.00000000000000000 ) ;
#24386=AXIS2_PLACEMENT_3D ( 'NONE', #41421, #37519, #24469 ) ;
#24387=CARTESIAN_POINT ( 'NONE',  ( 17.99999999999999645, 92.10690493017145286, -64.06707842432085442 ) ) ;
#24388=EDGE_CURVE ( 'NONE', #13634, #41864, #15943, .T. ) ;
#24389=ORIENTED_EDGE ( 'NONE', *, *, #8739, .T. ) ;
#24390=( LENGTH_UNIT ( ) NAMED_UNIT ( * ) SI_UNIT ( .MILLI., .METRE. ) );
#24395=EDGE_CURVE ( 'NONE', #15861, #42903, #26952, .T. ) ;
#24396=CARTESIAN_POINT ( 'NONE',  ( 17.99999999999999645, -111.2559044912527355, 32.83479428644638887 ) ) ;
#24397=ORIENTED_EDGE ( 'NONE', *, *, #34416, .F. ) ;
#24406=CARTESIAN_POINT ( 'NONE',  ( 9.000000000000001776, -11.65176648921111635, 115.4133282497342066 ) ) ;
#24410=ORIENTED_EDGE ( 'NONE', *, *, #1761, .F. ) ;
#24411=AXIS2_PLACEMENT_3D ( 'NONE', #35618, #5737, #19093 ) ;
#24413=CYLINDRICAL_SURFACE ( 'NONE', #5963, 120.5010000000000190 ) ;
#24415=ORIENTED_EDGE ( 'NONE', *, *, #36791, .F. ) ;
#24417=ORIENTED_EDGE ( 'NONE', *, *, #13485, .T. ) ;
#24418=CARTESIAN_POINT ( 'NONE',  ( 17.99999999999999645, -109.1131968884000258, 26.12628443611856355 ) ) ;
#24422=ORIENTED_EDGE ( 'NONE', *, *, #32149, .T. ) ;
#24423=CARTESIAN_POINT ( 'NONE',  ( 17.99999999999999645, 15.21076497709875497, -119.5371223922153519 ) ) ;
#24425=EDGE_CURVE ( 'NONE', #848, #31963, #18275, .T. ) ;
#24431=LINE ( 'NONE', #41164, #38285 ) ;
#24433=DIRECTION ( 'NONE',  ( 1.000000000000000000, 0.000000000000000000, 0.000000000000000000 ) ) ;
#24438=AXIS2_PLACEMENT_3D ( 'NONE', #15294, #11562, #8695 ) ;
#24439=ADVANCED_FACE ( 'NONE', ( #41326 ), #21765, .F. ) ;
#24440=CARTESIAN_POINT ( 'NONE',  ( -10.00000000000000000, 0.000000000000000000, 0.000000000000000000 ) ) ;
#24441=AXIS2_PLACEMENT_3D ( 'NONE', #31560, #11080, #1227 ) ;
#24450=DIRECTION ( 'NONE',  ( 0.000000000000000000, 0.000000000000000000, 1.000000000000000000 ) ) ;
#24452=EDGE_LOOP ( 'NONE', ( #42277, #26272, #739, #5434 ) ) ;
#24458=DIRECTION ( 'NONE',  ( -1.000000000000000000, -0.000000000000000000, -0.000000000000000000 ) ) ;
#24460=LINE ( 'NONE', #20979, #3064 ) ;
#24461=CARTESIAN_POINT ( 'NONE',  ( 17.99999999999999645, 0.000000000000000000, 0.000000000000000000 ) ) ;
#24469=DIRECTION ( 'NONE',  ( 0.000000000000000000, -0.9574220383620022368, -0.2886919473396315494 ) ) ;
#24471=CARTESIAN_POINT ( 'NONE',  ( 0.000000000000000000, 0.000000000000000000, 0.000000000000000000 ) ) ;
#24473=ADVANCED_FACE ( 'NONE', ( #8194 ), #21556, .F. ) ;
#24474=CIRCLE ( 'NONE', #8331, 59.00000000000000711 ) ;
#24478=ORIENTED_EDGE ( 'NONE', *, *, #33722, .F. ) ;
#24479=CARTESIAN_POINT ( 'NONE',  ( 17.99999999999999645, 0.000000000000000000, 0.000000000000000000 ) ) ;
#24480=ORIENTED_EDGE ( 'NONE', *, *, #37787, .F. ) ;
#24482=ORIENTED_EDGE ( 'NONE', *, *, #2840, .F. ) ;
#24484=DIRECTION ( 'NONE',  ( 0.000000000000000000, -0.9407002666710364558, 0.3392388661180213427 ) ) ;
#24485=VERTEX_POINT ( 'NONE', #31539 ) ;
#24487=DIRECTION ( 'NONE',  ( -1.000000000000000000, 0.000000000000000000, 0.000000000000000000 ) ) ;
#24490=CARTESIAN_POINT ( 'NONE',  ( 17.99999999999999645, -111.2721026680459602, 44.61974821237267719 ) ) ;
#24491=DIRECTION ( 'NONE',  ( 1.000000000000000000, 0.000000000000000000, 0.000000000000000000 ) ) ;
#24493=AXIS2_PLACEMENT_3D ( 'NONE', #6417, #35457, #25461 ) ;
#24495=DIRECTION ( 'NONE',  ( 0.000000000000000000, 0.000000000000000000, 1.000000000000000000 ) ) ;
#24500=ORIENTED_EDGE ( 'NONE', *, *, #24361, .T. ) ;
#24504=AXIS2_PLACEMENT_3D ( 'NONE', #39329, #6193, #39129 ) ;
#24506=CYLINDRICAL_SURFACE ( 'NONE', #20541, 59.00000000000000000 ) ;
#24507=DIRECTION ( 'NONE',  ( -1.000000000000000000, 0.000000000000000000, 0.000000000000000000 ) ) ;
#24508=CIRCLE ( 'NONE', #23102, 59.00000000000000711 ) ;
#24509=DIRECTION ( 'NONE',  ( 0.000000000000000000, 0.000000000000000000, 1.000000000000000000 ) ) ;
#24511=AXIS2_PLACEMENT_3D ( 'NONE', #10586, #6438, #40238 ) ;
#24512=FACE_OUTER_BOUND ( 'NONE', #7904, .T. ) ;
#24515=VECTOR ( 'NONE', #32278, 1000.000000000000000 ) ;
#24517=DIRECTION ( 'NONE',  ( -1.000000000000000000, 0.000000000000000000, 0.000000000000000000 ) ) ;
#24518=DIRECTION ( 'NONE',  ( -1.000000000000000000, -0.000000000000000000, -0.000000000000000000 ) ) ;
#24520=ORIENTED_EDGE ( 'NONE', *, *, #24308, .T. ) ;
#24525=ORIENTED_EDGE ( 'NONE', *, *, #27354, .T. ) ;
#24526=DIRECTION ( 'NONE',  ( 0.000000000000000000, 0.000000000000000000, 1.000000000000000000 ) ) ;
#24527=DIRECTION ( 'NONE',  ( 0.000000000000000000, 0.000000000000000000, 1.000000000000000000 ) ) ;
#24528=ORIENTED_EDGE ( 'NONE', *, *, #24768, .F. ) ;
#24533=EDGE_LOOP ( 'NONE', ( #17869, #20132, #39966, #42220 ) ) ;
#24537=ORIENTED_EDGE ( 'NONE', *, *, #2978, .T. ) ;
#24539=VECTOR ( 'NONE', #20129, 1000.000000000000000 ) ;
#24540=LINE ( 'NONE', #31275, #14306 ) ;
#24543=ORIENTED_EDGE ( 'NONE', *, *, #32482, .T. ) ;
#24547=EDGE_CURVE ( 'NONE', #3132, #8703, #15851, .T. ) ;
#24548=ADVANCED_FACE ( 'NONE', ( #10970 ), #24306, .F. ) ;
#24549=CARTESIAN_POINT ( 'NONE',  ( 9.000000000000001776, 35.78484819117633720, 110.3423972910434117 ) ) ;
#24550=DIRECTION ( 'NONE',  ( 1.000000000000000000, 0.000000000000000000, 0.000000000000000000 ) ) ;
#24555=ORIENTED_EDGE ( 'NONE', *, *, #2911, .F. ) ;
#24558=DIRECTION ( 'NONE',  ( 0.000000000000000000, 0.9407002666710341243, -0.3392388661180279485 ) ) ;
#24561=ORIENTED_EDGE ( 'NONE', *, *, #39319, .T. ) ;
#24563=ORIENTED_EDGE ( 'NONE', *, *, #42373, .F. ) ;
#24568=FACE_OUTER_BOUND ( 'NONE', #11268, .T. ) ;
#24581=DIRECTION ( 'NONE',  ( -1.000000000000000000, -0.000000000000000000, 0.000000000000000000 ) ) ;
#24583=CARTESIAN_POINT ( 'NONE',  ( 17.99999999999999645, -90.81729652456118629, -72.16798910853708549 ) ) ;
#24584=ORIENTED_EDGE ( 'NONE', *, *, #9882, .F. ) ;
#24589=ORIENTED_EDGE ( 'NONE', *, *, #16164, .F. ) ;
#24594=DIRECTION ( 'NONE',  ( 0.000000000000000000, 0.8747630845319591675, 0.4845508703326539823 ) ) ;
#24600=ORIENTED_EDGE ( 'NONE', *, *, #18176, .F. ) ;
#24602=DIRECTION ( 'NONE',  ( 0.000000000000000000, 0.000000000000000000, -1.000000000000000000 ) ) ;
#24603=CARTESIAN_POINT ( 'NONE',  ( 17.99999999999999645, -41.33768078145568836, 104.3046912715539918 ) ) ;
#24605=CYLINDRICAL_SURFACE ( 'NONE', #15583, 116.0000000000000000 ) ;
#24606=ORIENTED_EDGE ( 'NONE', *, *, #31018, .T. ) ;
#24609=CARTESIAN_POINT ( 'NONE',  ( 8.999999999999998224, 115.9750404417044081, 2.406240749597859718 ) ) ;
#24612=EDGE_CURVE ( 'NONE', #25122, #4616, #38019, .T. ) ;
#24615=DIRECTION ( 'NONE',  ( 1.000000000000000000, -0.000000000000000000, -0.000000000000000000 ) ) ;
#24618=CARTESIAN_POINT ( 'NONE',  ( 0.000000000000000000, 0.000000000000000000, 0.000000000000000000 ) ) ;
#24621=DIRECTION ( 'NONE',  ( 0.000000000000000000, 0.9968120070307500136, 0.07978610555308653096 ) ) ;
#24623=DIRECTION ( 'NONE',  ( 0.000000000000000000, 0.000000000000000000, 1.000000000000000000 ) ) ;
#24630=DIRECTION ( 'NONE',  ( 1.000000000000000000, 0.000000000000000000, 0.000000000000000000 ) ) ;
#24637=CARTESIAN_POINT ( 'NONE',  ( -10.00000000000000000, 0.000000000000000000, 0.000000000000000000 ) ) ;
#24638=CARTESIAN_POINT ( 'NONE',  ( 17.99999999999999645, 120.3696465864706937, -5.624871700594833435 ) ) ;
#24639=CARTESIAN_POINT ( 'NONE',  ( 0.000000000000000000, 0.000000000000000000, 0.000000000000000000 ) ) ;
#24640=ORIENTED_EDGE ( 'NONE', *, *, #9276, .F. ) ;
#24649=DIRECTION ( 'NONE',  ( 1.000000000000000000, 0.000000000000000000, 0.000000000000000000 ) ) ;
#24654=DIRECTION ( 'NONE',  ( 1.000000000000000000, 0.000000000000000000, 0.000000000000000000 ) ) ;
#24655=DIRECTION ( 'NONE',  ( 0.000000000000000000, 0.000000000000000000, -1.000000000000000000 ) ) ;
#24658=CYLINDRICAL_SURFACE ( 'NONE', #30857, 116.0000000000000000 ) ;
#24659=DIRECTION ( 'NONE',  ( 0.000000000000000000, 0.000000000000000000, 1.000000000000000000 ) ) ;
#24670=DIRECTION ( 'NONE',  ( 0.000000000000000000, 0.8477344278896721264, -0.5304209081197406306 ) ) ;
#24673=CARTESIAN_POINT ( 'NONE',  ( 17.99999999999999645, -11.41303419185048185, 111.6154788735835410 ) ) ;
#24674=AXIS2_PLACEMENT_3D ( 'NONE', #29562, #25676, #32394 ) ;
#24677=CARTESIAN_POINT ( 'NONE',  ( 17.99999999999999645, -66.49630760163661591, 90.36876423295966276 ) ) ;
#24678=CARTESIAN_POINT ( 'NONE',  ( -10.00000000000000000, 0.000000000000000000, 0.000000000000000000 ) ) ;
#24679=AXIS2_PLACEMENT_3D ( 'NONE', #39475, #39682, #15971 ) ;
#24682=FACE_OUTER_BOUND ( 'NONE', #20450, .T. ) ;
#24683=EDGE_CURVE ( 'NONE', #10297, #31034, #2566, .T. ) ;
#24684=EDGE_LOOP ( 'NONE', ( #38850, #17071 ) ) ;
#24685=EDGE_CURVE ( 'NONE', #31744, #10857, #12921, .T. ) ;
#24689=CARTESIAN_POINT ( 'NONE',  ( 17.99999999999999645, 0.000000000000000000, 0.000000000000000000 ) ) ;
#24691=CARTESIAN_POINT ( 'NONE',  ( 17.99999999999999645, -29.02167576844032482, -108.3790330702172611 ) ) ;
#24693=ORIENTED_EDGE ( 'NONE', *, *, #24174, .F. ) ;
#24694=LINE ( 'NONE', #18375, #36938 ) ;
#24700=CARTESIAN_POINT ( 'NONE',  ( 17.99999999999999645, -116.4607004671430417, 30.94182036827165660 ) ) ;
#24701=EDGE_CURVE ( 'NONE', #42903, #35448, #15997, .T. ) ;
#24702=DIRECTION ( 'NONE',  ( 0.000000000000000000, -0.8993121301712141413, -0.4373073204588656671 ) ) ;
#24704=CARTESIAN_POINT ( 'NONE',  ( 17.99999999999999645, 0.000000000000000000, 0.000000000000000000 ) ) ;
#24705=AXIS2_PLACEMENT_3D ( 'NONE', #29677, #42951, #35748 ) ;
#24706=DIRECTION ( 'NONE',  ( 0.000000000000000000, -0.9826841245925227453, 0.1852887240871045338 ) ) ;
#24707=ORIENTED_EDGE ( 'NONE', *, *, #27373, .F. ) ;
#24709=EDGE_CURVE ( 'NONE', #27433, #29671, #24842, .T. ) ;
#24711=CIRCLE ( 'NONE', #30255, 59.00000000000000711 ) ;
#24714=FACE_OUTER_BOUND ( 'NONE', #38979, .T. ) ;
#24716=EDGE_CURVE ( 'NONE', #6315, #23930, #19351, .T. ) ;
#24717=DIRECTION ( 'NONE',  ( -1.000000000000000000, 0.000000000000000000, -0.000000000000000000 ) ) ;
#24718=ORIENTED_EDGE ( 'NONE', *, *, #31071, .F. ) ;
#24726=CARTESIAN_POINT ( 'NONE',  ( 0.000000000000000000, -114.8812324315174038, -16.07179003769265080 ) ) ;
#24728=AXIS2_PLACEMENT_3D ( 'NONE', #24691, #37948, #34689 ) ;
#24730=AXIS2_PLACEMENT_3D ( 'NONE', #1955, #28810, #35335 ) ;
#24733=ORIENTED_EDGE ( 'NONE', *, *, #12084, .T. ) ;
#24736=VECTOR ( 'NONE', #41999, 1000.000000000000000 ) ;
#24738=ORIENTED_EDGE ( 'NONE', *, *, #31738, .T. ) ;
#24739=ADVANCED_FACE ( 'NONE', ( #29719 ), #2410, .F. ) ;
#24747=ORIENTED_EDGE ( 'NONE', *, *, #26192, .F. ) ;
#24748=CIRCLE ( 'NONE', #3044, 116.0000000000000000 ) ;
#24749=ORIENTED_EDGE ( 'NONE', *, *, #17198, .F. ) ;
#24750=CARTESIAN_POINT ( 'NONE',  ( 17.99999999999999645, -35.78484819117709748, 110.3423972910431701 ) ) ;
#24753=CARTESIAN_POINT ( 'NONE',  ( -10.00000000000000000, 0.000000000000000000, 0.000000000000000000 ) ) ;
#24755=ORIENTED_EDGE ( 'NONE', *, *, #4094, .F. ) ;
#24759=ORIENTED_EDGE ( 'NONE', *, *, #9139, .F. ) ;
#24762=CARTESIAN_POINT ( 'NONE',  ( 0.000000000000000000, 97.19627249181192497, -71.22763238166385236 ) ) ;
#24766=CIRCLE ( 'NONE', #17090, 120.5010000000000332 ) ;
#24768=EDGE_CURVE ( 'NONE', #39935, #16661, #28411, .T. ) ;
#24773=EDGE_CURVE ( 'NONE', #6952, #30129, #39503, .T. ) ;
#24776=AXIS2_PLACEMENT_3D ( 'NONE', #4715, #1646, #18732 ) ;
#24778=VERTEX_POINT ( 'NONE', #35791 ) ;
#24781=CARTESIAN_POINT ( 'NONE',  ( 17.99999999999999645, 0.000000000000000000, 0.000000000000000000 ) ) ;
#24783=DIRECTION ( 'NONE',  ( 1.000000000000000000, 0.000000000000000000, 0.000000000000000000 ) ) ;
#24784=AXIS2_PLACEMENT_3D ( 'NONE', #38245, #28670, #8151 ) ;
#24787=ORIENTED_EDGE ( 'NONE', *, *, #6249, .T. ) ;
#24794=AXIS2_PLACEMENT_3D ( 'NONE', #21554, #14762, #11476 ) ;
#24795=DIRECTION ( 'NONE',  ( 1.000000000000000000, 0.000000000000000000, 0.000000000000000000 ) ) ;
#24799=CYLINDRICAL_SURFACE ( 'NONE', #41195, 116.0000000000000000 ) ;
#24804=AXIS2_PLACEMENT_3D ( 'NONE', #25321, #24903, #32256 ) ;
#24806=ORIENTED_EDGE ( 'NONE', *, *, #32788, .T. ) ;
#24811=FACE_OUTER_BOUND ( 'NONE', #30971, .T. ) ;
#24820=CARTESIAN_POINT ( 'NONE',  ( 17.99999999999999645, 56.51398178981952469, -96.92493144647394843 ) ) ;
#24821=ORIENTED_EDGE ( 'NONE', *, *, #21003, .F. ) ;
#24828=ORIENTED_EDGE ( 'NONE', *, *, #12294, .F. ) ;
#24831=AXIS2_PLACEMENT_3D ( 'NONE', #36884, #6989, #26653 ) ;
#24833=CYLINDRICAL_SURFACE ( 'NONE', #27515, 120.5010000000000190 ) ;
#24836=CARTESIAN_POINT ( 'NONE',  ( 17.99999999999999645, 120.3696465864706227, 5.624871700596478341 ) ) ;
#24842=CIRCLE ( 'NONE', #5972, 58.99999999999999289 ) ;
#24843=DIRECTION ( 'NONE',  ( 1.000000000000000000, 0.000000000000000000, 0.000000000000000000 ) ) ;
#24844=VECTOR ( 'NONE', #6716, 1000.000000000000000 ) ;
#24847=ORIENTED_EDGE ( 'NONE', *, *, #36023, .F. ) ;
#24849=DIRECTION ( 'NONE',  ( 1.000000000000000000, 0.000000000000000000, 0.000000000000000000 ) ) ;
#24854=EDGE_LOOP ( 'NONE', ( #41737, #34339, #14925, #27956 ) ) ;
#24861=FACE_OUTER_BOUND ( 'NONE', #6576, .T. ) ;
#24862=AXIS2_PLACEMENT_3D ( 'NONE', #9048, #22401, #19123 ) ;
#24864=AXIS2_PLACEMENT_3D ( 'NONE', #21868, #2356, #35117 ) ;
#24865=EDGE_CURVE ( 'NONE', #40994, #18274, #30413, .T. ) ;
#24867=CARTESIAN_POINT ( 'NONE',  ( 17.99999999999999645, 0.000000000000000000, 0.000000000000000000 ) ) ;
#24868=DIRECTION ( 'NONE',  ( 0.000000000000000000, -0.2113826236296114103, -0.9774033898178695612 ) ) ;
#24869=ORIENTED_EDGE ( 'NONE', *, *, #5045, .F. ) ;
#24870=CARTESIAN_POINT ( 'NONE',  ( 0.000000000000000000, 0.000000000000000000, 0.000000000000000000 ) ) ;
#24872=CARTESIAN_POINT ( 'NONE',  ( 17.99999999999999645, -52.19040376560366923, -99.31985817764231683 ) ) ;
#24874=AXIS2_PLACEMENT_3D ( 'NONE', #41741, #8371, #11885 ) ;
#24878=CIRCLE ( 'NONE', #6687, 116.0000000000000000 ) ;
#24881=DIRECTION ( 'NONE',  ( 0.000000000000000000, 0.000000000000000000, 1.000000000000000000 ) ) ;
#24883=CARTESIAN_POINT ( 'NONE',  ( 9.000000000000001776, 0.6819280456829140968, 115.9979955608738749 ) ) ;
#24885=ORIENTED_EDGE ( 'NONE', *, *, #1250, .F. ) ;
#24889=ORIENTED_EDGE ( 'NONE', *, *, #17424, .F. ) ;
#24890=FACE_OUTER_BOUND ( 'NONE', #9109, .T. ) ;
#24895=ORIENTED_EDGE ( 'NONE', *, *, #28715, .T. ) ;
#24898=AXIS2_PLACEMENT_3D ( 'NONE', #601, #17898, #31174 ) ;
#24900=AXIS2_PLACEMENT_3D ( 'NONE', #17095, #13598, #34283 ) ;
#24901=DIRECTION ( 'NONE',  ( 0.000000000000000000, 0.000000000000000000, 1.000000000000000000 ) ) ;
#24903=DIRECTION ( 'NONE',  ( -1.000000000000000000, 0.000000000000000000, 0.000000000000000000 ) ) ;
#24905=CARTESIAN_POINT ( 'NONE',  ( 17.99999999999999645, 0.000000000000000000, 0.000000000000000000 ) ) ;
#24908=CARTESIAN_POINT ( 'NONE',  ( 9.000000000000001776, -101.8011932243951634, 55.61040422519296555 ) ) ;
#24909=DIRECTION ( 'NONE',  ( -1.000000000000000000, 0.000000000000000000, 0.000000000000000000 ) ) ;
#24911=CIRCLE ( 'NONE', #17933, 59.00000000000000000 ) ;
#24912=ORIENTED_EDGE ( 'NONE', *, *, #42382, .F. ) ;
#24915=AXIS2_PLACEMENT_3D ( 'NONE', #2056, #1415, #28293 ) ;
#24921=ORIENTED_EDGE ( 'NONE', *, *, #26069, .T. ) ;
#24923=DIRECTION ( 'NONE',  ( -1.000000000000000000, 0.000000000000000000, 0.000000000000000000 ) ) ;
#24929=CARTESIAN_POINT ( 'NONE',  ( -10.00000000000000000, 0.000000000000000000, 0.000000000000000000 ) ) ;
#24931=ORIENTED_EDGE ( 'NONE', *, *, #2403, .F. ) ;
#24934=CIRCLE ( 'NONE', #40176, 59.00000000000000000 ) ;
#24937=ORIENTED_EDGE ( 'NONE', *, *, #3080, .T. ) ;
#24940=DIRECTION ( 'NONE',  ( 0.000000000000000000, 0.9574220383620062336, -0.2886919473396183933 ) ) ;
#24946=DIRECTION ( 'NONE',  ( 0.000000000000000000, 0.000000000000000000, 1.000000000000000000 ) ) ;
#24948=AXIS2_PLACEMENT_3D ( 'NONE', #18667, #31060, #7702 ) ;
#24951=CARTESIAN_POINT ( 'NONE',  ( 0.000000000000000000, -72.00556975657644898, -86.04342158279462183 ) ) ;
#24955=DIRECTION ( 'NONE',  ( -1.000000000000000000, 0.000000000000000000, 0.000000000000000000 ) ) ;
#24960=EDGE_CURVE ( 'NONE', #22923, #15394, #16470, .T. ) ;
#24961=CIRCLE ( 'NONE', #20061, 120.5010000000000332 ) ;
#24962=ORIENTED_EDGE ( 'NONE', *, *, #43104, .F. ) ;
#24965=CIRCLE ( 'NONE', #30694, 59.00000000000000711 ) ;
#24966=DIRECTION ( 'NONE',  ( -1.000000000000000000, 0.000000000000000000, 0.000000000000000000 ) ) ;
#24969=VECTOR ( 'NONE', #5109, 1000.000000000000000 ) ;
#24971=DIRECTION ( 'NONE',  ( 1.000000000000000000, 0.000000000000000000, 0.000000000000000000 ) ) ;
#24972=DIRECTION ( 'NONE',  ( -1.000000000000000000, 0.000000000000000000, 0.000000000000000000 ) ) ;
#24974=CARTESIAN_POINT ( 'NONE',  ( 0.000000000000000000, 115.0622509503832589, 14.72000021165183803 ) ) ;
#24975=ORIENTED_EDGE ( 'NONE', *, *, #28898, .T. ) ;
#24983=DIRECTION ( 'NONE',  ( 0.000000000000000000, 0.000000000000000000, 1.000000000000000000 ) ) ;
#24984=CYLINDRICAL_SURFACE ( 'NONE', #17124, 59.00000000000000000 ) ;
#24985=ORIENTED_EDGE ( 'NONE', *, *, #25866, .F. ) ;
#24986=DIRECTION ( 'NONE',  ( 0.000000000000000000, 0.7865515558026395793, 0.6175246149461957046 ) ) ;
#24988=EDGE_LOOP ( 'NONE', ( #10154, #43137, #412, #37886 ) ) ;
#24992=DIRECTION ( 'NONE',  ( 1.000000000000000000, 0.000000000000000000, 0.000000000000000000 ) ) ;
#24993=DIRECTION ( 'NONE',  ( 1.000000000000000000, -0.000000000000000000, 0.000000000000000000 ) ) ;
#24997=ORIENTED_EDGE ( 'NONE', *, *, #1593, .F. ) ;
#25009=ORIENTED_EDGE ( 'NONE', *, *, #16561, .F. ) ;
#25014=AXIS2_PLACEMENT_3D ( 'NONE', #15418, #1202, #24594 ) ;
#25017=EDGE_CURVE ( 'NONE', #25282, #35178, #6006, .T. ) ;
#25018=ORIENTED_EDGE ( 'NONE', *, *, #10243, .T. ) ;
#25020=EDGE_LOOP ( 'NONE', ( #40208, #3964, #25219, #791 ) ) ;
#25022=DIRECTION ( 'NONE',  ( 0.000000000000000000, 0.000000000000000000, 1.000000000000000000 ) ) ;
#25024=DIRECTION ( 'NONE',  ( -1.000000000000000000, -0.000000000000000000, -0.000000000000000000 ) ) ;
#25025=DIRECTION ( 'NONE',  ( 0.000000000000000000, -0.8477344278896755680, 0.5304209081197351905 ) ) ;
#25029=AXIS2_PLACEMENT_3D ( 'NONE', #42051, #2332, #39000 ) ;
#25030=CARTESIAN_POINT ( 'NONE',  ( 17.99999999999999645, -83.49789599728724454, -86.88263557826851979 ) ) ;
#25031=ADVANCED_FACE ( 'NONE', ( #33614 ), #27754, .F. ) ;
#25042=ORIENTED_EDGE ( 'NONE', *, *, #1862, .F. ) ;
#25046=LINE ( 'NONE', #43056, #15036 ) ;
#25049=VERTEX_POINT ( 'NONE', #18384 ) ;
#25050=SHAPE_REPRESENTATION_RELATIONSHIP ( 'NONE' , 'NONE' ,  #19391, #21924 ) ;
#25051=CARTESIAN_POINT ( 'NONE',  ( 17.99999999999999645, -41.62036691425453228, -113.0850832732718914 ) ) ;
#25053=EDGE_CURVE ( 'NONE', #5216, #36925, #17957, .T. ) ;
#25056=EDGE_CURVE ( 'NONE', #41792, #37428, #42898, .T. ) ;
#25057=CARTESIAN_POINT ( 'NONE',  ( 17.99999999999999645, -86.84764344322910290, -76.89919913989835720 ) ) ;
#25058=AXIS2_PLACEMENT_3D ( 'NONE', #43143, #39212, #42698 ) ;
#25061=EDGE_CURVE ( 'NONE', #27792, #41792, #35249, .T. ) ;
#25062=VECTOR ( 'NONE', #33641, 1000.000000000000000 ) ;
#25063=FACE_OUTER_BOUND ( 'NONE', #40953, .T. ) ;
#25064=ORIENTED_EDGE ( 'NONE', *, *, #12384, .T. ) ;
#25069=CARTESIAN_POINT ( 'NONE',  ( 0.000000000000000000, -61.59243992711397198, -93.77976230226100540 ) ) ;
#25077=DIRECTION ( 'NONE',  ( -1.000000000000000000, 0.000000000000000000, -0.000000000000000000 ) ) ;
#25078=VERTEX_POINT ( 'NONE', #31230 ) ;
#25079=DIRECTION ( 'NONE',  ( 0.000000000000000000, 0.000000000000000000, 1.000000000000000000 ) ) ;
#25080=CARTESIAN_POINT ( 'NONE',  ( 17.99999999999999645, -21.55123232222554464, 118.5581519187671660 ) ) ;
#25081=ORIENTED_EDGE ( 'NONE', *, *, #39376, .T. ) ;
#25083=AXIS2_PLACEMENT_3D ( 'NONE', #20022, #40016, #33291 ) ;
#25084=CARTESIAN_POINT ( 'NONE',  ( 0.000000000000000000, 111.1352304691229733, -15.40237066878481720 ) ) ;
#25085=EDGE_CURVE ( 'NONE', #21881, #30236, #31093, .T. ) ;
#25086=AXIS2_PLACEMENT_3D ( 'NONE', #31259, #20829, #14904 ) ;
#25087=CARTESIAN_POINT ( 'NONE',  ( 17.99999999999999645, -57.69704296431110890, -105.7900857083235451 ) ) ;
#25088=DIRECTION ( 'NONE',  ( 1.000000000000000000, 0.000000000000000000, 0.000000000000000000 ) ) ;
#25092=DIRECTION ( 'NONE',  ( 0.000000000000000000, -0.5528000653612000770, 0.8333139190825106235 ) ) ;
#25094=DIRECTION ( 'NONE',  ( -1.000000000000000000, -0.000000000000000000, -0.000000000000000000 ) ) ;
#25097=ORIENTED_EDGE ( 'NONE', *, *, #17909, .T. ) ;
#25104=DIRECTION ( 'NONE',  ( -1.000000000000000000, -0.000000000000000000, -0.000000000000000000 ) ) ;
#25105=ADVANCED_FACE ( 'NONE', ( #8725 ), #31873, .F. ) ;
#25108=DIRECTION ( 'NONE',  ( 1.000000000000000000, -0.000000000000000000, 0.000000000000000000 ) ) ;
#25110=AXIS2_PLACEMENT_3D ( 'NONE', #1901, #35693, #15889 ) ;
#25112=ORIENTED_EDGE ( 'NONE', *, *, #26286, .F. ) ;
#25115=AXIS2_PLACEMENT_3D ( 'NONE', #30565, #20987, #21200 ) ;
#25116=ORIENTED_EDGE ( 'NONE', *, *, #11109, .T. ) ;
#25119=DIRECTION ( 'NONE',  ( -1.000000000000000000, -0.000000000000000000, -0.000000000000000000 ) ) ;
#25120=DIRECTION ( 'NONE',  ( 1.000000000000000000, 0.000000000000000000, 0.000000000000000000 ) ) ;
#25122=VERTEX_POINT ( 'NONE', #5237 ) ;
#25123=CARTESIAN_POINT ( 'NONE',  ( 0.000000000000000000, -111.2559044912527355, 32.83479428644638887 ) ) ;
#25125=ORIENTED_EDGE ( 'NONE', *, *, #34593, .T. ) ;
#25127=DIRECTION ( 'NONE',  ( -1.000000000000000000, -0.000000000000000000, 0.000000000000000000 ) ) ;
#25128=ORIENTED_EDGE ( 'NONE', *, *, #5504, .T. ) ;
#25130=CARTESIAN_POINT ( 'NONE',  ( 17.99999999999999645, 101.1403355683153933, -56.80345518653383152 ) ) ;
#25132=VERTEX_POINT ( 'NONE', #28405 ) ;
#25134=CARTESIAN_POINT ( 'NONE',  ( 17.99999999999999645, 110.3490479609629489, 20.28201389785587949 ) ) ;
#25136=ORIENTED_EDGE ( 'NONE', *, *, #5876, .T. ) ;
#25138=DIRECTION ( 'NONE',  ( -1.000000000000000000, 0.000000000000000000, 0.000000000000000000 ) ) ;
#25139=CYLINDRICAL_SURFACE ( 'NONE', #24730, 59.00000000000000000 ) ;
#25140=CYLINDRICAL_SURFACE ( 'NONE', #24864, 59.00000000000000000 ) ;
#25143=CYLINDRICAL_SURFACE ( 'NONE', #826, 59.00000000000000000 ) ;
#25145=LINE ( 'NONE', #14663, #29464 ) ;
#25147=CARTESIAN_POINT ( 'NONE',  ( 17.99999999999999645, 106.6051926090971023, 45.73109345704855855 ) ) ;
#25149=CARTESIAN_POINT ( 'NONE',  ( 17.99999999999999645, 95.38615066514064722, -59.07414607872728141 ) ) ;
#25153=DIRECTION ( 'NONE',  ( 0.000000000000000000, 0.9826841245925203028, 0.1852887240871181618 ) ) ;
#25154=AXIS2_PLACEMENT_3D ( 'NONE', #41447, #8085, #31233 ) ;
#25156=EDGE_CURVE ( 'NONE', #31728, #3775, #11331, .T. ) ;
#25158=ADVANCED_FACE ( 'NONE', ( #11819 ), #25143, .F. ) ;
#25159=CIRCLE ( 'NONE', #25825, 59.00000000000000000 ) ;
#25161=CARTESIAN_POINT ( 'NONE',  ( 9.000000000000001776, 23.85344185397347161, -113.5209818126988779 ) ) ;
#25163=CARTESIAN_POINT ( 'NONE',  ( 17.99999999999999645, 119.7318547011701497, 13.59315897125768124 ) ) ;
#25165=VECTOR ( 'NONE', #26630, 1000.000000000000000 ) ;
#25173=ORIENTED_EDGE ( 'NONE', *, *, #17913, .F. ) ;
#25174=DIRECTION ( 'NONE',  ( 0.000000000000000000, 0.000000000000000000, 1.000000000000000000 ) ) ;
#25175=DIRECTION ( 'NONE',  ( -1.000000000000000000, -0.000000000000000000, -0.000000000000000000 ) ) ;
#25176=ORIENTED_EDGE ( 'NONE', *, *, #280, .T. ) ;
#25178=ORIENTED_EDGE ( 'NONE', *, *, #13297, .T. ) ;
#25184=AXIS2_PLACEMENT_3D ( 'NONE', #23152, #13321, #16611 ) ;
#25186=CARTESIAN_POINT ( 'NONE',  ( 0.000000000000000000, -54.09091620264652533, -102.6166301549523467 ) ) ;
#25191=VECTOR ( 'NONE', #19797, 1000.000000000000000 ) ;
#25192=AXIS2_PLACEMENT_3D ( 'NONE', #2678, #16040, #12338 ) ;
#25208=DIRECTION ( 'NONE',  ( 0.000000000000000000, 0.000000000000000000, 1.000000000000000000 ) ) ;
#25211=EDGE_CURVE ( 'NONE', #9900, #30604, #25278, .T. ) ;
#25213=EDGE_LOOP ( 'NONE', ( #42264, #19865, #29811, #4680 ) ) ;
#25216=DIRECTION ( 'NONE',  ( 0.000000000000000000, 0.000000000000000000, 1.000000000000000000 ) ) ;
#25219=ORIENTED_EDGE ( 'NONE', *, *, #41343, .T. ) ;
#25226=DIRECTION ( 'NONE',  ( -1.000000000000000000, 0.000000000000000000, -0.000000000000000000 ) ) ;
#25230=ORIENTED_EDGE ( 'NONE', *, *, #38694, .F. ) ;
#25231=CYLINDRICAL_SURFACE ( 'NONE', #15877, 120.5010000000000190 ) ;
#25233=VECTOR ( 'NONE', #30947, 1000.000000000000000 ) ;
#25238=VERTEX_POINT ( 'NONE', #19023 ) ;
#25239=ADVANCED_FACE ( 'NONE', ( #22946 ), #42084, .F. ) ;
#25245=CARTESIAN_POINT ( 'NONE',  ( 17.99999999999999645, 75.03166794516924654, -94.29071961951432002 ) ) ;
#25246=DIRECTION ( 'NONE',  ( 0.000000000000000000, 0.000000000000000000, -1.000000000000000000 ) ) ;
#25251=DIRECTION ( 'NONE',  ( 0.000000000000000000, -0.9714298932647074114, -0.2373266998711250908 ) ) ;
#25252=CIRCLE ( 'NONE', #35654, 116.0000000000000000 ) ;
#25255=ORIENTED_EDGE ( 'NONE', *, *, #35351, .F. ) ;
#25256=CYLINDRICAL_SURFACE ( 'NONE', #24776, 116.0000000000000000 ) ;
#25257=EDGE_CURVE ( 'NONE', #5449, #38358, #34980, .T. ) ;
#25260=DIRECTION ( 'NONE',  ( 1.000000000000000000, -0.000000000000000000, -0.000000000000000000 ) ) ;
#25261=ADVANCED_FACE ( 'NONE', ( #39670 ), #9796, .F. ) ;
#25262=DIRECTION ( 'NONE',  ( 0.000000000000000000, 0.000000000000000000, 1.000000000000000000 ) ) ;
#25267=ORIENTED_EDGE ( 'NONE', *, *, #3351, .F. ) ;
#25268=CARTESIAN_POINT ( 'NONE',  ( -10.00000000000000000, 0.000000000000000000, 0.000000000000000000 ) ) ;
#25269=ORIENTED_EDGE ( 'NONE', *, *, #19564, .T. ) ;
#25270=DIRECTION ( 'NONE',  ( -1.000000000000000000, -0.000000000000000000, -0.000000000000000000 ) ) ;
#25273=ORIENTED_EDGE ( 'NONE', *, *, #27266, .T. ) ;
#25276=DIRECTION ( 'NONE',  ( 0.000000000000000000, 0.000000000000000000, 1.000000000000000000 ) ) ;
#25278=CIRCLE ( 'NONE', #41252, 59.00000000000000711 ) ;
#25280=AXIS2_PLACEMENT_3D ( 'NONE', #35120, #10946, #18174 ) ;
#25282=VERTEX_POINT ( 'NONE', #36186 ) ;
#25283=EDGE_CURVE ( 'NONE', #13787, #12118, #42718, .T. ) ;
#25285=ADVANCED_FACE ( 'NONE', ( #38821 ), #19230, .F. ) ;
#25287=EDGE_CURVE ( 'NONE', #3675, #719, #36395, .T. ) ;
#25290=DIRECTION ( 'NONE',  ( 1.000000000000000000, 0.000000000000000000, 0.000000000000000000 ) ) ;
#25292=ORIENTED_EDGE ( 'NONE', *, *, #33609, .F. ) ;
#25294=VERTEX_POINT ( 'NONE', #9153 ) ;
#25297=CARTESIAN_POINT ( 'NONE',  ( 0.000000000000000000, -111.2721026680461733, 14.38025178762581469 ) ) ;
#25299=LINE ( 'NONE', #25724, #2516 ) ;
#25300=VERTEX_POINT ( 'NONE', #22506 ) ;
#25303=DIRECTION ( 'NONE',  ( 0.000000000000000000, 0.000000000000000000, 1.000000000000000000 ) ) ;
#25304=CYLINDRICAL_SURFACE ( 'NONE', #31022, 59.00000000000000000 ) ;
#25306=VERTEX_POINT ( 'NONE', #15951 ) ;
#25309=DIRECTION ( 'NONE',  ( -1.000000000000000000, -0.000000000000000000, -0.000000000000000000 ) ) ;
#25310=EDGE_CURVE ( 'NONE', #7190, #21257, #18311, .T. ) ;
#25311=AXIS2_PLACEMENT_3D ( 'NONE', #15476, #28774, #25513 ) ;
#25315=AXIS2_PLACEMENT_3D ( 'NONE', #31160, #28755, #32015 ) ;
#25320=CARTESIAN_POINT ( 'NONE',  ( 17.99999999999999645, -117.6086855750636460, 26.24286718912065552 ) ) ;
#25321=CARTESIAN_POINT ( 'NONE',  ( 17.99999999999999645, 84.77518783075095143, 73.49448960231384831 ) ) ;
#25326=ORIENTED_EDGE ( 'NONE', *, *, #4376, .F. ) ;
#25328=CARTESIAN_POINT ( 'NONE',  ( 17.99999999999999645, 18.35539002514530793, -110.6858262410707994 ) ) ;
#25330=ADVANCED_FACE ( 'NONE', ( #12874 ), #26182, .F. ) ;
#25336=VERTEX_POINT ( 'NONE', #40527 ) ;
#25340=DIRECTION ( 'NONE',  ( 1.000000000000000000, -0.000000000000000000, -0.000000000000000000 ) ) ;
#25341=ORIENTED_EDGE ( 'NONE', *, *, #1347, .F. ) ;
#25343=LINE ( 'NONE', #25765, #23486 ) ;
#25346=ORIENTED_EDGE ( 'NONE', *, *, #2370, .F. ) ;
#25353=CYLINDRICAL_SURFACE ( 'NONE', #19557, 120.5010000000000190 ) ;
#25359=CARTESIAN_POINT ( 'NONE',  ( 17.99999999999999645, -89.07460286905796920, -81.15544420875052367 ) ) ;
#25361=CIRCLE ( 'NONE', #12110, 116.0000000000000000 ) ;
#25362=EDGE_CURVE ( 'NONE', #15430, #26216, #5727, .T. ) ;
#25365=LINE ( 'NONE', #27776, #22123 ) ;
#25366=DIRECTION ( 'NONE',  ( 0.000000000000000000, 0.000000000000000000, -1.000000000000000000 ) ) ;
#25372=ORIENTED_EDGE ( 'NONE', *, *, #42405, .T. ) ;
#25373=DIRECTION ( 'NONE',  ( 1.000000000000000000, 0.000000000000000000, 0.000000000000000000 ) ) ;
#25374=AXIS2_PLACEMENT_3D ( 'NONE', #29359, #8414, #35029 ) ;
#25377=CARTESIAN_POINT ( 'NONE',  ( 17.99999999999999645, -112.5120133921104753, -43.14554256761131512 ) ) ;
#25378=EDGE_CURVE ( 'NONE', #10354, #42137, #26643, .T. ) ;
#25379=EDGE_LOOP ( 'NONE', ( #33817, #19707, #15585, #7068 ) ) ;
#25380=DIRECTION ( 'NONE',  ( 0.000000000000000000, -0.3140767120219556952, 0.9493976084683790617 ) ) ;
#25381=EDGE_LOOP ( 'NONE', ( #13884, #19403, #38061, #6372 ) ) ;
#25383=ORIENTED_EDGE ( 'NONE', *, *, #27523, .T. ) ;
#25390=ORIENTED_EDGE ( 'NONE', *, *, #22872, .T. ) ;
#25391=ADVANCED_FACE ( 'NONE', ( #30104 ), #13317, .F. ) ;
#25393=AXIS2_PLACEMENT_3D ( 'NONE', #13546, #29918, #8486 ) ;
#25402=ORIENTED_EDGE ( 'NONE', *, *, #14546, .T. ) ;
#25404=DIRECTION ( 'NONE',  ( -1.000000000000000000, -0.000000000000000000, 0.000000000000000000 ) ) ;
#25405=ORIENTED_EDGE ( 'NONE', *, *, #5102, .T. ) ;
#25406=DIRECTION ( 'NONE',  ( -1.000000000000000000, -0.000000000000000000, -0.000000000000000000 ) ) ;
#25408=CARTESIAN_POINT ( 'NONE',  ( -10.00000000000000000, 0.000000000000000000, 0.000000000000000000 ) ) ;
#25409=ORIENTED_EDGE ( 'NONE', *, *, #35787, .T. ) ;
#25411=CIRCLE ( 'NONE', #6540, 59.00000000000000000 ) ;
#25413=ORIENTED_EDGE ( 'NONE', *, *, #32604, .F. ) ;
#25414=AXIS2_PLACEMENT_3D ( 'NONE', #39153, #19358, #38948 ) ;
#25419=AXIS2_PLACEMENT_3D ( 'NONE', #30698, #40691, #10404 ) ;
#25422=CIRCLE ( 'NONE', #12176, 59.00000000000000711 ) ;
#25423=ORIENTED_EDGE ( 'NONE', *, *, #12603, .F. ) ;
#25427=CARTESIAN_POINT ( 'NONE',  ( 17.99999999999999645, 114.6488492393084613, -37.09625815499892809 ) ) ;
#25431=ORIENTED_EDGE ( 'NONE', *, *, #12995, .T. ) ;
#25435=CIRCLE ( 'NONE', #6565, 116.0000000000000000 ) ;
#25436=VERTEX_POINT ( 'NONE', #33570 ) ;
#25438=ORIENTED_EDGE ( 'NONE', *, *, #35351, .T. ) ;
#25445=ORIENTED_EDGE ( 'NONE', *, *, #29851, .F. ) ;
#25448=EDGE_CURVE ( 'NONE', #13710, #38742, #7383, .T. ) ;
#25449=CARTESIAN_POINT ( 'NONE',  ( 17.99999999999999645, -120.2856157092986393, -7.201503623198056481 ) ) ;
#25456=AXIS2_PLACEMENT_3D ( 'NONE', #4443, #27837, #37615 ) ;
#25460=DIRECTION ( 'NONE',  ( 0.000000000000000000, 0.000000000000000000, 1.000000000000000000 ) ) ;
#25461=DIRECTION ( 'NONE',  ( 0.000000000000000000, 0.000000000000000000, 1.000000000000000000 ) ) ;
#25464=EDGE_CURVE ( 'NONE', #287, #21478, #10005, .T. ) ;
#25465=ORIENTED_EDGE ( 'NONE', *, *, #25813, .T. ) ;
#25466=CARTESIAN_POINT ( 'NONE',  ( 0.000000000000000000, 0.000000000000000000, 0.000000000000000000 ) ) ;
#25467=EDGE_CURVE ( 'NONE', #40494, #1834, #3870, .T. ) ;
#25468=FACE_OUTER_BOUND ( 'NONE', #951, .T. ) ;
#25473=CIRCLE ( 'NONE', #3098, 116.0000000000000000 ) ;
#25475=CARTESIAN_POINT ( 'NONE',  ( 17.99999999999999645, 0.000000000000000000, 0.000000000000000000 ) ) ;
#25476=VERTEX_POINT ( 'NONE', #26820 ) ;
#25478=AXIS2_PLACEMENT_3D ( 'NONE', #28583, #31843, #1712 ) ;
#25479=AXIS2_PLACEMENT_3D ( 'NONE', #30008, #40431, #6855 ) ;
#25481=EDGE_LOOP ( 'NONE', ( #2456, #5642, #34268, #17084 ) ) ;
#25482=CARTESIAN_POINT ( 'NONE',  ( 0.000000000000000000, 0.000000000000000000, 0.000000000000000000 ) ) ;
#25483=VERTEX_POINT ( 'NONE', #4093 ) ;
#25484=CARTESIAN_POINT ( 'NONE',  ( 0.000000000000000000, -91.65951123222531294, 71.09524597798055368 ) ) ;
#25485=EDGE_CURVE ( 'NONE', #2881, #9347, #12761, .T. ) ;
#25489=ORIENTED_EDGE ( 'NONE', *, *, #13223, .T. ) ;
#25491=CARTESIAN_POINT ( 'NONE',  ( 17.99999999999999645, -97.19627249181047546, -71.22763238166585609 ) ) ;
#25493=CARTESIAN_POINT ( 'NONE',  ( 17.99999999999999645, 101.1403355683146117, 56.80345518653518866 ) ) ;
#25494=CARTESIAN_POINT ( 'NONE',  ( 17.99999999999999645, -5.456439917445724319, 112.0647122740741963 ) ) ;
#25495=ORIENTED_EDGE ( 'NONE', *, *, #25813, .F. ) ;
#25499=AXIS2_PLACEMENT_3D ( 'NONE', #28875, #39288, #32557 ) ;
#25500=LINE ( 'NONE', #22242, #38376 ) ;
#25501=EDGE_CURVE ( 'NONE', #27165, #508, #35290, .T. ) ;
#25502=AXIS2_PLACEMENT_3D ( 'NONE', #27200, #7756, #34153 ) ;
#25507=CIRCLE ( 'NONE', #24831, 116.0000000000000000 ) ;
#25508=ORIENTED_EDGE ( 'NONE', *, *, #18917, .T. ) ;
#25510=CIRCLE ( 'NONE', #6642, 120.5010000000000190 ) ;
#25513=DIRECTION ( 'NONE',  ( 0.000000000000000000, 0.000000000000000000, 1.000000000000000000 ) ) ;
#25520=ORIENTED_EDGE ( 'NONE', *, *, #7153, .F. ) ;
#25522=CIRCLE ( 'NONE', #15753, 116.0000000000000000 ) ;
#25525=EDGE_LOOP ( 'NONE', ( #25341, #6076, #10017, #32746 ) ) ;
#25529=VERTEX_POINT ( 'NONE', #38550 ) ;
#25533=VECTOR ( 'NONE', #40422, 1000.000000000000000 ) ;
#25534=CARTESIAN_POINT ( 'NONE',  ( 0.000000000000000000, 116.4607004671432406, -30.94182036827089632 ) ) ;
#25535=ORIENTED_EDGE ( 'NONE', *, *, #21243, .F. ) ;
#25537=DIRECTION ( 'NONE',  ( -1.000000000000000000, -0.000000000000000000, -0.000000000000000000 ) ) ;
#25538=CIRCLE ( 'NONE', #9488, 120.5010000000000190 ) ;
#25540=AXIS2_PLACEMENT_3D ( 'NONE', #36570, #572, #10409 ) ;
#25545=AXIS2_PLACEMENT_3D ( 'NONE', #18285, #31550, #8411 ) ;
#25546=DIRECTION ( 'NONE',  ( -1.000000000000000000, -0.000000000000000000, -0.000000000000000000 ) ) ;
#25547=VECTOR ( 'NONE', #16330, 1000.000000000000000 ) ;
#25548=AXIS2_PLACEMENT_3D ( 'NONE', #867, #3923, #24281 ) ;
#25549=ORIENTED_EDGE ( 'NONE', *, *, #21940, .F. ) ;
#25551=EDGE_CURVE ( 'NONE', #26402, #4469, #10630, .T. ) ;
#25554=VERTEX_POINT ( 'NONE', #11776 ) ;
#25556=CARTESIAN_POINT ( 'NONE',  ( 17.99999999999999645, 93.26762629039428987, 76.29967815892386795 ) ) ;
#25558=DIRECTION ( 'NONE',  ( -1.000000000000000000, -0.000000000000000000, -0.000000000000000000 ) ) ;
#25561=DIRECTION ( 'NONE',  ( -1.000000000000000000, -0.000000000000000000, -0.000000000000000000 ) ) ;
#25566=CARTESIAN_POINT ( 'NONE',  ( 0.000000000000000000, -95.38615066513943930, -59.07414607872924250 ) ) ;
#25567=VECTOR ( 'NONE', #39276, 1000.000000000000000 ) ;
#25569=VECTOR ( 'NONE', #26759, 1000.000000000000000 ) ;
#25576=ADVANCED_FACE ( 'NONE', ( #1034 ), #15279, .F. ) ;
#25578=ORIENTED_EDGE ( 'NONE', *, *, #19036, .T. ) ;
#25579=AXIS2_PLACEMENT_3D ( 'NONE', #41802, #15644, #18746 ) ;
#25580=EDGE_CURVE ( 'NONE', #40340, #13758, #19042, .T. ) ;
#25584=LINE ( 'NONE', #27014, #8840 ) ;
#25585=DIRECTION ( 'NONE',  ( 0.000000000000000000, 0.000000000000000000, 1.000000000000000000 ) ) ;
#25593=DIRECTION ( 'NONE',  ( 0.000000000000000000, 0.000000000000000000, 1.000000000000000000 ) ) ;
#25594=CARTESIAN_POINT ( 'NONE',  ( 17.99999999999999645, 0.000000000000000000, 0.000000000000000000 ) ) ;
#25595=ORIENTED_EDGE ( 'NONE', *, *, #41477, .T. ) ;
#25600=ORIENTED_EDGE ( 'NONE', *, *, #34353, .F. ) ;
#25602=ORIENTED_EDGE ( 'NONE', *, *, #9276, .T. ) ;
#25603=CIRCLE ( 'NONE', #6063, 58.99999999999999289 ) ;
#25604=CARTESIAN_POINT ( 'NONE',  ( 17.99999999999999645, 24.22031524826126514, -109.5520369638034879 ) ) ;
#25606=ORIENTED_EDGE ( 'NONE', *, *, #4961, .F. ) ;
#25607=CARTESIAN_POINT ( 'NONE',  ( 17.99999999999999645, -115.5737863835462917, 9.934782381633276316 ) ) ;
#25609=DIRECTION ( 'NONE',  ( 0.000000000000000000, 0.000000000000000000, 1.000000000000000000 ) ) ;
#25611=DIRECTION ( 'NONE',  ( -1.000000000000000000, -0.000000000000000000, -0.000000000000000000 ) ) ;
#25614=LINE ( 'NONE', #22990, #16905 ) ;
#25615=DIRECTION ( 'NONE',  ( 0.000000000000000000, 0.9968120070307504577, -0.07978610555307977248 ) ) ;
#25616=FACE_OUTER_BOUND ( 'NONE', #27352, .T. ) ;
#25618=EDGE_LOOP ( 'NONE', ( #22520, #41001, #5895, #5631 ) ) ;
#25620=ORIENTED_EDGE ( 'NONE', *, *, #6280, .F. ) ;
#25621=DIRECTION ( 'NONE',  ( 1.000000000000000000, 0.000000000000000000, 0.000000000000000000 ) ) ;
#25622=CARTESIAN_POINT ( 'NONE',  ( 0.000000000000000000, 106.5605152861902951, 56.26142179985861702 ) ) ;
#25623=AXIS2_PLACEMENT_3D ( 'NONE', #34133, #18048, #37614 ) ;
#25626=ADVANCED_FACE ( 'NONE', ( #28355 ), #8465, .F. ) ;
#25628=AXIS2_PLACEMENT_3D ( 'NONE', #29052, #24955, #25585 ) ;
#25631=EDGE_CURVE ( 'NONE', #22284, #32317, #5049, .T. ) ;
#25634=AXIS2_PLACEMENT_3D ( 'NONE', #26055, #6392, #12542 ) ;
#25638=DIRECTION ( 'NONE',  ( 1.000000000000000000, 0.000000000000000000, 0.000000000000000000 ) ) ;
#25640=DIRECTION ( 'NONE',  ( 0.000000000000000000, 0.000000000000000000, 1.000000000000000000 ) ) ;
#25642=CARTESIAN_POINT ( 'NONE',  ( -10.00000000000000000, 0.000000000000000000, 0.000000000000000000 ) ) ;
#25646=CARTESIAN_POINT ( 'NONE',  ( 17.99999999999999645, 0.000000000000000000, 0.000000000000000000 ) ) ;
#25652=EDGE_LOOP ( 'NONE', ( #24348, #30753, #11168, #42238 ) ) ;
#25655=CARTESIAN_POINT ( 'NONE',  ( 17.99999999999999645, -117.6086855750632765, -26.24286718912224003 ) ) ;
#25657=CARTESIAN_POINT ( 'NONE',  ( 9.000000000000001776, -41.60679253225688967, -108.2814610871950265 ) ) ;
#25660=VERTEX_POINT ( 'NONE', #31180 ) ;
#25661=LINE ( 'NONE', #29340, #21711 ) ;
#25662=VECTOR ( 'NONE', #5952, 1000.000000000000000 ) ;
#25663=AXIS2_PLACEMENT_3D ( 'NONE', #20977, #34442, #404 ) ;
#25665=ORIENTED_EDGE ( 'NONE', *, *, #6525, .T. ) ;
#25666=CIRCLE ( 'NONE', #40243, 58.99999999999997868 ) ;
#25670=CARTESIAN_POINT ( 'NONE',  ( 0.000000000000000000, 78.18175027177430536, 85.69488855493025881 ) ) ;
#25672=VERTEX_POINT ( 'NONE', #1269 ) ;
#25676=DIRECTION ( 'NONE',  ( 1.000000000000000000, 0.000000000000000000, 0.000000000000000000 ) ) ;
#25681=CARTESIAN_POINT ( 'NONE',  ( 0.000000000000000000, 79.94368240339424858, 90.16373242487935613 ) ) ;
#25682=ORIENTED_EDGE ( 'NONE', *, *, #27484, .F. ) ;
#25683=ADVANCED_FACE ( 'NONE', ( #15046 ), #14613, .F. ) ;
#25684=CARTESIAN_POINT ( 'NONE',  ( 9.000000000000001776, -52.88069566989388903, -103.2454939717374032 ) ) ;
#25685=ORIENTED_EDGE ( 'NONE', *, *, #36752, .T. ) ;
#25691=EDGE_CURVE ( 'NONE', #20648, #33175, #7851, .T. ) ;
#25695=EDGE_LOOP ( 'NONE', ( #4396, #21368, #20711, #43025 ) ) ;
#25696=CARTESIAN_POINT ( 'NONE',  ( -10.00000000000000000, 0.000000000000000000, 0.000000000000000000 ) ) ;
#25697=AXIS2_PLACEMENT_3D ( 'NONE', #7921, #17786, #31063 ) ;
#25698=ORIENTED_EDGE ( 'NONE', *, *, #13590, .T. ) ;
#25700=DIRECTION ( 'NONE',  ( 1.000000000000000000, 0.000000000000000000, 0.000000000000000000 ) ) ;
#25701=EDGE_CURVE ( 'NONE', #20343, #33862, #19600, .T. ) ;
#25704=ORIENTED_EDGE ( 'NONE', *, *, #12557, .T. ) ;
#25705=DIRECTION ( 'NONE',  ( 1.000000000000000000, 0.000000000000000000, 0.000000000000000000 ) ) ;
#25706=EDGE_LOOP ( 'NONE', ( #32949, #5926, #38756, #24749 ) ) ;
#25707=LINE ( 'NONE', #32008, #15470 ) ;
#25708=DIRECTION ( 'NONE',  ( 0.000000000000000000, 0.000000000000000000, 1.000000000000000000 ) ) ;
#25712=FACE_OUTER_BOUND ( 'NONE', #41037, .T. ) ;
#25713=EDGE_CURVE ( 'NONE', #1487, #18549, #28983, .T. ) ;
#25716=ORIENTED_EDGE ( 'NONE', *, *, #717, .T. ) ;
#25718=ADVANCED_FACE ( 'NONE', ( #13050 ), #23100, .F. ) ;
#25721=FACE_OUTER_BOUND ( 'NONE', #8468, .T. ) ;
#25722=EDGE_CURVE ( 'NONE', #287, #41800, #13452, .T. ) ;
#25724=CARTESIAN_POINT ( 'NONE',  ( 8.999999999999998224, 68.63002662989747193, 93.51962064069530811 ) ) ;
#25725=VERTEX_POINT ( 'NONE', #6255 ) ;
#25727=FACE_OUTER_BOUND ( 'NONE', #16245, .T. ) ;
#25729=DIRECTION ( 'NONE',  ( -1.000000000000000000, 0.000000000000000000, 0.000000000000000000 ) ) ;
#25730=DIRECTION ( 'NONE',  ( 0.000000000000000000, 0.000000000000000000, 1.000000000000000000 ) ) ;
#25732=ORIENTED_EDGE ( 'NONE', *, *, #10869, .F. ) ;
#25736=CARTESIAN_POINT ( 'NONE',  ( 17.99999999999999645, 0.000000000000000000, 0.000000000000000000 ) ) ;
#25739=ORIENTED_EDGE ( 'NONE', *, *, #3326, .T. ) ;
#25743=ADVANCED_FACE ( 'NONE', ( #26354 ), #6045, .F. ) ;
#25746=DIRECTION ( 'NONE',  ( 0.000000000000000000, 0.000000000000000000, 1.000000000000000000 ) ) ;
#25747=CARTESIAN_POINT ( 'NONE',  ( 9.000000000000001776, 115.9387338813862129, -3.769613505534868736 ) ) ;
#25749=DIRECTION ( 'NONE',  ( -1.000000000000000000, -0.000000000000000000, -0.000000000000000000 ) ) ;
#25751=CARTESIAN_POINT ( 'NONE',  ( 17.99999999999999645, -90.81729652456213842, 72.16798910853589177 ) ) ;
#25753=VECTOR ( 'NONE', #10976, 1000.000000000000000 ) ;
#25754=VERTEX_POINT ( 'NONE', #26132 ) ;
#25757=ORIENTED_EDGE ( 'NONE', *, *, #11418, .T. ) ;
#25761=CARTESIAN_POINT ( 'NONE',  ( 17.99999999999999645, 63.24564713401792204, 102.5693868539697178 ) ) ;
#25762=EDGE_CURVE ( 'NONE', #28377, #21277, #33631, .T. ) ;
#25765=CARTESIAN_POINT ( 'NONE',  ( 17.99999999999999645, -10.40101730206288444, -120.0512800434972149 ) ) ;
#25766=EDGE_CURVE ( 'NONE', #12374, #38848, #28091, .T. ) ;
#25768=DIRECTION ( 'NONE',  ( 1.000000000000000000, 0.000000000000000000, 0.000000000000000000 ) ) ;
#25769=ORIENTED_EDGE ( 'NONE', *, *, #34628, .T. ) ;
#25771=VERTEX_POINT ( 'NONE', #18980 ) ;
#25775=DIRECTION ( 'NONE',  ( 0.000000000000000000, 0.000000000000000000, 1.000000000000000000 ) ) ;
#25777=AXIS2_PLACEMENT_3D ( 'NONE', #26846, #42741, #3250 ) ;
#25780=DIRECTION ( 'NONE',  ( 0.000000000000000000, 0.3140767120219428166, 0.9493976084683832806 ) ) ;
#25782=ORIENTED_EDGE ( 'NONE', *, *, #17212, .T. ) ;
#25783=DIRECTION ( 'NONE',  ( 1.000000000000000000, 0.000000000000000000, 0.000000000000000000 ) ) ;
#25784=ORIENTED_EDGE ( 'NONE', *, *, #32188, .F. ) ;
#25786=ADVANCED_FACE ( 'NONE', ( #25927 ), #5410, .F. ) ;
#25787=CARTESIAN_POINT ( 'NONE',  ( 0.000000000000000000, -59.47573314508669284, -99.59235496188668435 ) ) ;
#25789=EDGE_CURVE ( 'NONE', #34731, #1340, #16950, .T. ) ;
#25794=DIRECTION ( 'NONE',  ( 1.000000000000000000, 0.000000000000000000, 0.000000000000000000 ) ) ;
#25795=AXIS2_PLACEMENT_3D ( 'NONE', #23512, #35903, #33072 ) ;
#25798=ORIENTED_EDGE ( 'NONE', *, *, #18271, .T. ) ;
#25800=ADVANCED_FACE ( 'NONE', ( #9542 ), #32234, .F. ) ;
#25802=LINE ( 'NONE', #5492, #10332 ) ;
#25803=ORIENTED_EDGE ( 'NONE', *, *, #39091, .T. ) ;
#25806=VERTEX_POINT ( 'NONE', #8899 ) ;
#25811=CARTESIAN_POINT ( 'NONE',  ( 17.99999999999999645, 0.000000000000000000, 0.000000000000000000 ) ) ;
#25812=EDGE_CURVE ( 'NONE', #6504, #16031, #6440, .T. ) ;
#25813=EDGE_CURVE ( 'NONE', #42312, #27034, #1585, .T. ) ;
#25814=EDGE_CURVE ( 'NONE', #25997, #13195, #42647, .T. ) ;
#25816=ORIENTED_EDGE ( 'NONE', *, *, #36981, .F. ) ;
#25817=CARTESIAN_POINT ( 'NONE',  ( 0.000000000000000000, 119.7318547011703629, -13.59315897125607009 ) ) ;
#25818=DIRECTION ( 'NONE',  ( 0.000000000000000000, 0.3641605752528167539, 0.9313361774523405412 ) ) ;
#25821=CARTESIAN_POINT ( 'NONE',  ( 0.000000000000000000, 0.000000000000000000, 0.000000000000000000 ) ) ;
#25825=AXIS2_PLACEMENT_3D ( 'NONE', #8484, #2134, #17929 ) ;
#25826=VERTEX_POINT ( 'NONE', #7319 ) ;
#25827=CARTESIAN_POINT ( 'NONE',  ( 17.99999999999999645, -119.8996782608630838, 12.02323392193314966 ) ) ;
#25829=DIRECTION ( 'NONE',  ( 1.000000000000000000, -0.000000000000000000, -0.000000000000000000 ) ) ;
#25831=CIRCLE ( 'NONE', #38353, 59.00000000000000711 ) ;
#25837=DIRECTION ( 'NONE',  ( 1.000000000000000000, 0.000000000000000000, 0.000000000000000000 ) ) ;
#25839=EDGE_CURVE ( 'NONE', #4984, #23276, #9930, .T. ) ;
#25841=DIRECTION ( 'NONE',  ( 0.000000000000000000, -0.6783118362696222148, 0.7347741508630616369 ) ) ;
#25845=CARTESIAN_POINT ( 'NONE',  ( 17.99999999999999645, -11.65176648920959757, -115.4133282497343487 ) ) ;
#25852=ORIENTED_EDGE ( 'NONE', *, *, #33387, .F. ) ;
#25854=EDGE_LOOP ( 'NONE', ( #32174, #546, #8696, #6466 ) ) ;
#25855=CIRCLE ( 'NONE', #6999, 59.00000000000000000 ) ;
#25856=CARTESIAN_POINT ( 'NONE',  ( 17.99999999999999645, 95.31344542257733110, 66.11616384574480776 ) ) ;
#25857=CIRCLE ( 'NONE', #36965, 120.5010000000000332 ) ;
#25859=DIRECTION ( 'NONE',  ( 1.000000000000000000, 0.000000000000000000, 0.000000000000000000 ) ) ;
#25861=CIRCLE ( 'NONE', #1430, 120.5010000000000474 ) ;
#25864=ORIENTED_EDGE ( 'NONE', *, *, #9150, .F. ) ;
#25866=EDGE_CURVE ( 'NONE', #20175, #416, #28804, .T. ) ;
#25867=EDGE_CURVE ( 'NONE', #7485, #17487, #17413, .T. ) ;
#25870=EDGE_CURVE ( 'NONE', #25754, #37125, #42001, .T. ) ;
#25873=CARTESIAN_POINT ( 'NONE',  ( 17.99999999999999645, -112.5220807139882311, -28.19186676675956704 ) ) ;
#25875=CARTESIAN_POINT ( 'NONE',  ( 17.99999999999999645, 21.55123232222629426, -118.5581519187670096 ) ) ;
#25877=DIRECTION ( 'NONE',  ( 0.000000000000000000, -0.1062934856473723849, 0.9943348002101364269 ) ) ;
#25878=VERTEX_POINT ( 'NONE', #23945 ) ;
#25886=ORIENTED_EDGE ( 'NONE', *, *, #174, .T. ) ;
#25888=CARTESIAN_POINT ( 'NONE',  ( 17.99999999999999645, 111.7974656912331426, -9.465682155094398809 ) ) ;
#25892=CARTESIAN_POINT ( 'NONE',  ( 17.99999999999999645, 119.0898412705476943, -18.38751498043618682 ) ) ;
#25897=ORIENTED_EDGE ( 'NONE', *, *, #30981, .F. ) ;
#25898=DIRECTION ( 'NONE',  ( 0.000000000000000000, 0.000000000000000000, 1.000000000000000000 ) ) ;
#25901=CARTESIAN_POINT ( 'NONE',  ( 17.99999999999999645, 73.78980555658606022, 95.26571049922013401 ) ) ;
#25902=FACE_OUTER_BOUND ( 'NONE', #5148, .T. ) ;
#25903=CARTESIAN_POINT ( 'NONE',  ( 17.99999999999999645, 63.55543939553766108, 97.03971415477347762 ) ) ;
#25904=ORIENTED_EDGE ( 'NONE', *, *, #33799, .F. ) ;
#25906=DIRECTION ( 'NONE',  ( 1.000000000000000000, 0.000000000000000000, 0.000000000000000000 ) ) ;
#25907=DIRECTION ( 'NONE',  ( -1.000000000000000000, 0.000000000000000000, 0.000000000000000000 ) ) ;
#25908=EDGE_LOOP ( 'NONE', ( #41482, #5028, #34180, #23685 ) ) ;
#25910=DIRECTION ( 'NONE',  ( 0.000000000000000000, -2.752035887312358229E-14, -1.000000000000000000 ) ) ;
#25913=VERTEX_POINT ( 'NONE', #16972 ) ;
#25914=ORIENTED_EDGE ( 'NONE', *, *, #31037, .T. ) ;
#25916=DIRECTION ( 'NONE',  ( 1.000000000000000000, 0.000000000000000000, 0.000000000000000000 ) ) ;
#25927=FACE_OUTER_BOUND ( 'NONE', #23861, .T. ) ;
#25928=DIRECTION ( 'NONE',  ( 0.000000000000000000, 0.000000000000000000, 1.000000000000000000 ) ) ;
#25931=VERTEX_POINT ( 'NONE', #7111 ) ;
#25933=DIRECTION ( 'NONE',  ( 0.000000000000000000, 0.9996456111234524045, 0.02662052143777824190 ) ) ;
#25935=LINE ( 'NONE', #39195, #3130 ) ;
#25941=AXIS2_PLACEMENT_3D ( 'NONE', #32965, #36016, #18862 ) ;
#25942=EDGE_CURVE ( 'NONE', #18762, #25931, #16255, .T. ) ;
#25944=DIRECTION ( 'NONE',  ( -1.000000000000000000, -0.000000000000000000, -0.000000000000000000 ) ) ;
#25946=AXIS2_PLACEMENT_3D ( 'NONE', #26851, #23610, #40125 ) ;
#25949=DIRECTION ( 'NONE',  ( 1.000000000000000000, -0.000000000000000000, 0.000000000000000000 ) ) ;
#25957=ORIENTED_EDGE ( 'NONE', *, *, #5542, .F. ) ;
#25958=EDGE_CURVE ( 'NONE', #36617, #20671, #3670, .T. ) ;
#25959=ORIENTED_EDGE ( 'NONE', *, *, #26195, .T. ) ;
#25960=CYLINDRICAL_SURFACE ( 'NONE', #37917, 59.00000000000000000 ) ;
#25961=VERTEX_POINT ( 'NONE', #9952 ) ;
#25964=CARTESIAN_POINT ( 'NONE',  ( 0.000000000000000000, -103.1672962317654338, 44.09967643725834563 ) ) ;
#25965=ORIENTED_EDGE ( 'NONE', *, *, #41422, .T. ) ;
#25967=ADVANCED_FACE ( 'NONE', ( #20044 ), #14124, .F. ) ;
#25969=VECTOR ( 'NONE', #30312, 1000.000000000000000 ) ;
#25971=DIRECTION ( 'NONE',  ( 1.000000000000000000, -0.000000000000000000, 0.000000000000000000 ) ) ;
#25973=ORIENTED_EDGE ( 'NONE', *, *, #30631, .F. ) ;
#25974=DIRECTION ( 'NONE',  ( 1.000000000000000000, 0.000000000000000000, -0.000000000000000000 ) ) ;
#25976=EDGE_CURVE ( 'NONE', #9503, #22001, #39219, .T. ) ;
#25983=ORIENTED_EDGE ( 'NONE', *, *, #9764, .T. ) ;
#25990=CARTESIAN_POINT ( 'NONE',  ( 17.99999999999999645, -110.0562500189195561, -49.07252625220223052 ) ) ;
#25992=AXIS2_PLACEMENT_3D ( 'NONE', #19182, #32447, #2535 ) ;
#25995=DIRECTION ( 'NONE',  ( -1.000000000000000000, -0.000000000000000000, -0.000000000000000000 ) ) ;
#25997=VERTEX_POINT ( 'NONE', #41782 ) ;
#25998=DIRECTION ( 'NONE',  ( 0.000000000000000000, 0.000000000000000000, 1.000000000000000000 ) ) ;
#25999=DIRECTION ( 'NONE',  ( -1.000000000000000000, -0.000000000000000000, 0.000000000000000000 ) ) ;
#26000=VERTEX_POINT ( 'NONE', #7550 ) ;
#26007=DIRECTION ( 'NONE',  ( 0.000000000000000000, 0.6382441836448161654, 0.7698339834299096074 ) ) ;
#26008=DIRECTION ( 'NONE',  ( 0.000000000000000000, 0.000000000000000000, 1.000000000000000000 ) ) ;
#26010=ORIENTED_EDGE ( 'NONE', *, *, #22592, .F. ) ;
#26011=CYLINDRICAL_SURFACE ( 'NONE', #28691, 120.5010000000000190 ) ;
#26013=CARTESIAN_POINT ( 'NONE',  ( 17.99999999999999645, 27.83061035787113369, -117.2431154827794586 ) ) ;
#26014=CARTESIAN_POINT ( 'NONE',  ( 17.99999999999999645, -114.1529630473446986, -38.59523323561551678 ) ) ;
#26023=ORIENTED_EDGE ( 'NONE', *, *, #17667, .T. ) ;
#26031=AXIS2_PLACEMENT_3D ( 'NONE', #43117, #23735, #33521 ) ;
#26036=ADVANCED_FACE ( 'NONE', ( #38297 ), #31123, .F. ) ;
#26039=CARTESIAN_POINT ( 'NONE',  ( 0.000000000000000000, 0.000000000000000000, 0.000000000000000000 ) ) ;
#26040=VECTOR ( 'NONE', #14649, 1000.000000000000000 ) ;
#26048=AXIS2_PLACEMENT_3D ( 'NONE', #25408, #2853, #28877 ) ;
#26051=CARTESIAN_POINT ( 'NONE',  ( 17.99999999999999645, -54.09091620264652533, -102.6166301549523467 ) ) ;
#26052=VERTEX_POINT ( 'NONE', #25051 ) ;
#26055=CARTESIAN_POINT ( 'NONE',  ( 17.99999999999999645, 110.1579703617969130, -21.29539948940136540 ) ) ;
#26059=EDGE_LOOP ( 'NONE', ( #38816, #22881, #33602, #33900 ) ) ;
#26061=ORIENTED_EDGE ( 'NONE', *, *, #7862, .F. ) ;
#26064=ORIENTED_EDGE ( 'NONE', *, *, #33751, .T. ) ;
#26066=EDGE_CURVE ( 'NONE', #36553, #7888, #36415, .T. ) ;
#26069=EDGE_CURVE ( 'NONE', #29131, #12550, #8206, .T. ) ;
#26071=DIRECTION ( 'NONE',  ( 0.000000000000000000, 0.000000000000000000, 1.000000000000000000 ) ) ;
#26075=AXIS2_PLACEMENT_3D ( 'NONE', #21863, #35328, #12019 ) ;
#26078=DIRECTION ( 'NONE',  ( -1.000000000000000000, -0.000000000000000000, -0.000000000000000000 ) ) ;
#26082=CARTESIAN_POINT ( 'NONE',  ( 17.99999999999999645, 93.26762629039527042, -76.29967815892260319 ) ) ;
#26083=CARTESIAN_POINT ( 'NONE',  ( 0.000000000000000000, -92.10690493017105496, 64.06707842432145128 ) ) ;
#26084=EDGE_LOOP ( 'NONE', ( #24143, #35162, #35286, #35030 ) ) ;
#26085=AXIS2_PLACEMENT_3D ( 'NONE', #19452, #33147, #25780 ) ;
#26087=AXIS2_PLACEMENT_3D ( 'NONE', #35316, #32687, #2765 ) ;
#26088=EDGE_CURVE ( 'NONE', #26682, #16913, #17681, .T. ) ;
#26091=LINE ( 'NONE', #38729, #20682 ) ;
#26092=EDGE_CURVE ( 'NONE', #25238, #5363, #1616, .T. ) ;
#26097=DIRECTION ( 'NONE',  ( 0.000000000000000000, 0.000000000000000000, 1.000000000000000000 ) ) ;
#26099=EDGE_CURVE ( 'NONE', #18966, #37469, #39900, .T. ) ;
#26104=AXIS2_PLACEMENT_3D ( 'NONE', #3641, #13732, #34407 ) ;
#26108=ORIENTED_EDGE ( 'NONE', *, *, #5297, .T. ) ;
#26113=DIRECTION ( 'NONE',  ( 1.000000000000000000, 0.000000000000000000, 0.000000000000000000 ) ) ;
#26114=ORIENTED_EDGE ( 'NONE', *, *, #33421, .T. ) ;
#26116=DIRECTION ( 'NONE',  ( -1.000000000000000000, -0.000000000000000000, -0.000000000000000000 ) ) ;
#26117=AXIS2_PLACEMENT_3D ( 'NONE', #42899, #33089, #25933 ) ;
#26118=CARTESIAN_POINT ( 'NONE',  ( 17.99999999999999645, 110.1579703617966430, 21.29539948940285043 ) ) ;
#26120=CIRCLE ( 'NONE', #21975, 120.5010000000000332 ) ;
#26122=CARTESIAN_POINT ( 'NONE',  ( 17.99999999999999645, -105.7179949885870514, 37.57629584241652054 ) ) ;
#26126=CARTESIAN_POINT ( 'NONE',  ( 17.99999999999999645, 0.000000000000000000, 0.000000000000000000 ) ) ;
#26128=ORIENTED_EDGE ( 'NONE', *, *, #6662, .F. ) ;
#26129=DIRECTION ( 'NONE',  ( 1.000000000000000000, 0.000000000000000000, 0.000000000000000000 ) ) ;
#26132=CARTESIAN_POINT ( 'NONE',  ( 17.99999999999999645, -37.07968990261553444, 109.9140418541956308 ) ) ;
#26135=ORIENTED_EDGE ( 'NONE', *, *, #28767, .F. ) ;
#26137=CARTESIAN_POINT ( 'NONE',  ( 17.99999999999999645, -8.827181066045094227, -120.1772519049560231 ) ) ;
#26149=ORIENTED_EDGE ( 'NONE', *, *, #30930, .F. ) ;
#26151=CYLINDRICAL_SURFACE ( 'NONE', #29164, 59.00000000000000000 ) ;
#26152=DIRECTION ( 'NONE',  ( -1.000000000000000000, -0.000000000000000000, -0.000000000000000000 ) ) ;
#26153=CARTESIAN_POINT ( 'NONE',  ( 8.999999999999998224, 68.63002662989875091, -93.51962064069435598 ) ) ;
#26155=CARTESIAN_POINT ( 'NONE',  ( 17.99999999999999645, 92.25992191227393846, 77.51514567967427638 ) ) ;
#26160=VECTOR ( 'NONE', #11877, 1000.000000000000000 ) ;
#26161=ORIENTED_EDGE ( 'NONE', *, *, #37278, .T. ) ;
#26165=ORIENTED_EDGE ( 'NONE', *, *, #18536, .F. ) ;
#26167=VECTOR ( 'NONE', #11587, 1000.000000000000000 ) ;
#26169=VERTEX_POINT ( 'NONE', #29356 ) ;
#26170=DIRECTION ( 'NONE',  ( 0.000000000000000000, 0.000000000000000000, 1.000000000000000000 ) ) ;
#26171=ORIENTED_EDGE ( 'NONE', *, *, #22559, .F. ) ;
#26172=AXIS2_PLACEMENT_3D ( 'NONE', #13713, #10419, #7131 ) ;
#26176=CARTESIAN_POINT ( 'NONE',  ( 0.000000000000000000, 0.000000000000000000, 0.000000000000000000 ) ) ;
#26177=DIRECTION ( 'NONE',  ( 0.000000000000000000, 0.05322217484217219019, 0.9985826956767622775 ) ) ;
#26181=VERTEX_POINT ( 'NONE', #18725 ) ;
#26182=CYLINDRICAL_SURFACE ( 'NONE', #3618, 120.5010000000000190 ) ;
#26183=ORIENTED_EDGE ( 'NONE', *, *, #9795, .T. ) ;
#26185=CARTESIAN_POINT ( 'NONE',  ( 0.000000000000000000, 79.18387647320761857, 84.76976882518788159 ) ) ;
#26192=EDGE_CURVE ( 'NONE', #39703, #29060, #5111, .T. ) ;
#26194=AXIS2_PLACEMENT_3D ( 'NONE', #39227, #9354, #33133 ) ;
#26195=EDGE_CURVE ( 'NONE', #29429, #22119, #23921, .T. ) ;
#26196=VECTOR ( 'NONE', #37224, 1000.000000000000000 ) ;
#26201=DIRECTION ( 'NONE',  ( -1.000000000000000000, -0.000000000000000000, 0.000000000000000000 ) ) ;
#26205=VERTEX_POINT ( 'NONE', #9053 ) ;
#26207=DIRECTION ( 'NONE',  ( -1.000000000000000000, -0.000000000000000000, -0.000000000000000000 ) ) ;
#26210=EDGE_CURVE ( 'NONE', #28231, #36745, #25361, .T. ) ;
#26216=VERTEX_POINT ( 'NONE', #38932 ) ;
#26217=DIRECTION ( 'NONE',  ( 0.000000000000000000, 0.000000000000000000, 1.000000000000000000 ) ) ;
#26221=FACE_OUTER_BOUND ( 'NONE', #18058, .T. ) ;
#26224=ORIENTED_EDGE ( 'NONE', *, *, #2675, .F. ) ;
#26225=EDGE_CURVE ( 'NONE', #42671, #35898, #35066, .T. ) ;
#26228=AXIS2_PLACEMENT_3D ( 'NONE', #24302, #37558, #26894 ) ;
#26231=EDGE_CURVE ( 'NONE', #18907, #15552, #7911, .T. ) ;
#26235=DIRECTION ( 'NONE',  ( 0.000000000000000000, 0.000000000000000000, 1.000000000000000000 ) ) ;
#26236=ORIENTED_EDGE ( 'NONE', *, *, #12503, .F. ) ;
#26238=AXIS2_PLACEMENT_3D ( 'NONE', #360, #7582, #33114 ) ;
#26247=ADVANCED_FACE ( 'NONE', ( #39343 ), #15840, .F. ) ;
#26249=VERTEX_POINT ( 'NONE', #35652 ) ;
#26254=CARTESIAN_POINT ( 'NONE',  ( 0.000000000000000000, 0.000000000000000000, 0.000000000000000000 ) ) ;
#26256=DIRECTION ( 'NONE',  ( 0.000000000000000000, 0.000000000000000000, 1.000000000000000000 ) ) ;
#26258=EDGE_CURVE ( 'NONE', #18549, #8622, #14190, .T. ) ;
#26260=ORIENTED_EDGE ( 'NONE', *, *, #6607, .T. ) ;
#26263=LINE ( 'NONE', #23430, #7614 ) ;
#26265=CIRCLE ( 'NONE', #6746, 58.99999999999999289 ) ;
#26270=ORIENTED_EDGE ( 'NONE', *, *, #20460, .T. ) ;
#26272=ORIENTED_EDGE ( 'NONE', *, *, #20427, .T. ) ;
#26273=DIRECTION ( 'NONE',  ( -1.000000000000000000, 0.000000000000000000, 0.000000000000000000 ) ) ;
#26274=ORIENTED_EDGE ( 'NONE', *, *, #7152, .F. ) ;
#26276=ORIENTED_EDGE ( 'NONE', *, *, #28685, .F. ) ;
#26277=AXIS2_PLACEMENT_3D ( 'NONE', #38289, #5350, #8608 ) ;
#26280=DIRECTION ( 'NONE',  ( 1.000000000000000000, 0.000000000000000000, 0.000000000000000000 ) ) ;
#26286=EDGE_CURVE ( 'NONE', #8183, #41276, #37860, .T. ) ;
#26287=AXIS2_PLACEMENT_3D ( 'NONE', #32845, #42006, #6013 ) ;
#26291=FACE_OUTER_BOUND ( 'NONE', #29170, .T. ) ;
#26292=EDGE_LOOP ( 'NONE', ( #23117, #26861, #21169, #33343 ) ) ;
#26293=CARTESIAN_POINT ( 'NONE',  ( 17.99999999999999645, -34.03109950475805334, 115.5957406979048727 ) ) ;
#26294=CIRCLE ( 'NONE', #2583, 120.5010000000000474 ) ;
#26295=ORIENTED_EDGE ( 'NONE', *, *, #3396, .F. ) ;
#26300=AXIS2_PLACEMENT_3D ( 'NONE', #2291, #20989, #17491 ) ;
#26303=DIRECTION ( 'NONE',  ( 1.000000000000000000, 0.000000000000000000, 0.000000000000000000 ) ) ;
#26304=CIRCLE ( 'NONE', #36698, 116.0000000000000000 ) ;
#26305=ORIENTED_EDGE ( 'NONE', *, *, #1041, .F. ) ;
#26306=AXIS2_PLACEMENT_3D ( 'NONE', #24062, #37330, #20807 ) ;
#26317=DIRECTION ( 'NONE',  ( -1.000000000000000000, -0.000000000000000000, -0.000000000000000000 ) ) ;
#26320=VERTEX_POINT ( 'NONE', #19341 ) ;
#26325=FACE_OUTER_BOUND ( 'NONE', #35413, .T. ) ;
#26329=AXIS2_PLACEMENT_3D ( 'NONE', #28387, #1511, #4801 ) ;
#26334=DIRECTION ( 'NONE',  ( 1.000000000000000000, 0.000000000000000000, 0.000000000000000000 ) ) ;
#26336=AXIS2_PLACEMENT_3D ( 'NONE', #14743, #31088, #34787 ) ;
#26337=CARTESIAN_POINT ( 'NONE',  ( 9.000000000000001776, 23.85344185397197947, 113.5209818126991621 ) ) ;
#26341=LINE ( 'NONE', #43099, #8480 ) ;
#26343=CYLINDRICAL_SURFACE ( 'NONE', #25795, 116.0000000000000000 ) ;
#26344=AXIS2_PLACEMENT_3D ( 'NONE', #26126, #39615, #36547 ) ;
#26345=EDGE_CURVE ( 'NONE', #4115, #5703, #4150, .T. ) ;
#26348=EDGE_CURVE ( 'NONE', #20934, #7958, #24287, .T. ) ;
#26350=DIRECTION ( 'NONE',  ( 1.000000000000000000, 0.000000000000000000, 0.000000000000000000 ) ) ;
#26352=DIRECTION ( 'NONE',  ( 0.000000000000000000, 0.000000000000000000, 1.000000000000000000 ) ) ;
#26353=ORIENTED_EDGE ( 'NONE', *, *, #27560, .T. ) ;
#26354=FACE_OUTER_BOUND ( 'NONE', #5527, .T. ) ;
#26358=VERTEX_POINT ( 'NONE', #33840 ) ;
#26360=VECTOR ( 'NONE', #2274, 1000.000000000000000 ) ;
#26361=DIRECTION ( 'NONE',  ( 0.000000000000000000, -0.1590634960190596414, -0.9872683547213465527 ) ) ;
#26363=CIRCLE ( 'NONE', #34691, 59.00000000000000000 ) ;
#26364=CARTESIAN_POINT ( 'NONE',  ( 0.000000000000000000, 52.19040376560566585, -99.31985817764127944 ) ) ;
#26365=VERTEX_POINT ( 'NONE', #37326 ) ;
#26371=LINE ( 'NONE', #43130, #25547 ) ;
#26372=CARTESIAN_POINT ( 'NONE',  ( 8.999999999999998224, -59.47573314508800024, 99.59235496188593117 ) ) ;
#26375=CARTESIAN_POINT ( 'NONE',  ( -10.00000000000000000, 0.000000000000000000, 0.000000000000000000 ) ) ;
#26377=DIRECTION ( 'NONE',  ( 0.000000000000000000, 0.5076658003388352380, 0.8615540813938089570 ) ) ;
#26381=CYLINDRICAL_SURFACE ( 'NONE', #25058, 116.0000000000000000 ) ;
#26384=CIRCLE ( 'NONE', #38906, 116.0000000000000000 ) ;
#26385=CARTESIAN_POINT ( 'NONE',  ( 0.000000000000000000, 29.02167576844106023, 108.3790330702170621 ) ) ;
#26390=CARTESIAN_POINT ( 'NONE',  ( 17.99999999999999645, -112.1427988504408120, 3.502162136923045566 ) ) ;
#26392=AXIS2_PLACEMENT_3D ( 'NONE', #13176, #26469, #32578 ) ;
#26393=CARTESIAN_POINT ( 'NONE',  ( 17.99999999999999645, 45.89132998248186368, -102.3829004574625401 ) ) ;
#26400=CARTESIAN_POINT ( 'NONE',  ( 17.99999999999999645, 2.418575551220858877, 120.4767259403369053 ) ) ;
#26401=EDGE_CURVE ( 'NONE', #17636, #17009, #41342, .T. ) ;
#26402=VERTEX_POINT ( 'NONE', #20802 ) ;
#26403=CARTESIAN_POINT ( 'NONE',  ( 0.000000000000000000, -0.5156212287287311735, 112.1962860721878172 ) ) ;
#26406=CARTESIAN_POINT ( 'NONE',  ( 0.000000000000000000, 61.59243992711585491, -93.77976230225978327 ) ) ;
#26409=CARTESIAN_POINT ( 'NONE',  ( 0.000000000000000000, -115.9387338813861277, -3.769613505537241949 ) ) ;
#26412=EDGE_LOOP ( 'NONE', ( #26753, #30228, #16043, #29404 ) ) ;
#26416=AXIS2_PLACEMENT_3D ( 'NONE', #29116, #38904, #31953 ) ;
#26419=CARTESIAN_POINT ( 'NONE',  ( 0.000000000000000000, -6.854627147199490622, 115.7972974066013307 ) ) ;
#26420=ORIENTED_EDGE ( 'NONE', *, *, #41422, .F. ) ;
#26423=CARTESIAN_POINT ( 'NONE',  ( 17.99999999999999645, 0.000000000000000000, 0.000000000000000000 ) ) ;
#26424=ORIENTED_EDGE ( 'NONE', *, *, #27733, .T. ) ;
#26426=CARTESIAN_POINT ( 'NONE',  ( 17.99999999999999645, -62.45178862086154226, -93.20969140437570388 ) ) ;
#26436=AXIS2_PLACEMENT_3D ( 'NONE', #42779, #9427, #16667 ) ;
#26440=EDGE_LOOP ( 'NONE', ( #30680, #17917, #21022, #11036 ) ) ;
#26441=CARTESIAN_POINT ( 'NONE',  ( 0.000000000000000000, -78.75547124681428102, 91.20343606296975736 ) ) ;
#26442=DIRECTION ( 'NONE',  ( -1.000000000000000000, -0.000000000000000000, 0.000000000000000000 ) ) ;
#26444=DIRECTION ( 'NONE',  ( 0.000000000000000000, 0.000000000000000000, 1.000000000000000000 ) ) ;
#26454=DIRECTION ( 'NONE',  ( 0.000000000000000000, -0.9714298932647074114, -0.2373266998711251186 ) ) ;
#26455=EDGE_LOOP ( 'NONE', ( #264, #29739, #33887, #2500 ) ) ;
#26456=DIRECTION ( 'NONE',  ( 0.000000000000000000, 0.000000000000000000, 1.000000000000000000 ) ) ;
#26461=VERTEX_POINT ( 'NONE', #19764 ) ;
#26463=DIRECTION ( 'NONE',  ( -1.000000000000000000, -0.000000000000000000, -0.000000000000000000 ) ) ;
#26464=CIRCLE ( 'NONE', #33398, 120.5010000000000190 ) ;
#26469=DIRECTION ( 'NONE',  ( -1.000000000000000000, -0.000000000000000000, -0.000000000000000000 ) ) ;
#26470=EDGE_LOOP ( 'NONE', ( #6069, #10846, #24482, #30275 ) ) ;
#26471=DIRECTION ( 'NONE',  ( 0.000000000000000000, 0.000000000000000000, 1.000000000000000000 ) ) ;
#26473=DIRECTION ( 'NONE',  ( 0.000000000000000000, 0.000000000000000000, 1.000000000000000000 ) ) ;
#26475=ORIENTED_EDGE ( 'NONE', *, *, #33750, .F. ) ;
#26477=DIRECTION ( 'NONE',  ( -1.000000000000000000, 0.000000000000000000, -0.000000000000000000 ) ) ;
#26487=CARTESIAN_POINT ( 'NONE',  ( 9.000000000000001776, -112.8457601792517124, 26.86697618949339272 ) ) ;
#26489=EDGE_LOOP ( 'NONE', ( #34747, #33241, #16318, #13463 ) ) ;
#26491=ORIENTED_EDGE ( 'NONE', *, *, #33372, .T. ) ;
#26493=AXIS2_PLACEMENT_3D ( 'NONE', #35198, #5322, #15391 ) ;
#26494=CIRCLE ( 'NONE', #32070, 116.0000000000000000 ) ;
#26495=VECTOR ( 'NONE', #18856, 1000.000000000000000 ) ;
#26497=CARTESIAN_POINT ( 'NONE',  ( 17.99999999999999645, -21.55123232222554464, 118.5581519187671660 ) ) ;
#26498=CIRCLE ( 'NONE', #34178, 58.99999999999999289 ) ;
#26499=CYLINDRICAL_SURFACE ( 'NONE', #1754, 59.00000000000000000 ) ;
#26501=DIRECTION ( 'NONE',  ( 1.000000000000000000, 0.000000000000000000, 0.000000000000000000 ) ) ;
#26503=EDGE_CURVE ( 'NONE', #5464, #24053, #40800, .T. ) ;
#26506=CYLINDRICAL_SURFACE ( 'NONE', #4419, 59.00000000000000000 ) ;
#26508=VERTEX_POINT ( 'NONE', #34921 ) ;
#26512=DIRECTION ( 'NONE',  ( 1.000000000000000000, 0.000000000000000000, 0.000000000000000000 ) ) ;
#26515=DIRECTION ( 'NONE',  ( -1.000000000000000000, -0.000000000000000000, -0.000000000000000000 ) ) ;
#26518=ORIENTED_EDGE ( 'NONE', *, *, #23626, .F. ) ;
#26520=ORIENTED_EDGE ( 'NONE', *, *, #630, .T. ) ;
#26521=CIRCLE ( 'NONE', #7698, 59.00000000000000000 ) ;
#26527=DIRECTION ( 'NONE',  ( -1.000000000000000000, -0.000000000000000000, -0.000000000000000000 ) ) ;
#26528=AXIS2_PLACEMENT_3D ( 'NONE', #31798, #11298, #25276 ) ;
#26530=ORIENTED_EDGE ( 'NONE', *, *, #13244, .T. ) ;
#26540=ORIENTED_EDGE ( 'NONE', *, *, #18319, .F. ) ;
#26541=ORIENTED_EDGE ( 'NONE', *, *, #10177, .F. ) ;
#26546=CIRCLE ( 'NONE', #7720, 120.5010000000000190 ) ;
#26548=DIRECTION ( 'NONE',  ( 0.000000000000000000, 0.7865515558026436871, -0.6175246149461902645 ) ) ;
#26549=AXIS2_PLACEMENT_3D ( 'NONE', #30642, #26501, #13206 ) ;
#26553=ADVANCED_FACE ( 'NONE', ( #15326 ), #11379, .F. ) ;
#26556=CYLINDRICAL_SURFACE ( 'NONE', #40773, 120.5010000000000190 ) ;
#26560=CARTESIAN_POINT ( 'NONE',  ( 17.99999999999999645, 0.000000000000000000, 0.000000000000000000 ) ) ;
#26561=ORIENTED_EDGE ( 'NONE', *, *, #6345, .T. ) ;
#26563=CARTESIAN_POINT ( 'NONE',  ( 17.99999999999999645, 75.72520367775085504, 82.78868281116005789 ) ) ;
#26567=ORIENTED_EDGE ( 'NONE', *, *, #8739, .F. ) ;
#26568=LINE ( 'NONE', #33529, #26196 ) ;
#26569=EDGE_LOOP ( 'NONE', ( #7576, #41705, #6485, #37304 ) ) ;
#26574=EDGE_LOOP ( 'NONE', ( #26887, #37463, #35869, #2241 ) ) ;
#26575=ADVANCED_FACE ( 'NONE', ( #18181 ), #14667, .F. ) ;
#26576=DIRECTION ( 'NONE',  ( 0.000000000000000000, 0.9826841245925214130, -0.1852887240871113894 ) ) ;
#26579=EDGE_CURVE ( 'NONE', #28841, #16283, #13508, .T. ) ;
#26580=ADVANCED_FACE ( 'NONE', ( #27974 ), #2168, .F. ) ;
#26582=ORIENTED_EDGE ( 'NONE', *, *, #1110, .T. ) ;
#26583=DIRECTION ( 'NONE',  ( 0.000000000000000000, 0.7525707698561354686, 0.6585113790650420906 ) ) ;
#26584=CIRCLE ( 'NONE', #34723, 120.5010000000000332 ) ;
#26585=ORIENTED_EDGE ( 'NONE', *, *, #18398, .T. ) ;
#26588=CARTESIAN_POINT ( 'NONE',  ( 17.99999999999999645, -106.6051926090968180, -45.73109345704927620 ) ) ;
#26590=AXIS2_PLACEMENT_3D ( 'NONE', #3483, #29709, #36653 ) ;
#26592=DIRECTION ( 'NONE',  ( 0.000000000000000000, 0.000000000000000000, 1.000000000000000000 ) ) ;
#26598=VERTEX_POINT ( 'NONE', #35551 ) ;
#26605=ORIENTED_EDGE ( 'NONE', *, *, #31650, .T. ) ;
#26606=FACE_OUTER_BOUND ( 'NONE', #26470, .T. ) ;
#26611=CARTESIAN_POINT ( 'NONE',  ( 0.000000000000000000, -119.8996782608630838, 12.02323392193314966 ) ) ;
#26612=ORIENTED_EDGE ( 'NONE', *, *, #5243, .F. ) ;
#26618=ORIENTED_EDGE ( 'NONE', *, *, #13450, .F. ) ;
#26620=CIRCLE ( 'NONE', #40512, 116.0000000000000000 ) ;
#26623=DIRECTION ( 'NONE',  ( -1.000000000000000000, 0.000000000000000000, -0.000000000000000000 ) ) ;
#26624=DIRECTION ( 'NONE',  ( -1.000000000000000000, 0.000000000000000000, 0.000000000000000000 ) ) ;
#26630=DIRECTION ( 'NONE',  ( -1.000000000000000000, 0.000000000000000000, 0.000000000000000000 ) ) ;
#26635=CYLINDRICAL_SURFACE ( 'NONE', #29254, 116.0000000000000000 ) ;
#26636=DIRECTION ( 'NONE',  ( -1.000000000000000000, -0.000000000000000000, 0.000000000000000000 ) ) ;
#26638=CARTESIAN_POINT ( 'NONE',  ( -10.00000000000000000, 0.000000000000000000, 0.000000000000000000 ) ) ;
#26639=DIRECTION ( 'NONE',  ( 0.000000000000000000, 0.000000000000000000, 1.000000000000000000 ) ) ;
#26640=VERTEX_POINT ( 'NONE', #41681 ) ;
#26642=ORIENTED_EDGE ( 'NONE', *, *, #19895, .T. ) ;
#26643=CIRCLE ( 'NONE', #12031, 59.00000000000000000 ) ;
#26644=ORIENTED_EDGE ( 'NONE', *, *, #39073, .F. ) ;
#26645=CARTESIAN_POINT ( 'NONE',  ( 17.99999999999999645, 52.88069566989596382, -103.2454939717363516 ) ) ;
#26649=EDGE_LOOP ( 'NONE', ( #23248, #8258, #4802, #308 ) ) ;
#26650=DIRECTION ( 'NONE',  ( -1.000000000000000000, -0.000000000000000000, 0.000000000000000000 ) ) ;
#26651=AXIS2_PLACEMENT_3D ( 'NONE', #8493, #15081, #8704 ) ;
#26652=CYLINDRICAL_SURFACE ( 'NONE', #33801, 120.5010000000000190 ) ;
#26653=DIRECTION ( 'NONE',  ( 0.000000000000000000, 0.000000000000000000, 1.000000000000000000 ) ) ;
#26656=CIRCLE ( 'NONE', #16264, 59.00000000000000000 ) ;
#26659=CARTESIAN_POINT ( 'NONE',  ( 17.99999999999999645, 100.6739960869724655, -49.52796165323157851 ) ) ;
#26660=EDGE_CURVE ( 'NONE', #39282, #43150, #7936, .T. ) ;
#26661=DIRECTION ( 'NONE',  ( 0.000000000000000000, 0.000000000000000000, 1.000000000000000000 ) ) ;
#26665=EDGE_LOOP ( 'NONE', ( #11714, #42303, #33440, #34301 ) ) ;
#26669=CARTESIAN_POINT ( 'NONE',  ( 17.99999999999999645, 0.000000000000000000, 0.000000000000000000 ) ) ;
#26672=AXIS2_PLACEMENT_3D ( 'NONE', #17465, #385, #40093 ) ;
#26679=EDGE_CURVE ( 'NONE', #20934, #31940, #31651, .T. ) ;
#26682=VERTEX_POINT ( 'NONE', #39237 ) ;
#26684=ORIENTED_EDGE ( 'NONE', *, *, #5201, .T. ) ;
#26688=ORIENTED_EDGE ( 'NONE', *, *, #14490, .T. ) ;
#26692=DIRECTION ( 'NONE',  ( 0.000000000000000000, 0.000000000000000000, 1.000000000000000000 ) ) ;
#26693=VERTEX_POINT ( 'NONE', #39034 ) ;
#26694=DIRECTION ( 'NONE',  ( -1.000000000000000000, -0.000000000000000000, -0.000000000000000000 ) ) ;
#26697=CARTESIAN_POINT ( 'NONE',  ( 17.99999999999999645, 115.0622509503834578, -14.72000021165029082 ) ) ;
#26705=ORIENTED_EDGE ( 'NONE', *, *, #35416, .F. ) ;
#26707=CARTESIAN_POINT ( 'NONE',  ( 8.999999999999998224, -73.51007459736489125, 89.73443560133338792 ) ) ;
#26711=DIRECTION ( 'NONE',  ( 0.000000000000000000, -6.586068790149233915E-15, 1.000000000000000000 ) ) ;
#26712=STYLED_ITEM ( 'NONE', ( #14772 ), #21924 ) ;
#26714=CIRCLE ( 'NONE', #7892, 120.5010000000000332 ) ;
#26718=DIRECTION ( 'NONE',  ( -1.000000000000000000, 0.000000000000000000, -0.000000000000000000 ) ) ;
#26724=CIRCLE ( 'NONE', #18424, 120.5010000000000190 ) ;
#26725=CARTESIAN_POINT ( 'NONE',  ( 17.99999999999999645, -6.854627147199490622, 115.7972974066013307 ) ) ;
#26729=DIRECTION ( 'NONE',  ( -1.000000000000000000, 0.000000000000000000, 0.000000000000000000 ) ) ;
#26730=EDGE_CURVE ( 'NONE', #6975, #40301, #39462, .T. ) ;
#26733=CARTESIAN_POINT ( 'NONE',  ( 8.999999999999998224, 109.3506818544110217, 38.70953859161049593 ) ) ;
#26735=CARTESIAN_POINT ( 'NONE',  ( 0.000000000000000000, 110.3490479609629489, 20.28201389785587949 ) ) ;
#26743=ADVANCED_FACE ( 'NONE', ( #15956 ), #13323, .F. ) ;
#26745=CIRCLE ( 'NONE', #13525, 59.00000000000000000 ) ;
#26752=VERTEX_POINT ( 'NONE', #35977 ) ;
#26753=ORIENTED_EDGE ( 'NONE', *, *, #30788, .T. ) ;
#26754=DIRECTION ( 'NONE',  ( -1.000000000000000000, -0.000000000000000000, -0.000000000000000000 ) ) ;
#26757=CARTESIAN_POINT ( 'NONE',  ( 17.99999999999999645, -78.75547124681308730, -91.20343606297076633 ) ) ;
#26759=DIRECTION ( 'NONE',  ( -1.000000000000000000, -0.000000000000000000, 0.000000000000000000 ) ) ;
#26760=VERTEX_POINT ( 'NONE', #26409 ) ;
#26761=CARTESIAN_POINT ( 'NONE',  ( 17.99999999999999645, -18.35539002514308038, -110.6858262410711831 ) ) ;
#26762=ORIENTED_EDGE ( 'NONE', *, *, #36421, .T. ) ;
#26763=EDGE_CURVE ( 'NONE', #16394, #40591, #29535, .T. ) ;
#26767=EDGE_CURVE ( 'NONE', #31141, #13037, #23296, .T. ) ;
#26774=CIRCLE ( 'NONE', #7955, 116.0000000000000000 ) ;
#26775=EDGE_LOOP ( 'NONE', ( #40317, #11009, #19022, #1811 ) ) ;
#26779=DIRECTION ( 'NONE',  ( 0.000000000000000000, 0.000000000000000000, 1.000000000000000000 ) ) ;
#26783=ORIENTED_EDGE ( 'NONE', *, *, #33213, .F. ) ;
#26785=AXIS2_PLACEMENT_3D ( 'NONE', #24126, #26515, #36960 ) ;
#26788=CIRCLE ( 'NONE', #37923, 116.0000000000000000 ) ;
#26789=DIRECTION ( 'NONE',  ( -1.000000000000000000, -0.000000000000000000, -0.000000000000000000 ) ) ;
#26791=CYLINDRICAL_SURFACE ( 'NONE', #30965, 59.00000000000000000 ) ;
#26792=EDGE_LOOP ( 'NONE', ( #9341, #31750, #23955, #37359 ) ) ;
#26794=EDGE_CURVE ( 'NONE', #39040, #36371, #6516, .T. ) ;
#26803=ORIENTED_EDGE ( 'NONE', *, *, #22970, .F. ) ;
#26805=EDGE_LOOP ( 'NONE', ( #19024, #33979, #29272, #27917 ) ) ;
#26806=CARTESIAN_POINT ( 'NONE',  ( 17.99999999999999645, 0.000000000000000000, 0.000000000000000000 ) ) ;
#26810=CYLINDRICAL_SURFACE ( 'NONE', #12332, 120.5010000000000190 ) ;
#26815=DIRECTION ( 'NONE',  ( 1.000000000000000000, 0.000000000000000000, 0.000000000000000000 ) ) ;
#26816=DIRECTION ( 'NONE',  ( 1.000000000000000000, 0.000000000000000000, 0.000000000000000000 ) ) ;
#26818=EDGE_LOOP ( 'NONE', ( #25535, #16735, #28648, #42479 ) ) ;
#26819=AXIS2_PLACEMENT_3D ( 'NONE', #2437, #42154, #9662 ) ;
#26820=CARTESIAN_POINT ( 'NONE',  ( 17.99999999999999645, -5.492704054965900973, -115.8698847939556771 ) ) ;
#26821=DIRECTION ( 'NONE',  ( 0.000000000000000000, 0.000000000000000000, 1.000000000000000000 ) ) ;
#26825=EDGE_CURVE ( 'NONE', #384, #3752, #36474, .T. ) ;
#26828=CARTESIAN_POINT ( 'NONE',  ( 17.99999999999999645, -35.54274411428134073, 115.1399337407605259 ) ) ;
#26831=ORIENTED_EDGE ( 'NONE', *, *, #41538, .F. ) ;
#26834=CIRCLE ( 'NONE', #32400, 116.0000000000000000 ) ;
#26837=LINE ( 'NONE', #39474, #5416 ) ;
#26838=AXIS2_PLACEMENT_3D ( 'NONE', #42758, #13357, #12917 ) ;
#26839=ORIENTED_EDGE ( 'NONE', *, *, #17623, .F. ) ;
#26840=DIRECTION ( 'NONE',  ( 1.000000000000000000, -0.000000000000000000, -0.000000000000000000 ) ) ;
#26841=CIRCLE ( 'NONE', #8026, 120.5010000000000332 ) ;
#26843=EDGE_CURVE ( 'NONE', #9792, #25282, #17688, .T. ) ;
#26846=CARTESIAN_POINT ( 'NONE',  ( 17.99999999999999645, 0.000000000000000000, 0.000000000000000000 ) ) ;
#26847=CYLINDRICAL_SURFACE ( 'NONE', #13073, 59.00000000000000000 ) ;
#26851=CARTESIAN_POINT ( 'NONE',  ( 17.99999999999999645, 0.000000000000000000, 0.000000000000000000 ) ) ;
#26853=VECTOR ( 'NONE', #6637, 1000.000000000000000 ) ;
#26856=ORIENTED_EDGE ( 'NONE', *, *, #15882, .T. ) ;
#26857=AXIS2_PLACEMENT_3D ( 'NONE', #35208, #29325, #41757 ) ;
#26858=VERTEX_POINT ( 'NONE', #7389 ) ;
#26859=CARTESIAN_POINT ( 'NONE',  ( 17.99999999999999645, -68.61497464550522807, -99.05794392877676557 ) ) ;
#26861=ORIENTED_EDGE ( 'NONE', *, *, #2727, .T. ) ;
#26863=CARTESIAN_POINT ( 'NONE',  ( 17.99999999999999645, -61.59243992711397198, -93.77976230226100540 ) ) ;
#26864=DIRECTION ( 'NONE',  ( -1.000000000000000000, -0.000000000000000000, 0.000000000000000000 ) ) ;
#26865=ORIENTED_EDGE ( 'NONE', *, *, #19268, .T. ) ;
#26866=CARTESIAN_POINT ( 'NONE',  ( -10.00000000000000000, 0.000000000000000000, 0.000000000000000000 ) ) ;
#26872=DIRECTION ( 'NONE',  ( 0.000000000000000000, 0.000000000000000000, 1.000000000000000000 ) ) ;
#26874=EDGE_CURVE ( 'NONE', #33264, #33209, #27477, .T. ) ;
#26875=EDGE_CURVE ( 'NONE', #42811, #5127, #38572, .T. ) ;
#26876=AXIS2_PLACEMENT_3D ( 'NONE', #27903, #25088, #8015 ) ;
#26883=CIRCLE ( 'NONE', #26172, 59.00000000000000000 ) ;
#26887=ORIENTED_EDGE ( 'NONE', *, *, #4999, .T. ) ;
#26888=CIRCLE ( 'NONE', #18588, 59.00000000000000000 ) ;
#26894=DIRECTION ( 'NONE',  ( 0.000000000000000000, 0.000000000000000000, 1.000000000000000000 ) ) ;
#26900=CARTESIAN_POINT ( 'NONE',  ( 17.99999999999999645, 74.56001736500617483, 88.86396238369059120 ) ) ;
#26902=ORIENTED_EDGE ( 'NONE', *, *, #41839, .F. ) ;
#26904=DIRECTION ( 'NONE',  ( 0.000000000000000000, 0.000000000000000000, 1.000000000000000000 ) ) ;
#26906=ORIENTED_EDGE ( 'NONE', *, *, #6545, .T. ) ;
#26908=ORIENTED_EDGE ( 'NONE', *, *, #14790, .F. ) ;
#26910=CARTESIAN_POINT ( 'NONE',  ( 0.000000000000000000, -12.43843445475238063, -111.5058645182330963 ) ) ;
#26917=ORIENTED_EDGE ( 'NONE', *, *, #2029, .F. ) ;
#26918=DIRECTION ( 'NONE',  ( 0.000000000000000000, 0.000000000000000000, 1.000000000000000000 ) ) ;
#26926=DIRECTION ( 'NONE',  ( 0.000000000000000000, -0.9213119778704086382, -0.3888241754733309241 ) ) ;
#26927=ADVANCED_FACE ( 'NONE', ( #13968 ), #24009, .F. ) ;
#26928=EDGE_CURVE ( 'NONE', #28542, #6200, #3660, .T. ) ;
#26932=ORIENTED_EDGE ( 'NONE', *, *, #16069, .T. ) ;
#26933=EDGE_CURVE ( 'NONE', #5383, #40193, #35783, .T. ) ;
#26937=CYLINDRICAL_SURFACE ( 'NONE', #29735, 59.00000000000000000 ) ;
#26939=ORIENTED_EDGE ( 'NONE', *, *, #16250, .F. ) ;
#26940=AXIS2_PLACEMENT_3D ( 'NONE', #29289, #35167, #25818 ) ;
#26943=CARTESIAN_POINT ( 'NONE',  ( 0.000000000000000000, -96.25468616236614139, -72.49500943364587613 ) ) ;
#26945=ADVANCED_FACE ( 'NONE', ( #30318 ), #20750, .F. ) ;
#26946=ORIENTED_EDGE ( 'NONE', *, *, #10792, .T. ) ;
#26947=CARTESIAN_POINT ( 'NONE',  ( 17.99999999999999645, 103.4151313792870610, 61.85306461934443689 ) ) ;
#26948=CARTESIAN_POINT ( 'NONE',  ( 17.99999999999999645, 0.000000000000000000, 0.000000000000000000 ) ) ;
#26952=CIRCLE ( 'NONE', #8138, 120.5010000000000190 ) ;
#26957=VECTOR ( 'NONE', #9255, 1000.000000000000000 ) ;
#26963=EDGE_LOOP ( 'NONE', ( #34803, #23540, #40663, #36176 ) ) ;
#26965=DIRECTION ( 'NONE',  ( 0.000000000000000000, 0.9911528310040066403, 0.1327255272837255529 ) ) ;
#26968=EDGE_LOOP ( 'NONE', ( #29156, #3958, #28641, #25959 ) ) ;
#26971=AXIS2_PLACEMENT_3D ( 'NONE', #23546, #20070, #33335 ) ;
#26972=AXIS2_PLACEMENT_3D ( 'NONE', #35194, #15176, #18687 ) ;
#26973=CYLINDRICAL_SURFACE ( 'NONE', #36303, 59.00000000000000000 ) ;
#26980=AXIS2_PLACEMENT_3D ( 'NONE', #18837, #1548, #18404 ) ;
#26985=EDGE_CURVE ( 'NONE', #28381, #12448, #12142, .T. ) ;
#26986=CARTESIAN_POINT ( 'NONE',  ( 17.99999999999999645, -13.00789606333398218, -115.2683592318616235 ) ) ;
#26991=CARTESIAN_POINT ( 'NONE',  ( 17.99999999999999645, 0.000000000000000000, 0.000000000000000000 ) ) ;
#26992=CARTESIAN_POINT ( 'NONE',  ( 0.000000000000000000, 3.996885678773001604, 120.4346956066682282 ) ) ;
#26993=AXIS2_PLACEMENT_3D ( 'NONE', #21715, #24337, #1799 ) ;
#26996=ORIENTED_EDGE ( 'NONE', *, *, #38520, .F. ) ;
#27000=DIRECTION ( 'NONE',  ( -1.000000000000000000, -0.000000000000000000, 0.000000000000000000 ) ) ;
#27001=VERTEX_POINT ( 'NONE', #10901 ) ;
#27003=ADVANCED_FACE ( 'NONE', ( #5419 ), #34872, .F. ) ;
#27010=CARTESIAN_POINT ( 'NONE',  ( 17.99999999999999645, -107.5680526044917542, -31.89649718262205269 ) ) ;
#27011=VECTOR ( 'NONE', #8529, 1000.000000000000000 ) ;
#27012=AXIS2_PLACEMENT_3D ( 'NONE', #17553, #14482, #10986 ) ;
#27013=ORIENTED_EDGE ( 'NONE', *, *, #12932, .F. ) ;
#27014=CARTESIAN_POINT ( 'NONE',  ( 9.000000000000001776, -108.8880088604273766, -39.99251838046072294 ) ) ;
#27015=VERTEX_POINT ( 'NONE', #41630 ) ;
#27017=DIRECTION ( 'NONE',  ( 0.000000000000000000, 0.000000000000000000, 1.000000000000000000 ) ) ;
#27019=LINE ( 'NONE', #14147, #40742 ) ;
#27020=DIRECTION ( 'NONE',  ( -1.000000000000000000, -0.000000000000000000, -0.000000000000000000 ) ) ;
#27021=EDGE_LOOP ( 'NONE', ( #13567, #13352, #328, #7117 ) ) ;
#27022=CARTESIAN_POINT ( 'NONE',  ( 0.000000000000000000, 0.000000000000000000, 0.000000000000000000 ) ) ;
#27027=DIRECTION ( 'NONE',  ( -1.000000000000000000, -0.000000000000000000, 0.000000000000000000 ) ) ;
#27028=EDGE_CURVE ( 'NONE', #31846, #32645, #28132, .T. ) ;
#27029=CIRCLE ( 'NONE', #42344, 59.00000000000000000 ) ;
#27030=ORIENTED_EDGE ( 'NONE', *, *, #5461, .T. ) ;
#27032=EDGE_CURVE ( 'NONE', #13484, #5383, #18559, .T. ) ;
#27033=CARTESIAN_POINT ( 'NONE',  ( 8.999999999999998224, -86.84764344323014029, 76.89919913989720612 ) ) ;
#27034=VERTEX_POINT ( 'NONE', #38556 ) ;
#27036=VERTEX_POINT ( 'NONE', #35079 ) ;
#27037=DIRECTION ( 'NONE',  ( -1.000000000000000000, 0.000000000000000000, 0.000000000000000000 ) ) ;
#27040=CARTESIAN_POINT ( 'NONE',  ( 17.99999999999999645, 0.000000000000000000, 0.000000000000000000 ) ) ;
#27043=CARTESIAN_POINT ( 'NONE',  ( 17.99999999999999645, 40.37724737310206535, -104.6802291180863023 ) ) ;
#27045=CIRCLE ( 'NONE', #25663, 120.5010000000000474 ) ;
#27046=CARTESIAN_POINT ( 'NONE',  ( 0.000000000000000000, -29.86146781000025285, 112.0905559814577970 ) ) ;
#27047=CARTESIAN_POINT ( 'NONE',  ( 17.99999999999999645, 0.000000000000000000, 0.000000000000000000 ) ) ;
#27049=CIRCLE ( 'NONE', #40241, 120.5010000000000190 ) ;
#27050=ORIENTED_EDGE ( 'NONE', *, *, #8506, .F. ) ;
#27056=AXIS2_PLACEMENT_3D ( 'NONE', #15976, #36211, #19046 ) ;
#27061=EDGE_LOOP ( 'NONE', ( #27347, #21759, #8600, #3688 ) ) ;
#27065=DIRECTION ( 'NONE',  ( 0.000000000000000000, -2.140472356798500845E-14, -1.000000000000000000 ) ) ;
#27066=AXIS2_PLACEMENT_3D ( 'NONE', #1561, #7681, #24526 ) ;
#27071=VERTEX_POINT ( 'NONE', #4986 ) ;
#27076=AXIS2_PLACEMENT_3D ( 'NONE', #16240, #5955, #39314 ) ;
#27078=EDGE_CURVE ( 'NONE', #34811, #21374, #26788, .T. ) ;
#27079=DIRECTION ( 'NONE',  ( -1.000000000000000000, -0.000000000000000000, 0.000000000000000000 ) ) ;
#27081=CYLINDRICAL_SURFACE ( 'NONE', #22243, 116.0000000000000000 ) ;
#27083=DIRECTION ( 'NONE',  ( -1.000000000000000000, 0.000000000000000000, 0.000000000000000000 ) ) ;
#27087=CARTESIAN_POINT ( 'NONE',  ( 0.000000000000000000, -21.55123232222391394, -118.5581519187674360 ) ) ;
#27090=CARTESIAN_POINT ( 'NONE',  ( 17.99999999999999645, 0.000000000000000000, 0.000000000000000000 ) ) ;
#27091=EDGE_CURVE ( 'NONE', #10543, #5501, #11483, .T. ) ;
#27096=EDGE_CURVE ( 'NONE', #4115, #8700, #20559, .T. ) ;
#27099=CIRCLE ( 'NONE', #36100, 120.5010000000000332 ) ;
#27100=CARTESIAN_POINT ( 'NONE',  ( 0.000000000000000000, -46.83041522348427321, -101.9567785075606139 ) ) ;
#27103=VECTOR ( 'NONE', #22371, 1000.000000000000000 ) ;
#27106=EDGE_CURVE ( 'NONE', #12490, #37365, #27482, .T. ) ;
#27111=EDGE_CURVE ( 'NONE', #19328, #14493, #33753, .T. ) ;
#27124=VERTEX_POINT ( 'NONE', #8269 ) ;
#27125=DIRECTION ( 'NONE',  ( -1.000000000000000000, 0.000000000000000000, 0.000000000000000000 ) ) ;
#27127=EDGE_CURVE ( 'NONE', #29868, #40246, #12878, .T. ) ;
#27130=EDGE_CURVE ( 'NONE', #41070, #13955, #35298, .T. ) ;
#27133=EDGE_CURVE ( 'NONE', #6470, #8854, #18785, .T. ) ;
#27137=DIRECTION ( 'NONE',  ( -1.000000000000000000, 0.000000000000000000, -0.000000000000000000 ) ) ;
#27140=DIRECTION ( 'NONE',  ( -1.000000000000000000, -0.000000000000000000, -0.000000000000000000 ) ) ;
#27143=ORIENTED_EDGE ( 'NONE', *, *, #27560, .F. ) ;
#27147=ORIENTED_EDGE ( 'NONE', *, *, #6249, .F. ) ;
#27155=DIRECTION ( 'NONE',  ( 1.000000000000000000, 0.000000000000000000, 0.000000000000000000 ) ) ;
#27156=VERTEX_POINT ( 'NONE', #18987 ) ;
#27160=ORIENTED_EDGE ( 'NONE', *, *, #23679, .F. ) ;
#27165=VERTEX_POINT ( 'NONE', #6052 ) ;
#27169=LINE ( 'NONE', #39580, #38077 ) ;
#27171=CYLINDRICAL_SURFACE ( 'NONE', #24011, 59.00000000000000000 ) ;
#27172=VERTEX_POINT ( 'NONE', #32877 ) ;
#27174=ORIENTED_EDGE ( 'NONE', *, *, #4760, .F. ) ;
#27175=FACE_OUTER_BOUND ( 'NONE', #24854, .T. ) ;
#27177=ADVANCED_FACE ( 'NONE', ( #16113 ), #42259, .F. ) ;
#27180=ORIENTED_EDGE ( 'NONE', *, *, #24045, .F. ) ;
#27181=VERTEX_POINT ( 'NONE', #32670 ) ;
#27183=DIRECTION ( 'NONE',  ( -1.000000000000000000, 0.000000000000000000, 0.000000000000000000 ) ) ;
#27185=CARTESIAN_POINT ( 'NONE',  ( 17.99999999999999645, -96.25468616236614139, -72.49500943364587613 ) ) ;
#27186=AXIS2_PLACEMENT_3D ( 'NONE', #25642, #2439, #38900 ) ;
#27192=CARTESIAN_POINT ( 'NONE',  ( 0.000000000000000000, -59.07817985939071548, 105.0250430397506847 ) ) ;
#27193=CARTESIAN_POINT ( 'NONE',  ( 17.99999999999999645, 0.000000000000000000, 0.000000000000000000 ) ) ;
#27194=VERTEX_POINT ( 'NONE', #9753 ) ;
#27196=FACE_OUTER_BOUND ( 'NONE', #21480, .T. ) ;
#27198=EDGE_CURVE ( 'NONE', #41379, #7422, #21260, .T. ) ;
#27199=CARTESIAN_POINT ( 'NONE',  ( 17.99999999999999645, 0.000000000000000000, 0.000000000000000000 ) ) ;
#27200=CARTESIAN_POINT ( 'NONE',  ( 0.000000000000000000, 87.92975456462900752, 69.68953103478187927 ) ) ;
#27202=DIRECTION ( 'NONE',  ( -1.000000000000000000, 0.000000000000000000, 0.000000000000000000 ) ) ;
#27203=ORIENTED_EDGE ( 'NONE', *, *, #25085, .F. ) ;
#27204=CARTESIAN_POINT ( 'NONE',  ( 0.000000000000000000, -17.33727698085246871, 110.8498592715972961 ) ) ;
#27205=CARTESIAN_POINT ( 'NONE',  ( 17.99999999999999645, 0.000000000000000000, 0.000000000000000000 ) ) ;
#27208=DIRECTION ( 'NONE',  ( -1.000000000000000000, 0.000000000000000000, 0.000000000000000000 ) ) ;
#27211=CARTESIAN_POINT ( 'NONE',  ( 0.000000000000000000, -54.09091620264790379, 102.6166301549515936 ) ) ;
#27216=LINE ( 'NONE', #27874, #13126 ) ;
#27217=CIRCLE ( 'NONE', #11911, 120.5010000000000190 ) ;
#27223=DIRECTION ( 'NONE',  ( -1.000000000000000000, 0.000000000000000000, 0.000000000000000000 ) ) ;
#27224=ORIENTED_EDGE ( 'NONE', *, *, #24194, .T. ) ;
#27228=VERTEX_POINT ( 'NONE', #2748 ) ;
#27229=EDGE_CURVE ( 'NONE', #40591, #35323, #42678, .T. ) ;
#27233=CARTESIAN_POINT ( 'NONE',  ( 17.99999999999999645, -92.10690493017015967, -64.06707842432270184 ) ) ;
#27237=CARTESIAN_POINT ( 'NONE',  ( 17.99999999999999645, 97.89532456239568603, -54.81585448086097045 ) ) ;
#27239=VECTOR ( 'NONE', #27202, 1000.000000000000000 ) ;
#27242=ORIENTED_EDGE ( 'NONE', *, *, #12080, .T. ) ;
#27244=VERTEX_POINT ( 'NONE', #26137 ) ;
#27248=EDGE_CURVE ( 'NONE', #22633, #15523, #7970, .T. ) ;
#27250=CIRCLE ( 'NONE', #8428, 120.5010000000000190 ) ;
#27251=DIRECTION ( 'NONE',  ( 1.000000000000000000, 0.000000000000000000, 0.000000000000000000 ) ) ;
#27256=AXIS2_PLACEMENT_3D ( 'NONE', #9357, #35741, #29240 ) ;
#27257=CARTESIAN_POINT ( 'NONE',  ( 17.99999999999999645, 84.62908780824871258, 85.78116633471321961 ) ) ;
#27260=DIRECTION ( 'NONE',  ( 1.000000000000000000, 0.000000000000000000, 0.000000000000000000 ) ) ;
#27262=DIRECTION ( 'NONE',  ( -1.000000000000000000, 0.000000000000000000, -0.000000000000000000 ) ) ;
#27264=DIRECTION ( 'NONE',  ( -1.000000000000000000, 0.000000000000000000, 0.000000000000000000 ) ) ;
#27266=EDGE_CURVE ( 'NONE', #17290, #14958, #19822, .T. ) ;
#27271=AXIS2_PLACEMENT_3D ( 'NONE', #19748, #35640, #16472 ) ;
#27272=DIRECTION ( 'NONE',  ( 0.000000000000000000, 0.000000000000000000, 1.000000000000000000 ) ) ;
#27273=CIRCLE ( 'NONE', #62, 120.5010000000000190 ) ;
#27277=ORIENTED_EDGE ( 'NONE', *, *, #16007, .F. ) ;
#27279=CARTESIAN_POINT ( 'NONE',  ( -10.00000000000000000, 0.000000000000000000, 0.000000000000000000 ) ) ;
#27283=DIRECTION ( 'NONE',  ( -1.000000000000000000, 0.000000000000000000, -0.000000000000000000 ) ) ;
#27285=CIRCLE ( 'NONE', #8464, 59.00000000000000000 ) ;
#27292=EDGE_CURVE ( 'NONE', #17290, #3403, #10785, .T. ) ;
#27294=ORIENTED_EDGE ( 'NONE', *, *, #3282, .T. ) ;
#27300=ADVANCED_FACE ( 'NONE', ( #9316 ), #5625, .F. ) ;
#27302=VERTEX_POINT ( 'NONE', #32454 ) ;
#27303=DIRECTION ( 'NONE',  ( 0.000000000000000000, 0.000000000000000000, -1.000000000000000000 ) ) ;
#27305=AXIS2_PLACEMENT_3D ( 'NONE', #9942, #25916, #28969 ) ;
#27309=DIRECTION ( 'NONE',  ( 0.000000000000000000, -1.411300455031978955E-14, -1.000000000000000000 ) ) ;
#27316=ORIENTED_EDGE ( 'NONE', *, *, #11418, .F. ) ;
#27325=DIRECTION ( 'NONE',  ( -1.000000000000000000, -0.000000000000000000, 0.000000000000000000 ) ) ;
#27328=CARTESIAN_POINT ( 'NONE',  ( 0.000000000000000000, -45.89132998247981732, -102.3829004574634496 ) ) ;
#27332=ORIENTED_EDGE ( 'NONE', *, *, #41449, .T. ) ;
#27335=CARTESIAN_POINT ( 'NONE',  ( 0.000000000000000000, 111.9370513079675789, -44.61600100275059333 ) ) ;
#27341=ORIENTED_EDGE ( 'NONE', *, *, #26210, .T. ) ;
#27347=ORIENTED_EDGE ( 'NONE', *, *, #10122, .T. ) ;
#27349=ORIENTED_EDGE ( 'NONE', *, *, #21940, .T. ) ;
#27351=EDGE_CURVE ( 'NONE', #15394, #42205, #7330, .T. ) ;
#27352=EDGE_LOOP ( 'NONE', ( #17899, #24255, #20879, #11087 ) ) ;
#27354=EDGE_CURVE ( 'NONE', #8485, #20720, #3038, .T. ) ;
#27355=ORIENTED_EDGE ( 'NONE', *, *, #18598, .T. ) ;
#27360=CARTESIAN_POINT ( 'NONE',  ( 17.99999999999999645, -11.41303419184897017, -111.6154788735837116 ) ) ;
#27361=DIRECTION ( 'NONE',  ( 0.000000000000000000, 0.000000000000000000, 1.000000000000000000 ) ) ;
#27362=CARTESIAN_POINT ( 'NONE',  ( 17.99999999999999645, 0.000000000000000000, 0.000000000000000000 ) ) ;
#27363=ORIENTED_EDGE ( 'NONE', *, *, #12541, .F. ) ;
#27364=VECTOR ( 'NONE', #42034, 1000.000000000000000 ) ;
#27365=CARTESIAN_POINT ( 'NONE',  ( 17.99999999999999645, 94.83915810436481308, -59.94836581341496640 ) ) ;
#27373=EDGE_CURVE ( 'NONE', #31744, #21728, #17763, .T. ) ;
#27375=AXIS2_PLACEMENT_3D ( 'NONE', #17007, #20286, #10647 ) ;
#27377=ORIENTED_EDGE ( 'NONE', *, *, #41281, .F. ) ;
#27378=ORIENTED_EDGE ( 'NONE', *, *, #10257, .T. ) ;
#27382=DIRECTION ( 'NONE',  ( -1.000000000000000000, 0.000000000000000000, 0.000000000000000000 ) ) ;
#27383=ORIENTED_EDGE ( 'NONE', *, *, #18002, .F. ) ;
#27385=VERTEX_POINT ( 'NONE', #27211 ) ;
#27386=LINE ( 'NONE', #27608, #8167 ) ;
#27387=CARTESIAN_POINT ( 'NONE',  ( 0.000000000000000000, 0.000000000000000000, 0.000000000000000000 ) ) ;
#27389=VERTEX_POINT ( 'NONE', #37438 ) ;
#27397=DIRECTION ( 'NONE',  ( -1.000000000000000000, 0.000000000000000000, 0.000000000000000000 ) ) ;
#27401=CARTESIAN_POINT ( 'NONE',  ( 17.99999999999999645, -98.69720329640996681, 60.94966826379877745 ) ) ;
#27402=ORIENTED_EDGE ( 'NONE', *, *, #18629, .T. ) ;
#27408=FACE_OUTER_BOUND ( 'NONE', #36169, .T. ) ;
#27409=VERTEX_POINT ( 'NONE', #36563 ) ;
#27410=CYLINDRICAL_SURFACE ( 'NONE', #28623, 120.5010000000000190 ) ;
#27411=ORIENTED_EDGE ( 'NONE', *, *, #19705, .T. ) ;
#27413=DIRECTION ( 'NONE',  ( 1.000000000000000000, 0.000000000000000000, 0.000000000000000000 ) ) ;
#27414=EDGE_CURVE ( 'NONE', #6179, #34636, #42826, .T. ) ;
#27417=DIRECTION ( 'NONE',  ( 1.000000000000000000, 0.000000000000000000, 0.000000000000000000 ) ) ;
#27419=EDGE_CURVE ( 'NONE', #7533, #26358, #33063, .T. ) ;
#27421=EDGE_CURVE ( 'NONE', #11059, #35721, #28249, .T. ) ;
#27423=ORIENTED_EDGE ( 'NONE', *, *, #11107, .F. ) ;
#27426=ORIENTED_EDGE ( 'NONE', *, *, #26660, .F. ) ;
#27431=EDGE_CURVE ( 'NONE', #23269, #21931, #36538, .T. ) ;
#27433=VERTEX_POINT ( 'NONE', #10178 ) ;
#27437=CARTESIAN_POINT ( 'NONE',  ( 17.99999999999999645, 87.92975456462995965, -69.68953103478068556 ) ) ;
#27438=CARTESIAN_POINT ( 'NONE',  ( -10.00000000000000000, 0.000000000000000000, 0.000000000000000000 ) ) ;
#27441=ORIENTED_EDGE ( 'NONE', *, *, #29055, .T. ) ;
#27446=ORIENTED_EDGE ( 'NONE', *, *, #7862, .T. ) ;
#27449=CARTESIAN_POINT ( 'NONE',  ( 0.000000000000000000, 0.000000000000000000, 0.000000000000000000 ) ) ;
#27451=ORIENTED_EDGE ( 'NONE', *, *, #31905, .F. ) ;
#27453=AXIS2_PLACEMENT_3D ( 'NONE', #37934, #11795, #41416 ) ;
#27454=ORIENTED_EDGE ( 'NONE', *, *, #11172, .T. ) ;
#27455=CARTESIAN_POINT ( 'NONE',  ( 17.99999999999999645, -111.8797445107945236, 8.437727291342365987 ) ) ;
#27461=EDGE_LOOP ( 'NONE', ( #39959, #34372, #41766, #8226 ) ) ;
#27470=CARTESIAN_POINT ( 'NONE',  ( 0.000000000000000000, 0.000000000000000000, 0.000000000000000000 ) ) ;
#27472=EDGE_CURVE ( 'NONE', #12319, #33465, #20259, .T. ) ;
#27475=EDGE_CURVE ( 'NONE', #15430, #1492, #42113, .T. ) ;
#27477=LINE ( 'NONE', #26828, #3726 ) ;
#27482=CIRCLE ( 'NONE', #28212, 59.00000000000000711 ) ;
#27484=EDGE_CURVE ( 'NONE', #40651, #15607, #31554, .T. ) ;
#27485=AXIS2_PLACEMENT_3D ( 'NONE', #40061, #6484, #40290 ) ;
#27487=EDGE_CURVE ( 'NONE', #27181, #15605, #35853, .T. ) ;
#27488=DIRECTION ( 'NONE',  ( -1.000000000000000000, -0.000000000000000000, -0.000000000000000000 ) ) ;
#27492=DIRECTION ( 'NONE',  ( -0.000000000000000000, 0.000000000000000000, 1.000000000000000000 ) ) ;
#27493=CARTESIAN_POINT ( 'NONE',  ( 17.99999999999999645, 27.83061035786954918, 117.2431154827798281 ) ) ;
#27494=ORIENTED_EDGE ( 'NONE', *, *, #27788, .F. ) ;
#27498=DIRECTION ( 'NONE',  ( -1.000000000000000000, 0.000000000000000000, 0.000000000000000000 ) ) ;
#27500=CYLINDRICAL_SURFACE ( 'NONE', #37748, 120.5010000000000190 ) ;
#27504=DIRECTION ( 'NONE',  ( 0.000000000000000000, 0.000000000000000000, 1.000000000000000000 ) ) ;
#27508=DIRECTION ( 'NONE',  ( 0.000000000000000000, 0.9714298932647106311, -0.2373266998711119624 ) ) ;
#27512=CYLINDRICAL_SURFACE ( 'NONE', #16776, 59.00000000000000000 ) ;
#27515=AXIS2_PLACEMENT_3D ( 'NONE', #38087, #38302, #5140 ) ;
#27518=ORIENTED_EDGE ( 'NONE', *, *, #26092, .F. ) ;
#27519=DIRECTION ( 'NONE',  ( 0.000000000000000000, 0.000000000000000000, 1.000000000000000000 ) ) ;
#27523=EDGE_CURVE ( 'NONE', #25483, #3709, #21130, .T. ) ;
#27525=EDGE_LOOP ( 'NONE', ( #17968, #1063, #22517, #8255 ) ) ;
#27535=ADVANCED_FACE ( 'NONE', ( #4932 ), #25256, .F. ) ;
#27539=CIRCLE ( 'NONE', #24067, 58.99999999999999289 ) ;
#27542=EDGE_CURVE ( 'NONE', #14855, #29068, #8624, .T. ) ;
#27543=DIRECTION ( 'NONE',  ( 1.000000000000000000, 0.000000000000000000, 0.000000000000000000 ) ) ;
#27544=CIRCLE ( 'NONE', #29665, 116.0000000000000000 ) ;
#27547=AXIS2_PLACEMENT_3D ( 'NONE', #39800, #36753, #33490 ) ;
#27550=ORIENTED_EDGE ( 'NONE', *, *, #20498, .F. ) ;
#27551=CARTESIAN_POINT ( 'NONE',  ( 17.99999999999999645, 101.1249659627855806, -48.60055280209454054 ) ) ;
#27552=LINE ( 'NONE', #20595, #7502 ) ;
#27557=DIRECTION ( 'NONE',  ( 0.000000000000000000, -0.4132121857683668797, -0.9106347728549183396 ) ) ;
#27560=EDGE_CURVE ( 'NONE', #14617, #2185, #19873, .T. ) ;
#27561=AXIS2_PLACEMENT_3D ( 'NONE', #19077, #39722, #9211 ) ;
#27562=ORIENTED_EDGE ( 'NONE', *, *, #39011, .F. ) ;
#27572=CIRCLE ( 'NONE', #19243, 59.00000000000000711 ) ;
#27573=CARTESIAN_POINT ( 'NONE',  ( 17.99999999999999645, -95.31344542257689056, -66.11616384574544725 ) ) ;
#27576=AXIS2_PLACEMENT_3D ( 'NONE', #17140, #30850, #34114 ) ;
#27581=LINE ( 'NONE', #13861, #25533 ) ;
#27586=CIRCLE ( 'NONE', #8040, 59.00000000000000000 ) ;
#27588=FACE_OUTER_BOUND ( 'NONE', #11682, .T. ) ;
#27593=ADVANCED_FACE ( 'NONE', ( #25063 ), #24833, .F. ) ;
#27597=EDGE_CURVE ( 'NONE', #26000, #35433, #31775, .T. ) ;
#27598=DIRECTION ( 'NONE',  ( 0.000000000000000000, 2.587384167558627638E-15, -1.000000000000000000 ) ) ;
#27600=DIRECTION ( 'NONE',  ( -1.000000000000000000, -0.000000000000000000, -0.000000000000000000 ) ) ;
#27602=VECTOR ( 'NONE', #3220, 1000.000000000000000 ) ;
#27605=CARTESIAN_POINT ( 'NONE',  ( 0.000000000000000000, 52.88069566989596382, -103.2454939717363516 ) ) ;
#27606=EDGE_LOOP ( 'NONE', ( #10481, #12102, #16889, #18028 ) ) ;
#27607=DIRECTION ( 'NONE',  ( -1.000000000000000000, -0.000000000000000000, -0.000000000000000000 ) ) ;
#27608=CARTESIAN_POINT ( 'NONE',  ( 17.99999999999999645, -119.7318547011702634, 13.59315897125686412 ) ) ;
#27610=VECTOR ( 'NONE', #20251, 1000.000000000000000 ) ;
#27614=DIRECTION ( 'NONE',  ( 0.000000000000000000, 0.000000000000000000, 1.000000000000000000 ) ) ;
#27619=CIRCLE ( 'NONE', #7380, 58.99999999999999289 ) ;
#27625=EDGE_CURVE ( 'NONE', #32669, #267, #32401, .T. ) ;
#27632=AXIS2_PLACEMENT_3D ( 'NONE', #42134, #39879, #23149 ) ;
#27636=EDGE_LOOP ( 'NONE', ( #8994, #4492, #12018, #10894 ) ) ;
#27637=FACE_OUTER_BOUND ( 'NONE', #37797, .T. ) ;
#27639=EDGE_CURVE ( 'NONE', #2980, #8823, #28921, .T. ) ;
#27644=DIRECTION ( 'NONE',  ( -1.000000000000000000, -0.000000000000000000, 0.000000000000000000 ) ) ;
#27645=AXIS2_PLACEMENT_3D ( 'NONE', #25821, #8999, #25615 ) ;
#27648=ORIENTED_EDGE ( 'NONE', *, *, #12665, .T. ) ;
#27651=ORIENTED_EDGE ( 'NONE', *, *, #19705, .F. ) ;
#27665=ORIENTED_EDGE ( 'NONE', *, *, #27841, .T. ) ;
#27667=CARTESIAN_POINT ( 'NONE',  ( 17.99999999999999645, 87.92975456462900752, 69.68953103478187927 ) ) ;
#27670=CARTESIAN_POINT ( 'NONE',  ( 17.99999999999999645, 41.62036691425679180, -113.0850832732710529 ) ) ;
#27671=EDGE_LOOP ( 'NONE', ( #6894, #9041, #38545, #25178 ) ) ;
#27673=ORIENTED_EDGE ( 'NONE', *, *, #5677, .F. ) ;
#27678=ADVANCED_FACE ( 'NONE', ( #18934 ), #15434, .F. ) ;
#27679=DIRECTION ( 'NONE',  ( -1.000000000000000000, 0.000000000000000000, -0.000000000000000000 ) ) ;
#27683=EDGE_CURVE ( 'NONE', #19436, #40032, #8718, .T. ) ;
#27684=ADVANCED_FACE ( 'NONE', ( #36094 ), #35660, .F. ) ;
#27685=CIRCLE ( 'NONE', #14450, 59.00000000000000000 ) ;
#27688=LINE ( 'NONE', #40952, #8678 ) ;
#27689=ORIENTED_EDGE ( 'NONE', *, *, #11244, .F. ) ;
#27695=ORIENTED_EDGE ( 'NONE', *, *, #35904, .F. ) ;
#27697=CARTESIAN_POINT ( 'NONE',  ( 17.99999999999999645, 0.000000000000000000, 0.000000000000000000 ) ) ;
#27698=ORIENTED_EDGE ( 'NONE', *, *, #38768, .F. ) ;
#27705=VECTOR ( 'NONE', #2603, 1000.000000000000000 ) ;
#27708=DIRECTION ( 'NONE',  ( 1.000000000000000000, -0.000000000000000000, 0.000000000000000000 ) ) ;
#27711=EDGE_CURVE ( 'NONE', #15795, #15605, #35221, .T. ) ;
#27721=CARTESIAN_POINT ( 'NONE',  ( 17.99999999999999645, 75.72520367775197769, -82.78868281115903471 ) ) ;
#27724=CARTESIAN_POINT ( 'NONE',  ( 17.99999999999999645, -108.8684555192045025, -27.12806418649726936 ) ) ;
#27727=CARTESIAN_POINT ( 'NONE',  ( 17.99999999999999645, 0.000000000000000000, 0.000000000000000000 ) ) ;
#27729=ORIENTED_EDGE ( 'NONE', *, *, #4433, .F. ) ;
#27731=CARTESIAN_POINT ( 'NONE',  ( 17.99999999999999645, -3.996885678772183592, -120.4346956066682424 ) ) ;
#27732=DIRECTION ( 'NONE',  ( 0.000000000000000000, 1.599473849036242195E-14, -1.000000000000000000 ) ) ;
#27733=EDGE_CURVE ( 'NONE', #9792, #3101, #1039, .T. ) ;
#27735=ORIENTED_EDGE ( 'NONE', *, *, #26099, .F. ) ;
#27736=DIRECTION ( 'NONE',  ( 0.000000000000000000, -0.7865515558026355825, -0.6175246149462008116 ) ) ;
#27738=AXIS2_PLACEMENT_3D ( 'NONE', #39681, #36859, #6963 ) ;
#27739=AXIS2_PLACEMENT_3D ( 'NONE', #8292, #21647, #34902 ) ;
#27741=CIRCLE ( 'NONE', #7496, 116.0000000000000000 ) ;
#27746=FACE_OUTER_BOUND ( 'NONE', #26665, .T. ) ;
#27747=ORIENTED_EDGE ( 'NONE', *, *, #3401, .F. ) ;
#27748=AXIS2_PLACEMENT_3D ( 'NONE', #33435, #16683, #23431 ) ;
#27752=CARTESIAN_POINT ( 'NONE',  ( 17.99999999999999645, -110.3490479609630910, -20.28201389785511211 ) ) ;
#27753=VECTOR ( 'NONE', #12182, 1000.000000000000000 ) ;
#27754=CYLINDRICAL_SURFACE ( 'NONE', #37333, 120.5010000000000190 ) ;
#27757=CARTESIAN_POINT ( 'NONE',  ( -10.00000000000000000, 0.000000000000000000, 0.000000000000000000 ) ) ;
#27766=CIRCLE ( 'NONE', #17353, 58.99999999999998579 ) ;
#27767=VERTEX_POINT ( 'NONE', #26943 ) ;
#27775=CIRCLE ( 'NONE', #31250, 120.5010000000000332 ) ;
#27776=CARTESIAN_POINT ( 'NONE',  ( 9.000000000000001776, -17.77780072541773748, 114.6296200873375284 ) ) ;
#27777=CARTESIAN_POINT ( 'NONE',  ( 17.99999999999999645, -46.12538073176424547, 111.3235835452210267 ) ) ;
#27778=AXIS2_PLACEMENT_3D ( 'NONE', #28433, #28636, #1558 ) ;
#27781=ORIENTED_EDGE ( 'NONE', *, *, #41281, .T. ) ;
#27783=VERTEX_POINT ( 'NONE', #274 ) ;
#27786=ORIENTED_EDGE ( 'NONE', *, *, #9882, .T. ) ;
#27787=CARTESIAN_POINT ( 'NONE',  ( 9.000000000000001776, -114.1157422997284669, 20.82300072952894610 ) ) ;
#27788=EDGE_CURVE ( 'NONE', #11794, #27783, #19220, .T. ) ;
#27789=DIRECTION ( 'NONE',  ( 0.000000000000000000, 0.000000000000000000, 1.000000000000000000 ) ) ;
#27792=VERTEX_POINT ( 'NONE', #514 ) ;
#27794=VERTEX_POINT ( 'NONE', #37166 ) ;
#27797=ORIENTED_EDGE ( 'NONE', *, *, #11076, .T. ) ;
#27798=CARTESIAN_POINT ( 'NONE',  ( 0.000000000000000000, -115.9750404417044223, 2.406240749597103434 ) ) ;
#27800=AXIS2_PLACEMENT_3D ( 'NONE', #3897, #37723, #4337 ) ;
#27805=EDGE_CURVE ( 'NONE', #27156, #33352, #31024, .T. ) ;
#27810=CARTESIAN_POINT ( 'NONE',  ( 0.000000000000000000, 101.8011932243955613, -55.61040422519224791 ) ) ;
#27815=CARTESIAN_POINT ( 'NONE',  ( 17.99999999999999645, -80.02407177072905142, -78.64108602300026973 ) ) ;
#27816=DIRECTION ( 'NONE',  ( 1.000000000000000000, 0.000000000000000000, 0.000000000000000000 ) ) ;
#27824=LINE ( 'NONE', #4429, #1098 ) ;
#27828=CIRCLE ( 'NONE', #36854, 120.5010000000000190 ) ;
#27829=DIRECTION ( 'NONE',  ( -1.000000000000000000, -0.000000000000000000, -0.000000000000000000 ) ) ;
#27832=DIRECTION ( 'NONE',  ( 0.000000000000000000, 0.000000000000000000, 1.000000000000000000 ) ) ;
#27833=VERTEX_POINT ( 'NONE', #36955 ) ;
#27834=CARTESIAN_POINT ( 'NONE',  ( 17.99999999999999645, 18.35539002514530793, -110.6858262410707994 ) ) ;
#27836=CARTESIAN_POINT ( 'NONE',  ( 0.000000000000000000, 40.13512380273970592, 113.6206972269522737 ) ) ;
#27837=DIRECTION ( 'NONE',  ( -1.000000000000000000, 0.000000000000000000, -0.000000000000000000 ) ) ;
#27841=EDGE_CURVE ( 'NONE', #28053, #40741, #33681, .T. ) ;
#27852=ORIENTED_EDGE ( 'NONE', *, *, #2840, .T. ) ;
#27856=VECTOR ( 'NONE', #17610, 1000.000000000000000 ) ;
#27862=DIRECTION ( 'NONE',  ( 0.000000000000000000, -0.8993121301712229121, 0.4373073204588476259 ) ) ;
#27863=ORIENTED_EDGE ( 'NONE', *, *, #36191, .T. ) ;
#27865=CARTESIAN_POINT ( 'NONE',  ( 17.99999999999999645, 0.000000000000000000, 0.000000000000000000 ) ) ;
#27866=DIRECTION ( 'NONE',  ( 0.000000000000000000, 0.000000000000000000, 1.000000000000000000 ) ) ;
#27870=ORIENTED_EDGE ( 'NONE', *, *, #29035, .T. ) ;
#27873=ORIENTED_EDGE ( 'NONE', *, *, #25378, .T. ) ;
#27874=CARTESIAN_POINT ( 'NONE',  ( 17.99999999999999645, 119.7318547011701497, 13.59315897125768124 ) ) ;
#27876=CARTESIAN_POINT ( 'NONE',  ( -10.00000000000000000, 0.000000000000000000, 0.000000000000000000 ) ) ;
#27881=ORIENTED_EDGE ( 'NONE', *, *, #14202, .F. ) ;
#27885=DIRECTION ( 'NONE',  ( 1.000000000000000000, 0.000000000000000000, 0.000000000000000000 ) ) ;
#27886=AXIS2_PLACEMENT_3D ( 'NONE', #20059, #16781, #7341 ) ;
#27890=VERTEX_POINT ( 'NONE', #37172 ) ;
#27891=DIRECTION ( 'NONE',  ( 1.000000000000000000, 0.000000000000000000, 0.000000000000000000 ) ) ;
#27892=EDGE_LOOP ( 'NONE', ( #20056, #9690, #30716, #6665 ) ) ;
#27893=DIRECTION ( 'NONE',  ( 0.000000000000000000, -0.2631025642275284238, 0.9647678688145140402 ) ) ;
#27898=ORIENTED_EDGE ( 'NONE', *, *, #14377, .T. ) ;
#27901=EDGE_CURVE ( 'NONE', #33403, #27001, #6618, .T. ) ;
#27903=CARTESIAN_POINT ( 'NONE',  ( 0.000000000000000000, 0.000000000000000000, 0.000000000000000000 ) ) ;
#27904=ORIENTED_EDGE ( 'NONE', *, *, #41118, .F. ) ;
#27907=DIRECTION ( 'NONE',  ( 0.000000000000000000, 0.000000000000000000, 1.000000000000000000 ) ) ;
#27911=CARTESIAN_POINT ( 'NONE',  ( 17.99999999999999645, 73.78980555658732499, -95.26571049921918188 ) ) ;
#27913=DIRECTION ( 'NONE',  ( 1.000000000000000000, 0.000000000000000000, 0.000000000000000000 ) ) ;
#27917=ORIENTED_EDGE ( 'NONE', *, *, #21276, .F. ) ;
#27918=CIRCLE ( 'NONE', #15371, 120.5010000000000190 ) ;
#27919=CARTESIAN_POINT ( 'NONE',  ( 17.99999999999999645, -76.48293397876315680, 82.08917884620285577 ) ) ;
#27921=CIRCLE ( 'NONE', #34170, 59.00000000000000000 ) ;
#27924=EDGE_LOOP ( 'NONE', ( #4092, #17178, #41003, #23437 ) ) ;
#27925=CARTESIAN_POINT ( 'NONE',  ( 17.99999999999999645, -87.92975456462855277, -69.68953103478244770 ) ) ;
#27926=LINE ( 'NONE', #13967, #39742 ) ;
#27927=DIRECTION ( 'NONE',  ( -1.000000000000000000, -0.000000000000000000, -0.000000000000000000 ) ) ;
#27929=EDGE_CURVE ( 'NONE', #38358, #35775, #24125, .T. ) ;
#27934=EDGE_CURVE ( 'NONE', #24013, #4177, #9915, .T. ) ;
#27935=EDGE_CURVE ( 'NONE', #35201, #4402, #36573, .T. ) ;
#27940=CYLINDRICAL_SURFACE ( 'NONE', #1004, 120.5010000000000190 ) ;
#27941=CARTESIAN_POINT ( 'NONE',  ( 0.000000000000000000, 109.1131968883995000, 26.12628443612074847 ) ) ;
#27942=ORIENTED_EDGE ( 'NONE', *, *, #7405, .T. ) ;
#27943=CARTESIAN_POINT ( 'NONE',  ( 17.99999999999999645, 59.47573314508867526, -99.59235496188547643 ) ) ;
#27944=AXIS2_PLACEMENT_3D ( 'NONE', #8462, #32030, #31821 ) ;
#27948=LINE ( 'NONE', #30770, #19431 ) ;
#27950=CIRCLE ( 'NONE', #40352, 59.00000000000000711 ) ;
#27955=CARTESIAN_POINT ( 'NONE',  ( 17.99999999999999645, 69.72480978690171582, -92.70626138605946664 ) ) ;
#27956=ORIENTED_EDGE ( 'NONE', *, *, #19119, .T. ) ;
#27957=EDGE_CURVE ( 'NONE', #21604, #4304, #22039, .T. ) ;
#27962=VERTEX_POINT ( 'NONE', #4886 ) ;
#27963=DIRECTION ( 'NONE',  ( -1.000000000000000000, -0.000000000000000000, -0.000000000000000000 ) ) ;
#27965=ORIENTED_EDGE ( 'NONE', *, *, #2072, .F. ) ;
#27969=CARTESIAN_POINT ( 'NONE',  ( 17.99999999999999645, -110.1579703617964725, -21.29539948940357164 ) ) ;
#27970=AXIS2_PLACEMENT_3D ( 'NONE', #36083, #41982, #8613 ) ;
#27971=LINE ( 'NONE', #37321, #505 ) ;
#27972=ORIENTED_EDGE ( 'NONE', *, *, #6474, .T. ) ;
#27974=FACE_OUTER_BOUND ( 'NONE', #3030, .T. ) ;
#27978=DIRECTION ( 'NONE',  ( 0.000000000000000000, 0.000000000000000000, 1.000000000000000000 ) ) ;
#27980=CIRCLE ( 'NONE', #33519, 59.00000000000000711 ) ;
#27983=ORIENTED_EDGE ( 'NONE', *, *, #41711, .T. ) ;
#27985=EDGE_CURVE ( 'NONE', #5464, #15814, #27544, .T. ) ;
#27989=ADVANCED_FACE ( 'NONE', ( #41081 ), #1387, .F. ) ;
#27990=CIRCLE ( 'NONE', #2155, 116.0000000000000000 ) ;
#27992=LINE ( 'NONE', #27777, #22865 ) ;
#27993=CARTESIAN_POINT ( 'NONE',  ( 0.000000000000000000, 0.000000000000000000, 0.000000000000000000 ) ) ;
#27994=CARTESIAN_POINT ( 'NONE',  ( 17.99999999999999645, -104.0201923570372173, -51.34003878071168003 ) ) ;
#28001=CYLINDRICAL_SURFACE ( 'NONE', #30556, 59.00000000000000000 ) ;
#28004=DIRECTION ( 'NONE',  ( -1.000000000000000000, 0.000000000000000000, 0.000000000000000000 ) ) ;
#28008=AXIS2_PLACEMENT_3D ( 'NONE', #12598, #6451, #15669 ) ;
#28012=CIRCLE ( 'NONE', #9167, 58.99999999999998579 ) ;
#28022=DIRECTION ( 'NONE',  ( -1.000000000000000000, -0.000000000000000000, -0.000000000000000000 ) ) ;
#28026=DIRECTION ( 'NONE',  ( 1.000000000000000000, 0.000000000000000000, 0.000000000000000000 ) ) ;
#28027=ORIENTED_EDGE ( 'NONE', *, *, #29125, .T. ) ;
#28028=CARTESIAN_POINT ( 'NONE',  ( 17.99999999999999645, -88.56657216608570593, -68.87840567546012949 ) ) ;
#28030=CARTESIAN_POINT ( 'NONE',  ( 17.99999999999999645, -56.51398178981889941, 96.92493144647428949 ) ) ;
#28031=ORIENTED_EDGE ( 'NONE', *, *, #411, .F. ) ;
#28032=EDGE_CURVE ( 'NONE', #38476, #30500, #32417, .T. ) ;
#28035=CIRCLE ( 'NONE', #32888, 120.5010000000000474 ) ;
#28041=DIRECTION ( 'NONE',  ( 1.000000000000000000, 0.000000000000000000, 0.000000000000000000 ) ) ;
#28042=CARTESIAN_POINT ( 'NONE',  ( 8.999999999999998224, 48.55277268144325120, 105.3500273609081432 ) ) ;
#28046=ORIENTED_EDGE ( 'NONE', *, *, #35981, .T. ) ;
#28052=DIRECTION ( 'NONE',  ( 1.000000000000000000, 0.000000000000000000, 0.000000000000000000 ) ) ;
#28053=VERTEX_POINT ( 'NONE', #18688 ) ;
#28054=ORIENTED_EDGE ( 'NONE', *, *, #26401, .T. ) ;
#28055=DIRECTION ( 'NONE',  ( -1.000000000000000000, 0.000000000000000000, 0.000000000000000000 ) ) ;
#28056=DIRECTION ( 'NONE',  ( 0.000000000000000000, 0.000000000000000000, 1.000000000000000000 ) ) ;
#28057=ORIENTED_EDGE ( 'NONE', *, *, #35712, .F. ) ;
#28059=ORIENTED_EDGE ( 'NONE', *, *, #5132, .T. ) ;
#28062=DIRECTION ( 'NONE',  ( 1.000000000000000000, 0.000000000000000000, 0.000000000000000000 ) ) ;
#28065=AXIS2_PLACEMENT_3D ( 'NONE', #31644, #41444, #1742 ) ;
#28066=DIRECTION ( 'NONE',  ( 0.000000000000000000, 0.000000000000000000, 1.000000000000000000 ) ) ;
#28068=CIRCLE ( 'NONE', #34984, 120.5010000000000190 ) ;
#28071=DIRECTION ( 'NONE',  ( 0.000000000000000000, -0.5963673585384914322, -0.8027116379309710004 ) ) ;
#28073=DIRECTION ( 'NONE',  ( -1.000000000000000000, 0.000000000000000000, -0.000000000000000000 ) ) ;
#28074=ORIENTED_EDGE ( 'NONE', *, *, #19674, .T. ) ;
#28077=DIRECTION ( 'NONE',  ( -1.000000000000000000, -0.000000000000000000, -0.000000000000000000 ) ) ;
#28079=CARTESIAN_POINT ( 'NONE',  ( 17.99999999999999645, 87.92975456462995965, -69.68953103478068556 ) ) ;
#28084=ORIENTED_EDGE ( 'NONE', *, *, #22373, .F. ) ;
#28086=DIRECTION ( 'NONE',  ( 0.000000000000000000, -0.3140767120219362663, -0.9493976084683853900 ) ) ;
#28089=CARTESIAN_POINT ( 'NONE',  ( 0.000000000000000000, 97.89532456239497549, 54.81585448086229917 ) ) ;
#28091=CIRCLE ( 'NONE', #21833, 58.99999999999999289 ) ;
#28092=VERTEX_POINT ( 'NONE', #8373 ) ;
#28096=DIRECTION ( 'NONE',  ( 0.000000000000000000, -0.4610925014493326146, 0.8873520750565681015 ) ) ;
#28097=CIRCLE ( 'NONE', #5765, 120.5010000000000332 ) ;
#28099=ORIENTED_EDGE ( 'NONE', *, *, #25812, .T. ) ;
#28104=DIRECTION ( 'NONE',  ( -1.000000000000000000, -0.000000000000000000, 0.000000000000000000 ) ) ;
#28108=EDGE_CURVE ( 'NONE', #69, #42811, #35246, .T. ) ;
#28115=DIRECTION ( 'NONE',  ( 1.000000000000000000, 0.000000000000000000, 0.000000000000000000 ) ) ;
#28117=CARTESIAN_POINT ( 'NONE',  ( 17.99999999999999645, 115.5737863835463628, -9.934782381632540904 ) ) ;
#28120=CARTESIAN_POINT ( 'NONE',  ( 0.000000000000000000, 0.000000000000000000, 0.000000000000000000 ) ) ;
#28121=ORIENTED_EDGE ( 'NONE', *, *, #6366, .F. ) ;
#28123=FACE_OUTER_BOUND ( 'NONE', #29897, .T. ) ;
#28125=AXIS2_PLACEMENT_3D ( 'NONE', #33724, #768, #19814 ) ;
#28126=DIRECTION ( 'NONE',  ( 0.000000000000000000, -0.7525707698561306946, -0.6585113790650474197 ) ) ;
#28132=LINE ( 'NONE', #21832, #32354 ) ;
#28138=VECTOR ( 'NONE', #40351, 1000.000000000000000 ) ;
#28139=EDGE_CURVE ( 'NONE', #25754, #20175, #3173, .T. ) ;
#28142=DIRECTION ( 'NONE',  ( 1.000000000000000000, 0.000000000000000000, 0.000000000000000000 ) ) ;
#28148=DIRECTION ( 'NONE',  ( 1.000000000000000000, 0.000000000000000000, 0.000000000000000000 ) ) ;
#28151=VERTEX_POINT ( 'NONE', #22365 ) ;
#28156=CYLINDRICAL_SURFACE ( 'NONE', #34024, 59.00000000000000000 ) ;
#28158=ORIENTED_EDGE ( 'NONE', *, *, #1519, .F. ) ;
#28159=CYLINDRICAL_SURFACE ( 'NONE', #27739, 120.5010000000000190 ) ;
#28164=ORIENTED_EDGE ( 'NONE', *, *, #27472, .T. ) ;
#28165=CARTESIAN_POINT ( 'NONE',  ( 9.000000000000001776, 31.17727234463694330, 111.7317219465820983 ) ) ;
#28166=CARTESIAN_POINT ( 'NONE',  ( 0.000000000000000000, 40.37724737310206535, -104.6802291180863023 ) ) ;
#28167=ORIENTED_EDGE ( 'NONE', *, *, #14526, .T. ) ;
#28168=EDGE_CURVE ( 'NONE', #37962, #3822, #26888, .T. ) ;
#28169=DIRECTION ( 'NONE',  ( 1.000000000000000000, 0.000000000000000000, 0.000000000000000000 ) ) ;
#28170=CARTESIAN_POINT ( 'NONE',  ( 17.99999999999999645, -41.62036691425453228, -113.0850832732718914 ) ) ;
#28172=VERTEX_POINT ( 'NONE', #30119 ) ;
#28174=AXIS2_PLACEMENT_3D ( 'NONE', #2278, #28943, #42850 ) ;
#28177=LINE ( 'NONE', #38397, #21841 ) ;
#28178=AXIS2_PLACEMENT_3D ( 'NONE', #34224, #36849, #30957 ) ;
#28183=AXIS2_PLACEMENT_3D ( 'NONE', #21424, #1501, #21195 ) ;
#28186=CARTESIAN_POINT ( 'NONE',  ( 0.000000000000000000, 0.000000000000000000, 0.000000000000000000 ) ) ;
#28189=CARTESIAN_POINT ( 'NONE',  ( 0.000000000000000000, 0.000000000000000000, 0.000000000000000000 ) ) ;
#28193=ADVANCED_FACE ( 'NONE', ( #9223 ), #6753, .F. ) ;
#28194=AXIS2_PLACEMENT_3D ( 'NONE', #17969, #28415, #27978 ) ;
#28196=DIRECTION ( 'NONE',  ( -1.000000000000000000, 0.000000000000000000, 0.000000000000000000 ) ) ;
#28199=CARTESIAN_POINT ( 'NONE',  ( 0.000000000000000000, 92.10690493017145286, -64.06707842432085442 ) ) ;
#28200=AXIS2_PLACEMENT_3D ( 'NONE', #26806, #19216, #6085 ) ;
#28201=FACE_OUTER_BOUND ( 'NONE', #14004, .T. ) ;
#28202=CIRCLE ( 'NONE', #10041, 120.5010000000000190 ) ;
#28212=AXIS2_PLACEMENT_3D ( 'NONE', #11330, #41842, #21407 ) ;
#28218=ORIENTED_EDGE ( 'NONE', *, *, #27248, .T. ) ;
#28222=ORIENTED_EDGE ( 'NONE', *, *, #14435, .F. ) ;
#28225=EDGE_CURVE ( 'NONE', #12969, #29749, #7373, .T. ) ;
#28226=EDGE_CURVE ( 'NONE', #38713, #2041, #16835, .T. ) ;
#28230=AXIS2_PLACEMENT_3D ( 'NONE', #23047, #3115, #16486 ) ;
#28231=VERTEX_POINT ( 'NONE', #9016 ) ;
#28238=CARTESIAN_POINT ( 'NONE',  ( 9.000000000000001776, 47.31079789947627745, -105.9135893174946119 ) ) ;
#28240=CIRCLE ( 'NONE', #21285, 59.00000000000000000 ) ;
#28241=DIRECTION ( 'NONE',  ( 0.000000000000000000, 0.000000000000000000, 1.000000000000000000 ) ) ;
#28243=AXIS2_PLACEMENT_3D ( 'NONE', #35719, #2557, #15920 ) ;
#28246=CIRCLE ( 'NONE', #5231, 116.0000000000000000 ) ;
#28248=ORIENTED_EDGE ( 'NONE', *, *, #41591, .F. ) ;
#28249=CIRCLE ( 'NONE', #37954, 116.0000000000000000 ) ;
#28253=ORIENTED_EDGE ( 'NONE', *, *, #1358, .F. ) ;
#28254=LINE ( 'NONE', #35193, #38051 ) ;
#28256=EDGE_CURVE ( 'NONE', #33331, #36755, #16469, .T. ) ;
#28258=LINE ( 'NONE', #28042, #23321 ) ;
#28259=VERTEX_POINT ( 'NONE', #4110 ) ;
#28260=LINE ( 'NONE', #34992, #31933 ) ;
#28263=AXIS2_PLACEMENT_3D ( 'NONE', #661, #10067, #23847 ) ;
#28264=CARTESIAN_POINT ( 'NONE',  ( 9.000000000000001776, 115.6826031496113529, -8.575274253896266075 ) ) ;
#28269=CIRCLE ( 'NONE', #33803, 120.5010000000000474 ) ;
#28272=AXIS2_PLACEMENT_3D ( 'NONE', #28449, #11861, #19270 ) ;
#28276=VECTOR ( 'NONE', #10779, 1000.000000000000000 ) ;
#28278=ORIENTED_EDGE ( 'NONE', *, *, #29830, .T. ) ;
#28280=VECTOR ( 'NONE', #28775, 1000.000000000000000 ) ;
#28281=EDGE_LOOP ( 'NONE', ( #37107, #41427, #20191, #7084 ) ) ;
#28287=CARTESIAN_POINT ( 'NONE',  ( 0.000000000000000000, 76.48293397876260258, 82.08917884620340999 ) ) ;
#28293=DIRECTION ( 'NONE',  ( 0.000000000000000000, -0.9968120070307509017, 0.07978610555307336094 ) ) ;
#28294=DIRECTION ( 'NONE',  ( 1.000000000000000000, 0.000000000000000000, 0.000000000000000000 ) ) ;
#28297=VERTEX_POINT ( 'NONE', #40543 ) ;
#28303=AXIS2_PLACEMENT_3D ( 'NONE', #34969, #28022, #31703 ) ;
#28306=VECTOR ( 'NONE', #32750, 1000.000000000000000 ) ;
#28308=DIRECTION ( 'NONE',  ( 0.000000000000000000, 3.645859508832611499E-14, -1.000000000000000000 ) ) ;
#28311=CIRCLE ( 'NONE', #5292, 58.99999999999999289 ) ;
#28317=EDGE_CURVE ( 'NONE', #12545, #35437, #10139, .T. ) ;
#28318=AXIS2_PLACEMENT_3D ( 'NONE', #34089, #4393, #24527 ) ;
#28324=ORIENTED_EDGE ( 'NONE', *, *, #21126, .F. ) ;
#28325=CARTESIAN_POINT ( 'NONE',  ( 0.000000000000000000, 23.21237537461745859, 109.7700237000592836 ) ) ;
#28327=DIRECTION ( 'NONE',  ( -1.000000000000000000, -0.000000000000000000, -0.000000000000000000 ) ) ;
#28333=AXIS2_PLACEMENT_3D ( 'NONE', #35720, #16574, #39205 ) ;
#28336=VECTOR ( 'NONE', #16064, 1000.000000000000000 ) ;
#28337=CARTESIAN_POINT ( 'NONE',  ( 0.000000000000000000, 17.33727698085173330, 110.8498592715974098 ) ) ;
#28339=ORIENTED_EDGE ( 'NONE', *, *, #14931, .F. ) ;
#28348=CARTESIAN_POINT ( 'NONE',  ( 17.99999999999999645, -46.83041522348565167, 101.9567785075599744 ) ) ;
#28352=EDGE_CURVE ( 'NONE', #5962, #10039, #38731, .T. ) ;
#28353=AXIS2_PLACEMENT_3D ( 'NONE', #37247, #30084, #37470 ) ;
#28355=FACE_OUTER_BOUND ( 'NONE', #9247, .T. ) ;
#28356=CARTESIAN_POINT ( 'NONE',  ( 17.99999999999999645, -62.45178862086279992, 93.20969140437486544 ) ) ;
#28357=EDGE_CURVE ( 'NONE', #18949, #41859, #10173, .T. ) ;
#28364=AXIS2_PLACEMENT_3D ( 'NONE', #13020, #29585, #29174 ) ;
#28376=DIRECTION ( 'NONE',  ( 0.000000000000000000, 1.505387152034110654E-14, -1.000000000000000000 ) ) ;
#28377=VERTEX_POINT ( 'NONE', #40334 ) ;
#28378=CYLINDRICAL_SURFACE ( 'NONE', #28183, 59.00000000000000000 ) ;
#28380=AXIS2_PLACEMENT_3D ( 'NONE', #13093, #42938, #3216 ) ;
#28381=VERTEX_POINT ( 'NONE', #37072 ) ;
#28383=CARTESIAN_POINT ( 'NONE',  ( 17.99999999999999645, -57.40245293794601622, -96.40140491896693220 ) ) ;
#28386=CARTESIAN_POINT ( 'NONE',  ( 0.000000000000000000, 0.000000000000000000, 0.000000000000000000 ) ) ;
#28387=CARTESIAN_POINT ( 'NONE',  ( -10.00000000000000000, 0.000000000000000000, 0.000000000000000000 ) ) ;
#28392=ORIENTED_EDGE ( 'NONE', *, *, #878, .T. ) ;
#28393=DIRECTION ( 'NONE',  ( 0.000000000000000000, 0.000000000000000000, 1.000000000000000000 ) ) ;
#28396=DIRECTION ( 'NONE',  ( 0.000000000000000000, 0.000000000000000000, 1.000000000000000000 ) ) ;
#28398=ORIENTED_EDGE ( 'NONE', *, *, #33637, .F. ) ;
#28399=AXIS2_PLACEMENT_3D ( 'NONE', #8800, #35613, #22364 ) ;
#28400=DIRECTION ( 'NONE',  ( -1.000000000000000000, -0.000000000000000000, -0.000000000000000000 ) ) ;
#28404=AXIS2_PLACEMENT_3D ( 'NONE', #13887, #4448, #34352 ) ;
#28405=CARTESIAN_POINT ( 'NONE',  ( 17.99999999999999645, -35.54274411427983438, -115.1399337407609949 ) ) ;
#28407=DIRECTION ( 'NONE',  ( 1.000000000000000000, -0.000000000000000000, -0.000000000000000000 ) ) ;
#28411=CIRCLE ( 'NONE', #9569, 59.00000000000000711 ) ;
#28414=ORIENTED_EDGE ( 'NONE', *, *, #20698, .T. ) ;
#28415=DIRECTION ( 'NONE',  ( -1.000000000000000000, -0.000000000000000000, -0.000000000000000000 ) ) ;
#28421=DIRECTION ( 'NONE',  ( 0.000000000000000000, 0.7865515558026436871, -0.6175246149461902645 ) ) ;
#28422=DIRECTION ( 'NONE',  ( 0.000000000000000000, 0.000000000000000000, 1.000000000000000000 ) ) ;
#28423=EDGE_CURVE ( 'NONE', #19384, #30604, #8100, .T. ) ;
#28424=AXIS2_PLACEMENT_3D ( 'NONE', #11898, #25226, #34564 ) ;
#28427=VECTOR ( 'NONE', #31858, 1000.000000000000000 ) ;
#28428=ORIENTED_EDGE ( 'NONE', *, *, #36402, .T. ) ;
#28431=VECTOR ( 'NONE', #40795, 1000.000000000000000 ) ;
#28433=CARTESIAN_POINT ( 'NONE',  ( 17.99999999999999645, 0.000000000000000000, 0.000000000000000000 ) ) ;
#28437=DIRECTION ( 'NONE',  ( 0.000000000000000000, 0.3641605752528230266, -0.9313361774523382097 ) ) ;
#28441=ORIENTED_EDGE ( 'NONE', *, *, #8602, .T. ) ;
#28442=EDGE_CURVE ( 'NONE', #36927, #3403, #33196, .T. ) ;
#28447=ORIENTED_EDGE ( 'NONE', *, *, #5491, .F. ) ;
#28449=CARTESIAN_POINT ( 'NONE',  ( 17.99999999999999645, 11.41303419184972689, 111.6154788735836405 ) ) ;
#28452=EDGE_CURVE ( 'NONE', #17938, #10707, #34021, .T. ) ;
#28456=AXIS2_PLACEMENT_3D ( 'NONE', #9183, #1777, #41910 ) ;
#28459=CARTESIAN_POINT ( 'NONE',  ( 17.99999999999999645, 46.12538073176347808, 111.3235835452212825 ) ) ;
#28460=CARTESIAN_POINT ( 'NONE',  ( 0.000000000000000000, -107.5680526044921947, 31.89649718262059608 ) ) ;
#28461=AXIS2_PLACEMENT_3D ( 'NONE', #32098, #13544, #6324 ) ;
#28466=DIRECTION ( 'NONE',  ( 0.000000000000000000, -0.5528000653612000770, 0.8333139190825105125 ) ) ;
#28467=VECTOR ( 'NONE', #3362, 1000.000000000000000 ) ;
#28468=EDGE_LOOP ( 'NONE', ( #30573, #16461, #24210, #3023 ) ) ;
#28469=CARTESIAN_POINT ( 'NONE',  ( 8.999999999999998224, -90.81729652456118629, -72.16798910853708549 ) ) ;
#28478=DIRECTION ( 'NONE',  ( -1.000000000000000000, 0.000000000000000000, 0.000000000000000000 ) ) ;
#28479=CARTESIAN_POINT ( 'NONE',  ( 0.000000000000000000, 21.55123232222474172, 118.5581519187672654 ) ) ;
#28481=CARTESIAN_POINT ( 'NONE',  ( 17.99999999999999645, -88.56657216608662964, 68.87840567545892156 ) ) ;
#28483=EDGE_CURVE ( 'NONE', #25300, #42489, #24878, .T. ) ;
#28487=ORIENTED_EDGE ( 'NONE', *, *, #5677, .T. ) ;
#28490=CARTESIAN_POINT ( 'NONE',  ( 0.000000000000000000, 30.01658535635262481, 108.1077105353199102 ) ) ;
#28491=DIRECTION ( 'NONE',  ( -1.000000000000000000, -0.000000000000000000, -0.000000000000000000 ) ) ;
#28492=AXIS2_PLACEMENT_3D ( 'NONE', #6768, #23380, #20336 ) ;
#28493=AXIS2_PLACEMENT_3D ( 'NONE', #22060, #38801, #32058 ) ;
#28499=CIRCLE ( 'NONE', #36792, 120.5010000000000190 ) ;
#28500=DIRECTION ( 'NONE',  ( -1.000000000000000000, 0.000000000000000000, -0.000000000000000000 ) ) ;
#28502=EDGE_LOOP ( 'NONE', ( #3644, #27341, #30783, #7781 ) ) ;
#28504=ORIENTED_EDGE ( 'NONE', *, *, #32982, .T. ) ;
#28508=CARTESIAN_POINT ( 'NONE',  ( 0.000000000000000000, 56.51398178981825993, 96.92493144647468739 ) ) ;
#28514=DIRECTION ( 'NONE',  ( -1.000000000000000000, -0.000000000000000000, -0.000000000000000000 ) ) ;
#28515=ORIENTED_EDGE ( 'NONE', *, *, #681, .T. ) ;
#28518=( NAMED_UNIT ( * ) SI_UNIT ( $, .STERADIAN. ) SOLID_ANGLE_UNIT ( ) );
#28519=CARTESIAN_POINT ( 'NONE',  ( 17.99999999999999645, 12.43843445475317822, 111.5058645182329968 ) ) ;
#28520=DIRECTION ( 'NONE',  ( 0.000000000000000000, 0.000000000000000000, 1.000000000000000000 ) ) ;
#28525=AXIS2_PLACEMENT_3D ( 'NONE', #27834, #41087, #37824 ) ;
#28526=ORIENTED_EDGE ( 'NONE', *, *, #28951, .F. ) ;
#28528=DIRECTION ( 'NONE',  ( -1.000000000000000000, -0.000000000000000000, -0.000000000000000000 ) ) ;
#28533=ADVANCED_FACE ( 'NONE', ( #38999 ), #2331, .F. ) ;
#28534=DIRECTION ( 'NONE',  ( 1.000000000000000000, 0.000000000000000000, 0.000000000000000000 ) ) ;
#28537=DIRECTION ( 'NONE',  ( 1.000000000000000000, 0.000000000000000000, 0.000000000000000000 ) ) ;
#28538=ORIENTED_EDGE ( 'NONE', *, *, #21991, .T. ) ;
#28539=DIRECTION ( 'NONE',  ( -1.000000000000000000, -0.000000000000000000, -0.000000000000000000 ) ) ;
#28542=VERTEX_POINT ( 'NONE', #29000 ) ;
#28545=DIRECTION ( 'NONE',  ( 1.000000000000000000, 0.000000000000000000, 0.000000000000000000 ) ) ;
#28546=CARTESIAN_POINT ( 'NONE',  ( 0.000000000000000000, -82.63181128086679905, -81.41243003647058174 ) ) ;
#28548=ORIENTED_EDGE ( 'NONE', *, *, #17198, .T. ) ;
#28549=EDGE_CURVE ( 'NONE', #36814, #33745, #42271, .T. ) ;
#28550=DIRECTION ( 'NONE',  ( 1.000000000000000000, 0.000000000000000000, 0.000000000000000000 ) ) ;
#28552=CARTESIAN_POINT ( 'NONE',  ( 17.99999999999999645, 111.2721026680458749, 14.38025178762809908 ) ) ;
#28558=ORIENTED_EDGE ( 'NONE', *, *, #11867, .F. ) ;
#28563=LINE ( 'NONE', #32442, #36657 ) ;
#28564=VERTEX_POINT ( 'NONE', #15289 ) ;
#28568=DIRECTION ( 'NONE',  ( -1.000000000000000000, -0.000000000000000000, -0.000000000000000000 ) ) ;
#28570=ORIENTED_EDGE ( 'NONE', *, *, #25287, .F. ) ;
#28572=DIRECTION ( 'NONE',  ( 0.000000000000000000, 0.000000000000000000, 1.000000000000000000 ) ) ;
#28575=AXIS2_PLACEMENT_3D ( 'NONE', #30407, #481, #13841 ) ;
#28583=CARTESIAN_POINT ( 'NONE',  ( 17.99999999999999645, 6.486220790508443912, 112.0098273076987567 ) ) ;
#28584=DIRECTION ( 'NONE',  ( -1.000000000000000000, -0.000000000000000000, -0.000000000000000000 ) ) ;
#28585=ORIENTED_EDGE ( 'NONE', *, *, #33274, .T. ) ;
#28586=DIRECTION ( 'NONE',  ( 1.000000000000000000, -0.000000000000000000, -0.000000000000000000 ) ) ;
#28592=ORIENTED_EDGE ( 'NONE', *, *, #10275, .F. ) ;
#28593=EDGE_CURVE ( 'NONE', #37390, #32317, #26371, .T. ) ;
#28594=LINE ( 'NONE', #8289, #21809 ) ;
#28595=DIRECTION ( 'NONE',  ( -1.000000000000000000, -0.000000000000000000, -0.000000000000000000 ) ) ;
#28596=FACE_OUTER_BOUND ( 'NONE', #21905, .T. ) ;
#28597=ORIENTED_EDGE ( 'NONE', *, *, #27484, .T. ) ;
#28598=ORIENTED_EDGE ( 'NONE', *, *, #4376, .T. ) ;
#28599=DIRECTION ( 'NONE',  ( -1.000000000000000000, -0.000000000000000000, 0.000000000000000000 ) ) ;
#28600=AXIS2_PLACEMENT_3D ( 'NONE', #12004, #38364, #38158 ) ;
#28605=AXIS2_PLACEMENT_3D ( 'NONE', #19479, #22751, #15984 ) ;
#28609=CARTESIAN_POINT ( 'NONE',  ( 17.99999999999999645, 84.62908780824871258, 85.78116633471321961 ) ) ;
#28610=DIRECTION ( 'NONE',  ( -1.000000000000000000, 0.000000000000000000, 0.000000000000000000 ) ) ;
#28613=CARTESIAN_POINT ( 'NONE',  ( 0.000000000000000000, 101.1403355683153933, -56.80345518653383152 ) ) ;
#28615=DIRECTION ( 'NONE',  ( 0.000000000000000000, 0.000000000000000000, 1.000000000000000000 ) ) ;
#28618=DIRECTION ( 'NONE',  ( 0.000000000000000000, 0.2631025642275152676, 0.9647678688145175929 ) ) ;
#28620=AXIS2_PLACEMENT_3D ( 'NONE', #2167, #8953, #1965 ) ;
#28621=EDGE_LOOP ( 'NONE', ( #33990, #20584, #37726, #34472 ) ) ;
#28623=AXIS2_PLACEMENT_3D ( 'NONE', #33948, #4035, #13685 ) ;
#28627=CARTESIAN_POINT ( 'NONE',  ( 17.99999999999999645, 0.000000000000000000, 0.000000000000000000 ) ) ;
#28628=AXIS2_PLACEMENT_3D ( 'NONE', #17505, #37734, #10937 ) ;
#28631=EDGE_CURVE ( 'NONE', #38008, #40762, #31091, .T. ) ;
#28636=DIRECTION ( 'NONE',  ( -1.000000000000000000, -0.000000000000000000, -0.000000000000000000 ) ) ;
#28637=ORIENTED_EDGE ( 'NONE', *, *, #29504, .F. ) ;
#28638=EDGE_CURVE ( 'NONE', #8430, #3574, #22684, .T. ) ;
#28641=ORIENTED_EDGE ( 'NONE', *, *, #41534, .F. ) ;
#28645=CARTESIAN_POINT ( 'NONE',  ( 17.99999999999999645, -92.25992191227442163, 77.51514567967366531 ) ) ;
#28647=CIRCLE ( 'NONE', #17423, 116.0000000000000000 ) ;
#28648=ORIENTED_EDGE ( 'NONE', *, *, #1490, .T. ) ;
#28653=CARTESIAN_POINT ( 'NONE',  ( 8.999999999999998224, 112.8457601792515419, 26.86697618949414945 ) ) ;
#28656=EDGE_CURVE ( 'NONE', #33767, #23951, #3891, .T. ) ;
#28660=DIRECTION ( 'NONE',  ( 1.000000000000000000, 0.000000000000000000, 0.000000000000000000 ) ) ;
#28661=CARTESIAN_POINT ( 'NONE',  ( 17.99999999999999645, 0.000000000000000000, 0.000000000000000000 ) ) ;
#28663=AXIS2_PLACEMENT_3D ( 'NONE', #17442, #30285, #33544 ) ;
#28664=DIRECTION ( 'NONE',  ( 0.000000000000000000, 0.5528000653611888637, 0.8333139190825180620 ) ) ;
#28665=DIRECTION ( 'NONE',  ( 0.000000000000000000, 0.9826841245925214130, -0.1852887240871113894 ) ) ;
#28668=VECTOR ( 'NONE', #6943, 1000.000000000000000 ) ;
#28670=DIRECTION ( 'NONE',  ( 1.000000000000000000, 0.000000000000000000, 0.000000000000000000 ) ) ;
#28673=ORIENTED_EDGE ( 'NONE', *, *, #32377, .T. ) ;
#28674=VECTOR ( 'NONE', #25829, 1000.000000000000000 ) ;
#28676=EDGE_CURVE ( 'NONE', #17094, #17808, #33886, .T. ) ;
#28685=EDGE_CURVE ( 'NONE', #13380, #20648, #20689, .T. ) ;
#28687=ORIENTED_EDGE ( 'NONE', *, *, #19564, .F. ) ;
#28688=DIRECTION ( 'NONE',  ( 1.000000000000000000, 0.000000000000000000, 0.000000000000000000 ) ) ;
#28691=AXIS2_PLACEMENT_3D ( 'NONE', #6351, #22131, #2204 ) ;
#28693=AXIS2_PLACEMENT_3D ( 'NONE', #32747, #15358, #39268 ) ;
#28695=DIRECTION ( 'NONE',  ( 0.000000000000000000, 2.305124076552231752E-14, -1.000000000000000000 ) ) ;
#28696=CIRCLE ( 'NONE', #16838, 120.5010000000000190 ) ;
#28700=ORIENTED_EDGE ( 'NONE', *, *, #15582, .F. ) ;
#28704=DIRECTION ( 'NONE',  ( -1.000000000000000000, 0.000000000000000000, 0.000000000000000000 ) ) ;
#28709=DIRECTION ( 'NONE',  ( 0.000000000000000000, 0.9996456111234526265, -0.02662052143777152158 ) ) ;
#28714=CARTESIAN_POINT ( 'NONE',  ( 0.000000000000000000, 17.77780072541695944, 114.6296200873376563 ) ) ;
#28715=EDGE_CURVE ( 'NONE', #20659, #6259, #23967, .T. ) ;
#28717=CARTESIAN_POINT ( 'NONE',  ( 17.99999999999999645, -80.74349901498355564, -77.90224541347362219 ) ) ;
#28718=VERTEX_POINT ( 'NONE', #20274 ) ;
#28720=EDGE_LOOP ( 'NONE', ( #1714, #3174, #16839, #13281 ) ) ;
#28721=( NAMED_UNIT ( * ) PLANE_ANGLE_UNIT ( ) SI_UNIT ( $, .RADIAN. ) );
#28725=CARTESIAN_POINT ( 'NONE',  ( 0.000000000000000000, 11.65176648921033298, 115.4133282497342918 ) ) ;
#28731=ORIENTED_EDGE ( 'NONE', *, *, #23161, .F. ) ;
#28732=CARTESIAN_POINT ( 'NONE',  ( 0.000000000000000000, 17.77780072541854040, -114.6296200873374147 ) ) ;
#28733=FACE_OUTER_BOUND ( 'NONE', #29456, .T. ) ;
#28741=DIRECTION ( 'NONE',  ( -1.000000000000000000, -0.000000000000000000, -0.000000000000000000 ) ) ;
#28743=FACE_OUTER_BOUND ( 'NONE', #2129, .T. ) ;
#28746=ORIENTED_EDGE ( 'NONE', *, *, #19883, .T. ) ;
#28747=CARTESIAN_POINT ( 'NONE',  ( 17.99999999999999645, 0.000000000000000000, 0.000000000000000000 ) ) ;
#28750=FACE_OUTER_BOUND ( 'NONE', #27061, .T. ) ;
#28751=AXIS2_PLACEMENT_3D ( 'NONE', #2162, #25561, #5236 ) ;
#28755=DIRECTION ( 'NONE',  ( 1.000000000000000000, 0.000000000000000000, 0.000000000000000000 ) ) ;
#28760=DIRECTION ( 'NONE',  ( -1.000000000000000000, -0.000000000000000000, -0.000000000000000000 ) ) ;
#28764=ADVANCED_FACE ( 'NONE', ( #1234 ), #579, .F. ) ;
#28765=ADVANCED_FACE ( 'NONE', ( #34183 ), #7784, .F. ) ;
#28766=LINE ( 'NONE', #42028, #27753 ) ;
#28767=EDGE_CURVE ( 'NONE', #13442, #32233, #15148, .T. ) ;
#28769=CYLINDRICAL_SURFACE ( 'NONE', #41562, 116.0000000000000000 ) ;
#28772=EDGE_CURVE ( 'NONE', #12547, #41527, #20723, .T. ) ;
#28773=VERTEX_POINT ( 'NONE', #787 ) ;
#28774=DIRECTION ( 'NONE',  ( -1.000000000000000000, 0.000000000000000000, 0.000000000000000000 ) ) ;
#28775=DIRECTION ( 'NONE',  ( 1.000000000000000000, -0.000000000000000000, -0.000000000000000000 ) ) ;
#28778=CARTESIAN_POINT ( 'NONE',  ( 0.000000000000000000, 0.000000000000000000, 0.000000000000000000 ) ) ;
#28781=CARTESIAN_POINT ( 'NONE',  ( 8.999999999999998224, -94.52951811191606168, 67.23221107124869889 ) ) ;
#28786=CIRCLE ( 'NONE', #21838, 120.5010000000000190 ) ;
#28793=CARTESIAN_POINT ( 'NONE',  ( 17.99999999999999645, -16.77566611177856615, 119.3275660838941832 ) ) ;
#28794=ORIENTED_EDGE ( 'NONE', *, *, #2403, .T. ) ;
#28796=LINE ( 'NONE', #9774, #11943 ) ;
#28800=ORIENTED_EDGE ( 'NONE', *, *, #9863, .T. ) ;
#28801=CARTESIAN_POINT ( 'NONE',  ( 8.999999999999998224, -59.47573314508669284, -99.59235496188668435 ) ) ;
#28802=MANIFOLD_SOLID_BREP ( 'TeethCuts', #37943 ) ;
#28804=CIRCLE ( 'NONE', #18403, 120.5010000000000190 ) ;
#28805=VERTEX_POINT ( 'NONE', #34613 ) ;
#28806=CARTESIAN_POINT ( 'NONE',  ( 17.99999999999999645, -88.00363688980490906, -82.31555682352745862 ) ) ;
#28808=DIRECTION ( 'NONE',  ( 0.000000000000000000, 0.000000000000000000, 1.000000000000000000 ) ) ;
#28809=DIRECTION ( 'NONE',  ( 1.000000000000000000, 0.000000000000000000, -0.000000000000000000 ) ) ;
#28810=DIRECTION ( 'NONE',  ( -1.000000000000000000, 0.000000000000000000, 0.000000000000000000 ) ) ;
#28814=ORIENTED_EDGE ( 'NONE', *, *, #751, .T. ) ;
#28816=EDGE_CURVE ( 'NONE', #9979, #39267, #14444, .T. ) ;
#28818=CIRCLE ( 'NONE', #18413, 59.00000000000001421 ) ;
#28820=EDGE_LOOP ( 'NONE', ( #21687, #8120, #12061, #19985 ) ) ;
#28821=CARTESIAN_POINT ( 'NONE',  ( 17.99999999999999645, 0.000000000000000000, 0.000000000000000000 ) ) ;
#28823=EDGE_CURVE ( 'NONE', #6504, #10645, #9533, .T. ) ;
#28825=CARTESIAN_POINT ( 'NONE',  ( 17.99999999999999645, 0.000000000000000000, 0.000000000000000000 ) ) ;
#28827=VERTEX_POINT ( 'NONE', #2284 ) ;
#28830=ORIENTED_EDGE ( 'NONE', *, *, #21888, .T. ) ;
#28833=AXIS2_PLACEMENT_3D ( 'NONE', #42101, #32728, #3015 ) ;
#28834=CYLINDRICAL_SURFACE ( 'NONE', #3235, 120.5010000000000190 ) ;
#28835=DIRECTION ( 'NONE',  ( -1.000000000000000000, -0.000000000000000000, -0.000000000000000000 ) ) ;
#28839=ORIENTED_EDGE ( 'NONE', *, *, #18791, .T. ) ;
#28841=VERTEX_POINT ( 'NONE', #41586 ) ;
#28843=CIRCLE ( 'NONE', #40662, 116.0000000000000000 ) ;
#28844=DIRECTION ( 'NONE',  ( -1.000000000000000000, -0.000000000000000000, -0.000000000000000000 ) ) ;
#28845=VERTEX_POINT ( 'NONE', #8228 ) ;
#28846=CARTESIAN_POINT ( 'NONE',  ( 17.99999999999999645, 111.2721026680460596, -14.38025178762657852 ) ) ;
#28847=ORIENTED_EDGE ( 'NONE', *, *, #22749, .T. ) ;
#28848=CARTESIAN_POINT ( 'NONE',  ( 0.000000000000000000, -15.21076497709793252, 119.5371223922154797 ) ) ;
#28850=CIRCLE ( 'NONE', #37165, 120.5010000000000190 ) ;
#28857=EDGE_CURVE ( 'NONE', #1613, #13871, #32511, .T. ) ;
#28858=FACE_OUTER_BOUND ( 'NONE', #37914, .T. ) ;
#28861=AXIS2_PLACEMENT_3D ( 'NONE', #33107, #3194, #7135 ) ;
#28864=CARTESIAN_POINT ( 'NONE',  ( 9.000000000000001776, -23.85344185397118011, -113.5209818126993611 ) ) ;
#28865=DIRECTION ( 'NONE',  ( 1.000000000000000000, 0.000000000000000000, 0.000000000000000000 ) ) ;
#28868=CARTESIAN_POINT ( 'NONE',  ( 17.99999999999999645, -105.3681574666261298, -38.54638589714993202 ) ) ;
#28869=ORIENTED_EDGE ( 'NONE', *, *, #1603, .T. ) ;
#28873=AXIS2_PLACEMENT_3D ( 'NONE', #6932, #30728, #30935 ) ;
#28875=CARTESIAN_POINT ( 'NONE',  ( 17.99999999999999645, 0.000000000000000000, 0.000000000000000000 ) ) ;
#28876=EDGE_CURVE ( 'NONE', #6899, #5227, #38761, .T. ) ;
#28877=DIRECTION ( 'NONE',  ( 0.000000000000000000, 0.000000000000000000, 1.000000000000000000 ) ) ;
#28882=CIRCLE ( 'NONE', #16362, 120.5010000000000332 ) ;
#28884=CIRCLE ( 'NONE', #10043, 120.5010000000000332 ) ;
#28885=ORIENTED_EDGE ( 'NONE', *, *, #39091, .F. ) ;
#28886=DIRECTION ( 'NONE',  ( -1.000000000000000000, -0.000000000000000000, -0.000000000000000000 ) ) ;
#28890=CYLINDRICAL_SURFACE ( 'NONE', #4496, 120.5010000000000190 ) ;
#28893=CIRCLE ( 'NONE', #32358, 59.00000000000000000 ) ;
#28898=EDGE_CURVE ( 'NONE', #9338, #8713, #7437, .T. ) ;
#28901=CARTESIAN_POINT ( 'NONE',  ( 0.000000000000000000, -103.1672962317648512, -44.09967643725973119 ) ) ;
#28903=VERTEX_POINT ( 'NONE', #8433 ) ;
#28904=ORIENTED_EDGE ( 'NONE', *, *, #6996, .F. ) ;
#28906=DIRECTION ( 'NONE',  ( 0.000000000000000000, 0.000000000000000000, 1.000000000000000000 ) ) ;
#28908=LINE ( 'NONE', #42172, #34118 ) ;
#28911=ORIENTED_EDGE ( 'NONE', *, *, #22970, .T. ) ;
#28912=DIRECTION ( 'NONE',  ( 0.000000000000000000, -0.8993121301712231341, 0.4373073204588475704 ) ) ;
#28914=EDGE_CURVE ( 'NONE', #1568, #34811, #8133, .T. ) ;
#28916=ORIENTED_EDGE ( 'NONE', *, *, #3912, .F. ) ;
#28919=CARTESIAN_POINT ( 'NONE',  ( 17.99999999999999645, 103.1672962317657323, -44.09967643725766351 ) ) ;
#28921=CIRCLE ( 'NONE', #11510, 59.00000000000000711 ) ;
#28922=DIRECTION ( 'NONE',  ( 1.000000000000000000, 0.000000000000000000, 0.000000000000000000 ) ) ;
#28926=EDGE_CURVE ( 'NONE', #36617, #41769, #18655, .T. ) ;
#28928=DIRECTION ( 'NONE',  ( 0.000000000000000000, 0.000000000000000000, 1.000000000000000000 ) ) ;
#28934=EDGE_CURVE ( 'NONE', #6975, #41781, #40150, .T. ) ;
#28936=DIRECTION ( 'NONE',  ( 0.000000000000000000, 0.000000000000000000, 1.000000000000000000 ) ) ;
#28938=DIRECTION ( 'NONE',  ( -1.000000000000000000, -0.000000000000000000, -0.000000000000000000 ) ) ;
#28939=CARTESIAN_POINT ( 'NONE',  ( 17.99999999999999645, 59.47573314508733944, 99.59235496188628645 ) ) ;
#28943=DIRECTION ( 'NONE',  ( 1.000000000000000000, 0.000000000000000000, 0.000000000000000000 ) ) ;
#28944=CIRCLE ( 'NONE', #28272, 59.00000000000002132 ) ;
#28947=ORIENTED_EDGE ( 'NONE', *, *, #42657, .F. ) ;
#28948=EDGE_CURVE ( 'NONE', #14958, #37380, #21421, .T. ) ;
#28951=EDGE_CURVE ( 'NONE', #27015, #4469, #39367, .T. ) ;
#28954=ORIENTED_EDGE ( 'NONE', *, *, #4324, .T. ) ;
#28958=CARTESIAN_POINT ( 'NONE',  ( 17.99999999999999645, -91.65951123222436081, -71.09524597798180423 ) ) ;
#28959=CIRCLE ( 'NONE', #1770, 59.00000000000000000 ) ;
#28960=DIRECTION ( 'NONE',  ( 1.000000000000000000, 0.000000000000000000, 0.000000000000000000 ) ) ;
#28961=VERTEX_POINT ( 'NONE', #43082 ) ;
#28963=CARTESIAN_POINT ( 'NONE',  ( 0.000000000000000000, 24.22031524825977300, 109.5520369638038289 ) ) ;
#28964=EDGE_CURVE ( 'NONE', #18580, #15011, #5362, .T. ) ;
#28969=DIRECTION ( 'NONE',  ( 0.000000000000000000, 0.000000000000000000, -1.000000000000000000 ) ) ;
#28971=DIRECTION ( 'NONE',  ( -1.000000000000000000, 0.000000000000000000, 0.000000000000000000 ) ) ;
#28973=CYLINDRICAL_SURFACE ( 'NONE', #7506, 120.5010000000000190 ) ;
#28983=LINE ( 'NONE', #12406, #27364 ) ;
#28989=DIRECTION ( 'NONE',  ( -1.000000000000000000, 0.000000000000000000, 0.000000000000000000 ) ) ;
#28991=EDGE_LOOP ( 'NONE', ( #21860, #14963, #19558, #31489 ) ) ;
#28992=CARTESIAN_POINT ( 'NONE',  ( -10.00000000000000000, 0.000000000000000000, 0.000000000000000000 ) ) ;
#28995=CARTESIAN_POINT ( 'NONE',  ( 0.000000000000000000, -112.1427988504408120, 3.502162136923045566 ) ) ;
#29000=CARTESIAN_POINT ( 'NONE',  ( 0.000000000000000000, 19.12429268481864142, -114.4126803693777248 ) ) ;
#29002=CARTESIAN_POINT ( 'NONE',  ( 0.000000000000000000, 0.000000000000000000, 0.000000000000000000 ) ) ;
#29005=AXIS2_PLACEMENT_3D ( 'NONE', #37153, #33895, #27361 ) ;
#29007=EDGE_CURVE ( 'NONE', #40494, #4914, #39497, .T. ) ;
#29008=DIRECTION ( 'NONE',  ( -1.000000000000000000, 0.000000000000000000, -0.000000000000000000 ) ) ;
#29009=ORIENTED_EDGE ( 'NONE', *, *, #17609, .T. ) ;
#29017=VECTOR ( 'NONE', #40435, 1000.000000000000000 ) ;
#29018=ORIENTED_EDGE ( 'NONE', *, *, #11768, .F. ) ;
#29022=ORIENTED_EDGE ( 'NONE', *, *, #8471, .T. ) ;
#29026=DIRECTION ( 'NONE',  ( 0.000000000000000000, 0.000000000000000000, 1.000000000000000000 ) ) ;
#29027=DIRECTION ( 'NONE',  ( 0.000000000000000000, 0.4610925014493207352, 0.8873520750565743187 ) ) ;
#29028=CYLINDRICAL_SURFACE ( 'NONE', #7964, 116.0000000000000000 ) ;
#29033=ORIENTED_EDGE ( 'NONE', *, *, #23518, .T. ) ;
#29034=DIRECTION ( 'NONE',  ( 1.000000000000000000, 0.000000000000000000, 0.000000000000000000 ) ) ;
#29035=EDGE_CURVE ( 'NONE', #35216, #22361, #10981, .T. ) ;
#29037=VERTEX_POINT ( 'NONE', #9070 ) ;
#29039=AXIS2_PLACEMENT_3D ( 'NONE', #35590, #39075, #15362 ) ;
#29052=CARTESIAN_POINT ( 'NONE',  ( 17.99999999999999645, 0.000000000000000000, 0.000000000000000000 ) ) ;
#29053=AXIS2_PLACEMENT_3D ( 'NONE', #28030, #4423, #11660 ) ;
#29055=EDGE_CURVE ( 'NONE', #7775, #10543, #36316, .T. ) ;
#29056=FACE_OUTER_BOUND ( 'NONE', #6879, .T. ) ;
#29057=DIRECTION ( 'NONE',  ( 0.000000000000000000, 0.000000000000000000, 1.000000000000000000 ) ) ;
#29059=ADVANCED_FACE ( 'NONE', ( #9283 ), #6433, .F. ) ;
#29060=VERTEX_POINT ( 'NONE', #25901 ) ;
#29062=DIRECTION ( 'NONE',  ( 0.000000000000000000, 0.4610925014493207352, 0.8873520750565742077 ) ) ;
#29064=ORIENTED_EDGE ( 'NONE', *, *, #13849, .F. ) ;
#29066=CARTESIAN_POINT ( 'NONE',  ( 0.000000000000000000, 8.827181066047511848, -120.1772519049558667 ) ) ;
#29068=VERTEX_POINT ( 'NONE', #3135 ) ;
#29070=VERTEX_POINT ( 'NONE', #39157 ) ;
#29071=AXIS2_PLACEMENT_3D ( 'NONE', #7017, #40165, #23647 ) ;
#29074=EDGE_CURVE ( 'NONE', #31975, #36084, #22636, .T. ) ;
#29077=DIRECTION ( 'NONE',  ( -1.000000000000000000, 0.000000000000000000, -0.000000000000000000 ) ) ;
#29084=DIRECTION ( 'NONE',  ( -1.000000000000000000, 0.000000000000000000, -0.000000000000000000 ) ) ;
#29086=CARTESIAN_POINT ( 'NONE',  ( 17.99999999999999645, 104.6166166098445416, 50.11350645393712000 ) ) ;
#29089=DIRECTION ( 'NONE',  ( 1.000000000000000000, 0.000000000000000000, 0.000000000000000000 ) ) ;
#29090=ORIENTED_EDGE ( 'NONE', *, *, #10874, .F. ) ;
#29095=AXIS2_PLACEMENT_3D ( 'NONE', #31313, #14530, #31092 ) ;
#29098=AXIS2_PLACEMENT_3D ( 'NONE', #28627, #28835, #38207 ) ;
#29103=AXIS2_PLACEMENT_3D ( 'NONE', #11041, #4236, #7086 ) ;
#29106=CARTESIAN_POINT ( 'NONE',  ( 8.999999999999998224, 54.09091620264857880, -102.6166301549512525 ) ) ;
#29107=DIRECTION ( 'NONE',  ( 0.000000000000000000, 0.9968120070307504577, -0.07978610555307970309 ) ) ;
#29108=AXIS2_PLACEMENT_3D ( 'NONE', #42592, #19098, #26473 ) ;
#29110=FACE_OUTER_BOUND ( 'NONE', #33338, .T. ) ;
#29112=CARTESIAN_POINT ( 'NONE',  ( 0.000000000000000000, 96.25468616236763353, -72.49500943364391503 ) ) ;
#29113=ORIENTED_EDGE ( 'NONE', *, *, #28914, .F. ) ;
#29115=VERTEX_POINT ( 'NONE', #10367 ) ;
#29116=CARTESIAN_POINT ( 'NONE',  ( 17.99999999999999645, -91.51415974874635140, 64.91094698989267897 ) ) ;
#29118=EDGE_CURVE ( 'NONE', #4572, #28151, #26304, .T. ) ;
#29120=CARTESIAN_POINT ( 'NONE',  ( 17.99999999999999645, -59.07817985939071548, 105.0250430397506847 ) ) ;
#29121=ORIENTED_EDGE ( 'NONE', *, *, #16862, .T. ) ;
#29123=ORIENTED_EDGE ( 'NONE', *, *, #8092, .F. ) ;
#29125=EDGE_CURVE ( 'NONE', #11603, #9979, #27386, .T. ) ;
#29126=ORIENTED_EDGE ( 'NONE', *, *, #6545, .F. ) ;
#29131=VERTEX_POINT ( 'NONE', #40879 ) ;
#29133=AXIS2_PLACEMENT_3D ( 'NONE', #9875, #13610, #10529 ) ;
#29134=VECTOR ( 'NONE', #10914, 1000.000000000000000 ) ;
#29135=AXIS2_PLACEMENT_3D ( 'NONE', #24689, #38584, #8707 ) ;
#29136=DIRECTION ( 'NONE',  ( -1.000000000000000000, -0.000000000000000000, 0.000000000000000000 ) ) ;
#29140=CIRCLE ( 'NONE', #22225, 59.00000000000000711 ) ;
#29141=DIRECTION ( 'NONE',  ( 0.000000000000000000, 0.000000000000000000, 1.000000000000000000 ) ) ;
#29143=FACE_OUTER_BOUND ( 'NONE', #3972, .T. ) ;
#29150=VECTOR ( 'NONE', #315, 1000.000000000000000 ) ;
#29152=CARTESIAN_POINT ( 'NONE',  ( 0.000000000000000000, -75.72520367775034345, -82.78868281116056949 ) ) ;
#29154=ORIENTED_EDGE ( 'NONE', *, *, #32458, .T. ) ;
#29155=CARTESIAN_POINT ( 'NONE',  ( 8.999999999999998224, 115.9750404417044081, -2.406240749597859718 ) ) ;
#29156=ORIENTED_EDGE ( 'NONE', *, *, #9722, .T. ) ;
#29158=CARTESIAN_POINT ( 'NONE',  ( 9.000000000000001776, -115.9387338813861987, 3.769613505535687636 ) ) ;
#29159=AXIS2_PLACEMENT_3D ( 'NONE', #34296, #40604, #34088 ) ;
#29161=AXIS2_PLACEMENT_3D ( 'NONE', #17489, #10690, #11141 ) ;
#29164=AXIS2_PLACEMENT_3D ( 'NONE', #9765, #23322, #36580 ) ;
#29168=CYLINDRICAL_SURFACE ( 'NONE', #40214, 59.00000000000000000 ) ;
#29169=AXIS2_PLACEMENT_3D ( 'NONE', #27362, #31704, #14934 ) ;
#29170=EDGE_LOOP ( 'NONE', ( #7314, #1642, #11287, #9243 ) ) ;
#29171=VECTOR ( 'NONE', #2668, 1000.000000000000000 ) ;
#29172=DIRECTION ( 'NONE',  ( 1.000000000000000000, 0.000000000000000000, 0.000000000000000000 ) ) ;
#29174=DIRECTION ( 'NONE',  ( 0.000000000000000000, 2.305124076552231752E-14, -1.000000000000000000 ) ) ;
#29175=CARTESIAN_POINT ( 'NONE',  ( 0.000000000000000000, 94.83915810436481308, -59.94836581341496640 ) ) ;
#29177=CARTESIAN_POINT ( 'NONE',  ( 17.99999999999999645, 0.000000000000000000, 0.000000000000000000 ) ) ;
#29179=EDGE_CURVE ( 'NONE', #39420, #37944, #8882, .T. ) ;
#29184=DIRECTION ( 'NONE',  ( -1.000000000000000000, 0.000000000000000000, 0.000000000000000000 ) ) ;
#29185=VERTEX_POINT ( 'NONE', #33921 ) ;
#29188=CARTESIAN_POINT ( 'NONE',  ( -10.00000000000000000, 0.000000000000000000, 0.000000000000000000 ) ) ;
#29190=DIRECTION ( 'NONE',  ( 0.000000000000000000, -0.3641605752528294659, 0.9313361774523355452 ) ) ;
#29192=CARTESIAN_POINT ( 'NONE',  ( 17.99999999999999645, 51.27532863109503580, -99.79535634195073612 ) ) ;
#29198=EDGE_CURVE ( 'NONE', #32870, #32579, #4008, .T. ) ;
#29199=DIRECTION ( 'NONE',  ( 0.000000000000000000, 0.000000000000000000, 1.000000000000000000 ) ) ;
#29208=ORIENTED_EDGE ( 'NONE', *, *, #2675, .T. ) ;
#29214=CARTESIAN_POINT ( 'NONE',  ( 17.99999999999999645, -100.8494052988166345, -65.95368414179013428 ) ) ;
#29217=CARTESIAN_POINT ( 'NONE',  ( 0.000000000000000000, -96.25468616236712194, 72.49500943364459715 ) ) ;
#29221=CIRCLE ( 'NONE', #38939, 116.0000000000000000 ) ;
#29233=CARTESIAN_POINT ( 'NONE',  ( 0.000000000000000000, -87.74575819880217864, 75.87280091124446813 ) ) ;
#29235=CARTESIAN_POINT ( 'NONE',  ( 17.99999999999999645, 107.5680526044915410, 31.89649718262280231 ) ) ;
#29236=CARTESIAN_POINT ( 'NONE',  ( 8.999999999999998224, 64.69195966009891663, 96.28577441832274530 ) ) ;
#29237=CARTESIAN_POINT ( 'NONE',  ( 17.99999999999999645, -107.2885202478269946, 54.86040852957277281 ) ) ;
#29240=DIRECTION ( 'NONE',  ( 0.000000000000000000, -0.1062934856473723849, 0.9943348002101364269 ) ) ;
#29242=AXIS2_PLACEMENT_3D ( 'NONE', #9302, #28971, #42243 ) ;
#29243=CARTESIAN_POINT ( 'NONE',  ( -10.00000000000000000, 0.000000000000000000, 0.000000000000000000 ) ) ;
#29244=ADVANCED_FACE ( 'NONE', ( #20223 ), #13443, .F. ) ;
#29246=EDGE_CURVE ( 'NONE', #41404, #42055, #16942, .T. ) ;
#29247=EDGE_LOOP ( 'NONE', ( #26064, #27147, #36123, #40395 ) ) ;
#29249=CARTESIAN_POINT ( 'NONE',  ( 17.99999999999999645, -80.02407177073008882, 78.64108602299921813 ) ) ;
#29251=ADVANCED_FACE ( 'NONE', ( #27175 ), #15396, .F. ) ;
#29254=AXIS2_PLACEMENT_3D ( 'NONE', #39903, #38165, #7841 ) ;
#29256=DIRECTION ( 'NONE',  ( -1.000000000000000000, 0.000000000000000000, 0.000000000000000000 ) ) ;
#29262=CYLINDRICAL_SURFACE ( 'NONE', #14440, 120.5010000000000190 ) ;
#29263=DIRECTION ( 'NONE',  ( -1.000000000000000000, 0.000000000000000000, -0.000000000000000000 ) ) ;
#29264=LINE ( 'NONE', #25990, #8595 ) ;
#29267=ORIENTED_EDGE ( 'NONE', *, *, #32087, .F. ) ;
#29272=ORIENTED_EDGE ( 'NONE', *, *, #35516, .F. ) ;
#29274=CIRCLE ( 'NONE', #2753, 116.0000000000000000 ) ;
#29277=VERTEX_POINT ( 'NONE', #41531 ) ;
#29279=ORIENTED_EDGE ( 'NONE', *, *, #15882, .F. ) ;
#29280=ORIENTED_EDGE ( 'NONE', *, *, #10787, .T. ) ;
#29283=VERTEX_POINT ( 'NONE', #25427 ) ;
#29287=EDGE_LOOP ( 'NONE', ( #8732, #32763, #13139, #25402 ) ) ;
#29289=CARTESIAN_POINT ( 'NONE',  ( 17.99999999999999645, 0.000000000000000000, 0.000000000000000000 ) ) ;
#29293=CARTESIAN_POINT ( 'NONE',  ( 0.000000000000000000, 104.2166695095720854, -60.49278301857700768 ) ) ;
#29299=EDGE_CURVE ( 'NONE', #38233, #22186, #11895, .T. ) ;
#29301=ORIENTED_EDGE ( 'NONE', *, *, #42164, .T. ) ;
#29302=FACE_OUTER_BOUND ( 'NONE', #20429, .T. ) ;
#29303=CIRCLE ( 'NONE', #28628, 59.00000000000000000 ) ;
#29310=ORIENTED_EDGE ( 'NONE', *, *, #27414, .T. ) ;
#29314=DIRECTION ( 'NONE',  ( 1.000000000000000000, -0.000000000000000000, -0.000000000000000000 ) ) ;
#29315=LINE ( 'NONE', #39531, #22505 ) ;
#29317=EDGE_LOOP ( 'NONE', ( #9685, #10240, #9867, #35740 ) ) ;
#29319=ORIENTED_EDGE ( 'NONE', *, *, #27354, .F. ) ;
#29321=DIRECTION ( 'NONE',  ( 1.000000000000000000, 0.000000000000000000, 0.000000000000000000 ) ) ;
#29323=ADVANCED_FACE ( 'NONE', ( #35204 ), #21948, .F. ) ;
#29325=DIRECTION ( 'NONE',  ( -1.000000000000000000, 0.000000000000000000, 0.000000000000000000 ) ) ;
#29328=ORIENTED_EDGE ( 'NONE', *, *, #25976, .T. ) ;
#29330=EDGE_CURVE ( 'NONE', #40120, #710, #40179, .T. ) ;
#29331=DIRECTION ( 'NONE',  ( 1.000000000000000000, 0.000000000000000000, 0.000000000000000000 ) ) ;
#29338=AXIS2_PLACEMENT_3D ( 'NONE', #15467, #8665, #5176 ) ;
#29339=ORIENTED_EDGE ( 'NONE', *, *, #20884, .F. ) ;
#29340=CARTESIAN_POINT ( 'NONE',  ( 17.99999999999999645, -75.03166794516737070, -94.29071961951585479 ) ) ;
#29342=ORIENTED_EDGE ( 'NONE', *, *, #9407, .T. ) ;
#29343=LINE ( 'NONE', #32600, #9133 ) ;
#29344=ORIENTED_EDGE ( 'NONE', *, *, #6001, .F. ) ;
#29347=DIRECTION ( 'NONE',  ( -1.000000000000000000, 0.000000000000000000, 0.000000000000000000 ) ) ;
#29348=CARTESIAN_POINT ( 'NONE',  ( 0.000000000000000000, -112.1427988504407551, -3.502162136924565239 ) ) ;
#29350=CARTESIAN_POINT ( 'NONE',  ( 17.99999999999999645, 0.5156212287279957618, 112.1962860721878172 ) ) ;
#29351=ORIENTED_EDGE ( 'NONE', *, *, #42625, .F. ) ;
#29356=CARTESIAN_POINT ( 'NONE',  ( 0.000000000000000000, 95.31344542257821217, -66.11616384574354299 ) ) ;
#29359=CARTESIAN_POINT ( 'NONE',  ( 17.99999999999999645, 71.21168426767107462, 86.70160608319346807 ) ) ;
#29363=DIRECTION ( 'NONE',  ( -1.000000000000000000, -0.000000000000000000, -0.000000000000000000 ) ) ;
#29364=CIRCLE ( 'NONE', #24504, 116.0000000000000000 ) ;
#29365=CIRCLE ( 'NONE', #28693, 116.0000000000000000 ) ;
#29366=EDGE_CURVE ( 'NONE', #13380, #41947, #36011, .T. ) ;
#29367=ORIENTED_EDGE ( 'NONE', *, *, #22087, .F. ) ;
#29369=DIRECTION ( 'NONE',  ( 0.000000000000000000, 0.7865515558026394682, 0.6175246149461958156 ) ) ;
#29381=ORIENTED_EDGE ( 'NONE', *, *, #24709, .T. ) ;
#29382=DIRECTION ( 'NONE',  ( -1.000000000000000000, 0.000000000000000000, -0.000000000000000000 ) ) ;
#29383=CARTESIAN_POINT ( 'NONE',  ( 17.99999999999999645, -34.03109950475653989, -115.5957406979053133 ) ) ;
#29388=CARTESIAN_POINT ( 'NONE',  ( -10.00000000000000000, 0.000000000000000000, 0.000000000000000000 ) ) ;
#29390=ORIENTED_EDGE ( 'NONE', *, *, #20427, .F. ) ;
#29391=ORIENTED_EDGE ( 'NONE', *, *, #41286, .F. ) ;
#29392=DIRECTION ( 'NONE',  ( -1.000000000000000000, 0.000000000000000000, 0.000000000000000000 ) ) ;
#29396=DIRECTION ( 'NONE',  ( 0.000000000000000000, 0.000000000000000000, 1.000000000000000000 ) ) ;
#29398=DIRECTION ( 'NONE',  ( -1.000000000000000000, 0.000000000000000000, 0.000000000000000000 ) ) ;
#29402=ORIENTED_EDGE ( 'NONE', *, *, #3401, .T. ) ;
#29403=CYLINDRICAL_SURFACE ( 'NONE', #16101, 59.00000000000000000 ) ;
#29404=ORIENTED_EDGE ( 'NONE', *, *, #7738, .T. ) ;
#29406=DIRECTION ( 'NONE',  ( -1.000000000000000000, 0.000000000000000000, 0.000000000000000000 ) ) ;
#29409=DIRECTION ( 'NONE',  ( 0.000000000000000000, 0.3140767120219495334, -0.9493976084683810601 ) ) ;
#29415=EDGE_CURVE ( 'NONE', #8485, #2740, #21486, .T. ) ;
#29422=ORIENTED_EDGE ( 'NONE', *, *, #23142, .F. ) ;
#29426=DIRECTION ( 'NONE',  ( 0.000000000000000000, 0.000000000000000000, 1.000000000000000000 ) ) ;
#29428=CARTESIAN_POINT ( 'NONE',  ( 17.99999999999999645, 103.5682682299988500, -43.14958040911561454 ) ) ;
#29429=VERTEX_POINT ( 'NONE', #2869 ) ;
#29432=ADVANCED_FACE ( 'NONE', ( #3077 ), #12957, .F. ) ;
#29436=CIRCLE ( 'NONE', #19669, 59.00000000000000711 ) ;
#29437=ORIENTED_EDGE ( 'NONE', *, *, #15377, .F. ) ;
#29442=ORIENTED_EDGE ( 'NONE', *, *, #26579, .F. ) ;
#29443=LINE ( 'NONE', #12861, #5160 ) ;
#29445=DIRECTION ( 'NONE',  ( 0.000000000000000000, -0.4610925014493143514, -0.8873520750565775383 ) ) ;
#29448=CARTESIAN_POINT ( 'NONE',  ( 9.000000000000001776, -115.0622509503833442, 14.72000021165104755 ) ) ;
#29449=EDGE_LOOP ( 'NONE', ( #27863, #13793, #11928, #20339 ) ) ;
#29451=ADVANCED_FACE ( 'NONE', ( #22583 ), #39109, .F. ) ;
#29453=VERTEX_POINT ( 'NONE', #36261 ) ;
#29454=AXIS2_PLACEMENT_3D ( 'NONE', #5616, #35916, #29199 ) ;
#29456=EDGE_LOOP ( 'NONE', ( #2452, #7556, #28526, #6566 ) ) ;
#29458=VECTOR ( 'NONE', #30292, 1000.000000000000000 ) ;
#29464=VECTOR ( 'NONE', #34703, 1000.000000000000000 ) ;
#29467=ORIENTED_EDGE ( 'NONE', *, *, #31274, .F. ) ;
#29471=CARTESIAN_POINT ( 'NONE',  ( 17.99999999999999645, -105.7179949885865256, -37.57629584241794163 ) ) ;
#29475=EDGE_LOOP ( 'NONE', ( #18425, #11906, #8928, #23764 ) ) ;
#29477=CARTESIAN_POINT ( 'NONE',  ( 0.000000000000000000, 45.89132998248186368, -102.3829004574625401 ) ) ;
#29479=VERTEX_POINT ( 'NONE', #29753 ) ;
#29480=EDGE_CURVE ( 'NONE', #8238, #30765, #34664, .T. ) ;
#29487=AXIS2_PLACEMENT_3D ( 'NONE', #35345, #5667, #19025 ) ;
#29488=ORIENTED_EDGE ( 'NONE', *, *, #29851, .T. ) ;
#29493=CARTESIAN_POINT ( 'NONE',  ( 17.99999999999999645, -83.49789599728724454, -86.88263557826851979 ) ) ;
#29494=CARTESIAN_POINT ( 'NONE',  ( 17.99999999999999645, 100.8494052988179561, -65.95368414178808791 ) ) ;
#29496=DIRECTION ( 'NONE',  ( 0.000000000000000000, 0.000000000000000000, 1.000000000000000000 ) ) ;
#29497=EDGE_CURVE ( 'NONE', #37944, #2980, #6173, .T. ) ;
#29500=FACE_OUTER_BOUND ( 'NONE', #18033, .T. ) ;
#29502=CYLINDRICAL_SURFACE ( 'NONE', #36038, 116.0000000000000000 ) ;
#29503=EDGE_LOOP ( 'NONE', ( #26305, #17714, #16025, #9676 ) ) ;
#29504=EDGE_CURVE ( 'NONE', #38227, #17128, #19521, .T. ) ;
#29510=CYLINDRICAL_SURFACE ( 'NONE', #26048, 116.0000000000000000 ) ;
#29511=ORIENTED_EDGE ( 'NONE', *, *, #31620, .F. ) ;
#29516=EDGE_LOOP ( 'NONE', ( #40088, #8887, #28447, #17677 ) ) ;
#29520=CYLINDRICAL_SURFACE ( 'NONE', #30990, 120.5010000000000190 ) ;
#29523=DIRECTION ( 'NONE',  ( -1.000000000000000000, 0.000000000000000000, -0.000000000000000000 ) ) ;
#29525=DIRECTION ( 'NONE',  ( 1.000000000000000000, 0.000000000000000000, 0.000000000000000000 ) ) ;
#29526=EDGE_LOOP ( 'NONE', ( #16287, #29437, #592, #5909 ) ) ;
#29533=EDGE_CURVE ( 'NONE', #7030, #43001, #29829, .T. ) ;
#29535=CIRCLE ( 'NONE', #24705, 59.00000000000001421 ) ;
#29536=DIRECTION ( 'NONE',  ( 0.000000000000000000, -0.05322217484216513333, -0.9985826956767627216 ) ) ;
#29539=ORIENTED_EDGE ( 'NONE', *, *, #13196, .F. ) ;
#29541=CIRCLE ( 'NONE', #3704, 59.00000000000000711 ) ;
#29542=VERTEX_POINT ( 'NONE', #30613 ) ;
#29543=LINE ( 'NONE', #25657, #37570 ) ;
#29544=EDGE_LOOP ( 'NONE', ( #38384, #13286, #37419, #39617 ) ) ;
#29547=DIRECTION ( 'NONE',  ( -1.000000000000000000, -0.000000000000000000, 0.000000000000000000 ) ) ;
#29555=CARTESIAN_POINT ( 'NONE',  ( 17.99999999999999645, -109.4038418350907023, 50.51029986767514401 ) ) ;
#29559=AXIS2_PLACEMENT_3D ( 'NONE', #23339, #36601, #6723 ) ;
#29560=VERTEX_POINT ( 'NONE', #27335 ) ;
#29562=CARTESIAN_POINT ( 'NONE',  ( 0.000000000000000000, -101.1249659627859216, 48.60055280209385842 ) ) ;
#29564=CARTESIAN_POINT ( 'NONE',  ( 17.99999999999999645, 109.3506818544115617, -38.70953859160899668 ) ) ;
#29585=DIRECTION ( 'NONE',  ( -1.000000000000000000, -0.000000000000000000, -0.000000000000000000 ) ) ;
#29589=ORIENTED_EDGE ( 'NONE', *, *, #34123, .T. ) ;
#29592=LINE ( 'NONE', #29383, #4661 ) ;
#29594=CYLINDRICAL_SURFACE ( 'NONE', #41719, 59.00000000000000000 ) ;
#29595=LINE ( 'NONE', #9729, #15960 ) ;
#29596=ORIENTED_EDGE ( 'NONE', *, *, #2741, .T. ) ;
#29599=VECTOR ( 'NONE', #21181, 1000.000000000000000 ) ;
#29601=ORIENTED_EDGE ( 'NONE', *, *, #11472, .F. ) ;
#29603=CIRCLE ( 'NONE', #40717, 120.5010000000000190 ) ;
#29606=FACE_OUTER_BOUND ( 'NONE', #26059, .T. ) ;
#29608=FACE_OUTER_BOUND ( 'NONE', #4119, .T. ) ;
#29609=EDGE_CURVE ( 'NONE', #30056, #37428, #36045, .T. ) ;
#29610=DIRECTION ( 'NONE',  ( 0.000000000000000000, -0.9996456111234528485, 0.02662052143776447166 ) ) ;
#29613=VERTEX_POINT ( 'NONE', #805 ) ;
#29615=CIRCLE ( 'NONE', #28230, 116.0000000000000000 ) ;
#29617=CARTESIAN_POINT ( 'NONE',  ( 17.99999999999999645, 112.1702510623870381, -2.471285140322999840 ) ) ;
#29618=CARTESIAN_POINT ( 'NONE',  ( 17.99999999999999645, -84.62908780824814414, -85.78116633471378805 ) ) ;
#29620=DIRECTION ( 'NONE',  ( 0.000000000000000000, -0.9407002666710297945, -0.3392388661180402165 ) ) ;
#29621=VERTEX_POINT ( 'NONE', #13832 ) ;
#29624=AXIS2_PLACEMENT_3D ( 'NONE', #23992, #40731, #30303 ) ;
#29625=CARTESIAN_POINT ( 'NONE',  ( 17.99999999999999645, 88.56657216608705596, -68.87840567545838155 ) ) ;
#29629=ORIENTED_EDGE ( 'NONE', *, *, #8110, .F. ) ;
#29632=VECTOR ( 'NONE', #21576, 1000.000000000000000 ) ;
#29634=VECTOR ( 'NONE', #30027, 1000.000000000000000 ) ;
#29636=DIRECTION ( 'NONE',  ( 0.000000000000000000, -0.9911528310040056411, -0.1327255272837324085 ) ) ;
#29637=CARTESIAN_POINT ( 'NONE',  ( 17.99999999999999645, -34.74871106919691499, 106.6808302961370600 ) ) ;
#29638=CARTESIAN_POINT ( 'NONE',  ( 17.99999999999999645, 58.30069736313799211, -100.2847380560561419 ) ) ;
#29639=LINE ( 'NONE', #9770, #1817 ) ;
#29642=DIRECTION ( 'NONE',  ( -1.000000000000000000, -0.000000000000000000, -0.000000000000000000 ) ) ;
#29647=VECTOR ( 'NONE', #22352, 1000.000000000000000 ) ;
#29649=CARTESIAN_POINT ( 'NONE',  ( 17.99999999999999645, -117.9424311864590891, 24.69967462998996766 ) ) ;
#29650=CARTESIAN_POINT ( 'NONE',  ( 17.99999999999999645, -117.6086855750632765, -26.24286718912224003 ) ) ;
#29654=CIRCLE ( 'NONE', #331, 120.5010000000000048 ) ;
#29656=EDGE_CURVE ( 'NONE', #36478, #6009, #27552, .T. ) ;
#29665=AXIS2_PLACEMENT_3D ( 'NONE', #34337, #14520, #11887 ) ;
#29671=VERTEX_POINT ( 'NONE', #19952 ) ;
#29674=CARTESIAN_POINT ( 'NONE',  ( 17.99999999999999645, 109.4038418350910433, -50.51029986767441926 ) ) ;
#29677=CARTESIAN_POINT ( 'NONE',  ( 0.000000000000000000, 87.92975456462995965, -69.68953103478068556 ) ) ;
#29679=EDGE_CURVE ( 'NONE', #27833, #14651, #17338, .T. ) ;
#29686=VECTOR ( 'NONE', #31721, 1000.000000000000000 ) ;
#29688=CARTESIAN_POINT ( 'NONE',  ( 17.99999999999999645, 103.1672962317657323, -44.09967643725766351 ) ) ;
#29690=CYLINDRICAL_SURFACE ( 'NONE', #11425, 120.5010000000000190 ) ;
#29694=ORIENTED_EDGE ( 'NONE', *, *, #38804, .F. ) ;
#29696=DIRECTION ( 'NONE',  ( -1.000000000000000000, 0.000000000000000000, 0.000000000000000000 ) ) ;
#29697=DIRECTION ( 'NONE',  ( 1.000000000000000000, 0.000000000000000000, 0.000000000000000000 ) ) ;
#29703=ORIENTED_EDGE ( 'NONE', *, *, #27929, .F. ) ;
#29704=ADVANCED_FACE ( 'NONE', ( #7465 ), #24082, .F. ) ;
#29709=DIRECTION ( 'NONE',  ( -1.000000000000000000, -0.000000000000000000, 0.000000000000000000 ) ) ;
#29710=AXIS2_PLACEMENT_3D ( 'NONE', #5308, #14942, #15164 ) ;
#29712=VECTOR ( 'NONE', #21709, 1000.000000000000000 ) ;
#29715=ORIENTED_EDGE ( 'NONE', *, *, #16874, .F. ) ;
#29716=VECTOR ( 'NONE', #36959, 1000.000000000000000 ) ;
#29717=CARTESIAN_POINT ( 'NONE',  ( 17.99999999999999645, -2.418575551221673336, 120.4767259403368911 ) ) ;
#29719=FACE_OUTER_BOUND ( 'NONE', #9126, .T. ) ;
#29720=CIRCLE ( 'NONE', #1830, 116.0000000000000000 ) ;
#29721=CARTESIAN_POINT ( 'NONE',  ( 17.99999999999999645, 88.00363688980546328, 82.31555682352686176 ) ) ;
#29724=CARTESIAN_POINT ( 'NONE',  ( -10.00000000000000000, 0.000000000000000000, 0.000000000000000000 ) ) ;
#29725=ORIENTED_EDGE ( 'NONE', *, *, #12637, .T. ) ;
#29730=ORIENTED_EDGE ( 'NONE', *, *, #37959, .T. ) ;
#29731=CARTESIAN_POINT ( 'NONE',  ( 17.99999999999999645, 114.8812324315177023, -16.07179003769037351 ) ) ;
#29734=ORIENTED_EDGE ( 'NONE', *, *, #16759, .F. ) ;
#29735=AXIS2_PLACEMENT_3D ( 'NONE', #36951, #26718, #30006 ) ;
#29736=CARTESIAN_POINT ( 'NONE',  ( 17.99999999999999645, -113.8630351447207119, 22.16324045874372572 ) ) ;
#29739=ORIENTED_EDGE ( 'NONE', *, *, #17193, .F. ) ;
#29741=DIRECTION ( 'NONE',  ( 0.000000000000000000, -0.05322217484218559613, 0.9985826956767616114 ) ) ;
#29742=CYLINDRICAL_SURFACE ( 'NONE', #21475, 116.0000000000000000 ) ;
#29743=AXIS2_PLACEMENT_3D ( 'NONE', #37460, #3625, #30509 ) ;
#29746=DIRECTION ( 'NONE',  ( -1.000000000000000000, -0.000000000000000000, -0.000000000000000000 ) ) ;
#29747=VECTOR ( 'NONE', #39527, 1000.000000000000000 ) ;
#29748=DIRECTION ( 'NONE',  ( 0.000000000000000000, 0.8993121301712202476, -0.4373073204588531770 ) ) ;
#29749=VERTEX_POINT ( 'NONE', #17107 ) ;
#29753=CARTESIAN_POINT ( 'NONE',  ( 17.99999999999999645, -79.18387647320706435, -84.76976882518842160 ) ) ;
#29755=ORIENTED_EDGE ( 'NONE', *, *, #10282, .F. ) ;
#29757=DIRECTION ( 'NONE',  ( -1.000000000000000000, 0.000000000000000000, -0.000000000000000000 ) ) ;
#29758=CARTESIAN_POINT ( 'NONE',  ( 17.99999999999999645, 95.38615066514064722, -59.07414607872728141 ) ) ;
#29759=ORIENTED_EDGE ( 'NONE', *, *, #8968, .T. ) ;
#29761=ORIENTED_EDGE ( 'NONE', *, *, #34293, .T. ) ;
#29762=DIRECTION ( 'NONE',  ( -1.000000000000000000, 0.000000000000000000, -0.000000000000000000 ) ) ;
#29769=EDGE_CURVE ( 'NONE', #1690, #13634, #40937, .T. ) ;
#29770=ORIENTED_EDGE ( 'NONE', *, *, #1546, .F. ) ;
#29779=DIRECTION ( 'NONE',  ( -1.000000000000000000, -0.000000000000000000, -0.000000000000000000 ) ) ;
#29784=ORIENTED_EDGE ( 'NONE', *, *, #104, .T. ) ;
#29785=AXIS2_PLACEMENT_3D ( 'NONE', #10750, #30399, #1350 ) ;
#29787=CIRCLE ( 'NONE', #15215, 116.0000000000000000 ) ;
#29790=CIRCLE ( 'NONE', #25634, 58.99999999999999289 ) ;
#29795=DIRECTION ( 'NONE',  ( -1.000000000000000000, -0.000000000000000000, -0.000000000000000000 ) ) ;
#29796=AXIS2_PLACEMENT_3D ( 'NONE', #21535, #28491, #4441 ) ;
#29797=VERTEX_POINT ( 'NONE', #21255 ) ;
#29802=CIRCLE ( 'NONE', #42286, 59.00000000000000000 ) ;
#29807=DIRECTION ( 'NONE',  ( 1.000000000000000000, 0.000000000000000000, 0.000000000000000000 ) ) ;
#29811=ORIENTED_EDGE ( 'NONE', *, *, #24118, .T. ) ;
#29813=AXIS2_PLACEMENT_3D ( 'NONE', #33229, #29757, #472 ) ;
#29816=ORIENTED_EDGE ( 'NONE', *, *, #3282, .F. ) ;
#29819=CARTESIAN_POINT ( 'NONE',  ( 0.000000000000000000, 0.000000000000000000, 0.000000000000000000 ) ) ;
#29827=EDGE_CURVE ( 'NONE', #33572, #27194, #29140, .T. ) ;
#29828=DIRECTION ( 'NONE',  ( -1.000000000000000000, -0.000000000000000000, -0.000000000000000000 ) ) ;
#29829=CIRCLE ( 'NONE', #1236, 120.5010000000000474 ) ;
#29830=EDGE_CURVE ( 'NONE', #16376, #36189, #22908, .T. ) ;
#29831=DIRECTION ( 'NONE',  ( 1.000000000000000000, 0.000000000000000000, -0.000000000000000000 ) ) ;
#29833=ORIENTED_EDGE ( 'NONE', *, *, #9150, .T. ) ;
#29834=CARTESIAN_POINT ( 'NONE',  ( 17.99999999999999645, -114.1529630473452386, 38.59523323561398200 ) ) ;
#29840=DIRECTION ( 'NONE',  ( 0.000000000000000000, 1.599473849036242511E-14, -1.000000000000000000 ) ) ;
#29841=EDGE_LOOP ( 'NONE', ( #10508, #36235, #31526, #30383 ) ) ;
#29843=ORIENTED_EDGE ( 'NONE', *, *, #18626, .T. ) ;
#29844=DIRECTION ( 'NONE',  ( 0.000000000000000000, 0.8477344278896686847, 0.5304209081197462927 ) ) ;
#29847=AXIS2_PLACEMENT_3D ( 'NONE', #34944, #18205, #17996 ) ;
#29848=ADVANCED_FACE ( 'NONE', ( #24313 ), #1775, .F. ) ;
#29851=EDGE_CURVE ( 'NONE', #13195, #8854, #3335, .T. ) ;
#29857=ORIENTED_EDGE ( 'NONE', *, *, #27733, .F. ) ;
#29859=AXIS2_PLACEMENT_3D ( 'NONE', #23663, #42806, #3314 ) ;
#29862=VERTEX_POINT ( 'NONE', #19471 ) ;
#29863=AXIS2_PLACEMENT_3D ( 'NONE', #15128, #41704, #21897 ) ;
#29868=VERTEX_POINT ( 'NONE', #42743 ) ;
#29873=CYLINDRICAL_SURFACE ( 'NONE', #40137, 116.0000000000000000 ) ;
#29874=ORIENTED_EDGE ( 'NONE', *, *, #43160, .T. ) ;
#29880=EDGE_LOOP ( 'NONE', ( #18475, #11248, #13280, #26353, #38069, #30195, #12609, #34906, #8436, #33719, #34949, #122, #19781, #42149, #33106, #21910, #11094, #14063, #6779, #12844, #4460, #24397, #11021, #38923, #3626, #34820, #37533, #12818, #3036, #18045, #4439, #40236, #35699, #37410, #4516, #11443, #10379, #25698, #20908, #36489, #9706, #9992, #21693, #16791, #24885, #11540, #41710, #9451, #2366, #7539, #1726, #35228, #19322, #26906, #33501, #37731, #26475, #16070, #7468, #5085, #18925, #7915, #12872, #10265, #6337, #23891, #12595, #28031, #39481, #6215, #40874, #15508, #29511, #34320, #32898, #8336, #40211, #23066, #31684, #3079, #16881, #37386, #17044, #29390, #3975, #10660, #25465, #10650, #4398, #29998, #24314, #6400, #26902, #12302, #10042, #20202, #2659, #8357, #42124, #9493, #18834, #12754, #37563, #36875, #33645, #20326, #36675, #14722, #5663, #29929, #41228, #25957, #38722, #23709, #21533, #15767, #21993, #10815, #3392, #28558, #10206, #20503, #30980, #28158, #21685, #25620, #13733, #28911, #15584, #15491, #35301, #582, #18704, #17934, #24606, #38148, #11639, #15912, #35840, #37706, #20887, #34402, #37408, #25602, #12643, #15706, #31045, #30747, #16193, #37949, #39436, #5003, #13478, #15295, #19252, #15788, #36986, #33926, #20122, #4578, #36197, #16111, #12413, #19508, #39841, #36114, #7334, #7211, #32368, #5190, #41547, #29930, #12480, #13811, #12870, #32372, #35119, #16438, #12596, #12245, #34677, #23238, #15697, #34709, #16980, #16885, #25116, #28538, #6171, #26128, #29310, #2789, #4479, #9678, #36325, #6825, #25445, #20134, #6591, #19422, #17648, #40472, #30732, #11255, #34333, #40260, #30510, #2281, #37178, #11440, #10633, #30687, #11363, #30899, #13890, #3134, #32399, #8797, #29279, #13397, #37398, #34156, #5155, #37662, #23257, #40452, #31795, #20195, #14484, #5354, #39308, #19597, #3086, #25097, #21946, #30254, #18222, #18118, #177, #12863, #16783, #28504, #33743, #13355, #20614, #15763, #1841, #12520, #29154, #19983, #32425, #27881, #8018, #19338, #14122, #10830, #41779, #24787, #19809, #30121, #1232, #21214, #16689, #78, #39794, #24086, #29989, #27689, #13736, #26688, #20488, #39028, #20533, #4193, #23965, #748, #34544, #13655, #2674, #37238, #13626, #35967, #23615, #41059, #24525, #13240, #8369, #31952, #20706, #32113, #3315, #15598, #2017, #11239, #39145, #36136, #678, #30710, #40173, #23034, #6162, #24975, #21540, #27203, #18306, #30430, #23520, #7757, #22219, #20358, #5052, #7721, #30646, #36659, #41363, #6827, #18161, #8978, #21512, #29734, #38221, #25390, #34838, #16864, #32696, #21646, #6857, #6099, #34214, #10435, #29367, #39568, #17136, #40022, #12860, #22556, #3640, #18372, #20290, #29113, #29301, #21517, #3252, #21492, #2152, #14738, #20381, #22061, #14420, #27355, #20809, #23329, #19239, #24110, #30134, #18445, #3903, #9069, #15308, #38824, #20519, #5475, #17103, #30541, #14901, #35674, #23670, #3442, #37990, #39385, #5314, #25864, #2802, #28746, #26567, #864, #11802, #14665, #24889, #39251, #29280, #21602, #24584, #11191, #18014, #36265, #38249, #4500, #10091, #38466, #25413, #11946, #39565, #12351, #32153, #10749, #41319, #40568, #36341, #26171, #1002, #34303, #37850, #42838, #13959, #12141, #4751, #26839, #30075, #26491, #40392, #5325, #14532, #14585, #38264, #20293, #26762, #20483, #32382, #37602, #11485, #32618, #30664, #7545, #5614, #3063, #1420, #8598, #39169, #36364, #18923, #13949, #17766, #37872, #33497, #22331, #35672, #13101, #39698, #23822, #16700, #25704, #13440, #4174, #35409, #30143, #22972, #37821, #15562, #26108, #26165, #24478, #37522, #14071, #28253, #7815, #38727, #210, #19915, #21898, #36840, #43040, #4355, #34236, #19881, #39093, #42156, #20505, #31672, #6225, #23695, #40159, #39233, #15159, #1884, #20841, #37785 ) ) ;
#29881=FACE_OUTER_BOUND ( 'NONE', #27924, .T. ) ;
#29882=CIRCLE ( 'NONE', #11066, 120.5010000000000190 ) ;
#29890=CARTESIAN_POINT ( 'NONE',  ( 0.000000000000000000, -15.21076497709635156, -119.5371223922156503 ) ) ;
#29892=CARTESIAN_POINT ( 'NONE',  ( 0.000000000000000000, 72.00556975657703163, 86.04342158279412445 ) ) ;
#29895=ORIENTED_EDGE ( 'NONE', *, *, #14790, .T. ) ;
#29897=EDGE_LOOP ( 'NONE', ( #2183, #27942, #18790, #29770 ) ) ;
#29900=DIRECTION ( 'NONE',  ( 0.000000000000000000, -0.1590634960190788760, 0.9872683547213435551 ) ) ;
#29902=CARTESIAN_POINT ( 'NONE',  ( 9.000000000000001776, -109.3506818544107659, -38.70953859161123489 ) ) ;
#29906=CARTESIAN_POINT ( 'NONE',  ( 17.99999999999999645, 52.19040376560566585, -99.31985817764127944 ) ) ;
#29915=EDGE_CURVE ( 'NONE', #25913, #28841, #32945, .T. ) ;
#29918=DIRECTION ( 'NONE',  ( 1.000000000000000000, 0.000000000000000000, 0.000000000000000000 ) ) ;
#29920=ORIENTED_EDGE ( 'NONE', *, *, #743, .T. ) ;
#29922=CARTESIAN_POINT ( 'NONE',  ( 17.99999999999999645, 114.6488492393079781, 37.09625815500054102 ) ) ;
#29924=ORIENTED_EDGE ( 'NONE', *, *, #13645, .T. ) ;
#29929=ORIENTED_EDGE ( 'NONE', *, *, #36981, .T. ) ;
#29930=ORIENTED_EDGE ( 'NONE', *, *, #25691, .T. ) ;
#29933=ORIENTED_EDGE ( 'NONE', *, *, #19657, .T. ) ;
#29934=CARTESIAN_POINT ( 'NONE',  ( 9.000000000000001776, 11.65176648921033298, 115.4133282497342918 ) ) ;
#29935=AXIS2_PLACEMENT_3D ( 'NONE', #39754, #40405, #23445 ) ;
#29940=DIRECTION ( 'NONE',  ( 1.000000000000000000, 0.000000000000000000, 0.000000000000000000 ) ) ;
#29943=LINE ( 'NONE', #36441, #20586 ) ;
#29946=EDGE_CURVE ( 'NONE', #4177, #39762, #37496, .T. ) ;
#29949=ORIENTED_EDGE ( 'NONE', *, *, #26579, .T. ) ;
#29956=EDGE_CURVE ( 'NONE', #37810, #2041, #12452, .T. ) ;
#29957=CIRCLE ( 'NONE', #25110, 59.00000000000000711 ) ;
#29959=AXIS2_PLACEMENT_3D ( 'NONE', #35250, #28534, #7780 ) ;
#29961=CARTESIAN_POINT ( 'NONE',  ( 17.99999999999999645, 0.000000000000000000, 0.000000000000000000 ) ) ;
#29963=CARTESIAN_POINT ( 'NONE',  ( -10.00000000000000000, 0.000000000000000000, 0.000000000000000000 ) ) ;
#29966=CARTESIAN_POINT ( 'NONE',  ( 17.99999999999999645, 91.51415974874592507, 64.91094698989330425 ) ) ;
#29972=ORIENTED_EDGE ( 'NONE', *, *, #38768, .T. ) ;
#29975=ORIENTED_EDGE ( 'NONE', *, *, #16824, .F. ) ;
#29976=CARTESIAN_POINT ( 'NONE',  ( 17.99999999999999645, -98.69720329640912837, -60.94966826380012037 ) ) ;
#29981=DIRECTION ( 'NONE',  ( 0.000000000000000000, 0.000000000000000000, 1.000000000000000000 ) ) ;
#29987=ORIENTED_EDGE ( 'NONE', *, *, #39892, .F. ) ;
#29988=CYLINDRICAL_SURFACE ( 'NONE', #32859, 59.00000000000000000 ) ;
#29989=ORIENTED_EDGE ( 'NONE', *, *, #6924, .F. ) ;
#29991=AXIS2_PLACEMENT_3D ( 'NONE', #16678, #43022, #14191 ) ;
#29992=CIRCLE ( 'NONE', #13270, 116.0000000000000000 ) ;
#29993=CIRCLE ( 'NONE', #17495, 120.5010000000000332 ) ;
#29994=DIRECTION ( 'NONE',  ( -1.000000000000000000, -0.000000000000000000, -0.000000000000000000 ) ) ;
#29995=CARTESIAN_POINT ( 'NONE',  ( 17.99999999999999645, -54.09091620264790379, 102.6166301549515936 ) ) ;
#29996=AXIS2_PLACEMENT_3D ( 'NONE', #6328, #39683, #19673 ) ;
#29997=DIRECTION ( 'NONE',  ( 0.000000000000000000, 0.000000000000000000, 1.000000000000000000 ) ) ;
#29998=ORIENTED_EDGE ( 'NONE', *, *, #35311, .T. ) ;
#30000=EDGE_CURVE ( 'NONE', #17019, #10305, #12421, .T. ) ;
#30003=DIRECTION ( 'NONE',  ( 0.000000000000000000, -0.05322217484216511946, -0.9985826956767627216 ) ) ;
#30005=FACE_OUTER_BOUND ( 'NONE', #42910, .T. ) ;
#30006=DIRECTION ( 'NONE',  ( 0.000000000000000000, 0.000000000000000000, 1.000000000000000000 ) ) ;
#30007=ORIENTED_EDGE ( 'NONE', *, *, #42325, .F. ) ;
#30008=CARTESIAN_POINT ( 'NONE',  ( 17.99999999999999645, 111.1352304691227744, 15.40237066878635730 ) ) ;
#30009=EDGE_CURVE ( 'NONE', #28297, #23529, #34695, .T. ) ;
#30010=CIRCLE ( 'NONE', #23054, 59.00000000000000000 ) ;
#30013=EDGE_CURVE ( 'NONE', #15607, #22119, #36767, .T. ) ;
#30014=CARTESIAN_POINT ( 'NONE',  ( 17.99999999999999645, 0.000000000000000000, 0.000000000000000000 ) ) ;
#30018=AXIS2_PLACEMENT_3D ( 'NONE', #9949, #40033, #23299 ) ;
#30019=ORIENTED_EDGE ( 'NONE', *, *, #3598, .T. ) ;
#30021=EDGE_LOOP ( 'NONE', ( #30841, #26705, #20850, #19950 ) ) ;
#30022=VECTOR ( 'NONE', #34632, 1000.000000000000000 ) ;
#30023=DIRECTION ( 'NONE',  ( -1.000000000000000000, -0.000000000000000000, -0.000000000000000000 ) ) ;
#30024=CIRCLE ( 'NONE', #7733, 120.5010000000000474 ) ;
#30025=AXIS2_PLACEMENT_3D ( 'NONE', #37900, #21607, #21390 ) ;
#30027=DIRECTION ( 'NONE',  ( 1.000000000000000000, -0.000000000000000000, -0.000000000000000000 ) ) ;
#30030=DIRECTION ( 'NONE',  ( 0.000000000000000000, 0.000000000000000000, 1.000000000000000000 ) ) ;
#30034=VERTEX_POINT ( 'NONE', #629 ) ;
#30036=EDGE_CURVE ( 'NONE', #33918, #35878, #34035, .T. ) ;
#30038=EDGE_CURVE ( 'NONE', #15861, #18124, #20332, .T. ) ;
#30042=LINE ( 'NONE', #32435, #19864 ) ;
#30050=VERTEX_POINT ( 'NONE', #24029 ) ;
#30053=AXIS2_PLACEMENT_3D ( 'NONE', #24753, #14705, #24983 ) ;
#30056=VERTEX_POINT ( 'NONE', #16633 ) ;
#30058=CARTESIAN_POINT ( 'NONE',  ( 17.99999999999999645, 0.000000000000000000, 0.000000000000000000 ) ) ;
#30060=EDGE_CURVE ( 'NONE', #3503, #13758, #2618, .T. ) ;
#30065=CARTESIAN_POINT ( 'NONE',  ( 17.99999999999999645, -75.03166794516862126, 94.29071961951481740 ) ) ;
#30068=CYLINDRICAL_SURFACE ( 'NONE', #34144, 59.00000000000000000 ) ;
#30069=ORIENTED_EDGE ( 'NONE', *, *, #26066, .T. ) ;
#30071=CARTESIAN_POINT ( 'NONE',  ( 17.99999999999999645, 0.000000000000000000, 0.000000000000000000 ) ) ;
#30075=ORIENTED_EDGE ( 'NONE', *, *, #17174, .T. ) ;
#30076=LINE ( 'NONE', #10196, #39993 ) ;
#30078=DIRECTION ( 'NONE',  ( 0.000000000000000000, 0.000000000000000000, 1.000000000000000000 ) ) ;
#30084=DIRECTION ( 'NONE',  ( 1.000000000000000000, 0.000000000000000000, 0.000000000000000000 ) ) ;
#30087=EDGE_CURVE ( 'NONE', #42455, #42118, #41669, .T. ) ;
#30089=AXIS2_PLACEMENT_3D ( 'NONE', #32527, #6535, #23379 ) ;
#30091=EDGE_LOOP ( 'NONE', ( #27518, #3499, #10995, #18470 ) ) ;
#30093=EDGE_LOOP ( 'NONE', ( #198, #1022, #11692, #25489 ) ) ;
#30094=AXIS2_PLACEMENT_3D ( 'NONE', #39133, #22826, #40850 ) ;
#30097=CARTESIAN_POINT ( 'NONE',  ( 0.000000000000000000, -112.5220807139882311, -28.19186676675956704 ) ) ;
#30102=CARTESIAN_POINT ( 'NONE',  ( 0.000000000000000000, -92.25992191227339845, -77.51514567967485902 ) ) ;
#30104=FACE_OUTER_BOUND ( 'NONE', #16702, .T. ) ;
#30105=CARTESIAN_POINT ( 'NONE',  ( 0.000000000000000000, 0.000000000000000000, 0.000000000000000000 ) ) ;
#30106=ORIENTED_EDGE ( 'NONE', *, *, #14735, .F. ) ;
#30112=CIRCLE ( 'NONE', #28008, 130.0000000000000000 ) ;
#30114=ORIENTED_EDGE ( 'NONE', *, *, #26875, .T. ) ;
#30119=CARTESIAN_POINT ( 'NONE',  ( 17.99999999999999645, -64.58410930313458209, -101.7319213743688664 ) ) ;
#30120=CARTESIAN_POINT ( 'NONE',  ( 17.99999999999999645, 72.00556975657821113, -86.04342158279314390 ) ) ;
#30121=ORIENTED_EDGE ( 'NONE', *, *, #5831, .F. ) ;
#30123=DIRECTION ( 'NONE',  ( 0.000000000000000000, 0.000000000000000000, 1.000000000000000000 ) ) ;
#30125=ORIENTED_EDGE ( 'NONE', *, *, #10792, .F. ) ;
#30129=VERTEX_POINT ( 'NONE', #20774 ) ;
#30133=EDGE_CURVE ( 'NONE', #25132, #5730, #38180, .T. ) ;
#30134=ORIENTED_EDGE ( 'NONE', *, *, #2354, .F. ) ;
#30138=AXIS2_PLACEMENT_3D ( 'NONE', #10895, #23577, #24226 ) ;
#30143=ORIENTED_EDGE ( 'NONE', *, *, #6317, .T. ) ;
#30144=DIRECTION ( 'NONE',  ( -1.000000000000000000, 0.000000000000000000, -0.000000000000000000 ) ) ;
#30146=CARTESIAN_POINT ( 'NONE',  ( 17.99999999999999645, 0.000000000000000000, 0.000000000000000000 ) ) ;
#30148=CARTESIAN_POINT ( 'NONE',  ( 9.000000000000001776, 31.17727234463848163, -111.7317219465816862 ) ) ;
#30151=LINE ( 'NONE', #29717, #14804 ) ;
#30153=ADVANCED_FACE ( 'NONE', ( #33811 ), #26847, .F. ) ;
#30154=CARTESIAN_POINT ( 'NONE',  ( 17.99999999999999645, -117.9424311864590891, 24.69967462998996766 ) ) ;
#30156=FACE_OUTER_BOUND ( 'NONE', #19153, .T. ) ;
#30159=ORIENTED_EDGE ( 'NONE', *, *, #43094, .F. ) ;
#30168=CARTESIAN_POINT ( 'NONE',  ( 17.99999999999999645, -48.55277268144396174, 105.3500273609078306 ) ) ;
#30169=DIRECTION ( 'NONE',  ( 0.000000000000000000, -0.1590634960190595026, -0.9872683547213466637 ) ) ;
#30170=DIRECTION ( 'NONE',  ( 0.000000000000000000, 0.000000000000000000, 1.000000000000000000 ) ) ;
#30173=VERTEX_POINT ( 'NONE', #14642 ) ;
#30174=LINE ( 'NONE', #13831, #32017 ) ;
#30175=VECTOR ( 'NONE', #39881, 1000.000000000000000 ) ;
#30179=EDGE_CURVE ( 'NONE', #69, #2881, #34625, .T. ) ;
#30181=ORIENTED_EDGE ( 'NONE', *, *, #18112, .T. ) ;
#30184=DIRECTION ( 'NONE',  ( 0.000000000000000000, 0.9911528310040067513, 0.1327255272837256084 ) ) ;
#30186=DIRECTION ( 'NONE',  ( 0.000000000000000000, 0.000000000000000000, 1.000000000000000000 ) ) ;
#30192=EDGE_LOOP ( 'NONE', ( #21267, #8931, #42706, #18187 ) ) ;
#30195=ORIENTED_EDGE ( 'NONE', *, *, #22304, .F. ) ;
#30201=DIRECTION ( 'NONE',  ( -1.000000000000000000, -0.000000000000000000, -0.000000000000000000 ) ) ;
#30202=ORIENTED_EDGE ( 'NONE', *, *, #33507, .T. ) ;
#30203=CARTESIAN_POINT ( 'NONE',  ( 0.000000000000000000, -101.8011932243944386, -55.61040422519432980 ) ) ;
#30207=ORIENTED_EDGE ( 'NONE', *, *, #41973, .F. ) ;
#30208=CYLINDRICAL_SURFACE ( 'NONE', #284, 59.00000000000000000 ) ;
#30210=DIRECTION ( 'NONE',  ( -1.000000000000000000, -0.000000000000000000, -0.000000000000000000 ) ) ;
#30214=ORIENTED_EDGE ( 'NONE', *, *, #18854, .T. ) ;
#30219=DIRECTION ( 'NONE',  ( 0.000000000000000000, 0.9407002666710320149, 0.3392388661180340548 ) ) ;
#30221=LINE ( 'NONE', #13439, #30959 ) ;
#30222=ORIENTED_EDGE ( 'NONE', *, *, #39441, .F. ) ;
#30225=CARTESIAN_POINT ( 'NONE',  ( 9.000000000000001776, 101.8011932243955613, -55.61040422519224791 ) ) ;
#30228=ORIENTED_EDGE ( 'NONE', *, *, #28898, .F. ) ;
#30229=EDGE_LOOP ( 'NONE', ( #22753, #21308, #19096, #24251 ) ) ;
#30230=LINE ( 'NONE', #20018, #7735 ) ;
#30232=FACE_OUTER_BOUND ( 'NONE', #37586, .T. ) ;
#30233=CARTESIAN_POINT ( 'NONE',  ( 17.99999999999999645, -110.3490479609630910, 38.71798610214488434 ) ) ;
#30234=CIRCLE ( 'NONE', #38589, 59.00000000000000000 ) ;
#30236=VERTEX_POINT ( 'NONE', #28546 ) ;
#30238=CARTESIAN_POINT ( 'NONE',  ( 17.99999999999999645, 57.40245293794667703, 96.40140491896650587 ) ) ;
#30239=VECTOR ( 'NONE', #36706, 1000.000000000000000 ) ;
#30241=CARTESIAN_POINT ( 'NONE',  ( 0.000000000000000000, 114.1529630473454944, -38.59523323561318620 ) ) ;
#30242=VERTEX_POINT ( 'NONE', #28958 ) ;
#30244=DIRECTION ( 'NONE',  ( 0.000000000000000000, -0.7865515558026354714, -0.6175246149462008116 ) ) ;
#30245=DIRECTION ( 'NONE',  ( 0.000000000000000000, 1.411300455031978640E-14, -1.000000000000000000 ) ) ;
#30252=ORIENTED_EDGE ( 'NONE', *, *, #4189, .F. ) ;
#30254=ORIENTED_EDGE ( 'NONE', *, *, #28816, .F. ) ;
#30255=AXIS2_PLACEMENT_3D ( 'NONE', #2337, #32472, #35940 ) ;
#30263=CARTESIAN_POINT ( 'NONE',  ( 17.99999999999999645, -46.12538073176274622, -111.3235835452215952 ) ) ;
#30264=VERTEX_POINT ( 'NONE', #12383 ) ;
#30266=ADVANCED_FACE ( 'NONE', ( #32211 ), #21201, .F. ) ;
#30275=ORIENTED_EDGE ( 'NONE', *, *, #5423, .F. ) ;
#30276=ORIENTED_EDGE ( 'NONE', *, *, #14908, .T. ) ;
#30278=CIRCLE ( 'NONE', #19835, 116.0000000000000000 ) ;
#30279=DIRECTION ( 'NONE',  ( 1.000000000000000000, 0.000000000000000000, 0.000000000000000000 ) ) ;
#30280=AXIS2_PLACEMENT_3D ( 'NONE', #38356, #11781, #1276 ) ;
#30281=DIRECTION ( 'NONE',  ( 0.000000000000000000, 0.000000000000000000, 1.000000000000000000 ) ) ;
#30282=ORIENTED_EDGE ( 'NONE', *, *, #19414, .T. ) ;
#30283=DIRECTION ( 'NONE',  ( -1.000000000000000000, 0.000000000000000000, 0.000000000000000000 ) ) ;
#30285=DIRECTION ( 'NONE',  ( -1.000000000000000000, -0.000000000000000000, -0.000000000000000000 ) ) ;
#30287=CIRCLE ( 'NONE', #1707, 120.5010000000000332 ) ;
#30289=FACE_OUTER_BOUND ( 'NONE', #3099, .T. ) ;
#30291=FACE_OUTER_BOUND ( 'NONE', #20007, .T. ) ;
#30292=DIRECTION ( 'NONE',  ( -1.000000000000000000, 0.000000000000000000, 0.000000000000000000 ) ) ;
#30295=ADVANCED_FACE ( 'NONE', ( #35475 ), #15651, .F. ) ;
#30297=DIRECTION ( 'NONE',  ( 0.000000000000000000, 0.000000000000000000, 1.000000000000000000 ) ) ;
#30303=DIRECTION ( 'NONE',  ( 0.000000000000000000, 0.6382441836448211614, -0.7698339834299053885 ) ) ;
#30305=VECTOR ( 'NONE', #37681, 1000.000000000000000 ) ;
#30307=CARTESIAN_POINT ( 'NONE',  ( 0.000000000000000000, 13.00789606333472470, 115.2683592318615382 ) ) ;
#30311=VECTOR ( 'NONE', #42794, 1000.000000000000000 ) ;
#30312=DIRECTION ( 'NONE',  ( -1.000000000000000000, 0.000000000000000000, 0.000000000000000000 ) ) ;
#30313=DIRECTION ( 'NONE',  ( 0.000000000000000000, -0.9911528310040085277, 0.1327255272837126188 ) ) ;
#30314=VERTEX_POINT ( 'NONE', #3370 ) ;
#30315=FACE_OUTER_BOUND ( 'NONE', #26649, .T. ) ;
#30318=FACE_OUTER_BOUND ( 'NONE', #13947, .T. ) ;
#30322=ADVANCED_FACE ( 'NONE', ( #6439 ), #9727, .F. ) ;
#30323=ORIENTED_EDGE ( 'NONE', *, *, #26088, .T. ) ;
#30326=EDGE_CURVE ( 'NONE', #5730, #34051, #29592, .T. ) ;
#30329=CARTESIAN_POINT ( 'NONE',  ( 17.99999999999999645, 73.51007459736430860, 89.73443560133387109 ) ) ;
#30331=CIRCLE ( 'NONE', #37287, 59.00000000000000711 ) ;
#30335=ORIENTED_EDGE ( 'NONE', *, *, #41954, .F. ) ;
#30342=FACE_OUTER_BOUND ( 'NONE', #38392, .T. ) ;
#30344=VERTEX_POINT ( 'NONE', #12589 ) ;
#30345=CARTESIAN_POINT ( 'NONE',  ( 17.99999999999999645, 30.01658535635262481, 108.1077105353199102 ) ) ;
#30347=ADVANCED_FACE ( 'NONE', ( #9513 ), #32422, .F. ) ;
#30351=ORIENTED_EDGE ( 'NONE', *, *, #24768, .T. ) ;
#30357=CARTESIAN_POINT ( 'NONE',  ( 17.99999999999999645, -68.61497464550663494, 99.05794392877579924 ) ) ;
#30359=AXIS2_PLACEMENT_3D ( 'NONE', #34318, #24338, #3545 ) ;
#30360=LINE ( 'NONE', #30154, #14096 ) ;
#30363=CYLINDRICAL_SURFACE ( 'NONE', #30502, 116.0000000000000000 ) ;
#30364=CIRCLE ( 'NONE', #1061, 120.5010000000000190 ) ;
#30365=VERTEX_POINT ( 'NONE', #19371 ) ;
#30366=AXIS2_PLACEMENT_3D ( 'NONE', #37334, #7448, #14233 ) ;
#30369=ORIENTED_EDGE ( 'NONE', *, *, #30060, .T. ) ;
#30371=CIRCLE ( 'NONE', #40082, 120.5010000000000474 ) ;
#30376=EDGE_CURVE ( 'NONE', #1326, #9666, #3144, .T. ) ;
#30381=EDGE_CURVE ( 'NONE', #4296, #36528, #38114, .T. ) ;
#30382=AXIS2_PLACEMENT_3D ( 'NONE', #2981, #39438, #23131 ) ;
#30383=ORIENTED_EDGE ( 'NONE', *, *, #32193, .T. ) ;
#30385=LINE ( 'NONE', #23855, #29747 ) ;
#30387=FACE_OUTER_BOUND ( 'NONE', #28468, .T. ) ;
#30388=EDGE_LOOP ( 'NONE', ( #13885, #31584, #12299, #16178 ) ) ;
#30395=CIRCLE ( 'NONE', #2513, 59.00000000000000000 ) ;
#30396=FACE_OUTER_BOUND ( 'NONE', #7089, .T. ) ;
#30397=CARTESIAN_POINT ( 'NONE',  ( 0.000000000000000000, 5.456439917444967591, 112.0647122740742105 ) ) ;
#30398=VERTEX_POINT ( 'NONE', #9928 ) ;
#30399=DIRECTION ( 'NONE',  ( 1.000000000000000000, 0.000000000000000000, 0.000000000000000000 ) ) ;
#30407=CARTESIAN_POINT ( 'NONE',  ( 17.99999999999999645, 95.38615066513983720, 59.07414607872858170 ) ) ;
#30411=CARTESIAN_POINT ( 'NONE',  ( 17.99999999999999645, 76.48293397876373945, -82.08917884620232996 ) ) ;
#30413=CIRCLE ( 'NONE', #25548, 120.5010000000000190 ) ;
#30416=VECTOR ( 'NONE', #142, 1000.000000000000000 ) ;
#30423=CARTESIAN_POINT ( 'NONE',  ( 17.99999999999999645, 80.74349901498510462, -77.90224541347200216 ) ) ;
#30424=EDGE_LOOP ( 'NONE', ( #34389, #19111, #5948, #12748 ) ) ;
#30425=DIRECTION ( 'NONE',  ( 1.000000000000000000, 0.000000000000000000, 0.000000000000000000 ) ) ;
#30430=ORIENTED_EDGE ( 'NONE', *, *, #29827, .T. ) ;
#30433=CIRCLE ( 'NONE', #6029, 59.00000000000000711 ) ;
#30437=CYLINDRICAL_SURFACE ( 'NONE', #9458, 59.00000000000000000 ) ;
#30441=DIRECTION ( 'NONE',  ( 0.000000000000000000, -0.8183027759081742403, 0.5747874102143992747 ) ) ;
#30442=ADVANCED_FACE ( 'NONE', ( #32849 ), #19155, .F. ) ;
#30447=CIRCLE ( 'NONE', #22916, 59.00000000000000711 ) ;
#30449=DIRECTION ( 'NONE',  ( 0.000000000000000000, 0.000000000000000000, 1.000000000000000000 ) ) ;
#30451=CARTESIAN_POINT ( 'NONE',  ( 17.99999999999999645, 10.40101730206529140, -120.0512800434970018 ) ) ;
#30454=CARTESIAN_POINT ( 'NONE',  ( 0.000000000000000000, 105.7179949885863266, 37.57629584241859533 ) ) ;
#30464=DIRECTION ( 'NONE',  ( 0.000000000000000000, 0.1590634960190723812, -0.9872683547213445543 ) ) ;
#30469=CARTESIAN_POINT ( 'NONE',  ( 17.99999999999999645, 0.000000000000000000, 0.000000000000000000 ) ) ;
#30474=LINE ( 'NONE', #13680, #36777 ) ;
#30476=VERTEX_POINT ( 'NONE', #23920 ) ;
#30477=DIRECTION ( 'NONE',  ( -1.000000000000000000, -0.000000000000000000, 0.000000000000000000 ) ) ;
#30479=ORIENTED_EDGE ( 'NONE', *, *, #9814, .T. ) ;
#30480=DIRECTION ( 'NONE',  ( 0.000000000000000000, 0.000000000000000000, -1.000000000000000000 ) ) ;
#30484=ORIENTED_EDGE ( 'NONE', *, *, #17115, .F. ) ;
#30485=ADVANCED_FACE ( 'NONE', ( #14307 ), #21101, .F. ) ;
#30491=DIRECTION ( 'NONE',  ( 0.000000000000000000, 0.000000000000000000, 1.000000000000000000 ) ) ;
#30497=AXIS2_PLACEMENT_3D ( 'NONE', #19510, #16887, #30169 ) ;
#30500=VERTEX_POINT ( 'NONE', #14103 ) ;
#30502=AXIS2_PLACEMENT_3D ( 'NONE', #23197, #3701, #26661 ) ;
#30507=CARTESIAN_POINT ( 'NONE',  ( 8.999999999999998224, 91.65951123222582453, -71.09524597797991419 ) ) ;
#30509=DIRECTION ( 'NONE',  ( 0.000000000000000000, -0.9826841245925190815, -0.1852887240871243235 ) ) ;
#30510=ORIENTED_EDGE ( 'NONE', *, *, #13536, .T. ) ;
#30513=CARTESIAN_POINT ( 'NONE',  ( 0.000000000000000000, 114.1529630473449686, 38.59523323561477781 ) ) ;
#30516=AXIS2_PLACEMENT_3D ( 'NONE', #28348, #6671, #19390 ) ;
#30519=DIRECTION ( 'NONE',  ( 1.000000000000000000, 0.000000000000000000, 0.000000000000000000 ) ) ;
#30520=ORIENTED_EDGE ( 'NONE', *, *, #12503, .T. ) ;
#30521=VERTEX_POINT ( 'NONE', #40660 ) ;
#30527=DIRECTION ( 'NONE',  ( -1.000000000000000000, 0.000000000000000000, 0.000000000000000000 ) ) ;
#30529=VECTOR ( 'NONE', #17109, 1000.000000000000000 ) ;
#30531=CARTESIAN_POINT ( 'NONE',  ( 17.99999999999999645, 0.000000000000000000, 0.000000000000000000 ) ) ;
#30533=CIRCLE ( 'NONE', #3290, 116.0000000000000000 ) ;
#30538=VECTOR ( 'NONE', #2709, 1000.000000000000000 ) ;
#30541=ORIENTED_EDGE ( 'NONE', *, *, #19036, .F. ) ;
#30542=FACE_OUTER_BOUND ( 'NONE', #40463, .T. ) ;
#30548=CIRCLE ( 'NONE', #6047, 116.0000000000000000 ) ;
#30553=CARTESIAN_POINT ( 'NONE',  ( 17.99999999999999645, -120.3696465864705800, -5.624871700597302571 ) ) ;
#30556=AXIS2_PLACEMENT_3D ( 'NONE', #11406, #4175, #37572 ) ;
#30558=ORIENTED_EDGE ( 'NONE', *, *, #42508, .T. ) ;
#30561=FACE_OUTER_BOUND ( 'NONE', #4883, .T. ) ;
#30563=EDGE_LOOP ( 'NONE', ( #37650, #31553, #40608, #42121 ) ) ;
#30565=CARTESIAN_POINT ( 'NONE',  ( 0.000000000000000000, 0.000000000000000000, 0.000000000000000000 ) ) ;
#30568=ORIENTED_EDGE ( 'NONE', *, *, #39324, .T. ) ;
#30570=DIRECTION ( 'NONE',  ( -1.000000000000000000, -0.000000000000000000, -0.000000000000000000 ) ) ;
#30572=DIRECTION ( 'NONE',  ( 0.000000000000000000, 0.000000000000000000, 1.000000000000000000 ) ) ;
#30573=ORIENTED_EDGE ( 'NONE', *, *, #39319, .F. ) ;
#30577=EDGE_CURVE ( 'NONE', #2440, #21485, #12388, .T. ) ;
#30581=EDGE_CURVE ( 'NONE', #8080, #21257, #3991, .T. ) ;
#30582=EDGE_CURVE ( 'NONE', #16031, #24063, #30667, .T. ) ;
#30583=CARTESIAN_POINT ( 'NONE',  ( 0.000000000000000000, 0.000000000000000000, 0.000000000000000000 ) ) ;
#30584=DIRECTION ( 'NONE',  ( 1.000000000000000000, 0.000000000000000000, 0.000000000000000000 ) ) ;
#30586=DIRECTION ( 'NONE',  ( -1.000000000000000000, -0.000000000000000000, -0.000000000000000000 ) ) ;
#30589=DIRECTION ( 'NONE',  ( -1.000000000000000000, 0.000000000000000000, -0.000000000000000000 ) ) ;
#30590=LINE ( 'NONE', #21226, #28431 ) ;
#30592=ORIENTED_EDGE ( 'NONE', *, *, #37248, .T. ) ;
#30594=CARTESIAN_POINT ( 'NONE',  ( 9.000000000000001776, -25.18647942089817349, 113.2326863338526977 ) ) ;
#30598=CYLINDRICAL_SURFACE ( 'NONE', #4055, 59.00000000000000000 ) ;
#30604=VERTEX_POINT ( 'NONE', #295 ) ;
#30606=CARTESIAN_POINT ( 'NONE',  ( 17.99999999999999645, 0.000000000000000000, 0.000000000000000000 ) ) ;
#30608=LINE ( 'NONE', #40169, #9217 ) ;
#30611=ORIENTED_EDGE ( 'NONE', *, *, #1485, .F. ) ;
#30613=CARTESIAN_POINT ( 'NONE',  ( 0.000000000000000000, 88.00363688980654331, -82.31555682352568226 ) ) ;
#30615=AXIS2_PLACEMENT_3D ( 'NONE', #41866, #1941, #35892 ) ;
#30624=EDGE_LOOP ( 'NONE', ( #29539, #17822, #33711, #26996 ) ) ;
#30625=DIRECTION ( 'NONE',  ( 1.000000000000000000, 0.000000000000000000, 0.000000000000000000 ) ) ;
#30627=ADVANCED_FACE ( 'NONE', ( #30232 ), #10375, .F. ) ;
#30629=VERTEX_POINT ( 'NONE', #3785 ) ;
#30630=CYLINDRICAL_SURFACE ( 'NONE', #21025, 58.99999999999998579 ) ;
#30631=EDGE_CURVE ( 'NONE', #23227, #10688, #17168, .T. ) ;
#30636=EDGE_CURVE ( 'NONE', #214, #33572, #35003, .T. ) ;
#30642=CARTESIAN_POINT ( 'NONE',  ( 0.000000000000000000, 67.32409792376626001, -89.75376489259298296 ) ) ;
#30644=CARTESIAN_POINT ( 'NONE',  ( 17.99999999999999645, -111.9370513079672520, 44.61600100275137493 ) ) ;
#30646=ORIENTED_EDGE ( 'NONE', *, *, #4094, .T. ) ;
#30649=AXIS2_PLACEMENT_3D ( 'NONE', #6828, #10327, #29981 ) ;
#30651=ORIENTED_EDGE ( 'NONE', *, *, #19092, .T. ) ;
#30655=CARTESIAN_POINT ( 'NONE',  ( 17.99999999999999645, 110.3490479609632615, 38.71798610214565173 ) ) ;
#30664=ORIENTED_EDGE ( 'NONE', *, *, #16536, .F. ) ;
#30665=ORIENTED_EDGE ( 'NONE', *, *, #10294, .T. ) ;
#30667=LINE ( 'NONE', #40887, #510 ) ;
#30668=LINE ( 'NONE', #7528, #16018 ) ;
#30671=FACE_OUTER_BOUND ( 'NONE', #26455, .T. ) ;
#30672=ORIENTED_EDGE ( 'NONE', *, *, #22081, .T. ) ;
#30673=CIRCLE ( 'NONE', #36905, 58.99999999999999289 ) ;
#30677=EDGE_CURVE ( 'NONE', #22222, #8344, #23542, .T. ) ;
#30680=ORIENTED_EDGE ( 'NONE', *, *, #31645, .F. ) ;
#30681=EDGE_CURVE ( 'NONE', #30034, #42828, #38693, .T. ) ;
#30682=ORIENTED_EDGE ( 'NONE', *, *, #19762, .T. ) ;
#30685=DIRECTION ( 'NONE',  ( -1.000000000000000000, -0.000000000000000000, -0.000000000000000000 ) ) ;
#30687=ORIENTED_EDGE ( 'NONE', *, *, #38571, .T. ) ;
#30692=DIRECTION ( 'NONE',  ( -1.000000000000000000, -0.000000000000000000, 0.000000000000000000 ) ) ;
#30694=AXIS2_PLACEMENT_3D ( 'NONE', #41016, #17516, #24706 ) ;
#30698=CARTESIAN_POINT ( 'NONE',  ( 0.000000000000000000, 0.000000000000000000, 0.000000000000000000 ) ) ;
#30701=VECTOR ( 'NONE', #21636, 1000.000000000000000 ) ;
#30703=DIRECTION ( 'NONE',  ( -1.000000000000000000, 0.000000000000000000, -0.000000000000000000 ) ) ;
#30708=AXIS2_PLACEMENT_3D ( 'NONE', #24023, #13547, #6759 ) ;
#30710=ORIENTED_EDGE ( 'NONE', *, *, #42319, .T. ) ;
#30712=ORIENTED_EDGE ( 'NONE', *, *, #35668, .F. ) ;
#30713=DIRECTION ( 'NONE',  ( 0.000000000000000000, 0.9714298932647090767, 0.2373266998711185127 ) ) ;
#30715=CARTESIAN_POINT ( 'NONE',  ( 0.000000000000000000, 94.52951811191651643, -67.23221107124801676 ) ) ;
#30716=ORIENTED_EDGE ( 'NONE', *, *, #28715, .F. ) ;
#30721=DIRECTION ( 'NONE',  ( 0.000000000000000000, 0.000000000000000000, 1.000000000000000000 ) ) ;
#30722=EDGE_LOOP ( 'NONE', ( #15590, #24869, #22338, #17469 ) ) ;
#30724=DIRECTION ( 'NONE',  ( -1.000000000000000000, -0.000000000000000000, -0.000000000000000000 ) ) ;
#30725=ADVANCED_FACE ( 'NONE', ( #14752 ), #25231, .F. ) ;
#30726=EDGE_LOOP ( 'NONE', ( #2059, #7284, #24555, #34027 ) ) ;
#30727=AXIS2_PLACEMENT_3D ( 'NONE', #35287, #4764, #35070 ) ;
#30728=DIRECTION ( 'NONE',  ( 1.000000000000000000, 0.000000000000000000, 0.000000000000000000 ) ) ;
#30731=CIRCLE ( 'NONE', #14712, 120.5010000000000190 ) ;
#30732=ORIENTED_EDGE ( 'NONE', *, *, #22259, .T. ) ;
#30738=EDGE_LOOP ( 'NONE', ( #5999, #4671, #18871, #15310 ) ) ;
#30739=DIRECTION ( 'NONE',  ( 1.000000000000000000, 0.000000000000000000, 0.000000000000000000 ) ) ;
#30740=LINE ( 'NONE', #7379, #15101 ) ;
#30745=EDGE_CURVE ( 'NONE', #13758, #18148, #38477, .T. ) ;
#30747=ORIENTED_EDGE ( 'NONE', *, *, #22349, .T. ) ;
#30753=ORIENTED_EDGE ( 'NONE', *, *, #15773, .F. ) ;
#30761=DIRECTION ( 'NONE',  ( 0.000000000000000000, 0.000000000000000000, 1.000000000000000000 ) ) ;
#30762=ADVANCED_FACE ( 'NONE', ( #21954 ), #5550, .F. ) ;
#30763=DIRECTION ( 'NONE',  ( 1.000000000000000000, 0.000000000000000000, -0.000000000000000000 ) ) ;
#30765=VERTEX_POINT ( 'NONE', #42170 ) ;
#30770=CARTESIAN_POINT ( 'NONE',  ( 9.000000000000001776, 112.8457601792519256, -26.86697618949260402 ) ) ;
#30771=CARTESIAN_POINT ( 'NONE',  ( 17.99999999999999645, 41.33768078145502756, 104.3046912715542902 ) ) ;
#30774=CARTESIAN_POINT ( 'NONE',  ( 0.000000000000000000, -29.02167576844032482, -108.3790330702172611 ) ) ;
#30775=CARTESIAN_POINT ( 'NONE',  ( 0.000000000000000000, -105.7179949885865256, -37.57629584241794163 ) ) ;
#30777=LINE ( 'NONE', #13781, #535 ) ;
#30779=DIRECTION ( 'NONE',  ( 1.000000000000000000, 0.000000000000000000, 0.000000000000000000 ) ) ;
#30781=CARTESIAN_POINT ( 'NONE',  ( 17.99999999999999645, -111.8797445107945236, 8.437727291342365987 ) ) ;
#30783=ORIENTED_EDGE ( 'NONE', *, *, #19467, .F. ) ;
#30784=CYLINDRICAL_SURFACE ( 'NONE', #7267, 59.00000000000000000 ) ;
#30788=EDGE_CURVE ( 'NONE', #41859, #8713, #18264, .T. ) ;
#30790=AXIS2_PLACEMENT_3D ( 'NONE', #7541, #756, #3590 ) ;
#30793=DIRECTION ( 'NONE',  ( -1.000000000000000000, -0.000000000000000000, -0.000000000000000000 ) ) ;
#30800=ORIENTED_EDGE ( 'NONE', *, *, #33676, .T. ) ;
#30803=CARTESIAN_POINT ( 'NONE',  ( 17.99999999999999645, -19.12429268481792732, 114.4126803693778669 ) ) ;
#30804=ORIENTED_EDGE ( 'NONE', *, *, #23524, .T. ) ;
#30809=DIRECTION ( 'NONE',  ( 0.000000000000000000, 0.05322217484217209305, 0.9985826956767622775 ) ) ;
#30813=CARTESIAN_POINT ( 'NONE',  ( 0.000000000000000000, 0.000000000000000000, 0.000000000000000000 ) ) ;
#30815=ORIENTED_EDGE ( 'NONE', *, *, #42735, .T. ) ;
#30817=ORIENTED_EDGE ( 'NONE', *, *, #28442, .T. ) ;
#30819=AXIS2_PLACEMENT_3D ( 'NONE', #15096, #28400, #11589 ) ;
#30822=EDGE_LOOP ( 'NONE', ( #17248, #31820, #19891, #1515 ) ) ;
#30824=DIRECTION ( 'NONE',  ( 1.000000000000000000, -0.000000000000000000, -0.000000000000000000 ) ) ;
#30831=AXIS2_PLACEMENT_3D ( 'NONE', #27969, #16156, #25775 ) ;
#30836=VERTEX_POINT ( 'NONE', #42809 ) ;
#30837=CARTESIAN_POINT ( 'NONE',  ( 8.999999999999998224, 78.18175027177430536, 85.69488855493025881 ) ) ;
#30838=ORIENTED_EDGE ( 'NONE', *, *, #18112, .F. ) ;
#30840=EDGE_CURVE ( 'NONE', #9027, #15861, #29790, .T. ) ;
#30841=ORIENTED_EDGE ( 'NONE', *, *, #12039, .F. ) ;
#30843=ADVANCED_FACE ( 'NONE', ( #2454 ), #33002, .F. ) ;
#30844=LINE ( 'NONE', #26707, #777 ) ;
#30846=CARTESIAN_POINT ( 'NONE',  ( 17.99999999999999645, -111.7974656912329436, -9.465682155096647676 ) ) ;
#30848=ORIENTED_EDGE ( 'NONE', *, *, #31497, .T. ) ;
#30849=AXIS2_PLACEMENT_3D ( 'NONE', #9102, #22457, #5824 ) ;
#30850=DIRECTION ( 'NONE',  ( -1.000000000000000000, -0.000000000000000000, -0.000000000000000000 ) ) ;
#30851=DIRECTION ( 'NONE',  ( -1.000000000000000000, 0.000000000000000000, 0.000000000000000000 ) ) ;
#30857=AXIS2_PLACEMENT_3D ( 'NONE', #4313, #21621, #37495 ) ;
#30859=EDGE_CURVE ( 'NONE', #8016, #12374, #12805, .T. ) ;
#30860=VERTEX_POINT ( 'NONE', #25856 ) ;
#30862=EDGE_CURVE ( 'NONE', #16394, #17179, #3003, .T. ) ;
#30867=ORIENTED_EDGE ( 'NONE', *, *, #22492, .T. ) ;
#30870=DIRECTION ( 'NONE',  ( 1.000000000000000000, -0.000000000000000000, -0.000000000000000000 ) ) ;
#30873=CARTESIAN_POINT ( 'NONE',  ( 17.99999999999999645, 111.2721026680460596, -14.38025178762657852 ) ) ;
#30874=EDGE_LOOP ( 'NONE', ( #7902, #11585, #6601, #1129 ) ) ;
#30877=DIRECTION ( 'NONE',  ( 1.000000000000000000, 0.000000000000000000, 0.000000000000000000 ) ) ;
#30878=VECTOR ( 'NONE', #11063, 1000.000000000000000 ) ;
#30880=EDGE_LOOP ( 'NONE', ( #11840, #32906, #42897, #31290 ) ) ;
#30882=VERTEX_POINT ( 'NONE', #25655 ) ;
#30884=DIRECTION ( 'NONE',  ( -1.000000000000000000, -0.000000000000000000, 0.000000000000000000 ) ) ;
#30886=ORIENTED_EDGE ( 'NONE', *, *, #11544, .F. ) ;
#30895=DIRECTION ( 'NONE',  ( 1.000000000000000000, 0.000000000000000000, 0.000000000000000000 ) ) ;
#30896=CARTESIAN_POINT ( 'NONE',  ( 17.99999999999999645, 8.827181066047508295, -120.1772519049558667 ) ) ;
#30898=CARTESIAN_POINT ( 'NONE',  ( 0.000000000000000000, 23.85344185397347161, -113.5209818126988779 ) ) ;
#30899=ORIENTED_EDGE ( 'NONE', *, *, #16508, .F. ) ;
#30901=DIRECTION ( 'NONE',  ( 1.000000000000000000, 0.000000000000000000, 0.000000000000000000 ) ) ;
#30902=ORIENTED_EDGE ( 'NONE', *, *, #37737, .F. ) ;
#30903=CIRCLE ( 'NONE', #9991, 59.00000000000000711 ) ;
#30907=DIRECTION ( 'NONE',  ( 1.000000000000000000, 0.000000000000000000, 0.000000000000000000 ) ) ;
#30912=DIRECTION ( 'NONE',  ( 0.000000000000000000, 0.000000000000000000, 1.000000000000000000 ) ) ;
#30914=EDGE_CURVE ( 'NONE', #36853, #10288, #36062, .T. ) ;
#30915=ORIENTED_EDGE ( 'NONE', *, *, #5983, .F. ) ;
#30916=DIRECTION ( 'NONE',  ( 0.000000000000000000, 0.8993121301712203586, -0.4373073204588531215 ) ) ;
#30917=VERTEX_POINT ( 'NONE', #35834 ) ;
#30918=AXIS2_PLACEMENT_3D ( 'NONE', #35234, #5361, #18730 ) ;
#30930=EDGE_CURVE ( 'NONE', #18335, #42499, #2670, .T. ) ;
#30931=DIRECTION ( 'NONE',  ( 0.000000000000000000, -6.538873467836204094E-15, 1.000000000000000000 ) ) ;
#30932=CARTESIAN_POINT ( 'NONE',  ( 0.000000000000000000, 31.17727234463695041, 111.7317219465820983 ) ) ;
#30935=DIRECTION ( 'NONE',  ( 0.000000000000000000, 0.5963673585384969833, 0.8027116379309670036 ) ) ;
#30938=CARTESIAN_POINT ( 'NONE',  ( 0.000000000000000000, -23.10276247328017263, -118.2656051737072431 ) ) ;
#30939=ORIENTED_EDGE ( 'NONE', *, *, #36911, .F. ) ;
#30944=DIRECTION ( 'NONE',  ( 0.000000000000000000, 0.3641605752528230266, -0.9313361774523382097 ) ) ;
#30945=ORIENTED_EDGE ( 'NONE', *, *, #42095, .T. ) ;
#30947=DIRECTION ( 'NONE',  ( -1.000000000000000000, 0.000000000000000000, 0.000000000000000000 ) ) ;
#30948=FACE_OUTER_BOUND ( 'NONE', #7507, .T. ) ;
#30949=ORIENTED_EDGE ( 'NONE', *, *, #4360, .T. ) ;
#30954=DIRECTION ( 'NONE',  ( 1.000000000000000000, 0.000000000000000000, 0.000000000000000000 ) ) ;
#30956=CIRCLE ( 'NONE', #10778, 59.00000000000000000 ) ;
#30957=DIRECTION ( 'NONE',  ( 0.000000000000000000, -0.3641605752528101481, -0.9313361774523430947 ) ) ;
#30959=VECTOR ( 'NONE', #26729, 1000.000000000000000 ) ;
#30960=ORIENTED_EDGE ( 'NONE', *, *, #6023, .T. ) ;
#30965=AXIS2_PLACEMENT_3D ( 'NONE', #37027, #13287, #10640 ) ;
#30971=EDGE_LOOP ( 'NONE', ( #5628, #34924, #33008, #10447 ) ) ;
#30974=EDGE_CURVE ( 'NONE', #3514, #13787, #16297, .T. ) ;
#30975=ORIENTED_EDGE ( 'NONE', *, *, #3508, .F. ) ;
#30977=DIRECTION ( 'NONE',  ( 0.000000000000000000, -1.505387152034110654E-14, -1.000000000000000000 ) ) ;
#30980=ORIENTED_EDGE ( 'NONE', *, *, #39579, .T. ) ;
#30981=EDGE_CURVE ( 'NONE', #3101, #17781, #37357, .T. ) ;
#30986=ORIENTED_EDGE ( 'NONE', *, *, #21157, .F. ) ;
#30988=CARTESIAN_POINT ( 'NONE',  ( 17.99999999999999645, 59.07817985939141181, -105.0250430397503294 ) ) ;
#30989=ORIENTED_EDGE ( 'NONE', *, *, #30930, .T. ) ;
#30990=AXIS2_PLACEMENT_3D ( 'NONE', #42584, #35617, #5534 ) ;
#30992=DIRECTION ( 'NONE',  ( 1.000000000000000000, 0.000000000000000000, 0.000000000000000000 ) ) ;
#30995=CYLINDRICAL_SURFACE ( 'NONE', #1698, 59.00000000000000000 ) ;
#30998=CARTESIAN_POINT ( 'NONE',  ( 17.99999999999999645, -109.1131968883996848, -26.12628443612003437 ) ) ;
#30999=CIRCLE ( 'NONE', #19878, 116.0000000000000000 ) ;
#31002=DIRECTION ( 'NONE',  ( 0.000000000000000000, 0.1062934856473655570, -0.9943348002101372041 ) ) ;
#31003=DIRECTION ( 'NONE',  ( 0.000000000000000000, 0.000000000000000000, 1.000000000000000000 ) ) ;
#31004=VERTEX_POINT ( 'NONE', #37136 ) ;
#31009=EDGE_LOOP ( 'NONE', ( #21555, #17733, #10028, #28164 ) ) ;
#31010=CARTESIAN_POINT ( 'NONE',  ( 8.999999999999998224, 108.8880088604282008, -39.99251838045848473 ) ) ;
#31011=CARTESIAN_POINT ( 'NONE',  ( 17.99999999999999645, -23.85344185397275041, 113.5209818126990200 ) ) ;
#31018=EDGE_CURVE ( 'NONE', #15836, #4507, #32315, .T. ) ;
#31022=AXIS2_PLACEMENT_3D ( 'NONE', #18129, #15679, #25730 ) ;
#31023=LINE ( 'NONE', #4607, #41628 ) ;
#31024=CIRCLE ( 'NONE', #25479, 59.00000000000000711 ) ;
#31034=VERTEX_POINT ( 'NONE', #13839 ) ;
#31036=DIRECTION ( 'NONE',  ( 0.000000000000000000, 0.000000000000000000, 1.000000000000000000 ) ) ;
#31037=EDGE_CURVE ( 'NONE', #18907, #11646, #36923, .T. ) ;
#31041=CIRCLE ( 'NONE', #28263, 59.00000000000001421 ) ;
#31045=ORIENTED_EDGE ( 'NONE', *, *, #4062, .T. ) ;
#31047=CIRCLE ( 'NONE', #42845, 59.00000000000000711 ) ;
#31048=AXIS2_PLACEMENT_3D ( 'NONE', #5472, #9163, #18833 ) ;
#31055=EDGE_CURVE ( 'NONE', #24215, #9004, #13532, .T. ) ;
#31056=VECTOR ( 'NONE', #21366, 1000.000000000000000 ) ;
#31058=EDGE_CURVE ( 'NONE', #16222, #32693, #36464, .T. ) ;
#31059=LINE ( 'NONE', #1147, #31520 ) ;
#31060=DIRECTION ( 'NONE',  ( -1.000000000000000000, -0.000000000000000000, -0.000000000000000000 ) ) ;
#31062=CYLINDRICAL_SURFACE ( 'NONE', #41490, 120.5010000000000190 ) ;
#31063=DIRECTION ( 'NONE',  ( 0.000000000000000000, 0.9213119778704113028, 0.3888241754733244848 ) ) ;
#31065=CIRCLE ( 'NONE', #33163, 116.0000000000000000 ) ;
#31066=CARTESIAN_POINT ( 'NONE',  ( 17.99999999999999645, -106.5605152861907072, 56.26142179985788516 ) ) ;
#31067=CYLINDRICAL_SURFACE ( 'NONE', #13616, 59.00000000000000000 ) ;
#31069=DIRECTION ( 'NONE',  ( 0.000000000000000000, -0.9996456111234528485, 0.02662052143776447166 ) ) ;
#31071=EDGE_CURVE ( 'NONE', #33465, #36745, #17726, .T. ) ;
#31073=ORIENTED_EDGE ( 'NONE', *, *, #1761, .T. ) ;
#31074=VERTEX_POINT ( 'NONE', #7034 ) ;
#31081=AXIS2_PLACEMENT_3D ( 'NONE', #25964, #38595, #12656 ) ;
#31082=AXIS2_PLACEMENT_3D ( 'NONE', #6634, #33269, #3355 ) ;
#31083=ADVANCED_FACE ( 'NONE', ( #7475 ), #3965, .F. ) ;
#31084=EDGE_LOOP ( 'NONE', ( #38262, #5369, #25803, #27441 ) ) ;
#31087=DIRECTION ( 'NONE',  ( 0.000000000000000000, -0.05322217484218558226, 0.9985826956767615004 ) ) ;
#31088=DIRECTION ( 'NONE',  ( -1.000000000000000000, -0.000000000000000000, -0.000000000000000000 ) ) ;
#31091=CIRCLE ( 'NONE', #17895, 59.00000000000000711 ) ;
#31092=DIRECTION ( 'NONE',  ( 0.000000000000000000, 0.000000000000000000, 1.000000000000000000 ) ) ;
#31093=CIRCLE ( 'NONE', #28065, 59.00000000000000000 ) ;
#31100=CARTESIAN_POINT ( 'NONE',  ( 17.99999999999999645, 100.6739960869717834, 49.52796165323294986 ) ) ;
#31109=ADVANCED_FACE ( 'NONE', ( #903 ), #13400, .F. ) ;
#31110=AXIS2_PLACEMENT_3D ( 'NONE', #29428, #35937, #32469 ) ;
#31112=EDGE_CURVE ( 'NONE', #24346, #41108, #14427, .T. ) ;
#31114=AXIS2_PLACEMENT_3D ( 'NONE', #2205, #35789, #15565 ) ;
#31115=DIRECTION ( 'NONE',  ( 0.000000000000000000, 0.000000000000000000, 1.000000000000000000 ) ) ;
#31117=VERTEX_POINT ( 'NONE', #7852 ) ;
#31118=DIRECTION ( 'NONE',  ( 0.000000000000000000, -0.3641605752528102591, -0.9313361774523430947 ) ) ;
#31123=CYLINDRICAL_SURFACE ( 'NONE', #35732, 59.00000000000000000 ) ;
#31124=CARTESIAN_POINT ( 'NONE',  ( 0.000000000000000000, 0.000000000000000000, 0.000000000000000000 ) ) ;
#31127=AXIS2_PLACEMENT_3D ( 'NONE', #32636, #16284, #12581 ) ;
#31130=VECTOR ( 'NONE', #35958, 1000.000000000000000 ) ;
#31138=CIRCLE ( 'NONE', #29053, 59.00000000000000711 ) ;
#31140=ADVANCED_FACE ( 'NONE', ( #13996 ), #7192, .F. ) ;
#31141=VERTEX_POINT ( 'NONE', #30988 ) ;
#31150=CARTESIAN_POINT ( 'NONE',  ( 0.000000000000000000, 0.000000000000000000, 0.000000000000000000 ) ) ;
#31151=ORIENTED_EDGE ( 'NONE', *, *, #42085, .T. ) ;
#31158=ORIENTED_EDGE ( 'NONE', *, *, #11753, .T. ) ;
#31160=CARTESIAN_POINT ( 'NONE',  ( 17.99999999999999645, 84.77518783075197462, -73.49448960231268302 ) ) ;
#31162=CYLINDRICAL_SURFACE ( 'NONE', #5956, 59.00000000000000000 ) ;
#31163=VERTEX_POINT ( 'NONE', #4130 ) ;
#31164=DIRECTION ( 'NONE',  ( 1.000000000000000000, 0.000000000000000000, 0.000000000000000000 ) ) ;
#31165=ORIENTED_EDGE ( 'NONE', *, *, #29035, .F. ) ;
#31172=EDGE_CURVE ( 'NONE', #33598, #28845, #13786, .T. ) ;
#31174=DIRECTION ( 'NONE',  ( 0.000000000000000000, 0.6382441836448211614, -0.7698339834299053885 ) ) ;
#31176=DIRECTION ( 'NONE',  ( 0.000000000000000000, 0.1062934856473655293, -0.9943348002101370930 ) ) ;
#31178=EDGE_CURVE ( 'NONE', #433, #29621, #28850, .T. ) ;
#31180=CARTESIAN_POINT ( 'NONE',  ( 17.99999999999999645, 115.0622509503832589, 14.72000021165183803 ) ) ;
#31194=VECTOR ( 'NONE', #14022, 1000.000000000000000 ) ;
#31197=AXIS2_PLACEMENT_3D ( 'NONE', #1903, #34641, #2106 ) ;
#31198=DIRECTION ( 'NONE',  ( 1.000000000000000000, 0.000000000000000000, 0.000000000000000000 ) ) ;
#31199=DIRECTION ( 'NONE',  ( 1.000000000000000000, 0.000000000000000000, 0.000000000000000000 ) ) ;
#31201=CYLINDRICAL_SURFACE ( 'NONE', #4161, 59.00000000000000000 ) ;
#31202=ORIENTED_EDGE ( 'NONE', *, *, #5843, .T. ) ;
#31205=ORIENTED_EDGE ( 'NONE', *, *, #26348, .F. ) ;
#31210=CIRCLE ( 'NONE', #36749, 59.00000000000000000 ) ;
#31213=EDGE_LOOP ( 'NONE', ( #27852, #32068, #7479, #15243 ) ) ;
#31219=VERTEX_POINT ( 'NONE', #34463 ) ;
#31221=DIRECTION ( 'NONE',  ( 1.000000000000000000, -0.000000000000000000, -0.000000000000000000 ) ) ;
#31222=DIRECTION ( 'NONE',  ( -1.000000000000000000, 0.000000000000000000, 0.000000000000000000 ) ) ;
#31224=VECTOR ( 'NONE', #35995, 1000.000000000000000 ) ;
#31227=DIRECTION ( 'NONE',  ( 0.000000000000000000, -0.9714298932647122964, 0.2373266998711055509 ) ) ;
#31230=CARTESIAN_POINT ( 'NONE',  ( 17.99999999999999645, -59.07817985938929439, -105.0250430397515089 ) ) ;
#31231=EDGE_LOOP ( 'NONE', ( #32239, #37815, #30665, #1185 ) ) ;
#31232=CARTESIAN_POINT ( 'NONE',  ( 17.99999999999999645, 53.40478689619876462, -108.0204598100360016 ) ) ;
#31233=DIRECTION ( 'NONE',  ( 0.000000000000000000, 0.000000000000000000, 1.000000000000000000 ) ) ;
#31242=ADVANCED_FACE ( 'NONE', ( #17945 ), #10485, .F. ) ;
#31243=CARTESIAN_POINT ( 'NONE',  ( 0.000000000000000000, 73.51007459736430860, 89.73443560133387109 ) ) ;
#31245=DIRECTION ( 'NONE',  ( 0.000000000000000000, 0.000000000000000000, 1.000000000000000000 ) ) ;
#31250=AXIS2_PLACEMENT_3D ( 'NONE', #16232, #29525, #2865 ) ;
#31251=CARTESIAN_POINT ( 'NONE',  ( 0.000000000000000000, 103.1672962317651496, 44.09967643725903486 ) ) ;
#31252=CARTESIAN_POINT ( 'NONE',  ( 17.99999999999999645, -118.8387007424472159, 19.94628303336445185 ) ) ;
#31259=CARTESIAN_POINT ( 'NONE',  ( 17.99999999999999645, 0.000000000000000000, 0.000000000000000000 ) ) ;
#31263=DIRECTION ( 'NONE',  ( 0.000000000000000000, 0.05322217484217209305, 0.9985826956767622775 ) ) ;
#31267=EDGE_LOOP ( 'NONE', ( #17294, #2521, #15340, #17425 ) ) ;
#31274=EDGE_CURVE ( 'NONE', #189, #7533, #38596, .T. ) ;
#31275=CARTESIAN_POINT ( 'NONE',  ( 17.99999999999999645, 68.61497464550593861, 99.05794392877625398 ) ) ;
#31277=ADVANCED_FACE ( 'NONE', ( #37089 ), #11359, .F. ) ;
#31285=CARTESIAN_POINT ( 'NONE',  ( 17.99999999999999645, -83.49789599728842404, 86.88263557826738293 ) ) ;
#31286=CARTESIAN_POINT ( 'NONE',  ( 17.99999999999999645, -79.94368240339368015, -90.16373242487986772 ) ) ;
#31290=ORIENTED_EDGE ( 'NONE', *, *, #13485, .F. ) ;
#31304=LINE ( 'NONE', #11451, #14278 ) ;
#31305=CIRCLE ( 'NONE', #12498, 116.0000000000000000 ) ;
#31309=CARTESIAN_POINT ( 'NONE',  ( 0.000000000000000000, -94.83915810436441518, 59.94836581341558457 ) ) ;
#31312=EDGE_CURVE ( 'NONE', #25961, #9338, #34905, .T. ) ;
#31313=CARTESIAN_POINT ( 'NONE',  ( 17.99999999999999645, 0.000000000000000000, 0.000000000000000000 ) ) ;
#31317=CYLINDRICAL_SURFACE ( 'NONE', #32866, 120.5010000000000190 ) ;
#31319=ORIENTED_EDGE ( 'NONE', *, *, #21298, .T. ) ;
#31323=DIRECTION ( 'NONE',  ( -1.000000000000000000, 0.000000000000000000, 0.000000000000000000 ) ) ;
#31324=EDGE_CURVE ( 'NONE', #4914, #25878, #8647, .T. ) ;
#31325=DIRECTION ( 'NONE',  ( -1.000000000000000000, -0.000000000000000000, -0.000000000000000000 ) ) ;
#31331=CIRCLE ( 'NONE', #29935, 120.5010000000000190 ) ;
#31332=DIRECTION ( 'NONE',  ( 0.000000000000000000, 0.000000000000000000, 1.000000000000000000 ) ) ;
#31333=CARTESIAN_POINT ( 'NONE',  ( 0.000000000000000000, -120.3696465864706369, 5.624871700595674540 ) ) ;
#31335=CIRCLE ( 'NONE', #6923, 120.5010000000000474 ) ;
#31337=VERTEX_POINT ( 'NONE', #38588 ) ;
#31339=SURFACE_STYLE_FILL_AREA ( #7975 ) ;
#31341=LINE ( 'NONE', #41570, #21391 ) ;
#31347=ORIENTED_EDGE ( 'NONE', *, *, #1679, .T. ) ;
#31348=CARTESIAN_POINT ( 'NONE',  ( 8.999999999999998224, -54.09091620264791089, 102.6166301549515936 ) ) ;
#31349=LINE ( 'NONE', #7777, #17922 ) ;
#31352=CYLINDRICAL_SURFACE ( 'NONE', #11154, 120.5010000000000190 ) ;
#31356=AXIS2_PLACEMENT_3D ( 'NONE', #31949, #15589, #21942 ) ;
#31359=AXIS2_PLACEMENT_3D ( 'NONE', #36220, #19688, #13998 ) ;
#31360=EDGE_CURVE ( 'NONE', #32669, #10688, #20522, .T. ) ;
#31361=EDGE_CURVE ( 'NONE', #13665, #19271, #5226, .T. ) ;
#31363=ORIENTED_EDGE ( 'NONE', *, *, #28226, .T. ) ;
#31364=CARTESIAN_POINT ( 'NONE',  ( 17.99999999999999645, 98.69720329640956891, 60.94966826379944536 ) ) ;
#31365=ORIENTED_EDGE ( 'NONE', *, *, #14964, .T. ) ;
#31366=FACE_OUTER_BOUND ( 'NONE', #30388, .T. ) ;
#31368=CARTESIAN_POINT ( 'NONE',  ( 17.99999999999999645, -21.55123232222391394, -118.5581519187674360 ) ) ;
#31370=DIRECTION ( 'NONE',  ( 0.000000000000000000, 0.000000000000000000, 1.000000000000000000 ) ) ;
#31373=CARTESIAN_POINT ( 'NONE',  ( 0.000000000000000000, 0.000000000000000000, 0.000000000000000000 ) ) ;
#31374=FACE_OUTER_BOUND ( 'NONE', #11494, .T. ) ;
#31378=ORIENTED_EDGE ( 'NONE', *, *, #4262, .F. ) ;
#31379=DIRECTION ( 'NONE',  ( 1.000000000000000000, 0.000000000000000000, 0.000000000000000000 ) ) ;
#31383=CARTESIAN_POINT ( 'NONE',  ( 17.99999999999999645, 0.000000000000000000, 0.000000000000000000 ) ) ;
#31385=CARTESIAN_POINT ( 'NONE',  ( 9.000000000000001776, -110.8621702203451065, 34.14058016547500785 ) ) ;
#31386=FACE_OUTER_BOUND ( 'NONE', #29247, .T. ) ;
#31388=EDGE_CURVE ( 'NONE', #32231, #22539, #1729, .T. ) ;
#31389=AXIS2_PLACEMENT_3D ( 'NONE', #18357, #1499, #41196 ) ;
#31392=EDGE_CURVE ( 'NONE', #31117, #35437, #8938, .T. ) ;
#31393=AXIS2_PLACEMENT_3D ( 'NONE', #8503, #39223, #18813 ) ;
#31397=AXIS2_PLACEMENT_3D ( 'NONE', #24678, #21639, #8054 ) ;
#31398=FACE_OUTER_BOUND ( 'NONE', #29503, .T. ) ;
#31399=CARTESIAN_POINT ( 'NONE',  ( 0.000000000000000000, 0.000000000000000000, 0.000000000000000000 ) ) ;
#31402=EDGE_LOOP ( 'NONE', ( #42377, #36696, #20865, #8848 ) ) ;
#31405=ORIENTED_EDGE ( 'NONE', *, *, #3771, .T. ) ;
#31409=CARTESIAN_POINT ( 'NONE',  ( 0.000000000000000000, -90.81729652456118629, -72.16798910853708549 ) ) ;
#31411=ADVANCED_FACE ( 'NONE', ( #11810 ), #22070, .F. ) ;
#31414=DIRECTION ( 'NONE',  ( -1.000000000000000000, 0.000000000000000000, -0.000000000000000000 ) ) ;
#31417=CIRCLE ( 'NONE', #34887, 59.00000000000000000 ) ;
#31419=ORIENTED_EDGE ( 'NONE', *, *, #22427, .F. ) ;
#31422=AXIS2_PLACEMENT_3D ( 'NONE', #11964, #25290, #31807 ) ;
#31423=CIRCLE ( 'NONE', #25192, 59.00000000000000000 ) ;
#31424=ORIENTED_EDGE ( 'NONE', *, *, #37318, .F. ) ;
#31426=CARTESIAN_POINT ( 'NONE',  ( 0.000000000000000000, 0.000000000000000000, 0.000000000000000000 ) ) ;
#31427=DIRECTION ( 'NONE',  ( -1.000000000000000000, -0.000000000000000000, -0.000000000000000000 ) ) ;
#31430=FACE_OUTER_BOUND ( 'NONE', #14659, .T. ) ;
#31435=DIRECTION ( 'NONE',  ( 0.000000000000000000, -0.1590634960190595026, -0.9872683547213466637 ) ) ;
#31438=CYLINDRICAL_SURFACE ( 'NONE', #40073, 59.00000000000000000 ) ;
#31441=DIRECTION ( 'NONE',  ( 1.000000000000000000, 0.000000000000000000, 0.000000000000000000 ) ) ;
#31450=CARTESIAN_POINT ( 'NONE',  ( 17.99999999999999645, 0.000000000000000000, 0.000000000000000000 ) ) ;
#31451=CARTESIAN_POINT ( 'NONE',  ( 0.000000000000000000, 0.000000000000000000, 0.000000000000000000 ) ) ;
#31452=CIRCLE ( 'NONE', #12642, 58.99999999999999289 ) ;
#31454=ORIENTED_EDGE ( 'NONE', *, *, #15131, .T. ) ;
#31455=VECTOR ( 'NONE', #23074, 1000.000000000000000 ) ;
#31459=AXIS2_PLACEMENT_3D ( 'NONE', #7598, #2255, #15614 ) ;
#31462=ADVANCED_FACE ( 'NONE', ( #42500 ), #25960, .F. ) ;
#31468=VERTEX_POINT ( 'NONE', #13090 ) ;
#31473=ORIENTED_EDGE ( 'NONE', *, *, #19989, .T. ) ;
#31475=FACE_OUTER_BOUND ( 'NONE', #11966, .T. ) ;
#31478=ORIENTED_EDGE ( 'NONE', *, *, #32672, .T. ) ;
#31479=CIRCLE ( 'NONE', #9840, 58.99999999999998579 ) ;
#31481=FACE_OUTER_BOUND ( 'NONE', #33808, .T. ) ;
#31482=CIRCLE ( 'NONE', #4288, 58.99999999999998579 ) ;
#31483=ADVANCED_FACE ( 'NONE', ( #6291 ), #42935, .F. ) ;
#31486=CYLINDRICAL_SURFACE ( 'NONE', #30053, 116.0000000000000000 ) ;
#31488=DIRECTION ( 'NONE',  ( 0.000000000000000000, 0.000000000000000000, 1.000000000000000000 ) ) ;
#31489=ORIENTED_EDGE ( 'NONE', *, *, #29830, .F. ) ;
#31490=DIRECTION ( 'NONE',  ( -1.000000000000000000, -0.000000000000000000, -0.000000000000000000 ) ) ;
#31491=ORIENTED_EDGE ( 'NONE', *, *, #3246, .F. ) ;
#31494=CARTESIAN_POINT ( 'NONE',  ( 17.99999999999999645, 109.1131968883998695, -26.12628443611929896 ) ) ;
#31496=DIRECTION ( 'NONE',  ( 1.000000000000000000, 0.000000000000000000, 0.000000000000000000 ) ) ;
#31497=EDGE_CURVE ( 'NONE', #28805, #41404, #35118, .T. ) ;
#31498=CARTESIAN_POINT ( 'NONE',  ( 0.000000000000000000, 0.000000000000000000, 0.000000000000000000 ) ) ;
#31499=ORIENTED_EDGE ( 'NONE', *, *, #14841, .F. ) ;
#31504=CARTESIAN_POINT ( 'NONE',  ( 0.000000000000000000, -56.51398178981757070, -96.92493144647505687 ) ) ;
#31508=AXIS2_PLACEMENT_3D ( 'NONE', #33218, #3301, #26256 ) ;
#31510=LINE ( 'NONE', #21300, #29686 ) ;
#31518=ORIENTED_EDGE ( 'NONE', *, *, #16653, .T. ) ;
#31519=DIRECTION ( 'NONE',  ( 1.000000000000000000, 0.000000000000000000, 0.000000000000000000 ) ) ;
#31520=VECTOR ( 'NONE', #14498, 1000.000000000000000 ) ;
#31526=ORIENTED_EDGE ( 'NONE', *, *, #37560, .T. ) ;
#31529=ADVANCED_FACE ( 'NONE', ( #13303 ), #2777, .F. ) ;
#31532=ORIENTED_EDGE ( 'NONE', *, *, #1489, .F. ) ;
#31533=ADVANCED_FACE ( 'NONE', ( #23561 ), #20087, .F. ) ;
#31535=LINE ( 'NONE', #1622, #4199 ) ;
#31537=ORIENTED_EDGE ( 'NONE', *, *, #21673, .T. ) ;
#31538=AXIS2_PLACEMENT_3D ( 'NONE', #42945, #35744, #3224 ) ;
#31539=CARTESIAN_POINT ( 'NONE',  ( 0.000000000000000000, 10.40101730206529140, -120.0512800434970018 ) ) ;
#31542=CARTESIAN_POINT ( 'NONE',  ( 17.99999999999999645, -73.51007459736489125, 89.73443560133338792 ) ) ;
#31543=DIRECTION ( 'NONE',  ( -1.000000000000000000, -0.000000000000000000, -0.000000000000000000 ) ) ;
#31545=FACE_OUTER_BOUND ( 'NONE', #33994, .T. ) ;
#31547=ADVANCED_FACE ( 'NONE', ( #146 ), #36829, .F. ) ;
#31548=VECTOR ( 'NONE', #28407, 1000.000000000000000 ) ;
#31550=DIRECTION ( 'NONE',  ( -1.000000000000000000, -0.000000000000000000, -0.000000000000000000 ) ) ;
#31553=ORIENTED_EDGE ( 'NONE', *, *, #35197, .T. ) ;
#31554=LINE ( 'NONE', #14568, #29632 ) ;
#31556=CARTESIAN_POINT ( 'NONE',  ( 17.99999999999999645, 104.0201923570382405, -51.34003878070953419 ) ) ;
#31560=CARTESIAN_POINT ( 'NONE',  ( 0.000000000000000000, -111.8797445107945236, 8.437727291342365987 ) ) ;
#31561=EDGE_CURVE ( 'NONE', #11934, #34763, #29443, .T. ) ;
#31563=ORIENTED_EDGE ( 'NONE', *, *, #27597, .T. ) ;
#31564=FACE_OUTER_BOUND ( 'NONE', #4935, .T. ) ;
#31565=VERTEX_POINT ( 'NONE', #29233 ) ;
#31567=CARTESIAN_POINT ( 'NONE',  ( 17.99999999999999645, -11.41303419185048185, 111.6154788735835410 ) ) ;
#31568=AXIS2_PLACEMENT_3D ( 'NONE', #29388, #26116, #19380 ) ;
#31570=ORIENTED_EDGE ( 'NONE', *, *, #15526, .F. ) ;
#31571=DIRECTION ( 'NONE',  ( 0.000000000000000000, 0.000000000000000000, 1.000000000000000000 ) ) ;
#31580=CARTESIAN_POINT ( 'NONE',  ( 17.99999999999999645, -120.4984140710909344, 0.7894348306980537577 ) ) ;
#31581=EDGE_CURVE ( 'NONE', #8344, #9503, #369, .T. ) ;
#31582=DIRECTION ( 'NONE',  ( 0.000000000000000000, -0.7164567402983209599, 0.6976315211349787271 ) ) ;
#31584=ORIENTED_EDGE ( 'NONE', *, *, #11768, .T. ) ;
#31585=CARTESIAN_POINT ( 'NONE',  ( 0.000000000000000000, 114.1157422997285806, -20.82300072952825332 ) ) ;
#31589=DIRECTION ( 'NONE',  ( 0.000000000000000000, 0.000000000000000000, 1.000000000000000000 ) ) ;
#31591=CARTESIAN_POINT ( 'NONE',  ( -10.00000000000000000, 0.000000000000000000, 0.000000000000000000 ) ) ;
#31592=EDGE_LOOP ( 'NONE', ( #7381, #33349, #38216, #32140 ) ) ;
#31598=DIRECTION ( 'NONE',  ( -1.000000000000000000, -0.000000000000000000, 0.000000000000000000 ) ) ;
#31603=DIRECTION ( 'NONE',  ( 0.000000000000000000, 0.000000000000000000, 1.000000000000000000 ) ) ;
#31605=VERTEX_POINT ( 'NONE', #3643 ) ;
#31611=DIRECTION ( 'NONE',  ( 0.000000000000000000, 0.000000000000000000, 1.000000000000000000 ) ) ;
#31612=FACE_OUTER_BOUND ( 'NONE', #13159, .T. ) ;
#31613=AXIS2_PLACEMENT_3D ( 'NONE', #31504, #1590, #31069 ) ;
#31616=LINE ( 'NONE', #28793, #30701 ) ;
#31618=DIRECTION ( 'NONE',  ( 1.000000000000000000, 0.000000000000000000, -0.000000000000000000 ) ) ;
#31620=EDGE_CURVE ( 'NONE', #5769, #7227, #25411, .T. ) ;
#31622=VERTEX_POINT ( 'NONE', #30938 ) ;
#31624=CYLINDRICAL_SURFACE ( 'NONE', #41690, 59.00000000000000000 ) ;
#31625=VERTEX_POINT ( 'NONE', #11310 ) ;
#31628=DIRECTION ( 'NONE',  ( -1.000000000000000000, 0.000000000000000000, -0.000000000000000000 ) ) ;
#31635=ORIENTED_EDGE ( 'NONE', *, *, #9222, .F. ) ;
#31636=FACE_OUTER_BOUND ( 'NONE', #31801, .T. ) ;
#31637=DIRECTION ( 'NONE',  ( 1.000000000000000000, 0.000000000000000000, -0.000000000000000000 ) ) ;
#31640=VECTOR ( 'NONE', #25340, 1000.000000000000000 ) ;
#31643=CIRCLE ( 'NONE', #38601, 120.5010000000000190 ) ;
#31644=CARTESIAN_POINT ( 'NONE',  ( 0.000000000000000000, -30.01658535635190361, -108.1077105353201233 ) ) ;
#31645=EDGE_CURVE ( 'NONE', #7685, #38997, #42781, .T. ) ;
#31646=EDGE_CURVE ( 'NONE', #33231, #22420, #27688, .T. ) ;
#31647=ORIENTED_EDGE ( 'NONE', *, *, #13791, .T. ) ;
#31649=EDGE_CURVE ( 'NONE', #18913, #22284, #3854, .T. ) ;
#31650=EDGE_CURVE ( 'NONE', #33431, #42007, #33053, .T. ) ;
#31651=CIRCLE ( 'NONE', #26085, 59.00000000000000000 ) ;
#31655=CIRCLE ( 'NONE', #12849, 59.00000000000000000 ) ;
#31657=ORIENTED_EDGE ( 'NONE', *, *, #13190, .F. ) ;
#31658=CYLINDRICAL_SURFACE ( 'NONE', #28194, 116.0000000000000000 ) ;
#31660=ORIENTED_EDGE ( 'NONE', *, *, #33189, .T. ) ;
#31665=DIRECTION ( 'NONE',  ( -1.000000000000000000, -0.000000000000000000, -0.000000000000000000 ) ) ;
#31668=CIRCLE ( 'NONE', #16358, 58.99999999999999289 ) ;
#31672=ORIENTED_EDGE ( 'NONE', *, *, #17921, .T. ) ;
#31674=ORIENTED_EDGE ( 'NONE', *, *, #29915, .F. ) ;
#31677=AXIS2_PLACEMENT_3D ( 'NONE', #41955, #5318, #18690 ) ;
#31684=ORIENTED_EDGE ( 'NONE', *, *, #22144, .T. ) ;
#31687=CARTESIAN_POINT ( 'NONE',  ( 17.99999999999999645, 95.38615066513983720, 59.07414607872858170 ) ) ;
#31694=DIRECTION ( 'NONE',  ( 1.000000000000000000, 0.000000000000000000, 0.000000000000000000 ) ) ;
#31698=DIRECTION ( 'NONE',  ( 1.000000000000000000, 0.000000000000000000, 0.000000000000000000 ) ) ;
#31699=CARTESIAN_POINT ( 'NONE',  ( 0.000000000000000000, 116.0452958106480708, 32.46506308663498430 ) ) ;
#31701=EDGE_CURVE ( 'NONE', #40182, #18148, #42102, .T. ) ;
#31703=DIRECTION ( 'NONE',  ( 0.000000000000000000, 0.000000000000000000, 1.000000000000000000 ) ) ;
#31704=DIRECTION ( 'NONE',  ( 1.000000000000000000, 0.000000000000000000, 0.000000000000000000 ) ) ;
#31706=ORIENTED_EDGE ( 'NONE', *, *, #24248, .T. ) ;
#31711=CARTESIAN_POINT ( 'NONE',  ( 17.99999999999999645, 0.000000000000000000, 0.000000000000000000 ) ) ;
#31715=AXIS2_PLACEMENT_3D ( 'NONE', #17420, #7558, #774 ) ;
#31717=CIRCLE ( 'NONE', #14285, 58.99999999999998579 ) ;
#31721=DIRECTION ( 'NONE',  ( -1.000000000000000000, 0.000000000000000000, 0.000000000000000000 ) ) ;
#31725=DIRECTION ( 'NONE',  ( 1.000000000000000000, 0.000000000000000000, 0.000000000000000000 ) ) ;
#31728=VERTEX_POINT ( 'NONE', #41820 ) ;
#31729=DIRECTION ( 'NONE',  ( 0.000000000000000000, 0.000000000000000000, -1.000000000000000000 ) ) ;
#31730=CIRCLE ( 'NONE', #35902, 59.00000000000000711 ) ;
#31731=DIRECTION ( 'NONE',  ( -1.000000000000000000, -0.000000000000000000, 0.000000000000000000 ) ) ;
#31733=CARTESIAN_POINT ( 'NONE',  ( 17.99999999999999645, 11.41303419185120482, -111.6154788735834700 ) ) ;
#31736=ORIENTED_EDGE ( 'NONE', *, *, #21329, .T. ) ;
#31738=EDGE_CURVE ( 'NONE', #26000, #21350, #2384, .T. ) ;
#31740=DIRECTION ( 'NONE',  ( 1.000000000000000000, 0.000000000000000000, 0.000000000000000000 ) ) ;
#31741=CIRCLE ( 'NONE', #16421, 116.0000000000000000 ) ;
#31743=AXIS2_PLACEMENT_3D ( 'NONE', #26364, #19191, #39630 ) ;
#31744=VERTEX_POINT ( 'NONE', #12395 ) ;
#31745=AXIS2_PLACEMENT_3D ( 'NONE', #35257, #18747, #28096 ) ;
#31749=AXIS2_PLACEMENT_3D ( 'NONE', #42468, #13261, #39188 ) ;
#31750=ORIENTED_EDGE ( 'NONE', *, *, #33042, .T. ) ;
#31753=LINE ( 'NONE', #1410, #18255 ) ;
#31756=ORIENTED_EDGE ( 'NONE', *, *, #10930, .F. ) ;
#31758=CARTESIAN_POINT ( 'NONE',  ( 17.99999999999999645, -35.72777019205596361, -106.3569410558020962 ) ) ;
#31760=DIRECTION ( 'NONE',  ( 0.000000000000000000, -0.9826841245925190815, -0.1852887240871243513 ) ) ;
#31770=ORIENTED_EDGE ( 'NONE', *, *, #1347, .T. ) ;
#31771=CIRCLE ( 'NONE', #3848, 120.5010000000000332 ) ;
#31772=CIRCLE ( 'NONE', #1090, 58.99999999999999289 ) ;
#31775=LINE ( 'NONE', #29155, #1006 ) ;
#31778=EDGE_LOOP ( 'NONE', ( #8217, #11770, #19031, #42407 ) ) ;
#31779=CARTESIAN_POINT ( 'NONE',  ( 9.000000000000001776, -31.17727234463623631, -111.7317219465823115 ) ) ;
#31780=AXIS2_PLACEMENT_3D ( 'NONE', #24603, #35232, #28520 ) ;
#31783=AXIS2_PLACEMENT_3D ( 'NONE', #41952, #3460, #6962 ) ;
#31786=CARTESIAN_POINT ( 'NONE',  ( 17.99999999999999645, 0.000000000000000000, 0.000000000000000000 ) ) ;
#31790=FACE_OUTER_BOUND ( 'NONE', #17849, .T. ) ;
#31792=CARTESIAN_POINT ( 'NONE',  ( 17.99999999999999645, 0.000000000000000000, 0.000000000000000000 ) ) ;
#31795=ORIENTED_EDGE ( 'NONE', *, *, #31701, .F. ) ;
#31797=ORIENTED_EDGE ( 'NONE', *, *, #8944, .F. ) ;
#31798=CARTESIAN_POINT ( 'NONE',  ( 17.99999999999999645, 0.000000000000000000, 0.000000000000000000 ) ) ;
#31801=EDGE_LOOP ( 'NONE', ( #20596, #2345, #14172, #10326 ) ) ;
#31804=CIRCLE ( 'NONE', #27632, 116.0000000000000000 ) ;
#31806=AXIS2_PLACEMENT_3D ( 'NONE', #8668, #22452, #14820 ) ;
#31807=DIRECTION ( 'NONE',  ( 0.000000000000000000, 0.7865515558026394682, 0.6175246149461958156 ) ) ;
#31812=DIRECTION ( 'NONE',  ( 0.000000000000000000, 0.3641605752528168649, 0.9313361774523405412 ) ) ;
#31816=AXIS2_PLACEMENT_3D ( 'NONE', #19070, #12924, #22554 ) ;
#31817=AXIS2_PLACEMENT_3D ( 'NONE', #37928, #17479, #24017 ) ;
#31818=FACE_OUTER_BOUND ( 'NONE', #10607, .T. ) ;
#31819=CARTESIAN_POINT ( 'NONE',  ( 0.000000000000000000, -35.54274411428134073, 115.1399337407605259 ) ) ;
#31820=ORIENTED_EDGE ( 'NONE', *, *, #39111, .T. ) ;
#31821=DIRECTION ( 'NONE',  ( 0.000000000000000000, 0.000000000000000000, 1.000000000000000000 ) ) ;
#31822=EDGE_CURVE ( 'NONE', #38233, #41436, #24036, .T. ) ;
#31825=DIRECTION ( 'NONE',  ( 1.000000000000000000, 0.000000000000000000, 0.000000000000000000 ) ) ;
#31828=CARTESIAN_POINT ( 'NONE',  ( 0.000000000000000000, -110.1579703617964725, -21.29539948940357164 ) ) ;
#31829=CIRCLE ( 'NONE', #18630, 59.00000000000000000 ) ;
#31830=EDGE_CURVE ( 'NONE', #2394, #17019, #35059, .T. ) ;
#31835=ORIENTED_EDGE ( 'NONE', *, *, #26874, .T. ) ;
#31838=CIRCLE ( 'NONE', #8158, 59.00000000000000000 ) ;
#31840=AXIS2_PLACEMENT_3D ( 'NONE', #19670, #32935, #33744 ) ;
#31843=DIRECTION ( 'NONE',  ( 1.000000000000000000, 0.000000000000000000, 0.000000000000000000 ) ) ;
#31844=AXIS2_PLACEMENT_3D ( 'NONE', #31792, #28741, #24623 ) ;
#31845=CYLINDRICAL_SURFACE ( 'NONE', #24438, 59.00000000000000000 ) ;
#31846=VERTEX_POINT ( 'NONE', #31585 ) ;
#31850=EDGE_LOOP ( 'NONE', ( #12540, #18802, #9719, #3065 ) ) ;
#31855=EDGE_CURVE ( 'NONE', #7746, #40221, #31668, .T. ) ;
#31857=CARTESIAN_POINT ( 'NONE',  ( 9.000000000000001776, 98.69720329640956891, 60.94966826379944536 ) ) ;
#31858=DIRECTION ( 'NONE',  ( -1.000000000000000000, 0.000000000000000000, -0.000000000000000000 ) ) ;
#31859=EDGE_LOOP ( 'NONE', ( #17441, #8526, #25292, #746 ) ) ;
#31864=CARTESIAN_POINT ( 'NONE',  ( 17.99999999999999645, 47.31079789947627745, -105.9135893174946119 ) ) ;
#31865=CIRCLE ( 'NONE', #33936, 59.00000000000000000 ) ;
#31867=DIRECTION ( 'NONE',  ( 0.000000000000000000, 0.000000000000000000, 1.000000000000000000 ) ) ;
#31868=EDGE_LOOP ( 'NONE', ( #25346, #43144, #21409, #29816 ) ) ;
#31869=CIRCLE ( 'NONE', #500, 59.00000000000000000 ) ;
#31871=AXIS2_PLACEMENT_3D ( 'NONE', #7903, #20601, #33872 ) ;
#31873=CYLINDRICAL_SURFACE ( 'NONE', #33601, 120.5010000000000190 ) ;
#31874=ORIENTED_EDGE ( 'NONE', *, *, #31620, .T. ) ;
#31875=CARTESIAN_POINT ( 'NONE',  ( 9.000000000000001776, 41.60679253225764285, 108.2814610871947423 ) ) ;
#31876=AXIS2_PLACEMENT_3D ( 'NONE', #33484, #23706, #3571 ) ;
#31877=CARTESIAN_POINT ( 'NONE',  ( 17.99999999999999645, 75.03166794516801019, 94.29071961951534320 ) ) ;
#31891=AXIS2_PLACEMENT_3D ( 'NONE', #9448, #22804, #22585 ) ;
#31894=AXIS2_PLACEMENT_3D ( 'NONE', #18145, #40544, #27065 ) ;
#31896=VERTEX_POINT ( 'NONE', #21385 ) ;
#31898=ORIENTED_EDGE ( 'NONE', *, *, #39918, .F. ) ;
#31899=AXIS2_PLACEMENT_3D ( 'NONE', #12927, #40370, #26235 ) ;
#31902=CIRCLE ( 'NONE', #17327, 120.5010000000000474 ) ;
#31905=EDGE_CURVE ( 'NONE', #16730, #34938, #14275, .T. ) ;
#31911=CARTESIAN_POINT ( 'NONE',  ( 17.99999999999999645, 92.25992191227497585, -77.51514567967304004 ) ) ;
#31912=EDGE_LOOP ( 'NONE', ( #6990, #33418, #23251, #490 ) ) ;
#31916=VERTEX_POINT ( 'NONE', #36125 ) ;
#31918=CARTESIAN_POINT ( 'NONE',  ( 0.000000000000000000, 63.55543939553766108, 97.03971415477347762 ) ) ;
#31921=CARTESIAN_POINT ( 'NONE',  ( 9.000000000000001776, -115.9750404417044223, 2.406240749597103434 ) ) ;
#31927=DIRECTION ( 'NONE',  ( 0.000000000000000000, 0.000000000000000000, 1.000000000000000000 ) ) ;
#31930=AXIS2_PLACEMENT_3D ( 'NONE', #32404, #41994, #41578 ) ;
#31932=EDGE_CURVE ( 'NONE', #14426, #9049, #30042, .T. ) ;
#31933=VECTOR ( 'NONE', #1825, 1000.000000000000000 ) ;
#31934=ORIENTED_EDGE ( 'NONE', *, *, #14326, .F. ) ;
#31937=ADVANCED_FACE ( 'NONE', ( #12597 ), #16751, .F. ) ;
#31938=DIRECTION ( 'NONE',  ( -1.000000000000000000, -0.000000000000000000, -0.000000000000000000 ) ) ;
#31940=VERTEX_POINT ( 'NONE', #29834 ) ;
#31949=CARTESIAN_POINT ( 'NONE',  ( -10.00000000000000000, 0.000000000000000000, 0.000000000000000000 ) ) ;
#31950=ORIENTED_EDGE ( 'NONE', *, *, #7219, .F. ) ;
#31952=ORIENTED_EDGE ( 'NONE', *, *, #18892, .F. ) ;
#31953=DIRECTION ( 'NONE',  ( 0.000000000000000000, 0.8993121301712173610, 0.4373073204588593388 ) ) ;
#31958=CARTESIAN_POINT ( 'NONE',  ( 0.000000000000000000, -117.6086855750636460, 26.24286718912064487 ) ) ;
#31961=DIRECTION ( 'NONE',  ( 0.000000000000000000, -0.9213119778704086382, -0.3888241754733309241 ) ) ;
#31963=VERTEX_POINT ( 'NONE', #9941 ) ;
#31964=CIRCLE ( 'NONE', #26416, 59.00000000000000000 ) ;
#31967=AXIS2_PLACEMENT_3D ( 'NONE', #6378, #19949, #3515 ) ;
#31969=DIRECTION ( 'NONE',  ( -1.000000000000000000, -0.000000000000000000, -0.000000000000000000 ) ) ;
#31970=ORIENTED_EDGE ( 'NONE', *, *, #34295, .F. ) ;
#31975=VERTEX_POINT ( 'NONE', #42877 ) ;
#31977=CYLINDRICAL_SURFACE ( 'NONE', #37400, 59.00000000000000000 ) ;
#31978=LINE ( 'NONE', #1631, #34520 ) ;
#31979=ORIENTED_EDGE ( 'NONE', *, *, #4888, .F. ) ;
#31980=CARTESIAN_POINT ( 'NONE',  ( 17.99999999999999645, -29.36437154451924059, -116.8684075565139295 ) ) ;
#31983=DIRECTION ( 'NONE',  ( 0.000000000000000000, 0.000000000000000000, 1.000000000000000000 ) ) ;
#31993=CARTESIAN_POINT ( 'NONE',  ( 17.99999999999999645, 18.35539002514383711, 110.6858262410710410 ) ) ;
#32002=DIRECTION ( 'NONE',  ( 0.000000000000000000, 0.05322217484217219019, 0.9985826956767622775 ) ) ;
#32003=ORIENTED_EDGE ( 'NONE', *, *, #27934, .T. ) ;
#32004=EDGE_CURVE ( 'NONE', #38581, #41253, #24766, .T. ) ;
#32006=DIRECTION ( 'NONE',  ( 0.000000000000000000, -0.1062934856473523454, -0.9943348002101385363 ) ) ;
#32007=ORIENTED_EDGE ( 'NONE', *, *, #19819, .F. ) ;
#32008=CARTESIAN_POINT ( 'NONE',  ( 17.99999999999999645, -75.03166794516862126, 94.29071961951481740 ) ) ;
#32012=ORIENTED_EDGE ( 'NONE', *, *, #24388, .F. ) ;
#32015=DIRECTION ( 'NONE',  ( 0.000000000000000000, -0.2113826236296113270, -0.9774033898178695612 ) ) ;
#32017=VECTOR ( 'NONE', #20173, 1000.000000000000000 ) ;
#32020=DIRECTION ( 'NONE',  ( 0.000000000000000000, 0.000000000000000000, 1.000000000000000000 ) ) ;
#32026=EDGE_CURVE ( 'NONE', #11221, #21496, #6609, .T. ) ;
#32027=FACE_OUTER_BOUND ( 'NONE', #1317, .T. ) ;
#32030=DIRECTION ( 'NONE',  ( -1.000000000000000000, -0.000000000000000000, -0.000000000000000000 ) ) ;
#32032=DIRECTION ( 'NONE',  ( 1.000000000000000000, 0.000000000000000000, 0.000000000000000000 ) ) ;
#32033=CARTESIAN_POINT ( 'NONE',  ( 8.999999999999998224, -83.58328028049714931, 80.43528614701294543 ) ) ;
#32036=DIRECTION ( 'NONE',  ( 0.000000000000000000, 0.7525707698561399095, -0.6585113790650372056 ) ) ;
#32046=CARTESIAN_POINT ( 'NONE',  ( 17.99999999999999645, -88.56657216608662964, 68.87840567545892156 ) ) ;
#32049=DIRECTION ( 'NONE',  ( 0.000000000000000000, 0.000000000000000000, 1.000000000000000000 ) ) ;
#32052=CYLINDRICAL_SURFACE ( 'NONE', #26087, 59.00000000000000711 ) ;
#32058=DIRECTION ( 'NONE',  ( 0.000000000000000000, -0.6382441836448262684, 0.7698339834299010587 ) ) ;
#32059=EDGE_LOOP ( 'NONE', ( #14890, #23549, #13993, #27451 ) ) ;
#32061=ADVANCED_FACE ( 'NONE', ( #22655 ), #35899, .F. ) ;
#32064=EDGE_CURVE ( 'NONE', #2350, #32806, #35875, .T. ) ;
#32067=AXIS2_PLACEMENT_3D ( 'NONE', #29966, #37285, #29748 ) ;
#32068=ORIENTED_EDGE ( 'NONE', *, *, #5348, .F. ) ;
#32069=CARTESIAN_POINT ( 'NONE',  ( 17.99999999999999645, 12.43843445475471832, -111.5058645182328405 ) ) ;
#32070=AXIS2_PLACEMENT_3D ( 'NONE', #13924, #23536, #30912 ) ;
#32073=AXIS2_PLACEMENT_3D ( 'NONE', #38429, #37786, #14486 ) ;
#32078=FACE_OUTER_BOUND ( 'NONE', #14286, .T. ) ;
#32082=CARTESIAN_POINT ( 'NONE',  ( 0.000000000000000000, 27.83061035786954918, 117.2431154827798281 ) ) ;
#32083=DIRECTION ( 'NONE',  ( -1.000000000000000000, -0.000000000000000000, -0.000000000000000000 ) ) ;
#32085=DIRECTION ( 'NONE',  ( -1.000000000000000000, -0.000000000000000000, -0.000000000000000000 ) ) ;
#32087=EDGE_CURVE ( 'NONE', #41253, #34763, #16386, .T. ) ;
#32095=AXIS2_PLACEMENT_3D ( 'NONE', #31373, #1456, #42021 ) ;
#32097=DIRECTION ( 'NONE',  ( 0.000000000000000000, 0.000000000000000000, 1.000000000000000000 ) ) ;
#32098=CARTESIAN_POINT ( 'NONE',  ( 17.99999999999999645, 0.000000000000000000, 0.000000000000000000 ) ) ;
#32099=VECTOR ( 'NONE', #12228, 1000.000000000000000 ) ;
#32101=DIRECTION ( 'NONE',  ( -1.000000000000000000, -0.000000000000000000, -0.000000000000000000 ) ) ;
#32103=EDGE_CURVE ( 'NONE', #21287, #14763, #27539, .T. ) ;
#32104=EDGE_LOOP ( 'NONE', ( #19904, #13524, #12990, #12559 ) ) ;
#32110=CARTESIAN_POINT ( 'NONE',  ( 17.99999999999999645, -87.74575819880118388, -75.87280091124561920 ) ) ;
#32113=ORIENTED_EDGE ( 'NONE', *, *, #13591, .T. ) ;
#32114=ADVANCED_FACE ( 'NONE', ( #40025 ), #24984, .F. ) ;
#32116=DIRECTION ( 'NONE',  ( -1.000000000000000000, -0.000000000000000000, -0.000000000000000000 ) ) ;
#32118=ORIENTED_EDGE ( 'NONE', *, *, #27351, .T. ) ;
#32120=CIRCLE ( 'NONE', #29, 120.5010000000000332 ) ;
#32121=CARTESIAN_POINT ( 'NONE',  ( 17.99999999999999645, -107.2885202478269946, 54.86040852957277281 ) ) ;
#32122=ORIENTED_EDGE ( 'NONE', *, *, #41850, .T. ) ;
#32123=CARTESIAN_POINT ( 'NONE',  ( 17.99999999999999645, 98.39501399267960835, 53.91376164787712355 ) ) ;
#32125=AXIS2_PLACEMENT_3D ( 'NONE', #22819, #6190, #12548 ) ;
#32129=CIRCLE ( 'NONE', #34234, 116.0000000000000000 ) ;
#32130=LINE ( 'NONE', #24549, #15798 ) ;
#32131=DIRECTION ( 'NONE',  ( 1.000000000000000000, 0.000000000000000000, 0.000000000000000000 ) ) ;
#32135=AXIS2_PLACEMENT_3D ( 'NONE', #15948, #16151, #42080 ) ;
#32136=EDGE_LOOP ( 'NONE', ( #29090, #4880, #19655, #6798 ) ) ;
#32137=CARTESIAN_POINT ( 'NONE',  ( 0.000000000000000000, -34.74871106919551522, -106.6808302961375148 ) ) ;
#32138=EDGE_CURVE ( 'NONE', #27302, #30882, #5223, .T. ) ;
#32140=ORIENTED_EDGE ( 'NONE', *, *, #30681, .T. ) ;
#32144=ORIENTED_EDGE ( 'NONE', *, *, #19851, .F. ) ;
#32148=CARTESIAN_POINT ( 'NONE',  ( 17.99999999999999645, 0.000000000000000000, 0.000000000000000000 ) ) ;
#32149=EDGE_CURVE ( 'NONE', #27071, #29862, #36987, .T. ) ;
#32150=DIRECTION ( 'NONE',  ( 0.000000000000000000, 0.000000000000000000, 1.000000000000000000 ) ) ;
#32153=ORIENTED_EDGE ( 'NONE', *, *, #37368, .F. ) ;
#32154=CARTESIAN_POINT ( 'NONE',  ( 0.000000000000000000, 83.49789599728902090, -86.88263557826680028 ) ) ;
#32158=LINE ( 'NONE', #9024, #22860 ) ;
#32163=EDGE_CURVE ( 'NONE', #36189, #40193, #13464, .T. ) ;
#32164=AXIS2_PLACEMENT_3D ( 'NONE', #28919, #24649, #14170 ) ;
#32167=ORIENTED_EDGE ( 'NONE', *, *, #9084, .T. ) ;
#32169=EDGE_CURVE ( 'NONE', #3831, #25049, #25473, .T. ) ;
#32171=DIRECTION ( 'NONE',  ( 0.000000000000000000, -0.9968120070307493474, -0.07978610555309334496 ) ) ;
#32174=ORIENTED_EDGE ( 'NONE', *, *, #8131, .T. ) ;
#32180=LINE ( 'NONE', #32815, #14737 ) ;
#32188=EDGE_CURVE ( 'NONE', #30917, #12490, #5924, .T. ) ;
#32190=CARTESIAN_POINT ( 'NONE',  ( 17.99999999999999645, 57.69704296431325474, -105.7900857083224224 ) ) ;
#32193=EDGE_CURVE ( 'NONE', #1690, #5524, #24540, .T. ) ;
#32195=DIRECTION ( 'NONE',  ( 0.000000000000000000, 0.000000000000000000, 1.000000000000000000 ) ) ;
#32201=DIRECTION ( 'NONE',  ( 0.000000000000000000, -0.9996456111234529596, 0.02662052143776450636 ) ) ;
#32203=DIRECTION ( 'NONE',  ( -1.000000000000000000, -0.000000000000000000, -0.000000000000000000 ) ) ;
#32207=ORIENTED_EDGE ( 'NONE', *, *, #14322, .F. ) ;
#32209=VERTEX_POINT ( 'NONE', #14707 ) ;
#32210=CARTESIAN_POINT ( 'NONE',  ( 17.99999999999999645, -69.90696807222417419, -98.15042952503588936 ) ) ;
#32211=FACE_OUTER_BOUND ( 'NONE', #37617, .T. ) ;
#32212=AXIS2_PLACEMENT_3D ( 'NONE', #23788, #36842, #3445 ) ;
#32213=CARTESIAN_POINT ( 'NONE',  ( 17.99999999999999645, -112.1427988504407551, -3.502162136924565239 ) ) ;
#32214=CIRCLE ( 'NONE', #14836, 59.00000000000000000 ) ;
#32221=CARTESIAN_POINT ( 'NONE',  ( 0.000000000000000000, 0.000000000000000000, 0.000000000000000000 ) ) ;
#32222=ORIENTED_EDGE ( 'NONE', *, *, #5243, .T. ) ;
#32228=DIRECTION ( 'NONE',  ( 0.000000000000000000, 1.881733940042637923E-15, -1.000000000000000000 ) ) ;
#32229=CARTESIAN_POINT ( 'NONE',  ( 17.99999999999999645, 0.000000000000000000, 0.000000000000000000 ) ) ;
#32230=CYLINDRICAL_SURFACE ( 'NONE', #31806, 120.5010000000000190 ) ;
#32231=VERTEX_POINT ( 'NONE', #31918 ) ;
#32233=VERTEX_POINT ( 'NONE', #32121 ) ;
#32234=CYLINDRICAL_SURFACE ( 'NONE', #25311, 59.00000000000000000 ) ;
#32235=FACE_OUTER_BOUND ( 'NONE', #8691, .T. ) ;
#32237=ORIENTED_EDGE ( 'NONE', *, *, #23747, .F. ) ;
#32239=ORIENTED_EDGE ( 'NONE', *, *, #39664, .F. ) ;
#32240=EDGE_CURVE ( 'NONE', #31896, #35898, #17819, .T. ) ;
#32247=ORIENTED_EDGE ( 'NONE', *, *, #32138, .F. ) ;
#32251=ORIENTED_EDGE ( 'NONE', *, *, #12968, .F. ) ;
#32256=DIRECTION ( 'NONE',  ( 0.000000000000000000, 0.000000000000000000, 1.000000000000000000 ) ) ;
#32257=DIRECTION ( 'NONE',  ( 0.000000000000000000, 0.000000000000000000, 1.000000000000000000 ) ) ;
#32258=ORIENTED_EDGE ( 'NONE', *, *, #3528, .F. ) ;
#32259=DIRECTION ( 'NONE',  ( 0.000000000000000000, 0.000000000000000000, 1.000000000000000000 ) ) ;
#32267=EDGE_CURVE ( 'NONE', #43001, #20513, #28944, .T. ) ;
#32269=ORIENTED_EDGE ( 'NONE', *, *, #16677, .F. ) ;
#32271=ORIENTED_EDGE ( 'NONE', *, *, #26794, .T. ) ;
#32272=DIRECTION ( 'NONE',  ( 0.000000000000000000, 0.000000000000000000, 1.000000000000000000 ) ) ;
#32273=CARTESIAN_POINT ( 'NONE',  ( 17.99999999999999645, -35.72777019205596361, -106.3569410558020962 ) ) ;
#32278=DIRECTION ( 'NONE',  ( -1.000000000000000000, 0.000000000000000000, 0.000000000000000000 ) ) ;
#32280=CIRCLE ( 'NONE', #26031, 59.00000000000000000 ) ;
#32281=CARTESIAN_POINT ( 'NONE',  ( -10.00000000000000000, 0.000000000000000000, 0.000000000000000000 ) ) ;
#32285=DIRECTION ( 'NONE',  ( -1.000000000000000000, -0.000000000000000000, -0.000000000000000000 ) ) ;
#32290=DIRECTION ( 'NONE',  ( -1.000000000000000000, 0.000000000000000000, 0.000000000000000000 ) ) ;
#32292=EDGE_LOOP ( 'NONE', ( #3738, #28054, #40328, #15257 ) ) ;
#32293=ADVANCED_FACE ( 'NONE', ( #28858 ), #12497, .F. ) ;
#32297=CIRCLE ( 'NONE', #41345, 120.5010000000000190 ) ;
#32298=FACE_OUTER_BOUND ( 'NONE', #39184, .T. ) ;
#32300=LINE ( 'NONE', #5481, #33255 ) ;
#32301=EDGE_CURVE ( 'NONE', #24349, #5717, #15359, .T. ) ;
#32305=EDGE_LOOP ( 'NONE', ( #16920, #12225, #4598, #27454 ) ) ;
#32310=ORIENTED_EDGE ( 'NONE', *, *, #23210, .F. ) ;
#32315=CIRCLE ( 'NONE', #12131, 120.5010000000000474 ) ;
#32316=EDGE_CURVE ( 'NONE', #16818, #7516, #26841, .T. ) ;
#32317=VERTEX_POINT ( 'NONE', #5915 ) ;
#32319=CARTESIAN_POINT ( 'NONE',  ( 17.99999999999999645, 89.07460286905958924, -81.15544420874873310 ) ) ;
#32321=ORIENTED_EDGE ( 'NONE', *, *, #12794, .T. ) ;
#32325=VERTEX_POINT ( 'NONE', #2630 ) ;
#32326=CARTESIAN_POINT ( 'NONE',  ( 17.99999999999999645, 0.000000000000000000, 0.000000000000000000 ) ) ;
#32327=AXIS2_PLACEMENT_3D ( 'NONE', #4791, #4552, #20982 ) ;
#32330=DIRECTION ( 'NONE',  ( -1.000000000000000000, -0.000000000000000000, -0.000000000000000000 ) ) ;
#32331=CARTESIAN_POINT ( 'NONE',  ( 17.99999999999999645, 0.000000000000000000, 0.000000000000000000 ) ) ;
#32339=AXIS2_PLACEMENT_3D ( 'NONE', #28186, #41240, #15111 ) ;
#32340=ORIENTED_EDGE ( 'NONE', *, *, #31561, .T. ) ;
#32341=CARTESIAN_POINT ( 'NONE',  ( 0.000000000000000000, 51.98489025774451733, -108.7109110710156159 ) ) ;
#32348=EDGE_LOOP ( 'NONE', ( #21396, #31419, #32916, #34889 ) ) ;
#32349=AXIS2_PLACEMENT_3D ( 'NONE', #23908, #27382, #37176 ) ;
#32350=ORIENTED_EDGE ( 'NONE', *, *, #30974, .T. ) ;
#32351=DIRECTION ( 'NONE',  ( -1.000000000000000000, -0.000000000000000000, -0.000000000000000000 ) ) ;
#32353=CARTESIAN_POINT ( 'NONE',  ( 17.99999999999999645, -84.09610293794118263, 74.27057253242982426 ) ) ;
#32354=VECTOR ( 'NONE', #25108, 1000.000000000000000 ) ;
#32356=CARTESIAN_POINT ( 'NONE',  ( 0.000000000000000000, -2.418575551220017328, -120.4767259403369053 ) ) ;
#32357=CYLINDRICAL_SURFACE ( 'NONE', #2054, 59.00000000000000000 ) ;
#32358=AXIS2_PLACEMENT_3D ( 'NONE', #29175, #12586, #22002 ) ;
#32360=DIRECTION ( 'NONE',  ( 0.000000000000000000, 0.000000000000000000, 1.000000000000000000 ) ) ;
#32361=EDGE_LOOP ( 'NONE', ( #33854, #17855, #41639, #6194 ) ) ;
#32362=DIRECTION ( 'NONE',  ( -1.000000000000000000, -0.000000000000000000, -0.000000000000000000 ) ) ;
#32365=DIRECTION ( 'NONE',  ( 1.000000000000000000, 0.000000000000000000, 0.000000000000000000 ) ) ;
#32366=ORIENTED_EDGE ( 'NONE', *, *, #21450, .T. ) ;
#32368=ORIENTED_EDGE ( 'NONE', *, *, #8602, .F. ) ;
#32372=ORIENTED_EDGE ( 'NONE', *, *, #17193, .T. ) ;
#32376=VERTEX_POINT ( 'NONE', #5506 ) ;
#32377=EDGE_CURVE ( 'NONE', #21133, #13162, #17070, .T. ) ;
#32381=CIRCLE ( 'NONE', #10810, 120.5010000000000332 ) ;
#32382=ORIENTED_EDGE ( 'NONE', *, *, #21032, .F. ) ;
#32385=DIRECTION ( 'NONE',  ( -1.000000000000000000, 0.000000000000000000, 0.000000000000000000 ) ) ;
#32387=AXIS2_PLACEMENT_3D ( 'NONE', #8216, #1216, #7983 ) ;
#32393=CIRCLE ( 'NONE', #7307, 120.5010000000000190 ) ;
#32394=DIRECTION ( 'NONE',  ( 0.000000000000000000, -0.05322217484218558226, 0.9985826956767615004 ) ) ;
#32399=ORIENTED_EDGE ( 'NONE', *, *, #10949, .T. ) ;
#32400=AXIS2_PLACEMENT_3D ( 'NONE', #31711, #25406, #38664 ) ;
#32401=LINE ( 'NONE', #25684, #40020 ) ;
#32404=CARTESIAN_POINT ( 'NONE',  ( 0.000000000000000000, 0.000000000000000000, 0.000000000000000000 ) ) ;
#32409=AXIS2_PLACEMENT_3D ( 'NONE', #19694, #3484, #26008 ) ;
#32410=CARTESIAN_POINT ( 'NONE',  ( 17.99999999999999645, 17.77780072541695944, 114.6296200873376563 ) ) ;
#32413=CYLINDRICAL_SURFACE ( 'NONE', #4695, 116.0000000000000000 ) ;
#32415=DIRECTION ( 'NONE',  ( -1.000000000000000000, 0.000000000000000000, 0.000000000000000000 ) ) ;
#32416=VECTOR ( 'NONE', #23120, 1000.000000000000000 ) ;
#32417=CIRCLE ( 'NONE', #2464, 59.00000000000000711 ) ;
#32418=CARTESIAN_POINT ( 'NONE',  ( 17.99999999999999645, 35.78484819117785776, -110.3423972910429143 ) ) ;
#32419=CARTESIAN_POINT ( 'NONE',  ( 17.99999999999999645, 0.000000000000000000, 0.000000000000000000 ) ) ;
#32420=VERTEX_POINT ( 'NONE', #432 ) ;
#32421=LINE ( 'NONE', #5386, #42566 ) ;
#32422=CYLINDRICAL_SURFACE ( 'NONE', #8843, 59.00000000000000000 ) ;
#32423=AXIS2_PLACEMENT_3D ( 'NONE', #7736, #21097, #21315 ) ;
#32425=ORIENTED_EDGE ( 'NONE', *, *, #23368, .F. ) ;
#32428=ADVANCED_FACE ( 'NONE', ( #23397 ), #6349, .F. ) ;
#32429=DIRECTION ( 'NONE',  ( 0.000000000000000000, 0.000000000000000000, 1.000000000000000000 ) ) ;
#32431=EDGE_CURVE ( 'NONE', #42007, #15552, #10494, .T. ) ;
#32433=ORIENTED_EDGE ( 'NONE', *, *, #16677, .T. ) ;
#32434=ORIENTED_EDGE ( 'NONE', *, *, #39892, .T. ) ;
#32435=CARTESIAN_POINT ( 'NONE',  ( 9.000000000000001776, 41.60679253225906393, -108.2814610871942165 ) ) ;
#32438=CARTESIAN_POINT ( 'NONE',  ( 0.000000000000000000, -110.3490479609630910, -20.28201389785511211 ) ) ;
#32441=CIRCLE ( 'NONE', #26876, 120.5010000000000190 ) ;
#32442=CARTESIAN_POINT ( 'NONE',  ( 17.99999999999999645, 34.03109950475727175, 115.5957406979051285 ) ) ;
#32443=VERTEX_POINT ( 'NONE', #36658 ) ;
#32447=DIRECTION ( 'NONE',  ( 1.000000000000000000, 0.000000000000000000, 0.000000000000000000 ) ) ;
#32448=DIRECTION ( 'NONE',  ( 1.000000000000000000, 0.000000000000000000, 0.000000000000000000 ) ) ;
#32450=DIRECTION ( 'NONE',  ( 1.000000000000000000, 0.000000000000000000, 0.000000000000000000 ) ) ;
#32454=CARTESIAN_POINT ( 'NONE',  ( 17.99999999999999645, -117.9424311864587480, -24.69967462999156638 ) ) ;
#32456=ADVANCED_FACE ( 'NONE', ( #2833 ), #33185, .F. ) ;
#32458=EDGE_CURVE ( 'NONE', #29185, #18549, #30364, .T. ) ;
#32459=CARTESIAN_POINT ( 'NONE',  ( 8.999999999999998224, -74.56001736500559218, -88.86396238369110279 ) ) ;
#32466=DIRECTION ( 'NONE',  ( -1.000000000000000000, -0.000000000000000000, -0.000000000000000000 ) ) ;
#32469=DIRECTION ( 'NONE',  ( 0.000000000000000000, 0.1062934856473655293, -0.9943348002101370930 ) ) ;
#32472=DIRECTION ( 'NONE',  ( 1.000000000000000000, 0.000000000000000000, 0.000000000000000000 ) ) ;
#32477=CARTESIAN_POINT ( 'NONE',  ( 17.99999999999999645, -104.2166695095716591, 60.49278301857773243 ) ) ;
#32478=EDGE_LOOP ( 'NONE', ( #31970, #2510, #21119, #32003 ) ) ;
#32480=EDGE_CURVE ( 'NONE', #39282, #5822, #23623, .T. ) ;
#32482=EDGE_CURVE ( 'NONE', #12118, #24229, #25507, .T. ) ;
#32483=EDGE_CURVE ( 'NONE', #10144, #5055, #6783, .T. ) ;
#32485=ORIENTED_EDGE ( 'NONE', *, *, #14881, .T. ) ;
#32486=EDGE_CURVE ( 'NONE', #27767, #17459, #42168, .T. ) ;
#32489=DIRECTION ( 'NONE',  ( -1.000000000000000000, 0.000000000000000000, -0.000000000000000000 ) ) ;
#32490=ORIENTED_EDGE ( 'NONE', *, *, #21622, .T. ) ;
#32492=CARTESIAN_POINT ( 'NONE',  ( 17.99999999999999645, -92.25992191227339845, -77.51514567967485902 ) ) ;
#32494=CARTESIAN_POINT ( 'NONE',  ( 17.99999999999999645, 0.000000000000000000, 0.000000000000000000 ) ) ;
#32500=AXIS2_PLACEMENT_3D ( 'NONE', #12293, #33571, #30313 ) ;
#32501=VERTEX_POINT ( 'NONE', #36434 ) ;
#32502=FACE_OUTER_BOUND ( 'NONE', #17192, .T. ) ;
#32504=CARTESIAN_POINT ( 'NONE',  ( 17.99999999999999645, 0.000000000000000000, 0.000000000000000000 ) ) ;
#32508=CIRCLE ( 'NONE', #42926, 120.5010000000000190 ) ;
#32509=DIRECTION ( 'NONE',  ( 1.000000000000000000, 0.000000000000000000, 0.000000000000000000 ) ) ;
#32511=CIRCLE ( 'NONE', #25579, 116.0000000000000000 ) ;
#32516=LINE ( 'NONE', #42529, #33226 ) ;
#32518=DIRECTION ( 'NONE',  ( -1.000000000000000000, -0.000000000000000000, -0.000000000000000000 ) ) ;
#32523=CYLINDRICAL_SURFACE ( 'NONE', #35483, 58.99999999999998579 ) ;
#32524=CARTESIAN_POINT ( 'NONE',  ( 9.000000000000001776, 111.2559044912529345, -32.83479428644565701 ) ) ;
#32527=CARTESIAN_POINT ( 'NONE',  ( 0.000000000000000000, 0.000000000000000000, 0.000000000000000000 ) ) ;
#32528=CARTESIAN_POINT ( 'NONE',  ( 0.000000000000000000, -116.0452958106478434, -32.46506308663576590 ) ) ;
#32529=EDGE_CURVE ( 'NONE', #36025, #24485, #2453, .T. ) ;
#32530=ORIENTED_EDGE ( 'NONE', *, *, #17271, .T. ) ;
#32536=CARTESIAN_POINT ( 'NONE',  ( 17.99999999999999645, -115.0622509503833442, 14.72000021165104755 ) ) ;
#32542=CARTESIAN_POINT ( 'NONE',  ( -10.00000000000000000, 0.000000000000000000, 0.000000000000000000 ) ) ;
#32548=AXIS2_PLACEMENT_3D ( 'NONE', #14930, #38239, #17784 ) ;
#32550=ADVANCED_FACE ( 'NONE', ( #10706 ), #31438, .F. ) ;
#32552=LINE ( 'NONE', #9412, #3203 ) ;
#32554=VERTEX_POINT ( 'NONE', #3918 ) ;
#32557=DIRECTION ( 'NONE',  ( 0.000000000000000000, 0.000000000000000000, 1.000000000000000000 ) ) ;
#32558=DIRECTION ( 'NONE',  ( -1.000000000000000000, -0.000000000000000000, 0.000000000000000000 ) ) ;
#32560=ORIENTED_EDGE ( 'NONE', *, *, #25870, .T. ) ;
#32565=VECTOR ( 'NONE', #36891, 1000.000000000000000 ) ;
#32566=CIRCLE ( 'NONE', #20787, 116.0000000000000000 ) ;
#32574=LINE ( 'NONE', #2656, #19190 ) ;
#32578=DIRECTION ( 'NONE',  ( 0.000000000000000000, 0.000000000000000000, 1.000000000000000000 ) ) ;
#32579=VERTEX_POINT ( 'NONE', #1312 ) ;
#32580=DIRECTION ( 'NONE',  ( -1.000000000000000000, -0.000000000000000000, 0.000000000000000000 ) ) ;
#32582=CYLINDRICAL_SURFACE ( 'NONE', #31891, 59.00000000000000000 ) ;
#32583=EDGE_CURVE ( 'NONE', #6410, #13842, #18545, .T. ) ;
#32586=LINE ( 'NONE', #3523, #29171 ) ;
#32587=ORIENTED_EDGE ( 'NONE', *, *, #1784, .F. ) ;
#32590=VERTEX_POINT ( 'NONE', #20561 ) ;
#32595=CARTESIAN_POINT ( 'NONE',  ( 17.99999999999999645, 5.456439917446431309, -112.0647122740741253 ) ) ;
#32597=ORIENTED_EDGE ( 'NONE', *, *, #26843, .F. ) ;
#32600=CARTESIAN_POINT ( 'NONE',  ( 17.99999999999999645, -35.54274411427983438, -115.1399337407609949 ) ) ;
#32601=ORIENTED_EDGE ( 'NONE', *, *, #41954, .T. ) ;
#32603=CIRCLE ( 'NONE', #11013, 58.99999999999999289 ) ;
#32604=EDGE_CURVE ( 'NONE', #40591, #9049, #31741, .T. ) ;
#32607=CARTESIAN_POINT ( 'NONE',  ( 17.99999999999999645, 59.07817985939002625, 105.0250430397510968 ) ) ;
#32610=LINE ( 'NONE', #42829, #41857 ) ;
#32613=DIRECTION ( 'NONE',  ( -1.000000000000000000, 0.000000000000000000, -0.000000000000000000 ) ) ;
#32615=CYLINDRICAL_SURFACE ( 'NONE', #25374, 59.00000000000000000 ) ;
#32617=CIRCLE ( 'NONE', #8853, 59.00000000000001421 ) ;
#32618=ORIENTED_EDGE ( 'NONE', *, *, #20755, .T. ) ;
#32619=DIRECTION ( 'NONE',  ( 1.000000000000000000, 0.000000000000000000, 0.000000000000000000 ) ) ;
#32620=ADVANCED_FACE ( 'NONE', ( #37741 ), #8079, .F. ) ;
#32622=LINE ( 'NONE', #2702, #14370 ) ;
#32624=CARTESIAN_POINT ( 'NONE',  ( -10.00000000000000000, 0.000000000000000000, 0.000000000000000000 ) ) ;
#32627=CIRCLE ( 'NONE', #29161, 58.99999999999999289 ) ;
#32630=AXIS2_PLACEMENT_3D ( 'NONE', #36808, #36154, #39637 ) ;
#32632=LINE ( 'NONE', #36313, #30538 ) ;
#32636=CARTESIAN_POINT ( 'NONE',  ( 0.000000000000000000, -5.456439917444183330, -112.0647122740742390 ) ) ;
#32637=DIRECTION ( 'NONE',  ( -1.000000000000000000, 0.000000000000000000, 0.000000000000000000 ) ) ;
#32640=CARTESIAN_POINT ( 'NONE',  ( 0.000000000000000000, -107.5680526044917542, -31.89649718262205269 ) ) ;
#32641=ADVANCED_FACE ( 'NONE', ( #4577 ), #17952, .F. ) ;
#32642=CARTESIAN_POINT ( 'NONE',  ( 9.000000000000001776, -107.1354928292872728, 44.47455650398029547 ) ) ;
#32644=CARTESIAN_POINT ( 'NONE',  ( -10.00000000000000000, 0.000000000000000000, 0.000000000000000000 ) ) ;
#32645=VERTEX_POINT ( 'NONE', #18172 ) ;
#32647=CARTESIAN_POINT ( 'NONE',  ( 8.999999999999998224, 83.58328028049660929, 80.43528614701352808 ) ) ;
#32652=VERTEX_POINT ( 'NONE', #14870 ) ;
#32656=CARTESIAN_POINT ( 'NONE',  ( 17.99999999999999645, 0.000000000000000000, 0.000000000000000000 ) ) ;
#32657=EDGE_CURVE ( 'NONE', #26052, #32990, #24277, .T. ) ;
#32663=DIRECTION ( 'NONE',  ( -1.000000000000000000, -0.000000000000000000, 0.000000000000000000 ) ) ;
#32664=ORIENTED_EDGE ( 'NONE', *, *, #2722, .F. ) ;
#32665=DIRECTION ( 'NONE',  ( -1.000000000000000000, 0.000000000000000000, 0.000000000000000000 ) ) ;
#32669=VERTEX_POINT ( 'NONE', #38182 ) ;
#32670=CARTESIAN_POINT ( 'NONE',  ( 17.99999999999999645, -103.4151313792866489, -61.85306461934516875 ) ) ;
#32672=EDGE_CURVE ( 'NONE', #31034, #21299, #14214, .T. ) ;
#32673=CARTESIAN_POINT ( 'NONE',  ( 17.99999999999999645, -104.6166166098448826, 50.11350645393640235 ) ) ;
#32674=EDGE_LOOP ( 'NONE', ( #21001, #10098, #20898, #41093 ) ) ;
#32676=EDGE_CURVE ( 'NONE', #17317, #30034, #42851, .T. ) ;
#32679=ORIENTED_EDGE ( 'NONE', *, *, #38829, .T. ) ;
#32680=DIRECTION ( 'NONE',  ( -1.000000000000000000, -0.000000000000000000, -0.000000000000000000 ) ) ;
#32686=ORIENTED_EDGE ( 'NONE', *, *, #32486, .F. ) ;
#32687=DIRECTION ( 'NONE',  ( -1.000000000000000000, 0.000000000000000000, 0.000000000000000000 ) ) ;
#32693=VERTEX_POINT ( 'NONE', #38391 ) ;
#32694=CARTESIAN_POINT ( 'NONE',  ( 0.000000000000000000, 0.000000000000000000, 0.000000000000000000 ) ) ;
#32696=ORIENTED_EDGE ( 'NONE', *, *, #24865, .T. ) ;
#32698=VERTEX_POINT ( 'NONE', #8720 ) ;
#32700=EDGE_LOOP ( 'NONE', ( #21584, #42189, #17594, #40905 ) ) ;
#32701=DIRECTION ( 'NONE',  ( -1.000000000000000000, 0.000000000000000000, -0.000000000000000000 ) ) ;
#32704=CARTESIAN_POINT ( 'NONE',  ( 0.000000000000000000, 42.87700105098607395, 107.7847984684006377 ) ) ;
#32707=CYLINDRICAL_SURFACE ( 'NONE', #9822, 120.5010000000000190 ) ;
#32709=CIRCLE ( 'NONE', #39048, 59.00000000000000000 ) ;
#32715=CIRCLE ( 'NONE', #23597, 120.5010000000000332 ) ;
#32716=CARTESIAN_POINT ( 'NONE',  ( 17.99999999999999645, 0.000000000000000000, 0.000000000000000000 ) ) ;
#32719=ADVANCED_FACE ( 'NONE', ( #11815 ), #25140, .F. ) ;
#32724=ADVANCED_FACE ( 'NONE', ( #18601 ), #12232, .F. ) ;
#32728=DIRECTION ( 'NONE',  ( -1.000000000000000000, -0.000000000000000000, -0.000000000000000000 ) ) ;
#32733=CIRCLE ( 'NONE', #668, 58.99999999999999289 ) ;
#32737=CIRCLE ( 'NONE', #12554, 59.00000000000000711 ) ;
#32739=DIRECTION ( 'NONE',  ( 1.000000000000000000, 0.000000000000000000, 0.000000000000000000 ) ) ;
#32740=ORIENTED_EDGE ( 'NONE', *, *, #26730, .T. ) ;
#32741=DIRECTION ( 'NONE',  ( 0.000000000000000000, -0.7865515558026479059, 0.6175246149461850464 ) ) ;
#32742=VERTEX_POINT ( 'NONE', #35336 ) ;
#32744=DIRECTION ( 'NONE',  ( 0.000000000000000000, 0.000000000000000000, 1.000000000000000000 ) ) ;
#32746=ORIENTED_EDGE ( 'NONE', *, *, #1976, .F. ) ;
#32747=CARTESIAN_POINT ( 'NONE',  ( 17.99999999999999645, 0.000000000000000000, 0.000000000000000000 ) ) ;
#32748=EDGE_CURVE ( 'NONE', #22186, #27071, #31772, .T. ) ;
#32750=DIRECTION ( 'NONE',  ( -1.000000000000000000, -0.000000000000000000, 0.000000000000000000 ) ) ;
#32753=DIRECTION ( 'NONE',  ( 1.000000000000000000, 0.000000000000000000, 0.000000000000000000 ) ) ;
#32755=AXIS2_PLACEMENT_3D ( 'NONE', #3452, #23583, #39675 ) ;
#32756=DIRECTION ( 'NONE',  ( -1.000000000000000000, 0.000000000000000000, 0.000000000000000000 ) ) ;
#32757=CYLINDRICAL_SURFACE ( 'NONE', #21291, 59.00000000000000000 ) ;
#32758=DIRECTION ( 'NONE',  ( 1.000000000000000000, 0.000000000000000000, 0.000000000000000000 ) ) ;
#32759=ORIENTED_EDGE ( 'NONE', *, *, #25053, .F. ) ;
#32763=ORIENTED_EDGE ( 'NONE', *, *, #23264, .F. ) ;
#32768=ORIENTED_EDGE ( 'NONE', *, *, #17361, .T. ) ;
#32769=EDGE_CURVE ( 'NONE', #33431, #36528, #1956, .T. ) ;
#32779=CYLINDRICAL_SURFACE ( 'NONE', #33906, 116.0000000000000000 ) ;
#32780=DIRECTION ( 'NONE',  ( 1.000000000000000000, 0.000000000000000000, 0.000000000000000000 ) ) ;
#32782=CYLINDRICAL_SURFACE ( 'NONE', #6972, 116.0000000000000000 ) ;
#32785=VERTEX_POINT ( 'NONE', #9147 ) ;
#32787=DIRECTION ( 'NONE',  ( -1.000000000000000000, 0.000000000000000000, 0.000000000000000000 ) ) ;
#32788=EDGE_CURVE ( 'NONE', #27036, #11189, #2485, .T. ) ;
#32789=CIRCLE ( 'NONE', #24493, 116.0000000000000000 ) ;
#32791=DIRECTION ( 'NONE',  ( 0.000000000000000000, -0.9407002666710296834, -0.3392388661180399945 ) ) ;
#32792=VERTEX_POINT ( 'NONE', #8299 ) ;
#32798=FACE_OUTER_BOUND ( 'NONE', #16771, .T. ) ;
#32806=VERTEX_POINT ( 'NONE', #8946 ) ;
#32811=CYLINDRICAL_SURFACE ( 'NONE', #1506, 120.5010000000000190 ) ;
#32812=DIRECTION ( 'NONE',  ( 0.000000000000000000, -0.5076658003388467844, 0.8615540813938020737 ) ) ;
#32814=EDGE_LOOP ( 'NONE', ( #25782, #22689, #9029, #5912 ) ) ;
#32815=CARTESIAN_POINT ( 'NONE',  ( 17.99999999999999645, 120.4984140710909344, -0.7894348306988416830 ) ) ;
#32817=CARTESIAN_POINT ( 'NONE',  ( 17.99999999999999645, 0.000000000000000000, 0.000000000000000000 ) ) ;
#32820=CYLINDRICAL_SURFACE ( 'NONE', #35140, 120.5010000000000190 ) ;
#32822=ORIENTED_EDGE ( 'NONE', *, *, #21843, .T. ) ;
#32825=DIRECTION ( 'NONE',  ( 1.000000000000000000, -0.000000000000000000, -0.000000000000000000 ) ) ;
#32831=DIRECTION ( 'NONE',  ( 1.000000000000000000, 0.000000000000000000, 0.000000000000000000 ) ) ;
#32835=AXIS2_PLACEMENT_3D ( 'NONE', #11462, #21100, #4900 ) ;
#32841=EDGE_LOOP ( 'NONE', ( #4408, #28441, #31570, #3554 ) ) ;
#32842=VECTOR ( 'NONE', #37588, 1000.000000000000000 ) ;
#32843=DIRECTION ( 'NONE',  ( 0.000000000000000000, -0.1590634960190596414, -0.9872683547213465527 ) ) ;
#32845=CARTESIAN_POINT ( 'NONE',  ( 17.99999999999999645, 105.7179949885867956, -37.57629584241721687 ) ) ;
#32848=DIRECTION ( 'NONE',  ( 1.000000000000000000, -0.000000000000000000, -0.000000000000000000 ) ) ;
#32849=FACE_OUTER_BOUND ( 'NONE', #13022, .T. ) ;
#32850=CARTESIAN_POINT ( 'NONE',  ( 17.99999999999999645, -41.33768078145432412, -104.3046912715545318 ) ) ;
#32852=ORIENTED_EDGE ( 'NONE', *, *, #16579, .F. ) ;
#32857=ORIENTED_EDGE ( 'NONE', *, *, #34966, .F. ) ;
#32858=DIRECTION ( 'NONE',  ( 1.000000000000000000, 0.000000000000000000, 0.000000000000000000 ) ) ;
#32859=AXIS2_PLACEMENT_3D ( 'NONE', #42, #13410, #39972 ) ;
#32860=EDGE_CURVE ( 'NONE', #35004, #43080, #25538, .T. ) ;
#32863=LINE ( 'NONE', #3384, #11844 ) ;
#32864=AXIS2_PLACEMENT_3D ( 'NONE', #11970, #28760, #27907 ) ;
#32865=DIRECTION ( 'NONE',  ( -1.000000000000000000, 0.000000000000000000, -0.000000000000000000 ) ) ;
#32866=AXIS2_PLACEMENT_3D ( 'NONE', #40658, #953, #37405 ) ;
#32869=DIRECTION ( 'NONE',  ( -1.000000000000000000, 0.000000000000000000, -0.000000000000000000 ) ) ;
#32870=VERTEX_POINT ( 'NONE', #152 ) ;
#32872=CARTESIAN_POINT ( 'NONE',  ( -10.00000000000000000, 0.000000000000000000, 0.000000000000000000 ) ) ;
#32877=CARTESIAN_POINT ( 'NONE',  ( 0.000000000000000000, 74.56001736500736854, -88.86396238368961065 ) ) ;
#32880=DIRECTION ( 'NONE',  ( 0.000000000000000000, -1.246648735278247733E-14, -1.000000000000000000 ) ) ;
#32881=ORIENTED_EDGE ( 'NONE', *, *, #6924, .T. ) ;
#32887=ORIENTED_EDGE ( 'NONE', *, *, #10832, .T. ) ;
#32888=AXIS2_PLACEMENT_3D ( 'NONE', #40573, #29940, #10708 ) ;
#32889=DIRECTION ( 'NONE',  ( -1.000000000000000000, 0.000000000000000000, 0.000000000000000000 ) ) ;
#32892=LINE ( 'NONE', #16332, #32416 ) ;
#32893=CIRCLE ( 'NONE', #38462, 116.0000000000000000 ) ;
#32895=ORIENTED_EDGE ( 'NONE', *, *, #10611, .T. ) ;
#32897=CARTESIAN_POINT ( 'NONE',  ( -10.00000000000000000, 0.000000000000000000, 0.000000000000000000 ) ) ;
#32898=ORIENTED_EDGE ( 'NONE', *, *, #14298, .T. ) ;
#32903=ORIENTED_EDGE ( 'NONE', *, *, #14931, .T. ) ;
#32904=CARTESIAN_POINT ( 'NONE',  ( 17.99999999999999645, -73.51007459736368332, -89.73443560133438268 ) ) ;
#32906=ORIENTED_EDGE ( 'NONE', *, *, #25722, .T. ) ;
#32907=ORIENTED_EDGE ( 'NONE', *, *, #27841, .F. ) ;
#32909=EDGE_CURVE ( 'NONE', #38864, #25476, #36836, .T. ) ;
#32910=ORIENTED_EDGE ( 'NONE', *, *, #30013, .F. ) ;
#32912=DIRECTION ( 'NONE',  ( 0.000000000000000000, -0.6382441836448108363, -0.7698339834299139373 ) ) ;
#32913=EDGE_CURVE ( 'NONE', #35004, #30836, #7396, .T. ) ;
#32914=CARTESIAN_POINT ( 'NONE',  ( 17.99999999999999645, 111.9370513079669394, 44.61600100275212100 ) ) ;
#32915=FACE_OUTER_BOUND ( 'NONE', #30874, .T. ) ;
#32916=ORIENTED_EDGE ( 'NONE', *, *, #22730, .T. ) ;
#32922=DIRECTION ( 'NONE',  ( 0.000000000000000000, 0.000000000000000000, 1.000000000000000000 ) ) ;
#32923=ORIENTED_EDGE ( 'NONE', *, *, #18243, .F. ) ;
#32924=CARTESIAN_POINT ( 'NONE',  ( 0.000000000000000000, 111.9370513079669394, 44.61600100275212100 ) ) ;
#32926=DIRECTION ( 'NONE',  ( 1.000000000000000000, 0.000000000000000000, 0.000000000000000000 ) ) ;
#32931=EDGE_LOOP ( 'NONE', ( #25383, #12394, #20334, #31151 ) ) ;
#32935=DIRECTION ( 'NONE',  ( -1.000000000000000000, -0.000000000000000000, -0.000000000000000000 ) ) ;
#32938=ADVANCED_FACE ( 'NONE', ( #32915 ), #6299, .F. ) ;
#32944=CYLINDRICAL_SURFACE ( 'NONE', #10333, 120.5010000000000190 ) ;
#32945=LINE ( 'NONE', #32524, #31224 ) ;
#32946=ORIENTED_EDGE ( 'NONE', *, *, #3285, .T. ) ;
#32949=ORIENTED_EDGE ( 'NONE', *, *, #40981, .F. ) ;
#32950=DIRECTION ( 'NONE',  ( 1.000000000000000000, 0.000000000000000000, 0.000000000000000000 ) ) ;
#32951=ORIENTED_EDGE ( 'NONE', *, *, #42840, .F. ) ;
#32954=LINE ( 'NONE', #33394, #16745 ) ;
#32955=EDGE_CURVE ( 'NONE', #34051, #13299, #15770, .T. ) ;
#32958=DIRECTION ( 'NONE',  ( 0.000000000000000000, 9.408669700213189617E-16, -1.000000000000000000 ) ) ;
#32961=EDGE_CURVE ( 'NONE', #39267, #37232, #23348, .T. ) ;
#32964=VERTEX_POINT ( 'NONE', #16149 ) ;
#32965=CARTESIAN_POINT ( 'NONE',  ( 17.99999999999999645, 0.000000000000000000, 0.000000000000000000 ) ) ;
#32968=CARTESIAN_POINT ( 'NONE',  ( 17.99999999999999645, 57.40245293794799153, -96.40140491896575270 ) ) ;
#32970=CYLINDRICAL_SURFACE ( 'NONE', #6804, 59.00000000000000000 ) ;
#32975=FACE_OUTER_BOUND ( 'NONE', #15073, .T. ) ;
#32977=VERTEX_POINT ( 'NONE', #42712 ) ;
#32982=EDGE_CURVE ( 'NONE', #33745, #6849, #4586, .T. ) ;
#32983=CIRCLE ( 'NONE', #16291, 116.0000000000000000 ) ;
#32984=ORIENTED_EDGE ( 'NONE', *, *, #29179, .T. ) ;
#32986=FACE_OUTER_BOUND ( 'NONE', #31868, .T. ) ;
#32989=CARTESIAN_POINT ( 'NONE',  ( 0.000000000000000000, 110.3490479609632615, 38.71798610214565173 ) ) ;
#32990=VERTEX_POINT ( 'NONE', #9586 ) ;
#32994=DIRECTION ( 'NONE',  ( 1.000000000000000000, -0.000000000000000000, 0.000000000000000000 ) ) ;
#32996=DIRECTION ( 'NONE',  ( -1.000000000000000000, -0.000000000000000000, -0.000000000000000000 ) ) ;
#33002=CYLINDRICAL_SURFACE ( 'NONE', #11441, 59.00000000000000000 ) ;
#33004=ORIENTED_EDGE ( 'NONE', *, *, #2717, .T. ) ;
#33005=CARTESIAN_POINT ( 'NONE',  ( 17.99999999999999645, 97.89532456239497549, 54.81585448086229917 ) ) ;
#33008=ORIENTED_EDGE ( 'NONE', *, *, #31932, .F. ) ;
#33010=EDGE_CURVE ( 'NONE', #42002, #40772, #5284, .T. ) ;
#33017=EDGE_LOOP ( 'NONE', ( #34182, #7930, #34901, #39064 ) ) ;
#33019=CARTESIAN_POINT ( 'NONE',  ( 0.000000000000000000, 51.27532863109503580, -99.79535634195073612 ) ) ;
#33021=CYLINDRICAL_SURFACE ( 'NONE', #15740, 59.00000000000001421 ) ;
#33023=DIRECTION ( 'NONE',  ( 0.000000000000000000, 0.1590634960190655256, 0.9872683547213456645 ) ) ;
#33029=EDGE_CURVE ( 'NONE', #34279, #37209, #12965, .T. ) ;
#33031=DIRECTION ( 'NONE',  ( -1.000000000000000000, -0.000000000000000000, -0.000000000000000000 ) ) ;
#33036=AXIS2_PLACEMENT_3D ( 'NONE', #32419, #5794, #38524 ) ;
#33042=EDGE_CURVE ( 'NONE', #27124, #6594, #8086, .T. ) ;
#33044=EDGE_LOOP ( 'NONE', ( #31473, #1527, #40406, #30949 ) ) ;
#33047=CIRCLE ( 'NONE', #14267, 116.0000000000000000 ) ;
#33048=DIRECTION ( 'NONE',  ( -1.000000000000000000, -0.000000000000000000, -0.000000000000000000 ) ) ;
#33050=DIRECTION ( 'NONE',  ( -1.000000000000000000, 0.000000000000000000, -0.000000000000000000 ) ) ;
#33053=CIRCLE ( 'NONE', #13593, 58.99999999999999289 ) ;
#33055=VECTOR ( 'NONE', #10887, 1000.000000000000000 ) ;
#33056=DIRECTION ( 'NONE',  ( 1.000000000000000000, 0.000000000000000000, 0.000000000000000000 ) ) ;
#33060=EDGE_CURVE ( 'NONE', #27794, #34636, #7596, .T. ) ;
#33063=CIRCLE ( 'NONE', #24073, 59.00000000000000711 ) ;
#33067=CIRCLE ( 'NONE', #13602, 58.99999999999999289 ) ;
#33068=ORIENTED_EDGE ( 'NONE', *, *, #15831, .F. ) ;
#33072=DIRECTION ( 'NONE',  ( 0.000000000000000000, 0.000000000000000000, 1.000000000000000000 ) ) ;
#33073=DIRECTION ( 'NONE',  ( -1.000000000000000000, 0.000000000000000000, 0.000000000000000000 ) ) ;
#33077=ADVANCED_FACE ( 'NONE', ( #37261 ), #17247, .F. ) ;
#33078=AXIS2_PLACEMENT_3D ( 'NONE', #38449, #8569, #21928 ) ;
#33080=DIRECTION ( 'NONE',  ( -1.000000000000000000, -0.000000000000000000, -0.000000000000000000 ) ) ;
#33084=CYLINDRICAL_SURFACE ( 'NONE', #42013, 116.0000000000000000 ) ;
#33088=VECTOR ( 'NONE', #34958, 1000.000000000000000 ) ;
#33089=DIRECTION ( 'NONE',  ( 1.000000000000000000, 0.000000000000000000, 0.000000000000000000 ) ) ;
#33097=AXIS2_PLACEMENT_3D ( 'NONE', #12144, #5576, #32195 ) ;
#33099=AXIS2_PLACEMENT_3D ( 'NONE', #29758, #10321, #29536 ) ;
#33100=ORIENTED_EDGE ( 'NONE', *, *, #23365, .F. ) ;
#33106=ORIENTED_EDGE ( 'NONE', *, *, #33439, .F. ) ;
#33107=CARTESIAN_POINT ( 'NONE',  ( 17.99999999999999645, 0.000000000000000000, 0.000000000000000000 ) ) ;
#33108=ORIENTED_EDGE ( 'NONE', *, *, #26730, .F. ) ;
#33114=DIRECTION ( 'NONE',  ( 0.000000000000000000, 0.000000000000000000, 1.000000000000000000 ) ) ;
#33115=DIRECTION ( 'NONE',  ( 0.000000000000000000, 0.9714298932647090767, 0.2373266998711184850 ) ) ;
#33119=ORIENTED_EDGE ( 'NONE', *, *, #19171, .F. ) ;
#33121=EDGE_CURVE ( 'NONE', #17019, #28172, #38753, .T. ) ;
#33122=AXIS2_PLACEMENT_3D ( 'NONE', #24295, #20577, #33850 ) ;
#33123=ORIENTED_EDGE ( 'NONE', *, *, #14303, .T. ) ;
#33125=ORIENTED_EDGE ( 'NONE', *, *, #5374, .F. ) ;
#33130=AXIS2_PLACEMENT_3D ( 'NONE', #10170, #32448, #16545 ) ;
#33131=AXIS2_PLACEMENT_3D ( 'NONE', #11132, #24458, #21418 ) ;
#33133=DIRECTION ( 'NONE',  ( 0.000000000000000000, -0.9574220383620080099, 0.2886919473396124536 ) ) ;
#33134=ORIENTED_EDGE ( 'NONE', *, *, #10225, .T. ) ;
#33142=ORIENTED_EDGE ( 'NONE', *, *, #24227, .F. ) ;
#33144=EDGE_CURVE ( 'NONE', #26640, #18784, #13720, .T. ) ;
#33147=DIRECTION ( 'NONE',  ( 1.000000000000000000, 0.000000000000000000, 0.000000000000000000 ) ) ;
#33150=EDGE_LOOP ( 'NONE', ( #31934, #6290, #28598, #41268 ) ) ;
#33154=VECTOR ( 'NONE', #39449, 1000.000000000000000 ) ;
#33155=VECTOR ( 'NONE', #15003, 1000.000000000000000 ) ;
#33156=EDGE_CURVE ( 'NONE', #35643, #13412, #6028, .T. ) ;
#33159=VECTOR ( 'NONE', #4784, 1000.000000000000000 ) ;
#33163=AXIS2_PLACEMENT_3D ( 'NONE', #22697, #6077, #15136 ) ;
#33166=LINE ( 'NONE', #29922, #23692 ) ;
#33167=DIRECTION ( 'NONE',  ( -1.000000000000000000, 0.000000000000000000, -0.000000000000000000 ) ) ;
#33168=EDGE_LOOP ( 'NONE', ( #15641, #24759, #30611, #12579 ) ) ;
#33169=CARTESIAN_POINT ( 'NONE',  ( 17.99999999999999645, 101.1249659627855806, -48.60055280209454054 ) ) ;
#33170=CARTESIAN_POINT ( 'NONE',  ( 17.99999999999999645, 0.6819280456829140968, 115.9979955608738749 ) ) ;
#33175=VERTEX_POINT ( 'NONE', #1686 ) ;
#33176=DIRECTION ( 'NONE',  ( -1.000000000000000000, -0.000000000000000000, -0.000000000000000000 ) ) ;
#33180=AXIS2_PLACEMENT_3D ( 'NONE', #21282, #31496, #28664 ) ;
#33183=EDGE_CURVE ( 'NONE', #9004, #5428, #38130, .T. ) ;
#33184=CIRCLE ( 'NONE', #9521, 120.5010000000000474 ) ;
#33185=CYLINDRICAL_SURFACE ( 'NONE', #21345, 59.00000000000000000 ) ;
#33189=EDGE_CURVE ( 'NONE', #37254, #26682, #25299, .T. ) ;
#33190=CIRCLE ( 'NONE', #16496, 116.0000000000000000 ) ;
#33193=ADVANCED_FACE ( 'NONE', ( #15673 ), #12401, .F. ) ;
#33194=CARTESIAN_POINT ( 'NONE',  ( 17.99999999999999645, 0.000000000000000000, 0.000000000000000000 ) ) ;
#33196=CIRCLE ( 'NONE', #3206, 116.0000000000000000 ) ;
#33199=ORIENTED_EDGE ( 'NONE', *, *, #16565, .F. ) ;
#33200=CIRCLE ( 'NONE', #2497, 58.99999999999999289 ) ;
#33202=ORIENTED_EDGE ( 'NONE', *, *, #12637, .F. ) ;
#33203=CARTESIAN_POINT ( 'NONE',  ( 0.000000000000000000, -101.1403355683150096, 56.80345518653453496 ) ) ;
#33209=VERTEX_POINT ( 'NONE', #31819 ) ;
#33210=ORIENTED_EDGE ( 'NONE', *, *, #42606, .T. ) ;
#33211=FACE_OUTER_BOUND ( 'NONE', #1356, .T. ) ;
#33213=EDGE_CURVE ( 'NONE', #8627, #2881, #28563, .T. ) ;
#33214=CIRCLE ( 'NONE', #18640, 58.99999999999999289 ) ;
#33216=ADVANCED_FACE ( 'NONE', ( #38544 ), #32230, .F. ) ;
#33218=CARTESIAN_POINT ( 'NONE',  ( -10.00000000000000000, 0.000000000000000000, 0.000000000000000000 ) ) ;
#33219=CIRCLE ( 'NONE', #6061, 59.00000000000000711 ) ;
#33221=VERTEX_POINT ( 'NONE', #11769 ) ;
#33224=CARTESIAN_POINT ( 'NONE',  ( 0.000000000000000000, 58.30069736313667050, 100.2847380560568951 ) ) ;
#33226=VECTOR ( 'NONE', #1001, 1000.000000000000000 ) ;
#33228=( GEOMETRIC_REPRESENTATION_CONTEXT ( 3 ) GLOBAL_UNCERTAINTY_ASSIGNED_CONTEXT ( ( #309 ) ) GLOBAL_UNIT_ASSIGNED_CONTEXT ( ( #5379, #4731, #21996 ) ) REPRESENTATION_CONTEXT ( 'NONE', 'WORKASPACE' ) );
#33229=CARTESIAN_POINT ( 'NONE',  ( 17.99999999999999645, 112.1427988504408404, -3.502162136922268409 ) ) ;
#33230=DIRECTION ( 'NONE',  ( 0.000000000000000000, 0.000000000000000000, 1.000000000000000000 ) ) ;
#33231=VERTEX_POINT ( 'NONE', #41384 ) ;
#33233=ORIENTED_EDGE ( 'NONE', *, *, #7623, .F. ) ;
#33236=EDGE_LOOP ( 'NONE', ( #765, #8762, #35022, #5753 ) ) ;
#33239=AXIS2_PLACEMENT_3D ( 'NONE', #31758, #1852, #9896 ) ;
#33241=ORIENTED_EDGE ( 'NONE', *, *, #12641, .T. ) ;
#33243=ORIENTED_EDGE ( 'NONE', *, *, #16393, .T. ) ;
#33252=DIRECTION ( 'NONE',  ( -1.000000000000000000, -0.000000000000000000, 0.000000000000000000 ) ) ;
#33255=VECTOR ( 'NONE', #29263, 1000.000000000000000 ) ;
#33257=VECTOR ( 'NONE', #19053, 1000.000000000000000 ) ;
#33261=DIRECTION ( 'NONE',  ( 0.000000000000000000, 0.000000000000000000, 1.000000000000000000 ) ) ;
#33263=AXIS2_PLACEMENT_3D ( 'NONE', #26735, #30023, #20881 ) ;
#33264=VERTEX_POINT ( 'NONE', #42247 ) ;
#33265=AXIS2_PLACEMENT_3D ( 'NONE', #34278, #14231, #24509 ) ;
#33267=EDGE_CURVE ( 'NONE', #31975, #2667, #35974, .T. ) ;
#33269=DIRECTION ( 'NONE',  ( 1.000000000000000000, 0.000000000000000000, 0.000000000000000000 ) ) ;
#33270=CARTESIAN_POINT ( 'NONE',  ( 17.99999999999999645, 110.0562500189205224, -49.07252625220001363 ) ) ;
#33273=ADVANCED_FACE ( 'NONE', ( #18975 ), #28769, .F. ) ;
#33274=EDGE_CURVE ( 'NONE', #26169, #34763, #22793, .T. ) ;
#33275=FACE_OUTER_BOUND ( 'NONE', #317, .T. ) ;
#33277=LINE ( 'NONE', #26733, #28467 ) ;
#33280=AXIS2_PLACEMENT_3D ( 'NONE', #24, #7239, #236 ) ;
#33282=EDGE_CURVE ( 'NONE', #29453, #821, #33184, .T. ) ;
#33285=ORIENTED_EDGE ( 'NONE', *, *, #13054, .F. ) ;
#33290=AXIS2_PLACEMENT_3D ( 'NONE', #21945, #28688, #21739 ) ;
#33291=DIRECTION ( 'NONE',  ( 0.000000000000000000, -0.8993121301712143634, -0.4373073204588656115 ) ) ;
#33292=ORIENTED_EDGE ( 'NONE', *, *, #12084, .F. ) ;
#33294=CARTESIAN_POINT ( 'NONE',  ( 0.000000000000000000, 23.10276247328255650, -118.2656051737067600 ) ) ;
#33295=AXIS2_PLACEMENT_3D ( 'NONE', #41257, #18414, #14691 ) ;
#33296=DIRECTION ( 'NONE',  ( 0.000000000000000000, 0.6382441836448160544, 0.7698339834299096074 ) ) ;
#33297=ORIENTED_EDGE ( 'NONE', *, *, #19349, .F. ) ;
#33298=ORIENTED_EDGE ( 'NONE', *, *, #11977, .F. ) ;
#33304=CARTESIAN_POINT ( 'NONE',  ( 8.999999999999998224, -74.56001736500675747, 88.86396238369010803 ) ) ;
#33307=ORIENTED_EDGE ( 'NONE', *, *, #2354, .T. ) ;
#33309=FACE_OUTER_BOUND ( 'NONE', #40398, .T. ) ;
#33314=CIRCLE ( 'NONE', #32630, 116.0000000000000000 ) ;
#33319=CIRCLE ( 'NONE', #14538, 120.5010000000000190 ) ;
#33326=EDGE_CURVE ( 'NONE', #25300, #25826, #6890, .T. ) ;
#33328=DIRECTION ( 'NONE',  ( -1.000000000000000000, -0.000000000000000000, -0.000000000000000000 ) ) ;
#33331=VERTEX_POINT ( 'NONE', #23515 ) ;
#33333=CARTESIAN_POINT ( 'NONE',  ( 17.99999999999999645, -84.77518783075045405, -73.49448960231443095 ) ) ;
#33335=DIRECTION ( 'NONE',  ( 0.000000000000000000, 0.000000000000000000, -1.000000000000000000 ) ) ;
#33336=VERTEX_POINT ( 'NONE', #16307 ) ;
#33337=DIRECTION ( 'NONE',  ( -1.000000000000000000, -0.000000000000000000, -0.000000000000000000 ) ) ;
#33338=EDGE_LOOP ( 'NONE', ( #7853, #42503, #29933, #34955 ) ) ;
#33339=CARTESIAN_POINT ( 'NONE',  ( 17.99999999999999645, 40.37724737310070111, 104.6802291180868565 ) ) ;
#33343=ORIENTED_EDGE ( 'NONE', *, *, #31055, .F. ) ;
#33347=CARTESIAN_POINT ( 'NONE',  ( 0.000000000000000000, 41.62036691425530677, 113.0850832732715787 ) ) ;
#33349=ORIENTED_EDGE ( 'NONE', *, *, #5504, .F. ) ;
#33350=ORIENTED_EDGE ( 'NONE', *, *, #32004, .F. ) ;
#33352=VERTEX_POINT ( 'NONE', #39394 ) ;
#33356=CARTESIAN_POINT ( 'NONE',  ( 17.99999999999999645, 3.996885678773026029, 120.4346956066682424 ) ) ;
#33357=CARTESIAN_POINT ( 'NONE',  ( 0.000000000000000000, 97.89532456239568603, -54.81585448086097045 ) ) ;
#33363=EDGE_LOOP ( 'NONE', ( #21027, #7010, #38587, #32485 ) ) ;
#33365=DIRECTION ( 'NONE',  ( 0.000000000000000000, 0.7525707698561396874, -0.6585113790650372056 ) ) ;
#33366=SHAPE_DEFINITION_REPRESENTATION ( #12683, #19391 ) ;
#33367=DIRECTION ( 'NONE',  ( 1.000000000000000000, 0.000000000000000000, 0.000000000000000000 ) ) ;
#33372=EDGE_CURVE ( 'NONE', #5717, #17009, #24159, .T. ) ;
#33374=CIRCLE ( 'NONE', #40332, 120.5010000000000190 ) ;
#33379=FACE_OUTER_BOUND ( 'NONE', #24684, .T. ) ;
#33386=ORIENTED_EDGE ( 'NONE', *, *, #6837, .F. ) ;
#33387=EDGE_CURVE ( 'NONE', #29060, #24778, #14404, .T. ) ;
#33394=CARTESIAN_POINT ( 'NONE',  ( 8.999999999999998224, -64.69195966009822030, -96.28577441832322847 ) ) ;
#33398=AXIS2_PLACEMENT_3D ( 'NONE', #12334, #41969, #39124 ) ;
#33399=CIRCLE ( 'NONE', #26436, 116.0000000000000000 ) ;
#33403=VERTEX_POINT ( 'NONE', #22889 ) ;
#33410=DIRECTION ( 'NONE',  ( 0.000000000000000000, -0.8183027759081622499, -0.5747874102144165942 ) ) ;
#33411=DIRECTION ( 'NONE',  ( -1.000000000000000000, -0.000000000000000000, 0.000000000000000000 ) ) ;
#33416=CARTESIAN_POINT ( 'NONE',  ( 17.99999999999999645, 111.1352304691229733, -15.40237066878481720 ) ) ;
#33418=ORIENTED_EDGE ( 'NONE', *, *, #20319, .F. ) ;
#33421=EDGE_CURVE ( 'NONE', #7262, #8485, #13470, .T. ) ;
#33424=VECTOR ( 'NONE', #2077, 1000.000000000000000 ) ;
#33426=CYLINDRICAL_SURFACE ( 'NONE', #26228, 59.00000000000000000 ) ;
#33427=DIRECTION ( 'NONE',  ( -1.000000000000000000, -0.000000000000000000, -0.000000000000000000 ) ) ;
#33431=VERTEX_POINT ( 'NONE', #16539 ) ;
#33433=ORIENTED_EDGE ( 'NONE', *, *, #36048, .F. ) ;
#33434=CARTESIAN_POINT ( 'NONE',  ( -10.00000000000000000, 1.592040838891559450E-14, -130.0000000000000000 ) ) ;
#33435=CARTESIAN_POINT ( 'NONE',  ( 17.99999999999999645, 11.41303419185120482, -111.6154788735834700 ) ) ;
#33437=CARTESIAN_POINT ( 'NONE',  ( 17.99999999999999645, -17.77780072541623113, -114.6296200873377842 ) ) ;
#33438=CARTESIAN_POINT ( 'NONE',  ( 0.000000000000000000, 35.54274411428215075, -115.1399337407602701 ) ) ;
#33439=EDGE_CURVE ( 'NONE', #19109, #5464, #42232, .T. ) ;
#33440=ORIENTED_EDGE ( 'NONE', *, *, #40638, .T. ) ;
#33441=CARTESIAN_POINT ( 'NONE',  ( 17.99999999999999645, 82.63181128086733906, 81.41243003647002752 ) ) ;
#33442=ORIENTED_EDGE ( 'NONE', *, *, #12173, .T. ) ;
#33449=DIRECTION ( 'NONE',  ( -1.000000000000000000, -0.000000000000000000, -0.000000000000000000 ) ) ;
#33450=ORIENTED_EDGE ( 'NONE', *, *, #40099, .T. ) ;
#33452=ORIENTED_EDGE ( 'NONE', *, *, #15658, .T. ) ;
#33458=CARTESIAN_POINT ( 'NONE',  ( 17.99999999999999645, 0.000000000000000000, 0.000000000000000000 ) ) ;
#33461=DIRECTION ( 'NONE',  ( 0.000000000000000000, 0.000000000000000000, 1.000000000000000000 ) ) ;
#33463=DIRECTION ( 'NONE',  ( 0.000000000000000000, -0.9826841245925228563, 0.1852887240871046171 ) ) ;
#33465=VERTEX_POINT ( 'NONE', #40469 ) ;
#33468=DIRECTION ( 'NONE',  ( 0.000000000000000000, 0.000000000000000000, -1.000000000000000000 ) ) ;
#33470=ORIENTED_EDGE ( 'NONE', *, *, #20460, .F. ) ;
#33471=ADVANCED_FACE ( 'NONE', ( #27408 ), #24384, .F. ) ;
#33475=CARTESIAN_POINT ( 'NONE',  ( 17.99999999999999645, -103.1672962317648512, -44.09967643725973119 ) ) ;
#33476=CARTESIAN_POINT ( 'NONE',  ( 0.000000000000000000, -29.36437154452078246, 116.8684075565134890 ) ) ;
#33477=CARTESIAN_POINT ( 'NONE',  ( 17.99999999999999645, 0.000000000000000000, 0.000000000000000000 ) ) ;
#33482=EDGE_LOOP ( 'NONE', ( #32664, #1208, #34387, #4467 ) ) ;
#33484=CARTESIAN_POINT ( 'NONE',  ( 17.99999999999999645, -97.89532456239460601, -54.81585448086294576 ) ) ;
#33488=CYLINDRICAL_SURFACE ( 'NONE', #7453, 116.0000000000000000 ) ;
#33489=CIRCLE ( 'NONE', #14718, 120.5010000000000190 ) ;
#33490=DIRECTION ( 'NONE',  ( 0.000000000000000000, 0.000000000000000000, 1.000000000000000000 ) ) ;
#33492=ORIENTED_EDGE ( 'NONE', *, *, #37666, .T. ) ;
#33493=CARTESIAN_POINT ( 'NONE',  ( 17.99999999999999645, -5.492704054967489924, 115.8698847939556202 ) ) ;
#33495=DIRECTION ( 'NONE',  ( 1.000000000000000000, -0.000000000000000000, 0.000000000000000000 ) ) ;
#33496=CARTESIAN_POINT ( 'NONE',  ( 17.99999999999999645, 0.000000000000000000, 0.000000000000000000 ) ) ;
#33497=ORIENTED_EDGE ( 'NONE', *, *, #33274, .F. ) ;
#33500=LINE ( 'NONE', #3585, #14051 ) ;
#33501=ORIENTED_EDGE ( 'NONE', *, *, #26286, .T. ) ;
#33503=CARTESIAN_POINT ( 'NONE',  ( 0.000000000000000000, 46.83041522348636931, -101.9567785075596618 ) ) ;
#33506=EDGE_CURVE ( 'NONE', #41947, #7746, #10604, .T. ) ;
#33507=EDGE_CURVE ( 'NONE', #25878, #6181, #7106, .T. ) ;
#33508=LINE ( 'NONE', #20245, #21494 ) ;
#33519=AXIS2_PLACEMENT_3D ( 'NONE', #7805, #6344, #32958 ) ;
#33521=DIRECTION ( 'NONE',  ( 0.000000000000000000, -0.9911528310040084166, 0.1327255272837126743 ) ) ;
#33522=ORIENTED_EDGE ( 'NONE', *, *, #30582, .F. ) ;
#33523=AXIS2_PLACEMENT_3D ( 'NONE', #30454, #40011, #33700 ) ;
#33525=VERTEX_POINT ( 'NONE', #13905 ) ;
#33529=CARTESIAN_POINT ( 'NONE',  ( 9.000000000000001776, -23.85344185397275041, 113.5209818126990200 ) ) ;
#33535=VERTEX_POINT ( 'NONE', #26986 ) ;
#33538=DIRECTION ( 'NONE',  ( -1.000000000000000000, 0.000000000000000000, 0.000000000000000000 ) ) ;
#33541=ORIENTED_EDGE ( 'NONE', *, *, #17154, .F. ) ;
#33544=DIRECTION ( 'NONE',  ( 0.000000000000000000, 0.000000000000000000, 1.000000000000000000 ) ) ;
#33547=AXIS2_PLACEMENT_3D ( 'NONE', #41058, #4860, #24986 ) ;
#33549=ORIENTED_EDGE ( 'NONE', *, *, #23835, .F. ) ;
#33552=CIRCLE ( 'NONE', #10575, 116.0000000000000000 ) ;
#33553=VERTEX_POINT ( 'NONE', #37846 ) ;
#33555=EDGE_LOOP ( 'NONE', ( #1982, #28814, #12697, #38775 ) ) ;
#33562=EDGE_CURVE ( 'NONE', #8378, #27124, #34369, .T. ) ;
#33566=DIRECTION ( 'NONE',  ( 1.000000000000000000, 0.000000000000000000, -0.000000000000000000 ) ) ;
#33567=DIRECTION ( 'NONE',  ( -1.000000000000000000, 0.000000000000000000, -0.000000000000000000 ) ) ;
#33568=EDGE_CURVE ( 'NONE', #40564, #719, #12922, .T. ) ;
#33569=ORIENTED_EDGE ( 'NONE', *, *, #2813, .F. ) ;
#33570=CARTESIAN_POINT ( 'NONE',  ( 17.99999999999999645, -75.03166794516737070, -94.29071961951585479 ) ) ;
#33571=DIRECTION ( 'NONE',  ( 1.000000000000000000, 0.000000000000000000, 0.000000000000000000 ) ) ;
#33572=VERTEX_POINT ( 'NONE', #4253 ) ;
#33573=DIRECTION ( 'NONE',  ( 0.000000000000000000, 0.000000000000000000, 1.000000000000000000 ) ) ;
#33584=CARTESIAN_POINT ( 'NONE',  ( 17.99999999999999645, 111.8797445107943531, 8.437727291344614855 ) ) ;
#33587=DIRECTION ( 'NONE',  ( -1.000000000000000000, -0.000000000000000000, 0.000000000000000000 ) ) ;
#33589=CARTESIAN_POINT ( 'NONE',  ( 0.000000000000000000, -10.40101730206447961, 120.0512800434970728 ) ) ;
#33595=ORIENTED_EDGE ( 'NONE', *, *, #14398, .T. ) ;
#33596=CARTESIAN_POINT ( 'NONE',  ( 17.99999999999999645, 0.000000000000000000, 0.000000000000000000 ) ) ;
#33598=VERTEX_POINT ( 'NONE', #17836 ) ;
#33599=LINE ( 'NONE', #17058, #5418 ) ;
#33601=AXIS2_PLACEMENT_3D ( 'NONE', #18821, #38186, #1526 ) ;
#33602=ORIENTED_EDGE ( 'NONE', *, *, #40938, .F. ) ;
#33604=CIRCLE ( 'NONE', #11333, 58.99999999999998579 ) ;
#33606=VERTEX_POINT ( 'NONE', #35021 ) ;
#33607=CIRCLE ( 'NONE', #22509, 116.0000000000000000 ) ;
#33609=EDGE_CURVE ( 'NONE', #34488, #19682, #31978, .T. ) ;
#33613=CIRCLE ( 'NONE', #6421, 116.0000000000000000 ) ;
#33614=FACE_OUTER_BOUND ( 'NONE', #5106, .T. ) ;
#33615=FACE_OUTER_BOUND ( 'NONE', #1137, .T. ) ;
#33628=DIRECTION ( 'NONE',  ( -1.000000000000000000, -0.000000000000000000, -0.000000000000000000 ) ) ;
#33631=CIRCLE ( 'NONE', #41287, 116.0000000000000000 ) ;
#33636=CARTESIAN_POINT ( 'NONE',  ( 17.99999999999999645, -83.58328028049713510, 80.43528614701295965 ) ) ;
#33637=EDGE_CURVE ( 'NONE', #41108, #6459, #24199, .T. ) ;
#33638=ORIENTED_EDGE ( 'NONE', *, *, #9084, .F. ) ;
#33640=ORIENTED_EDGE ( 'NONE', *, *, #12353, .F. ) ;
#33641=DIRECTION ( 'NONE',  ( -1.000000000000000000, 0.000000000000000000, -0.000000000000000000 ) ) ;
#33642=EDGE_CURVE ( 'NONE', #37671, #20999, #31047, .T. ) ;
#33643=AXIS2_PLACEMENT_3D ( 'NONE', #36845, #30954, #24230 ) ;
#33645=ORIENTED_EDGE ( 'NONE', *, *, #34572, .F. ) ;
#33649=LINE ( 'NONE', #37353, #24301 ) ;
#33650=ORIENTED_EDGE ( 'NONE', *, *, #24190, .F. ) ;
#33658=EDGE_CURVE ( 'NONE', #12767, #13702, #6636, .T. ) ;
#33659=ORIENTED_EDGE ( 'NONE', *, *, #36093, .F. ) ;
#33660=DIRECTION ( 'NONE',  ( 0.000000000000000000, -0.6382441836448109473, -0.7698339834299138262 ) ) ;
#33664=DIRECTION ( 'NONE',  ( -1.000000000000000000, -0.000000000000000000, -0.000000000000000000 ) ) ;
#33667=ORIENTED_EDGE ( 'NONE', *, *, #28226, .F. ) ;
#33668=CARTESIAN_POINT ( 'NONE',  ( 9.000000000000001776, 5.492704054968225336, -115.8698847939555776 ) ) ;
#33673=CARTESIAN_POINT ( 'NONE',  ( 0.000000000000000000, 0.000000000000000000, 0.000000000000000000 ) ) ;
#33676=EDGE_CURVE ( 'NONE', #28259, #36486, #42162, .T. ) ;
#33680=AXIS2_PLACEMENT_3D ( 'NONE', #23666, #26694, #10092 ) ;
#33681=LINE ( 'NONE', #24119, #34497 ) ;
#33682=EDGE_LOOP ( 'NONE', ( #24962, #36667, #18752, #39921 ) ) ;
#33683=CARTESIAN_POINT ( 'NONE',  ( 8.999999999999998224, -90.81729652456212420, 72.16798910853589177 ) ) ;
#33684=AXIS2_PLACEMENT_3D ( 'NONE', #39290, #31938, #9424 ) ;
#33688=DIRECTION ( 'NONE',  ( 0.000000000000000000, 0.000000000000000000, 1.000000000000000000 ) ) ;
#33697=CYLINDRICAL_SURFACE ( 'NONE', #12911, 59.00000000000000000 ) ;
#33698=ORIENTED_EDGE ( 'NONE', *, *, #32301, .F. ) ;
#33700=DIRECTION ( 'NONE',  ( 0.000000000000000000, 1.881733940042638318E-15, -1.000000000000000000 ) ) ;
#33702=DIRECTION ( 'NONE',  ( 0.000000000000000000, 0.000000000000000000, 1.000000000000000000 ) ) ;
#33703=CARTESIAN_POINT ( 'NONE',  ( 17.99999999999999645, 0.000000000000000000, 0.000000000000000000 ) ) ;
#33705=ORIENTED_EDGE ( 'NONE', *, *, #33988, .F. ) ;
#33711=ORIENTED_EDGE ( 'NONE', *, *, #4324, .F. ) ;
#33712=DIRECTION ( 'NONE',  ( -1.000000000000000000, 0.000000000000000000, 0.000000000000000000 ) ) ;
#33713=DIRECTION ( 'NONE',  ( 1.000000000000000000, 0.000000000000000000, 0.000000000000000000 ) ) ;
#33717=AXIS2_PLACEMENT_3D ( 'NONE', #25149, #12041, #28615 ) ;
#33719=ORIENTED_EDGE ( 'NONE', *, *, #9407, .F. ) ;
#33720=CARTESIAN_POINT ( 'NONE',  ( 17.99999999999999645, 23.21237537461889389, -109.7700237000589709 ) ) ;
#33722=EDGE_CURVE ( 'NONE', #29560, #15632, #33798, .T. ) ;
#33723=CIRCLE ( 'NONE', #32327, 59.00000000000000711 ) ;
#33724=CARTESIAN_POINT ( 'NONE',  ( 0.000000000000000000, 92.10690493017060021, 64.06707842432207656 ) ) ;
#33725=FACE_OUTER_BOUND ( 'NONE', #30722, .T. ) ;
#33726=EDGE_CURVE ( 'NONE', #6952, #26365, #19920, .T. ) ;
#33728=CARTESIAN_POINT ( 'NONE',  ( 17.99999999999999645, -108.8684555192045025, -27.12806418649726936 ) ) ;
#33729=EDGE_LOOP ( 'NONE', ( #28794, #20182, #13880, #22009 ) ) ;
#33733=ORIENTED_EDGE ( 'NONE', *, *, #9429, .T. ) ;
#33737=CARTESIAN_POINT ( 'NONE',  ( 0.000000000000000000, 46.12538073176499154, -111.3235835452206715 ) ) ;
#33741=CARTESIAN_POINT ( 'NONE',  ( 17.99999999999999645, 80.74349901498408144, 77.90224541347306797 ) ) ;
#33743=ORIENTED_EDGE ( 'NONE', *, *, #7405, .F. ) ;
#33744=DIRECTION ( 'NONE',  ( 0.000000000000000000, 0.000000000000000000, -1.000000000000000000 ) ) ;
#33745=VERTEX_POINT ( 'NONE', #31333 ) ;
#33747=CIRCLE ( 'NONE', #20555, 59.00000000000001421 ) ;
#33750=EDGE_CURVE ( 'NONE', #26640, #19094, #5353, .T. ) ;
#33751=EDGE_CURVE ( 'NONE', #21496, #32501, #25046, .T. ) ;
#33752=ADVANCED_FACE ( 'NONE', ( #29143 ), #33021, .F. ) ;
#33753=CIRCLE ( 'NONE', #7275, 116.0000000000000000 ) ;
#33755=ORIENTED_EDGE ( 'NONE', *, *, #20258, .T. ) ;
#33760=CARTESIAN_POINT ( 'NONE',  ( -10.00000000000000000, 0.000000000000000000, 0.000000000000000000 ) ) ;
#33763=FACE_OUTER_BOUND ( 'NONE', #26084, .T. ) ;
#33767=VERTEX_POINT ( 'NONE', #5980 ) ;
#33768=CARTESIAN_POINT ( 'NONE',  ( 0.000000000000000000, 0.000000000000000000, 0.000000000000000000 ) ) ;
#33769=ORIENTED_EDGE ( 'NONE', *, *, #21673, .F. ) ;
#33773=DIRECTION ( 'NONE',  ( 1.000000000000000000, 0.000000000000000000, 0.000000000000000000 ) ) ;
#33775=AXIS2_PLACEMENT_3D ( 'NONE', #14813, #11527, #8246 ) ;
#33778=CYLINDRICAL_SURFACE ( 'NONE', #35269, 116.0000000000000000 ) ;
#33779=VERTEX_POINT ( 'NONE', #42411 ) ;
#33780=ADVANCED_FACE ( 'NONE', ( #26291 ), #26499, .F. ) ;
#33781=CIRCLE ( 'NONE', #21321, 120.5010000000000474 ) ;
#33787=DIRECTION ( 'NONE',  ( -1.000000000000000000, -0.000000000000000000, -0.000000000000000000 ) ) ;
#33789=DIRECTION ( 'NONE',  ( -1.000000000000000000, -0.000000000000000000, -0.000000000000000000 ) ) ;
#33790=DIRECTION ( 'NONE',  ( -1.000000000000000000, -0.000000000000000000, -0.000000000000000000 ) ) ;
#33796=DIRECTION ( 'NONE',  ( 0.000000000000000000, -0.9826841245925227453, 0.1852887240871045060 ) ) ;
#33798=CIRCLE ( 'NONE', #1056, 59.00000000000000000 ) ;
#33799=EDGE_CURVE ( 'NONE', #28297, #23414, #2686, .T. ) ;
#33801=AXIS2_PLACEMENT_3D ( 'NONE', #30146, #23622, #22756 ) ;
#33803=AXIS2_PLACEMENT_3D ( 'NONE', #31451, #41024, #11170 ) ;
#33804=CARTESIAN_POINT ( 'NONE',  ( 18.00000000000000000, 0.000000000000000000, -116.0000000000000000 ) ) ;
#33805=FACE_OUTER_BOUND ( 'NONE', #21813, .T. ) ;
#33806=CIRCLE ( 'NONE', #34524, 120.5010000000000332 ) ;
#33808=EDGE_LOOP ( 'NONE', ( #42749, #17994, #5931, #11662 ) ) ;
#33811=FACE_OUTER_BOUND ( 'NONE', #27636, .T. ) ;
#33814=VECTOR ( 'NONE', #31598, 1000.000000000000000 ) ;
#33815=LINE ( 'NONE', #21203, #7105 ) ;
#33817=ORIENTED_EDGE ( 'NONE', *, *, #34670, .T. ) ;
#33822=DIRECTION ( 'NONE',  ( 0.000000000000000000, 0.000000000000000000, 1.000000000000000000 ) ) ;
#33825=CARTESIAN_POINT ( 'NONE',  ( 17.99999999999999645, 0.000000000000000000, 0.000000000000000000 ) ) ;
#33826=EDGE_LOOP ( 'NONE', ( #28392, #14970, #36790, #34045 ) ) ;
#33828=CARTESIAN_POINT ( 'NONE',  ( 17.99999999999999645, 0.000000000000000000, 0.000000000000000000 ) ) ;
#33832=CYLINDRICAL_SURFACE ( 'NONE', #16932, 59.00000000000000000 ) ;
#33834=CARTESIAN_POINT ( 'NONE',  ( 17.99999999999999645, 111.9370513079675789, -44.61600100275060043 ) ) ;
#33836=ADVANCED_FACE ( 'NONE', ( #39337 ), #12558, .F. ) ;
#33838=AXIS2_PLACEMENT_3D ( 'NONE', #11077, #30907, #28086 ) ;
#33840=CARTESIAN_POINT ( 'NONE',  ( 17.99999999999999645, 25.18647942089742031, 113.2326863338528824 ) ) ;
#33842=ORIENTED_EDGE ( 'NONE', *, *, #36026, .F. ) ;
#33845=CIRCLE ( 'NONE', #25545, 116.0000000000000000 ) ;
#33849=AXIS2_PLACEMENT_3D ( 'NONE', #9502, #42854, #34285 ) ;
#33850=DIRECTION ( 'NONE',  ( 0.000000000000000000, 0.000000000000000000, 1.000000000000000000 ) ) ;
#33854=ORIENTED_EDGE ( 'NONE', *, *, #34945, .T. ) ;
#33855=CARTESIAN_POINT ( 'NONE',  ( 0.000000000000000000, -48.55277268144259040, -105.3500273609084843 ) ) ;
#33857=ADVANCED_FACE ( 'NONE', ( #6199 ), #35854, .F. ) ;
#33862=VERTEX_POINT ( 'NONE', #16260 ) ;
#33866=DIRECTION ( 'NONE',  ( -1.000000000000000000, 0.000000000000000000, 0.000000000000000000 ) ) ;
#33867=ORIENTED_EDGE ( 'NONE', *, *, #34512, .T. ) ;
#33870=DIRECTION ( 'NONE',  ( 1.000000000000000000, 0.000000000000000000, 0.000000000000000000 ) ) ;
#33872=DIRECTION ( 'NONE',  ( 0.000000000000000000, 0.5528000653611945259, -0.8333139190825141762 ) ) ;
#33873=CIRCLE ( 'NONE', #29039, 120.5010000000000190 ) ;
#33874=ORIENTED_EDGE ( 'NONE', *, *, #7321, .F. ) ;
#33876=DIRECTION ( 'NONE',  ( 1.000000000000000000, 0.000000000000000000, 0.000000000000000000 ) ) ;
#33878=CIRCLE ( 'NONE', #1822, 59.00000000000000711 ) ;
#33880=DIRECTION ( 'NONE',  ( 0.000000000000000000, -0.1062934856473723155, 0.9943348002101364269 ) ) ;
#33882=EDGE_CURVE ( 'NONE', #3612, #6418, #6407, .T. ) ;
#33884=ORIENTED_EDGE ( 'NONE', *, *, #13909, .T. ) ;
#33885=DIRECTION ( 'NONE',  ( 1.000000000000000000, 0.000000000000000000, 0.000000000000000000 ) ) ;
#33886=CIRCLE ( 'NONE', #38052, 116.0000000000000000 ) ;
#33887=ORIENTED_EDGE ( 'NONE', *, *, #8266, .F. ) ;
#33894=CIRCLE ( 'NONE', #6728, 120.5010000000000190 ) ;
#33895=DIRECTION ( 'NONE',  ( -1.000000000000000000, -0.000000000000000000, -0.000000000000000000 ) ) ;
#33900=ORIENTED_EDGE ( 'NONE', *, *, #41893, .F. ) ;
#33901=DIRECTION ( 'NONE',  ( 0.000000000000000000, -6.586068790149233915E-15, 1.000000000000000000 ) ) ;
#33906=AXIS2_PLACEMENT_3D ( 'NONE', #29963, #13171, #9661 ) ;
#33907=DIRECTION ( 'NONE',  ( 0.000000000000000000, 0.9826841245925215240, -0.1852887240871114727 ) ) ;
#33910=ORIENTED_EDGE ( 'NONE', *, *, #16069, .F. ) ;
#33913=VECTOR ( 'NONE', #7346, 1000.000000000000000 ) ;
#33915=DIRECTION ( 'NONE',  ( 0.000000000000000000, 0.000000000000000000, 1.000000000000000000 ) ) ;
#33916=EDGE_CURVE ( 'NONE', #42499, #40120, #14367, .T. ) ;
#33917=AXIS2_PLACEMENT_3D ( 'NONE', #32273, #8716, #8943 ) ;
#33918=VERTEX_POINT ( 'NONE', #9257 ) ;
#33920=ORIENTED_EDGE ( 'NONE', *, *, #24174, .T. ) ;
#33921=CARTESIAN_POINT ( 'NONE',  ( 0.000000000000000000, -120.3696465864705800, -5.624871700597306123 ) ) ;
#33923=CARTESIAN_POINT ( 'NONE',  ( 17.99999999999999645, -94.83915810436441518, 59.94836581341558457 ) ) ;
#33924=FACE_OUTER_BOUND ( 'NONE', #1245, .T. ) ;
#33925=ORIENTED_EDGE ( 'NONE', *, *, #33916, .T. ) ;
#33926=ORIENTED_EDGE ( 'NONE', *, *, #18292, .F. ) ;
#33927=DIRECTION ( 'NONE',  ( 0.000000000000000000, 0.000000000000000000, 1.000000000000000000 ) ) ;
#33932=ORIENTED_EDGE ( 'NONE', *, *, #34848, .T. ) ;
#33936=AXIS2_PLACEMENT_3D ( 'NONE', #31733, #949, #14746 ) ;
#33938=CARTESIAN_POINT ( 'NONE',  ( 17.99999999999999645, 0.000000000000000000, 0.000000000000000000 ) ) ;
#33945=CIRCLE ( 'NONE', #8883, 120.5010000000000332 ) ;
#33948=CARTESIAN_POINT ( 'NONE',  ( 17.99999999999999645, 0.000000000000000000, 0.000000000000000000 ) ) ;
#33949=EDGE_CURVE ( 'NONE', #18075, #41485, #27581, .T. ) ;
#33952=DIRECTION ( 'NONE',  ( 1.000000000000000000, -0.000000000000000000, -0.000000000000000000 ) ) ;
#33953=DIRECTION ( 'NONE',  ( 0.000000000000000000, 0.6783118362696173298, -0.7347741508630661889 ) ) ;
#33954=AXIS2_PLACEMENT_3D ( 'NONE', #8561, #11429, #34759 ) ;
#33957=CARTESIAN_POINT ( 'NONE',  ( -10.00000000000000000, 0.000000000000000000, 0.000000000000000000 ) ) ;
#33960=ORIENTED_EDGE ( 'NONE', *, *, #19103, .F. ) ;
#33963=DIRECTION ( 'NONE',  ( -1.000000000000000000, -0.000000000000000000, -0.000000000000000000 ) ) ;
#33967=DIRECTION ( 'NONE',  ( 0.000000000000000000, 0.000000000000000000, 1.000000000000000000 ) ) ;
#33969=ORIENTED_EDGE ( 'NONE', *, *, #27028, .T. ) ;
#33978=DIRECTION ( 'NONE',  ( -1.000000000000000000, 0.000000000000000000, -0.000000000000000000 ) ) ;
#33979=ORIENTED_EDGE ( 'NONE', *, *, #25448, .T. ) ;
#33983=CYLINDRICAL_SURFACE ( 'NONE', #36822, 59.00000000000000000 ) ;
#33985=AXIS2_PLACEMENT_3D ( 'NONE', #29192, #6455, #29610 ) ;
#33988=EDGE_CURVE ( 'NONE', #15479, #33535, #37319, .T. ) ;
#33989=FACE_OUTER_BOUND ( 'NONE', #41750, .T. ) ;
#33990=ORIENTED_EDGE ( 'NONE', *, *, #13436, .T. ) ;
#33992=EDGE_LOOP ( 'NONE', ( #35230, #22402, #38046, #11846 ) ) ;
#33994=EDGE_LOOP ( 'NONE', ( #6379, #12389, #22472, #23758 ) ) ;
#33999=CARTESIAN_POINT ( 'NONE',  ( 17.99999999999999645, -93.26762629039475883, 76.29967815892324268 ) ) ;
#34001=CIRCLE ( 'NONE', #11008, 58.99999999999999289 ) ;
#34002=DIRECTION ( 'NONE',  ( 0.000000000000000000, 0.1062934856473588541, 0.9943348002101377592 ) ) ;
#34003=CARTESIAN_POINT ( 'NONE',  ( 8.999999999999998224, 113.8630351447205697, 22.16324045874448601 ) ) ;
#34004=VECTOR ( 'NONE', #17207, 1000.000000000000000 ) ;
#34006=AXIS2_PLACEMENT_3D ( 'NONE', #34534, #4646, #1370 ) ;
#34008=DIRECTION ( 'NONE',  ( 0.000000000000000000, 0.000000000000000000, 1.000000000000000000 ) ) ;
#34011=ORIENTED_EDGE ( 'NONE', *, *, #43064, .T. ) ;
#34012=DIRECTION ( 'NONE',  ( 1.000000000000000000, -0.000000000000000000, -0.000000000000000000 ) ) ;
#34015=CARTESIAN_POINT ( 'NONE',  ( 17.99999999999999645, 0.000000000000000000, 0.000000000000000000 ) ) ;
#34020=ADVANCED_FACE ( 'NONE', ( #40853 ), #31062, .F. ) ;
#34021=LINE ( 'NONE', #14186, #4599 ) ;
#34022=DIRECTION ( 'NONE',  ( -1.000000000000000000, -0.000000000000000000, 0.000000000000000000 ) ) ;
#34024=AXIS2_PLACEMENT_3D ( 'NONE', #10694, #37524, #4564 ) ;
#34026=DIRECTION ( 'NONE',  ( 0.000000000000000000, 0.4610925014493267859, -0.8873520750565710991 ) ) ;
#34027=ORIENTED_EDGE ( 'NONE', *, *, #40099, .F. ) ;
#34029=CARTESIAN_POINT ( 'NONE',  ( 17.99999999999999645, -79.94368240339368015, -90.16373242487986772 ) ) ;
#34030=CIRCLE ( 'NONE', #42360, 116.0000000000000000 ) ;
#34034=DIRECTION ( 'NONE',  ( 0.000000000000000000, 0.000000000000000000, 1.000000000000000000 ) ) ;
#34035=LINE ( 'NONE', #17282, #4734 ) ;
#34038=ADVANCED_FACE ( 'NONE', ( #7053 ), #14500, .F. ) ;
#34040=CARTESIAN_POINT ( 'NONE',  ( 0.000000000000000000, -106.5605152861899256, -56.26142179985931335 ) ) ;
#34042=CYLINDRICAL_SURFACE ( 'NONE', #3985, 116.0000000000000000 ) ;
#34045=ORIENTED_EDGE ( 'NONE', *, *, #25766, .T. ) ;
#34050=DIRECTION ( 'NONE',  ( -1.000000000000000000, -0.000000000000000000, -0.000000000000000000 ) ) ;
#34051=VERTEX_POINT ( 'NONE', #36724 ) ;
#34052=CYLINDRICAL_SURFACE ( 'NONE', #18313, 116.0000000000000000 ) ;
#34056=ADVANCED_FACE ( 'NONE', ( #10773 ), #10111, .F. ) ;
#34058=DIRECTION ( 'NONE',  ( -1.000000000000000000, -0.000000000000000000, -0.000000000000000000 ) ) ;
#34059=EDGE_CURVE ( 'NONE', #37862, #36952, #34552, .T. ) ;
#34061=CYLINDRICAL_SURFACE ( 'NONE', #42332, 59.00000000000000000 ) ;
#34062=AXIS2_PLACEMENT_3D ( 'NONE', #38469, #32580, #2662 ) ;
#34068=CARTESIAN_POINT ( 'NONE',  ( 17.99999999999999645, 0.000000000000000000, 0.000000000000000000 ) ) ;
#34069=CARTESIAN_POINT ( 'NONE',  ( 17.99999999999999645, 21.55123232222629426, -118.5581519187670096 ) ) ;
#34070=DIRECTION ( 'NONE',  ( 1.000000000000000000, 0.000000000000000000, 0.000000000000000000 ) ) ;
#34075=DIRECTION ( 'NONE',  ( -1.000000000000000000, -0.000000000000000000, -0.000000000000000000 ) ) ;
#34076=CYLINDRICAL_SURFACE ( 'NONE', #17985, 116.0000000000000000 ) ;
#34077=DIRECTION ( 'NONE',  ( 0.000000000000000000, 0.000000000000000000, 1.000000000000000000 ) ) ;
#34084=EDGE_LOOP ( 'NONE', ( #27494, #23924, #18756, #1813 ) ) ;
#34085=ADVANCED_FACE ( 'NONE', ( #260 ), #37378, .F. ) ;
#34088=DIRECTION ( 'NONE',  ( 0.000000000000000000, 0.3140767120219427611, 0.9493976084683832806 ) ) ;
#34089=CARTESIAN_POINT ( 'NONE',  ( 0.000000000000000000, 0.000000000000000000, 0.000000000000000000 ) ) ;
#34090=EDGE_LOOP ( 'NONE', ( #43068, #35430, #35504, #34879 ) ) ;
#34110=CARTESIAN_POINT ( 'NONE',  ( 17.99999999999999645, 2.418575551222434949, -120.4767259403368911 ) ) ;
#34114=DIRECTION ( 'NONE',  ( 0.000000000000000000, 0.000000000000000000, 1.000000000000000000 ) ) ;
#34115=AXIS2_PLACEMENT_3D ( 'NONE', #5945, #16022, #22367 ) ;
#34118=VECTOR ( 'NONE', #9884, 1000.000000000000000 ) ;
#34123=EDGE_CURVE ( 'NONE', #23473, #31625, #3846, .T. ) ;
#34125=CARTESIAN_POINT ( 'NONE',  ( 0.000000000000000000, 100.6739960869724655, -49.52796165323157851 ) ) ;
#34126=CARTESIAN_POINT ( 'NONE',  ( 17.99999999999999645, -78.75547124681308730, -91.20343606297076633 ) ) ;
#34129=DIRECTION ( 'NONE',  ( 0.000000000000000000, -0.9407002666710296834, -0.3392388661180399945 ) ) ;
#34131=CARTESIAN_POINT ( 'NONE',  ( 9.000000000000001776, 52.88069566989454273, 103.2454939717370905 ) ) ;
#34133=CARTESIAN_POINT ( 'NONE',  ( 0.000000000000000000, 0.000000000000000000, 0.000000000000000000 ) ) ;
#34140=DIRECTION ( 'NONE',  ( 0.000000000000000000, -0.2113826236296114103, -0.9774033898178695612 ) ) ;
#34142=CARTESIAN_POINT ( 'NONE',  ( 17.99999999999999645, -57.69704296431255131, 105.7900857083227777 ) ) ;
#34144=AXIS2_PLACEMENT_3D ( 'NONE', #33741, #3829, #20703 ) ;
#34149=VERTEX_POINT ( 'NONE', #15366 ) ;
#34151=DIRECTION ( 'NONE',  ( 0.000000000000000000, -2.928448444191355855E-14, -1.000000000000000000 ) ) ;
#34153=DIRECTION ( 'NONE',  ( 0.000000000000000000, 0.9213119778704139673, -0.3888241754733182676 ) ) ;
#34154=ORIENTED_EDGE ( 'NONE', *, *, #27421, .T. ) ;
#34156=ORIENTED_EDGE ( 'NONE', *, *, #37737, .T. ) ;
#34158=LINE ( 'NONE', #10400, #27610 ) ;
#34163=ADVANCED_FACE ( 'NONE', ( #12081 ), #38240, .F. ) ;
#34167=EDGE_LOOP ( 'NONE', ( #5973, #24197, #26939, #19307 ) ) ;
#34169=CIRCLE ( 'NONE', #15405, 116.0000000000000000 ) ;
#34170=AXIS2_PLACEMENT_3D ( 'NONE', #22438, #5806, #2512 ) ;
#34174=AXIS2_PLACEMENT_3D ( 'NONE', #27040, #3436, #149 ) ;
#34178=AXIS2_PLACEMENT_3D ( 'NONE', #10469, #7409, #10919 ) ;
#34180=ORIENTED_EDGE ( 'NONE', *, *, #7020, .T. ) ;
#34182=ORIENTED_EDGE ( 'NONE', *, *, #36396, .F. ) ;
#34183=FACE_OUTER_BOUND ( 'NONE', #32931, .T. ) ;
#34185=CARTESIAN_POINT ( 'NONE',  ( -10.00000000000000000, 0.000000000000000000, 0.000000000000000000 ) ) ;
#34186=VERTEX_POINT ( 'NONE', #2010 ) ;
#34187=CARTESIAN_POINT ( 'NONE',  ( 9.000000000000001776, -111.2559044912527355, 32.83479428644638887 ) ) ;
#34188=ORIENTED_EDGE ( 'NONE', *, *, #35668, .T. ) ;
#34191=DIRECTION ( 'NONE',  ( 0.000000000000000000, 0.000000000000000000, 1.000000000000000000 ) ) ;
#34193=ORIENTED_EDGE ( 'NONE', *, *, #33658, .F. ) ;
#34194=AXIS2_PLACEMENT_3D ( 'NONE', #611, #14619, #823 ) ;
#34198=AXIS2_PLACEMENT_3D ( 'NONE', #9478, #22830, #25877 ) ;
#34207=CARTESIAN_POINT ( 'NONE',  ( 9.000000000000001776, 101.8011932243948081, 55.61040422519366189 ) ) ;
#34209=CARTESIAN_POINT ( 'NONE',  ( 0.000000000000000000, 111.2721026680460596, -14.38025178762657852 ) ) ;
#34210=ORIENTED_EDGE ( 'NONE', *, *, #16477, .T. ) ;
#34213=EDGE_CURVE ( 'NONE', #21728, #40564, #35398, .T. ) ;
#34214=ORIENTED_EDGE ( 'NONE', *, *, #5596, .T. ) ;
#34218=ORIENTED_EDGE ( 'NONE', *, *, #4301, .F. ) ;
#34219=DIRECTION ( 'NONE',  ( -1.000000000000000000, -0.000000000000000000, 0.000000000000000000 ) ) ;
#34221=DIRECTION ( 'NONE',  ( -1.000000000000000000, -0.000000000000000000, -0.000000000000000000 ) ) ;
#34224=CARTESIAN_POINT ( 'NONE',  ( 0.000000000000000000, 72.00556975657821113, -86.04342158279314390 ) ) ;
#34226=ORIENTED_EDGE ( 'NONE', *, *, #41178, .F. ) ;
#34228=EDGE_CURVE ( 'NONE', #42811, #26205, #32130, .T. ) ;
#34230=CARTESIAN_POINT ( 'NONE',  ( 17.99999999999999645, 0.000000000000000000, 0.000000000000000000 ) ) ;
#34231=CIRCLE ( 'NONE', #23803, 116.0000000000000000 ) ;
#34234=AXIS2_PLACEMENT_3D ( 'NONE', #3576, #39802, #33927 ) ;
#34236=ORIENTED_EDGE ( 'NONE', *, *, #4360, .F. ) ;
#34237=LINE ( 'NONE', #38366, #13542 ) ;
#34238=LINE ( 'NONE', #39899, #15414 ) ;
#34239=ORIENTED_EDGE ( 'NONE', *, *, #34293, .F. ) ;
#34241=DIRECTION ( 'NONE',  ( -1.000000000000000000, -0.000000000000000000, 0.000000000000000000 ) ) ;
#34244=CIRCLE ( 'NONE', #32164, 58.99999999999999289 ) ;
#34252=DIRECTION ( 'NONE',  ( 0.000000000000000000, -0.7164567402983066380, -0.6976315211349934930 ) ) ;
#34256=ORIENTED_EDGE ( 'NONE', *, *, #32169, .T. ) ;
#34257=DIRECTION ( 'NONE',  ( -1.000000000000000000, 0.000000000000000000, -0.000000000000000000 ) ) ;
#34259=VERTEX_POINT ( 'NONE', #31285 ) ;
#34260=FACE_OUTER_BOUND ( 'NONE', #33236, .T. ) ;
#34261=EDGE_CURVE ( 'NONE', #13842, #36952, #21716, .T. ) ;
#34265=CARTESIAN_POINT ( 'NONE',  ( 17.99999999999999645, 92.10690493017060021, 64.06707842432207656 ) ) ;
#34267=CARTESIAN_POINT ( 'NONE',  ( 17.99999999999999645, -106.5605152861899256, -56.26142179985931335 ) ) ;
#34268=ORIENTED_EDGE ( 'NONE', *, *, #30745, .F. ) ;
#34271=DIRECTION ( 'NONE',  ( -1.000000000000000000, 0.000000000000000000, 0.000000000000000000 ) ) ;
#34274=ORIENTED_EDGE ( 'NONE', *, *, #8893, .T. ) ;
#34275=DIRECTION ( 'NONE',  ( 0.000000000000000000, 0.000000000000000000, 1.000000000000000000 ) ) ;
#34277=EDGE_CURVE ( 'NONE', #23398, #21330, #7391, .T. ) ;
#34278=CARTESIAN_POINT ( 'NONE',  ( 17.99999999999999645, 107.2703412112699368, -32.88383143828351507 ) ) ;
#34279=VERTEX_POINT ( 'NONE', #1582 ) ;
#34283=DIRECTION ( 'NONE',  ( 0.000000000000000000, 0.9714298932647090767, 0.2373266998711184850 ) ) ;
#34284=DIRECTION ( 'NONE',  ( 0.000000000000000000, -0.9714298932647122964, 0.2373266998711056064 ) ) ;
#34285=DIRECTION ( 'NONE',  ( 0.000000000000000000, -5.351180891996252112E-15, -1.000000000000000000 ) ) ;
#34288=EDGE_LOOP ( 'NONE', ( #22898, #20554, #24931, #18358 ) ) ;
#34291=DIRECTION ( 'NONE',  ( 0.000000000000000000, 0.000000000000000000, 1.000000000000000000 ) ) ;
#34293=EDGE_CURVE ( 'NONE', #37232, #30500, #31804, .T. ) ;
#34294=VERTEX_POINT ( 'NONE', #13749 ) ;
#34295=EDGE_CURVE ( 'NONE', #37603, #4177, #10193, .T. ) ;
#34296=CARTESIAN_POINT ( 'NONE',  ( 17.99999999999999645, -76.48293397876315680, 82.08917884620285577 ) ) ;
#34299=AXIS2_PLACEMENT_3D ( 'NONE', #42930, #9575, #5855 ) ;
#34301=ORIENTED_EDGE ( 'NONE', *, *, #40703, .T. ) ;
#34302=DIRECTION ( 'NONE',  ( -1.000000000000000000, -0.000000000000000000, 0.000000000000000000 ) ) ;
#34303=ORIENTED_EDGE ( 'NONE', *, *, #33642, .T. ) ;
#34304=AXIS2_PLACEMENT_3D ( 'NONE', #15953, #12877, #8727 ) ;
#34305=VERTEX_POINT ( 'NONE', #10229 ) ;
#34309=ORIENTED_EDGE ( 'NONE', *, *, #24227, .T. ) ;
#34310=DIRECTION ( 'NONE',  ( 0.000000000000000000, 0.000000000000000000, 1.000000000000000000 ) ) ;
#34313=CARTESIAN_POINT ( 'NONE',  ( 17.99999999999999645, 37.07968990261625208, -109.9140418541953750 ) ) ;
#34316=DIRECTION ( 'NONE',  ( 1.000000000000000000, 0.000000000000000000, 0.000000000000000000 ) ) ;
#34317=CARTESIAN_POINT ( 'NONE',  ( 0.000000000000000000, 117.9424311864592312, -24.69967462998914698 ) ) ;
#34318=CARTESIAN_POINT ( 'NONE',  ( 17.99999999999999645, 0.000000000000000000, 0.000000000000000000 ) ) ;
#34320=ORIENTED_EDGE ( 'NONE', *, *, #3957, .T. ) ;
#34324=VERTEX_POINT ( 'NONE', #26611 ) ;
#34327=ADVANCED_FACE ( 'NONE', ( #25616 ), #3448, .F. ) ;
#34329=ORIENTED_EDGE ( 'NONE', *, *, #104, .F. ) ;
#34332=CIRCLE ( 'NONE', #2264, 58.99999999999999289 ) ;
#34333=ORIENTED_EDGE ( 'NONE', *, *, #23524, .F. ) ;
#34335=DIRECTION ( 'NONE',  ( 0.000000000000000000, 0.000000000000000000, 1.000000000000000000 ) ) ;
#34337=CARTESIAN_POINT ( 'NONE',  ( 0.000000000000000000, 0.000000000000000000, 0.000000000000000000 ) ) ;
#34339=ORIENTED_EDGE ( 'NONE', *, *, #26258, .F. ) ;
#34344=ADVANCED_FACE ( 'NONE', ( #17027 ), #37055, .F. ) ;
#34346=EDGE_CURVE ( 'NONE', #14329, #23796, #16490, .T. ) ;
#34348=CARTESIAN_POINT ( 'NONE',  ( 17.99999999999999645, 79.94368240339426279, 90.16373242487935613 ) ) ;
#34351=CARTESIAN_POINT ( 'NONE',  ( 17.99999999999999645, 0.000000000000000000, 0.000000000000000000 ) ) ;
#34352=DIRECTION ( 'NONE',  ( 0.000000000000000000, 0.000000000000000000, 1.000000000000000000 ) ) ;
#34353=EDGE_CURVE ( 'NONE', #39721, #36486, #40826, .T. ) ;
#34357=FACE_OUTER_BOUND ( 'NONE', #11716, .T. ) ;
#34358=ORIENTED_EDGE ( 'NONE', *, *, #26195, .F. ) ;
#34360=DIRECTION ( 'NONE',  ( -1.000000000000000000, -0.000000000000000000, 0.000000000000000000 ) ) ;
#34361=EDGE_CURVE ( 'NONE', #11603, #3472, #5991, .T. ) ;
#34362=DIRECTION ( 'NONE',  ( 1.000000000000000000, -0.000000000000000000, 0.000000000000000000 ) ) ;
#34369=LINE ( 'NONE', #552, #35304 ) ;
#34371=DIRECTION ( 'NONE',  ( 1.000000000000000000, 0.000000000000000000, 0.000000000000000000 ) ) ;
#34372=ORIENTED_EDGE ( 'NONE', *, *, #23747, .T. ) ;
#34373=CARTESIAN_POINT ( 'NONE',  ( 0.000000000000000000, 0.000000000000000000, 0.000000000000000000 ) ) ;
#34376=CARTESIAN_POINT ( 'NONE',  ( 0.000000000000000000, 25.18647942089742031, 113.2326863338528824 ) ) ;
#34379=ORIENTED_EDGE ( 'NONE', *, *, #2029, .T. ) ;
#34382=DIRECTION ( 'NONE',  ( 0.000000000000000000, 0.000000000000000000, 1.000000000000000000 ) ) ;
#34383=DIRECTION ( 'NONE',  ( 1.000000000000000000, 0.000000000000000000, -0.000000000000000000 ) ) ;
#34387=ORIENTED_EDGE ( 'NONE', *, *, #16618, .F. ) ;
#34388=CYLINDRICAL_SURFACE ( 'NONE', #38820, 120.5010000000000190 ) ;
#34389=ORIENTED_EDGE ( 'NONE', *, *, #16477, .F. ) ;
#34390=AXIS2_PLACEMENT_3D ( 'NONE', #34068, #14229, #22840 ) ;
#34391=CARTESIAN_POINT ( 'NONE',  ( 0.000000000000000000, 0.000000000000000000, 0.000000000000000000 ) ) ;
#34395=ADVANCED_FACE ( 'NONE', ( #1378 ), #1589, .F. ) ;
#34401=CARTESIAN_POINT ( 'NONE',  ( 0.000000000000000000, 0.000000000000000000, 0.000000000000000000 ) ) ;
#34402=ORIENTED_EDGE ( 'NONE', *, *, #35439, .F. ) ;
#34403=CARTESIAN_POINT ( 'NONE',  ( 17.99999999999999645, 0.000000000000000000, 0.000000000000000000 ) ) ;
#34405=AXIS2_PLACEMENT_3D ( 'NONE', #17262, #6956, #37273 ) ;
#34407=DIRECTION ( 'NONE',  ( 0.000000000000000000, 0.000000000000000000, 1.000000000000000000 ) ) ;
#34409=CIRCLE ( 'NONE', #17736, 116.0000000000000000 ) ;
#34411=DIRECTION ( 'NONE',  ( 0.000000000000000000, -2.663829608872859574E-14, -1.000000000000000000 ) ) ;
#34416=EDGE_CURVE ( 'NONE', #34617, #36642, #6705, .T. ) ;
#34417=CARTESIAN_POINT ( 'NONE',  ( 17.99999999999999645, 16.77566611177777034, 119.3275660838943111 ) ) ;
#34422=CARTESIAN_POINT ( 'NONE',  ( 17.99999999999999645, -105.7179949885870514, 37.57629584241652054 ) ) ;
#34423=ORIENTED_EDGE ( 'NONE', *, *, #30087, .F. ) ;
#34425=CARTESIAN_POINT ( 'NONE',  ( 0.000000000000000000, 0.000000000000000000, 0.000000000000000000 ) ) ;
#34427=ORIENTED_EDGE ( 'NONE', *, *, #22846, .F. ) ;
#34433=CARTESIAN_POINT ( 'NONE',  ( 0.000000000000000000, 0.000000000000000000, 0.000000000000000000 ) ) ;
#34435=AXIS2_PLACEMENT_3D ( 'NONE', #40440, #6639, #33688 ) ;
#34442=DIRECTION ( 'NONE',  ( 1.000000000000000000, 0.000000000000000000, 0.000000000000000000 ) ) ;
#34444=CARTESIAN_POINT ( 'NONE',  ( 17.99999999999999645, -92.10690493017105496, 64.06707842432145128 ) ) ;
#34446=EDGE_CURVE ( 'NONE', #18211, #25660, #20675, .T. ) ;
#34447=LINE ( 'NONE', #1715, #3012 ) ;
#34449=VECTOR ( 'NONE', #4421, 1000.000000000000000 ) ;
#34457=ORIENTED_EDGE ( 'NONE', *, *, #10177, .T. ) ;
#34458=CARTESIAN_POINT ( 'NONE',  ( 17.99999999999999645, -87.74575819880217864, 75.87280091124446813 ) ) ;
#34460=AXIS2_PLACEMENT_3D ( 'NONE', #3381, #9737, #19588 ) ;
#34461=EDGE_CURVE ( 'NONE', #32652, #13915, #12430, .T. ) ;
#34462=VECTOR ( 'NONE', #16355, 1000.000000000000000 ) ;
#34463=CARTESIAN_POINT ( 'NONE',  ( 17.99999999999999645, -37.07968990261405651, -109.9140418541961282 ) ) ;
#34464=ORIENTED_EDGE ( 'NONE', *, *, #33421, .F. ) ;
#34466=DIRECTION ( 'NONE',  ( 1.000000000000000000, 0.000000000000000000, 0.000000000000000000 ) ) ;
#34467=CARTESIAN_POINT ( 'NONE',  ( 17.99999999999999645, -15.21076497709635156, -119.5371223922156503 ) ) ;
#34468=ADVANCED_FACE ( 'NONE', ( #6068 ), #29873, .F. ) ;
#34470=CARTESIAN_POINT ( 'NONE',  ( 17.99999999999999645, 0.000000000000000000, 0.000000000000000000 ) ) ;
#34472=ORIENTED_EDGE ( 'NONE', *, *, #39810, .T. ) ;
#34476=LINE ( 'NONE', #10952, #40930 ) ;
#34480=CARTESIAN_POINT ( 'NONE',  ( 0.000000000000000000, 0.000000000000000000, 0.000000000000000000 ) ) ;
#34483=ORIENTED_EDGE ( 'NONE', *, *, #38068, .T. ) ;
#34485=CARTESIAN_POINT ( 'NONE',  ( 0.000000000000000000, 6.854627147200274884, -115.7972974066012881 ) ) ;
#34487=CARTESIAN_POINT ( 'NONE',  ( 0.000000000000000000, 110.8621702203448649, 34.14058016547577523 ) ) ;
#34488=VERTEX_POINT ( 'NONE', #43136 ) ;
#34494=CIRCLE ( 'NONE', #8714, 59.00000000000000000 ) ;
#34495=DIRECTION ( 'NONE',  ( 0.000000000000000000, 1.411300455031978640E-14, -1.000000000000000000 ) ) ;
#34496=LINE ( 'NONE', #31252, #42978 ) ;
#34497=VECTOR ( 'NONE', #43067, 1000.000000000000000 ) ;
#34500=VECTOR ( 'NONE', #2873, 1000.000000000000000 ) ;
#34504=DIRECTION ( 'NONE',  ( 0.000000000000000000, 0.000000000000000000, 1.000000000000000000 ) ) ;
#34506=ORIENTED_EDGE ( 'NONE', *, *, #18162, .T. ) ;
#34507=CYLINDRICAL_SURFACE ( 'NONE', #12440, 59.00000000000000000 ) ;
#34509=VERTEX_POINT ( 'NONE', #25534 ) ;
#34512=EDGE_CURVE ( 'NONE', #42903, #32742, #24155, .T. ) ;
#34514=ORIENTED_EDGE ( 'NONE', *, *, #29497, .F. ) ;
#34517=EDGE_CURVE ( 'NONE', #25122, #39322, #29639, .T. ) ;
#34520=VECTOR ( 'NONE', #18922, 1000.000000000000000 ) ;
#34522=DIRECTION ( 'NONE',  ( 1.000000000000000000, 0.000000000000000000, 0.000000000000000000 ) ) ;
#34524=AXIS2_PLACEMENT_3D ( 'NONE', #28189, #41459, #2325 ) ;
#34529=CIRCLE ( 'NONE', #15748, 59.00000000000000000 ) ;
#34534=CARTESIAN_POINT ( 'NONE',  ( 17.99999999999999645, -0.5156212287287311735, 112.1962860721878172 ) ) ;
#34537=AXIS2_PLACEMENT_3D ( 'NONE', #11850, #24972, #9779 ) ;
#34544=ORIENTED_EDGE ( 'NONE', *, *, #30381, .T. ) ;
#34549=ORIENTED_EDGE ( 'NONE', *, *, #30009, .T. ) ;
#34552=CIRCLE ( 'NONE', #2483, 116.0000000000000000 ) ;
#34554=DIRECTION ( 'NONE',  ( 0.000000000000000000, 0.5528000653611945259, -0.8333139190825142872 ) ) ;
#34556=EDGE_CURVE ( 'NONE', #29115, #36343, #4617, .T. ) ;
#34560=CARTESIAN_POINT ( 'NONE',  ( 17.99999999999999645, -78.18175027177490222, 85.69488855492974722 ) ) ;
#34563=AXIS2_PLACEMENT_3D ( 'NONE', #32046, #2130, #24901 ) ;
#34564=DIRECTION ( 'NONE',  ( 0.000000000000000000, 0.000000000000000000, 1.000000000000000000 ) ) ;
#34567=VERTEX_POINT ( 'NONE', #29217 ) ;
#34572=EDGE_CURVE ( 'NONE', #32209, #32785, #30395, .T. ) ;
#34577=EDGE_CURVE ( 'NONE', #4569, #3310, #5636, .T. ) ;
#34578=CARTESIAN_POINT ( 'NONE',  ( 8.999999999999998224, 54.09091620264722877, 102.6166301549519488 ) ) ;
#34581=CARTESIAN_POINT ( 'NONE',  ( -10.00000000000000000, 0.000000000000000000, 0.000000000000000000 ) ) ;
#34583=AXIS2_PLACEMENT_3D ( 'NONE', #9125, #15921, #38793 ) ;
#34584=FACE_OUTER_BOUND ( 'NONE', #33363, .T. ) ;
#34587=CARTESIAN_POINT ( 'NONE',  ( 9.000000000000001776, 114.8812324315177023, -16.07179003769037351 ) ) ;
#34589=VERTEX_POINT ( 'NONE', #15701 ) ;
#34592=DIRECTION ( 'NONE',  ( -1.000000000000000000, 0.000000000000000000, -0.000000000000000000 ) ) ;
#34593=EDGE_CURVE ( 'NONE', #39974, #17009, #12843, .T. ) ;
#34596=CARTESIAN_POINT ( 'NONE',  ( 17.99999999999999645, 105.7179949885863266, 37.57629584241859533 ) ) ;
#34599=ADVANCED_FACE ( 'NONE', ( #17219 ), #10194, .F. ) ;
#34602=VECTOR ( 'NONE', #4700, 1000.000000000000000 ) ;
#34603=ORIENTED_EDGE ( 'NONE', *, *, #36950, .F. ) ;
#34604=LINE ( 'NONE', #40486, #16628 ) ;
#34605=CARTESIAN_POINT ( 'NONE',  ( 0.000000000000000000, -89.07460286905904923, 81.15544420874930154 ) ) ;
#34611=DIRECTION ( 'NONE',  ( 0.000000000000000000, 0.000000000000000000, 1.000000000000000000 ) ) ;
#34612=ORIENTED_EDGE ( 'NONE', *, *, #6141, .T. ) ;
#34613=CARTESIAN_POINT ( 'NONE',  ( 0.000000000000000000, 106.5605152861910909, -56.26142179985713909 ) ) ;
#34615=AXIS2_PLACEMENT_3D ( 'NONE', #34185, #27020, #30281 ) ;
#34617=VERTEX_POINT ( 'NONE', #13496 ) ;
#34618=DIRECTION ( 'NONE',  ( 1.000000000000000000, 0.000000000000000000, 0.000000000000000000 ) ) ;
#34620=CARTESIAN_POINT ( 'NONE',  ( 17.99999999999999645, 0.000000000000000000, 0.000000000000000000 ) ) ;
#34625=CIRCLE ( 'NONE', #21452, 120.5010000000000474 ) ;
#34626=ORIENTED_EDGE ( 'NONE', *, *, #31581, .F. ) ;
#34628=EDGE_CURVE ( 'NONE', #6200, #3612, #12998, .T. ) ;
#34632=DIRECTION ( 'NONE',  ( 1.000000000000000000, -0.000000000000000000, 0.000000000000000000 ) ) ;
#34636=VERTEX_POINT ( 'NONE', #7573 ) ;
#34639=CARTESIAN_POINT ( 'NONE',  ( 0.000000000000000000, -118.8387007424472159, 19.94628303336444475 ) ) ;
#34640=AXIS2_PLACEMENT_3D ( 'NONE', #13860, #40420, #14068 ) ;
#34641=DIRECTION ( 'NONE',  ( -1.000000000000000000, 0.000000000000000000, -0.000000000000000000 ) ) ;
#34645=CARTESIAN_POINT ( 'NONE',  ( 17.99999999999999645, 17.77780072541854040, -114.6296200873374147 ) ) ;
#34653=EDGE_CURVE ( 'NONE', #8703, #27194, #16525, .T. ) ;
#34656=AXIS2_PLACEMENT_3D ( 'NONE', #30606, #14032, #28422 ) ;
#34657=CIRCLE ( 'NONE', #37416, 59.00000000000000711 ) ;
#34659=DIRECTION ( 'NONE',  ( -1.000000000000000000, -0.000000000000000000, -0.000000000000000000 ) ) ;
#34663=ORIENTED_EDGE ( 'NONE', *, *, #874, .F. ) ;
#34664=CIRCLE ( 'NONE', #17300, 120.5010000000000332 ) ;
#34667=ORIENTED_EDGE ( 'NONE', *, *, #19051, .T. ) ;
#34668=CARTESIAN_POINT ( 'NONE',  ( 17.99999999999999645, -120.3696465864706369, 5.624871700595674540 ) ) ;
#34669=AXIS2_PLACEMENT_3D ( 'NONE', #12400, #22450, #19173 ) ;
#34670=EDGE_CURVE ( 'NONE', #13195, #23588, #16788, .T. ) ;
#34675=CARTESIAN_POINT ( 'NONE',  ( 17.99999999999999645, 110.0562500189205224, -49.07252625220001363 ) ) ;
#34677=ORIENTED_EDGE ( 'NONE', *, *, #7254, .F. ) ;
#34679=FACE_OUTER_BOUND ( 'NONE', #8809, .T. ) ;
#34680=ORIENTED_EDGE ( 'NONE', *, *, #7652, .F. ) ;
#34681=VECTOR ( 'NONE', #19313, 1000.000000000000000 ) ;
#34687=AXIS2_PLACEMENT_3D ( 'NONE', #30120, #13120, #20324 ) ;
#34689=DIRECTION ( 'NONE',  ( 0.000000000000000000, 0.000000000000000000, 1.000000000000000000 ) ) ;
#34691=AXIS2_PLACEMENT_3D ( 'NONE', #19782, #6431, #12789 ) ;
#34692=DIRECTION ( 'NONE',  ( 0.000000000000000000, 0.000000000000000000, 1.000000000000000000 ) ) ;
#34695=CIRCLE ( 'NONE', #11050, 116.0000000000000000 ) ;
#34697=DIRECTION ( 'NONE',  ( -1.000000000000000000, -0.000000000000000000, -0.000000000000000000 ) ) ;
#34703=DIRECTION ( 'NONE',  ( -1.000000000000000000, -0.000000000000000000, 0.000000000000000000 ) ) ;
#34705=DIRECTION ( 'NONE',  ( -1.000000000000000000, 0.000000000000000000, -0.000000000000000000 ) ) ;
#34707=DIRECTION ( 'NONE',  ( 0.000000000000000000, 0.000000000000000000, 1.000000000000000000 ) ) ;
#34709=ORIENTED_EDGE ( 'NONE', *, *, #4427, .T. ) ;
#34713=CIRCLE ( 'NONE', #15931, 58.99999999999999289 ) ;
#34715=AXIS2_PLACEMENT_3D ( 'NONE', #7626, #1294, #34034 ) ;
#34722=CIRCLE ( 'NONE', #15936, 58.99999999999999289 ) ;
#34723=AXIS2_PLACEMENT_3D ( 'NONE', #39774, #23892, #50 ) ;
#34724=CIRCLE ( 'NONE', #21546, 59.00000000000001421 ) ;
#34727=FACE_OUTER_BOUND ( 'NONE', #12770, .T. ) ;
#34729=CARTESIAN_POINT ( 'NONE',  ( 17.99999999999999645, -13.00789606333550097, 115.2683592318614672 ) ) ;
#34731=VERTEX_POINT ( 'NONE', #10638 ) ;
#34734=LINE ( 'NONE', #5053, #25753 ) ;
#34741=ORIENTED_EDGE ( 'NONE', *, *, #38286, .F. ) ;
#34743=EDGE_CURVE ( 'NONE', #40301, #25300, #15832, .T. ) ;
#34747=ORIENTED_EDGE ( 'NONE', *, *, #31112, .F. ) ;
#34753=ORIENTED_EDGE ( 'NONE', *, *, #4262, .T. ) ;
#34758=DIRECTION ( 'NONE',  ( 0.000000000000000000, 0.4132121857683728749, 0.9106347728549155640 ) ) ;
#34759=DIRECTION ( 'NONE',  ( 0.000000000000000000, 0.000000000000000000, 1.000000000000000000 ) ) ;
#34760=CARTESIAN_POINT ( 'NONE',  ( 9.000000000000001776, -25.18647942089668490, -113.2326863338530245 ) ) ;
#34761=DIRECTION ( 'NONE',  ( -1.000000000000000000, 0.000000000000000000, -0.000000000000000000 ) ) ;
#34762=EDGE_CURVE ( 'NONE', #5703, #3775, #1157, .T. ) ;
#34763=VERTEX_POINT ( 'NONE', #30715 ) ;
#34765=CYLINDRICAL_SURFACE ( 'NONE', #41532, 120.5010000000000190 ) ;
#34770=ORIENTED_EDGE ( 'NONE', *, *, #41973, .T. ) ;
#34772=ADVANCED_FACE ( 'NONE', ( #790 ), #40058, .F. ) ;
#34773=EDGE_LOOP ( 'NONE', ( #36770, #21173, #9184, #5928 ) ) ;
#34776=DIRECTION ( 'NONE',  ( -1.000000000000000000, -0.000000000000000000, -0.000000000000000000 ) ) ;
#34782=CIRCLE ( 'NONE', #20183, 116.0000000000000000 ) ;
#34784=CYLINDRICAL_SURFACE ( 'NONE', #42335, 120.5010000000000190 ) ;
#34785=EDGE_LOOP ( 'NONE', ( #27983, #4348, #7739, #21423 ) ) ;
#34787=DIRECTION ( 'NONE',  ( 0.000000000000000000, 0.000000000000000000, -1.000000000000000000 ) ) ;
#34790=ORIENTED_EDGE ( 'NONE', *, *, #15255, .F. ) ;
#34792=CARTESIAN_POINT ( 'NONE',  ( 0.000000000000000000, -83.58328028049608349, -80.43528614701409651 ) ) ;
#34793=DIRECTION ( 'NONE',  ( -1.000000000000000000, 0.000000000000000000, 0.000000000000000000 ) ) ;
#34803=ORIENTED_EDGE ( 'NONE', *, *, #3400, .T. ) ;
#34804=CARTESIAN_POINT ( 'NONE',  ( 17.99999999999999645, 62.45178862086215332, 93.20969140437529177 ) ) ;
#34808=AXIS2_PLACEMENT_3D ( 'NONE', #6158, #23416, #19503 ) ;
#34809=FACE_OUTER_BOUND ( 'NONE', #18595, .T. ) ;
#34811=VERTEX_POINT ( 'NONE', #22000 ) ;
#34820=ORIENTED_EDGE ( 'NONE', *, *, #1790, .F. ) ;
#34822=ORIENTED_EDGE ( 'NONE', *, *, #33637, .T. ) ;
#34830=FACE_OUTER_BOUND ( 'NONE', #30624, .T. ) ;
#34831=VERTEX_POINT ( 'NONE', #27670 ) ;
#34832=CARTESIAN_POINT ( 'NONE',  ( 0.000000000000000000, 112.1702510623870381, -2.471285140322999840 ) ) ;
#34833=CIRCLE ( 'NONE', #24441, 58.99999999999999289 ) ;
#34838=ORIENTED_EDGE ( 'NONE', *, *, #27111, .F. ) ;
#34842=VERTEX_POINT ( 'NONE', #11293 ) ;
#34843=ADVANCED_FACE ( 'NONE', ( #5382 ), #1237, .F. ) ;
#34844=LINE ( 'NONE', #38117, #3210 ) ;
#34848=EDGE_CURVE ( 'NONE', #1340, #40004, #7786, .T. ) ;
#34851=FACE_OUTER_BOUND ( 'NONE', #7331, .T. ) ;
#34852=ORIENTED_EDGE ( 'NONE', *, *, #40653, .F. ) ;
#34855=CARTESIAN_POINT ( 'NONE',  ( 0.000000000000000000, 47.58001226230536673, 110.7096808509485300 ) ) ;
#34857=DIRECTION ( 'NONE',  ( 1.000000000000000000, 0.000000000000000000, 0.000000000000000000 ) ) ;
#34859=DIRECTION ( 'NONE',  ( -1.000000000000000000, -0.000000000000000000, -0.000000000000000000 ) ) ;
#34860=ORIENTED_EDGE ( 'NONE', *, *, #24425, .F. ) ;
#34864=DIRECTION ( 'NONE',  ( 1.000000000000000000, 0.000000000000000000, 0.000000000000000000 ) ) ;
#34865=LINE ( 'NONE', #18337, #24104 ) ;
#34869=ORIENTED_EDGE ( 'NONE', *, *, #13155, .F. ) ;
#34870=CARTESIAN_POINT ( 'NONE',  ( 17.99999999999999645, 104.0201923570375300, 51.34003878071097660 ) ) ;
#34872=CYLINDRICAL_SURFACE ( 'NONE', #30280, 116.0000000000000000 ) ;
#34875=ORIENTED_EDGE ( 'NONE', *, *, #22136, .T. ) ;
#34879=ORIENTED_EDGE ( 'NONE', *, *, #14090, .F. ) ;
#34881=CIRCLE ( 'NONE', #13975, 59.00000000000000000 ) ;
#34882=DIRECTION ( 'NONE',  ( 1.000000000000000000, -0.000000000000000000, -0.000000000000000000 ) ) ;
#34884=FACE_OUTER_BOUND ( 'NONE', #34773, .T. ) ;
#34887=AXIS2_PLACEMENT_3D ( 'NONE', #42465, #26129, #19810 ) ;
#34889=ORIENTED_EDGE ( 'NONE', *, *, #42114, .T. ) ;
#34891=CARTESIAN_POINT ( 'NONE',  ( 17.99999999999999645, -40.13512380274045199, 113.6206972269520179 ) ) ;
#34893=CIRCLE ( 'NONE', #734, 58.99999999999999289 ) ;
#34894=ORIENTED_EDGE ( 'NONE', *, *, #22618, .F. ) ;
#34897=CYLINDRICAL_SURFACE ( 'NONE', #40984, 116.0000000000000000 ) ;
#34901=ORIENTED_EDGE ( 'NONE', *, *, #24395, .T. ) ;
#34902=DIRECTION ( 'NONE',  ( 0.000000000000000000, 0.000000000000000000, 1.000000000000000000 ) ) ;
#34905=LINE ( 'NONE', #28806, #7229 ) ;
#34906=ORIENTED_EDGE ( 'NONE', *, *, #38569, .T. ) ;
#34908=DIRECTION ( 'NONE',  ( -1.000000000000000000, 0.000000000000000000, 0.000000000000000000 ) ) ;
#34909=CARTESIAN_POINT ( 'NONE',  ( 17.99999999999999645, -82.63181128086789329, 81.41243003646944487 ) ) ;
#34910=CARTESIAN_POINT ( 'NONE',  ( 17.99999999999999645, 83.58328028049768932, -80.43528614701241963 ) ) ;
#34912=ORIENTED_EDGE ( 'NONE', *, *, #20866, .F. ) ;
#34913=CYLINDRICAL_SURFACE ( 'NONE', #1524, 59.00000000000000000 ) ;
#34914=DIRECTION ( 'NONE',  ( 0.000000000000000000, -0.8993121301712143634, -0.4373073204588656115 ) ) ;
#34916=ORIENTED_EDGE ( 'NONE', *, *, #20884, .T. ) ;
#34918=AXIS2_PLACEMENT_3D ( 'NONE', #24387, #28073, #4468 ) ;
#34919=DIRECTION ( 'NONE',  ( 0.000000000000000000, 0.000000000000000000, 1.000000000000000000 ) ) ;
#34921=CARTESIAN_POINT ( 'NONE',  ( 0.000000000000000000, -97.19627249181046125, -71.22763238166585609 ) ) ;
#34924=ORIENTED_EDGE ( 'NONE', *, *, #32604, .T. ) ;
#34925=CARTESIAN_POINT ( 'NONE',  ( 0.000000000000000000, 64.58410930313661424, -101.7319213743675732 ) ) ;
#34928=ORIENTED_EDGE ( 'NONE', *, *, #19068, .T. ) ;
#34933=AXIS2_PLACEMENT_3D ( 'NONE', #39334, #32385, #29141 ) ;
#34935=CARTESIAN_POINT ( 'NONE',  ( 17.99999999999999645, -113.8630351447204134, -22.16324045874526405 ) ) ;
#34936=DIRECTION ( 'NONE',  ( 1.000000000000000000, 0.000000000000000000, 0.000000000000000000 ) ) ;
#34938=VERTEX_POINT ( 'NONE', #2923 ) ;
#34941=CYLINDRICAL_SURFACE ( 'NONE', #18801, 59.00000000000000000 ) ;
#34943=ORIENTED_EDGE ( 'NONE', *, *, #10444, .T. ) ;
#34944=CARTESIAN_POINT ( 'NONE',  ( 17.99999999999999645, 24.22031524826126514, -109.5520369638034879 ) ) ;
#34945=EDGE_CURVE ( 'NONE', #27962, #39003, #39593, .T. ) ;
#34946=CARTESIAN_POINT ( 'NONE',  ( 17.99999999999999645, 29.36437154452156761, -116.8684075565133043 ) ) ;
#34949=ORIENTED_EDGE ( 'NONE', *, *, #25958, .F. ) ;
#34950=AXIS2_PLACEMENT_3D ( 'NONE', #37585, #31490, #18012 ) ;
#34953=AXIS2_PLACEMENT_3D ( 'NONE', #24872, #28115, #25092 ) ;
#34955=ORIENTED_EDGE ( 'NONE', *, *, #12294, .T. ) ;
#34957=AXIS2_PLACEMENT_3D ( 'NONE', #26638, #39483, #25998 ) ;
#34958=DIRECTION ( 'NONE',  ( -1.000000000000000000, 0.000000000000000000, -0.000000000000000000 ) ) ;
#34960=EDGE_CURVE ( 'NONE', #40092, #32698, #4654, .T. ) ;
#34963=CARTESIAN_POINT ( 'NONE',  ( 0.000000000000000000, -8.827181066045094227, -120.1772519049560231 ) ) ;
#34966=EDGE_CURVE ( 'NONE', #29868, #6044, #5588, .T. ) ;
#34969=CARTESIAN_POINT ( 'NONE',  ( 17.99999999999999645, 0.000000000000000000, 0.000000000000000000 ) ) ;
#34970=DIRECTION ( 'NONE',  ( -1.000000000000000000, 0.000000000000000000, -0.000000000000000000 ) ) ;
#34973=FACE_OUTER_BOUND ( 'NONE', #11114, .T. ) ;
#34975=DIRECTION ( 'NONE',  ( 0.000000000000000000, -0.9996456111234522934, -0.02662052143778445568 ) ) ;
#34977=DIRECTION ( 'NONE',  ( -1.000000000000000000, -0.000000000000000000, -0.000000000000000000 ) ) ;
#34978=VERTEX_POINT ( 'NONE', #2286 ) ;
#34980=CIRCLE ( 'NONE', #31538, 120.5010000000000190 ) ;
#34981=CIRCLE ( 'NONE', #21805, 120.5010000000000190 ) ;
#34984=AXIS2_PLACEMENT_3D ( 'NONE', #7309, #33713, #3800 ) ;
#34986=DIRECTION ( 'NONE',  ( 1.000000000000000000, 0.000000000000000000, 0.000000000000000000 ) ) ;
#34990=DIRECTION ( 'NONE',  ( 0.000000000000000000, 0.9968120070307499025, 0.07978610555308651708 ) ) ;
#34992=CARTESIAN_POINT ( 'NONE',  ( 9.000000000000001776, 29.86146781000101669, -112.0905559814575696 ) ) ;
#34994=CARTESIAN_POINT ( 'NONE',  ( 17.99999999999999645, 10.40101730206366959, 120.0512800434971581 ) ) ;
#34995=CIRCLE ( 'NONE', #19008, 116.0000000000000000 ) ;
#34996=CARTESIAN_POINT ( 'NONE',  ( 17.99999999999999645, -101.1249659627859216, 48.60055280209385842 ) ) ;
#35000=ORIENTED_EDGE ( 'NONE', *, *, #2376, .F. ) ;
#35001=CARTESIAN_POINT ( 'NONE',  ( 17.99999999999999645, -35.72777019205738469, 106.3569410558016273 ) ) ;
#35003=LINE ( 'NONE', #25030, #1199 ) ;
#35004=VERTEX_POINT ( 'NONE', #6435 ) ;
#35010=EDGE_CURVE ( 'NONE', #36814, #276, #33214, .T. ) ;
#35011=CARTESIAN_POINT ( 'NONE',  ( 0.000000000000000000, 84.77518783075095143, 73.49448960231384831 ) ) ;
#35014=AXIS2_PLACEMENT_3D ( 'NONE', #8032, #34864, #28126 ) ;
#35019=CYLINDRICAL_SURFACE ( 'NONE', #26277, 59.00000000000001421 ) ;
#35020=CIRCLE ( 'NONE', #13458, 116.0000000000000000 ) ;
#35021=CARTESIAN_POINT ( 'NONE',  ( 17.99999999999999645, -68.63002662989811142, 93.51962064069482494 ) ) ;
#35022=ORIENTED_EDGE ( 'NONE', *, *, #2813, .T. ) ;
#35023=CARTESIAN_POINT ( 'NONE',  ( 0.000000000000000000, -91.51415974874549875, -64.91094698989387268 ) ) ;
#35024=ORIENTED_EDGE ( 'NONE', *, *, #9472, .T. ) ;
#35025=AXIS2_PLACEMENT_3D ( 'NONE', #9155, #15524, #12462 ) ;
#35027=CARTESIAN_POINT ( 'NONE',  ( 17.99999999999999645, 0.000000000000000000, 0.000000000000000000 ) ) ;
#35029=DIRECTION ( 'NONE',  ( 0.000000000000000000, 0.000000000000000000, 1.000000000000000000 ) ) ;
#35030=ORIENTED_EDGE ( 'NONE', *, *, #32913, .T. ) ;
#35031=EDGE_CURVE ( 'NONE', #22633, #26052, #35300, .T. ) ;
#35032=EDGE_LOOP ( 'NONE', ( #1214, #11303, #5810, #19059 ) ) ;
#35033=DIRECTION ( 'NONE',  ( 0.000000000000000000, 0.000000000000000000, -1.000000000000000000 ) ) ;
#35034=ADVANCED_FACE ( 'NONE', ( #28743 ), #42642, .F. ) ;
#35039=AXIS2_PLACEMENT_3D ( 'NONE', #40264, #10835, #556 ) ;
#35041=DIRECTION ( 'NONE',  ( 0.000000000000000000, -0.8477344278896755680, 0.5304209081197350795 ) ) ;
#35042=ORIENTED_EDGE ( 'NONE', *, *, #612, .F. ) ;
#35045=VERTEX_POINT ( 'NONE', #32418 ) ;
#35047=EDGE_LOOP ( 'NONE', ( #34514, #12085, #18733, #8136 ) ) ;
#35052=ORIENTED_EDGE ( 'NONE', *, *, #26767, .F. ) ;
#35054=CARTESIAN_POINT ( 'NONE',  ( 17.99999999999999645, -107.1354928292872728, 44.47455650398029547 ) ) ;
#35059=LINE ( 'NONE', #8888, #17787 ) ;
#35061=DIRECTION ( 'NONE',  ( -1.000000000000000000, -0.000000000000000000, -0.000000000000000000 ) ) ;
#35063=DIRECTION ( 'NONE',  ( -1.000000000000000000, -0.000000000000000000, -0.000000000000000000 ) ) ;
#35066=CIRCLE ( 'NONE', #19101, 116.0000000000000000 ) ;
#35067=ADVANCED_FACE ( 'NONE', ( #25902 ), #5793, .F. ) ;
#35068=DIRECTION ( 'NONE',  ( 0.000000000000000000, -0.9714298932647122964, 0.2373266998711056064 ) ) ;
#35070=DIRECTION ( 'NONE',  ( 0.000000000000000000, 0.8477344278896686847, 0.5304209081197462927 ) ) ;
#35073=DIRECTION ( 'NONE',  ( 1.000000000000000000, -0.000000000000000000, 0.000000000000000000 ) ) ;
#35074=CARTESIAN_POINT ( 'NONE',  ( 0.000000000000000000, 0.000000000000000000, 0.000000000000000000 ) ) ;
#35076=ORIENTED_EDGE ( 'NONE', *, *, #32583, .T. ) ;
#35079=CARTESIAN_POINT ( 'NONE',  ( 0.000000000000000000, -73.78980555658671392, 95.26571049921966505 ) ) ;
#35081=VECTOR ( 'NONE', #9314, 1000.000000000000000 ) ;
#35086=EDGE_CURVE ( 'NONE', #37209, #22175, #492, .T. ) ;
#35087=EDGE_CURVE ( 'NONE', #5323, #13299, #13777, .T. ) ;
#35090=EDGE_LOOP ( 'NONE', ( #42386, #6945, #10525, #2946 ) ) ;
#35092=DIRECTION ( 'NONE',  ( -1.000000000000000000, -0.000000000000000000, -0.000000000000000000 ) ) ;
#35094=VECTOR ( 'NONE', #27708, 1000.000000000000000 ) ;
#35095=CARTESIAN_POINT ( 'NONE',  ( 0.000000000000000000, -117.9424311864590891, 24.69967462998996766 ) ) ;
#35097=CARTESIAN_POINT ( 'NONE',  ( 0.000000000000000000, 114.6488492393084613, -37.09625815499892809 ) ) ;
#35099=ORIENTED_EDGE ( 'NONE', *, *, #6677, .T. ) ;
#35110=DIRECTION ( 'NONE',  ( 1.000000000000000000, 0.000000000000000000, 0.000000000000000000 ) ) ;
#35111=AXIS2_PLACEMENT_3D ( 'NONE', #28079, #772, #1213 ) ;
#35112=ORIENTED_EDGE ( 'NONE', *, *, #33882, .F. ) ;
#35115=ADVANCED_FACE ( 'NONE', ( #7290 ), #735, .F. ) ;
#35117=DIRECTION ( 'NONE',  ( 0.000000000000000000, 0.000000000000000000, 1.000000000000000000 ) ) ;
#35118=CIRCLE ( 'NONE', #39981, 59.00000000000000000 ) ;
#35119=ORIENTED_EDGE ( 'NONE', *, *, #28483, .F. ) ;
#35120=CARTESIAN_POINT ( 'NONE',  ( -10.00000000000000000, 0.000000000000000000, 0.000000000000000000 ) ) ;
#35123=CARTESIAN_POINT ( 'NONE',  ( 17.99999999999999645, 0.000000000000000000, 0.000000000000000000 ) ) ;
#35124=VECTOR ( 'NONE', #13698, 1000.000000000000000 ) ;
#35125=DIRECTION ( 'NONE',  ( -1.000000000000000000, 0.000000000000000000, 0.000000000000000000 ) ) ;
#35130=ORIENTED_EDGE ( 'NONE', *, *, #25310, .T. ) ;
#35131=DIRECTION ( 'NONE',  ( 0.000000000000000000, 0.000000000000000000, 1.000000000000000000 ) ) ;
#35133=ADVANCED_FACE ( 'NONE', ( #10368 ), #33488, .F. ) ;
#35134=EDGE_CURVE ( 'NONE', #29671, #33221, #15865, .T. ) ;
#35140=AXIS2_PLACEMENT_3D ( 'NONE', #20805, #21023, #34275 ) ;
#35143=CARTESIAN_POINT ( 'NONE',  ( 0.000000000000000000, -90.81729652456213842, 72.16798910853589177 ) ) ;
#35152=ORIENTED_EDGE ( 'NONE', *, *, #3083, .F. ) ;
#35153=CARTESIAN_POINT ( 'NONE',  ( 17.99999999999999645, 6.486220790509957368, -112.0098273076986715 ) ) ;
#35155=ORIENTED_EDGE ( 'NONE', *, *, #9446, .F. ) ;
#35162=ORIENTED_EDGE ( 'NONE', *, *, #21835, .T. ) ;
#35163=LINE ( 'NONE', #5282, #11272 ) ;
#35164=CARTESIAN_POINT ( 'NONE',  ( 17.99999999999999645, 69.90696807222620635, -98.15042952503443985 ) ) ;
#35165=ORIENTED_EDGE ( 'NONE', *, *, #36924, .T. ) ;
#35166=CARTESIAN_POINT ( 'NONE',  ( 0.000000000000000000, 111.2721026680460596, -14.38025178762657852 ) ) ;
#35167=DIRECTION ( 'NONE',  ( 1.000000000000000000, 0.000000000000000000, 0.000000000000000000 ) ) ;
#35169=DIRECTION ( 'NONE',  ( 0.000000000000000000, 0.2631025642275218179, -0.9647678688145158166 ) ) ;
#35173=DIRECTION ( 'NONE',  ( 1.000000000000000000, 0.000000000000000000, 0.000000000000000000 ) ) ;
#35174=VECTOR ( 'NONE', #18659, 1000.000000000000000 ) ;
#35175=VERTEX_POINT ( 'NONE', #20012 ) ;
#35176=AXIS2_PLACEMENT_3D ( 'NONE', #26176, #6297, #19647 ) ;
#35177=DIRECTION ( 'NONE',  ( 1.000000000000000000, 0.000000000000000000, 0.000000000000000000 ) ) ;
#35178=VERTEX_POINT ( 'NONE', #20433 ) ;
#35179=CIRCLE ( 'NONE', #28243, 58.99999999999998579 ) ;
#35187=EDGE_CURVE ( 'NONE', #32376, #2948, #14098, .T. ) ;
#35191=VERTEX_POINT ( 'NONE', #39799 ) ;
#35193=CARTESIAN_POINT ( 'NONE',  ( 17.99999999999999645, -106.5605152861907072, 56.26142179985788516 ) ) ;
#35194=CARTESIAN_POINT ( 'NONE',  ( 17.99999999999999645, 112.1702510623870381, -2.471285140322999840 ) ) ;
#35196=CYLINDRICAL_SURFACE ( 'NONE', #31677, 59.00000000000000000 ) ;
#35197=EDGE_CURVE ( 'NONE', #37254, #32443, #8867, .T. ) ;
#35198=CARTESIAN_POINT ( 'NONE',  ( 17.99999999999999645, 105.3681574666264282, 38.54638589714925700 ) ) ;
#35199=ORIENTED_EDGE ( 'NONE', *, *, #11291, .F. ) ;
#35201=VERTEX_POINT ( 'NONE', #9924 ) ;
#35202=DIRECTION ( 'NONE',  ( 0.000000000000000000, -0.8993121301712141413, -0.4373073204588656671 ) ) ;
#35203=CIRCLE ( 'NONE', #25499, 116.0000000000000000 ) ;
#35204=FACE_OUTER_BOUND ( 'NONE', #18947, .T. ) ;
#35205=EDGE_CURVE ( 'NONE', #29131, #8886, #22150, .T. ) ;
#35208=CARTESIAN_POINT ( 'NONE',  ( 17.99999999999999645, 0.000000000000000000, 0.000000000000000000 ) ) ;
#35209=ORIENTED_EDGE ( 'NONE', *, *, #33326, .F. ) ;
#35210=AXIS2_PLACEMENT_3D ( 'NONE', #8733, #25783, #35554 ) ;
#35216=VERTEX_POINT ( 'NONE', #3365 ) ;
#35221=CIRCLE ( 'NONE', #342, 116.0000000000000000 ) ;
#35222=CARTESIAN_POINT ( 'NONE',  ( 17.99999999999999645, 47.58001226230686598, -110.7096808509478763 ) ) ;
#35223=VECTOR ( 'NONE', #1833, 1000.000000000000000 ) ;
#35224=EDGE_LOOP ( 'NONE', ( #37090, #9162, #20387, #231 ) ) ;
#35228=ORIENTED_EDGE ( 'NONE', *, *, #28857, .F. ) ;
#35230=ORIENTED_EDGE ( 'NONE', *, *, #8499, .T. ) ;
#35232=DIRECTION ( 'NONE',  ( -1.000000000000000000, 0.000000000000000000, 0.000000000000000000 ) ) ;
#35234=CARTESIAN_POINT ( 'NONE',  ( 17.99999999999999645, -80.74349901498355564, -77.90224541347362219 ) ) ;
#35235=AXIS2_PLACEMENT_3D ( 'NONE', #30846, #6846, #33461 ) ;
#35236=ORIENTED_EDGE ( 'NONE', *, *, #9038, .T. ) ;
#35239=CARTESIAN_POINT ( 'NONE',  ( 0.000000000000000000, -40.37724737310141165, 104.6802291180865865 ) ) ;
#35240=AXIS2_PLACEMENT_3D ( 'NONE', #35402, #38025, #1806 ) ;
#35241=ORIENTED_EDGE ( 'NONE', *, *, #42373, .T. ) ;
#35242=DIRECTION ( 'NONE',  ( -1.000000000000000000, -0.000000000000000000, -0.000000000000000000 ) ) ;
#35244=CARTESIAN_POINT ( 'NONE',  ( 17.99999999999999645, 0.000000000000000000, 0.000000000000000000 ) ) ;
#35246=CIRCLE ( 'NONE', #1071, 59.00000000000000000 ) ;
#35249=CIRCLE ( 'NONE', #6689, 120.5010000000000190 ) ;
#35250=CARTESIAN_POINT ( 'NONE',  ( 17.99999999999999645, -46.83041522348427321, -101.9567785075606139 ) ) ;
#35251=EDGE_CURVE ( 'NONE', #1122, #29131, #14465, .T. ) ;
#35254=DIRECTION ( 'NONE',  ( -1.000000000000000000, 0.000000000000000000, 0.000000000000000000 ) ) ;
#35255=ORIENTED_EDGE ( 'NONE', *, *, #25766, .F. ) ;
#35256=EDGE_CURVE ( 'NONE', #16155, #32590, #9552, .T. ) ;
#35257=CARTESIAN_POINT ( 'NONE',  ( 17.99999999999999645, -112.1702510623870666, 2.471285140322257323 ) ) ;
#35267=DIRECTION ( 'NONE',  ( -1.000000000000000000, -0.000000000000000000, -0.000000000000000000 ) ) ;
#35268=AXIS2_PLACEMENT_3D ( 'NONE', #2415, #10006, #15783 ) ;
#35269=AXIS2_PLACEMENT_3D ( 'NONE', #9406, #3868, #3652 ) ;
#35273=DIRECTION ( 'NONE',  ( -1.000000000000000000, 0.000000000000000000, -0.000000000000000000 ) ) ;
#35274=CARTESIAN_POINT ( 'NONE',  ( 8.999999999999998224, 37.07968990261482389, 109.9140418541958724 ) ) ;
#35277=EDGE_CURVE ( 'NONE', #1814, #35938, #31865, .T. ) ;
#35281=DIRECTION ( 'NONE',  ( -1.000000000000000000, -0.000000000000000000, 0.000000000000000000 ) ) ;
#35286=ORIENTED_EDGE ( 'NONE', *, *, #22427, .T. ) ;
#35287=CARTESIAN_POINT ( 'NONE',  ( 17.99999999999999645, 0.000000000000000000, 0.000000000000000000 ) ) ;
#35290=LINE ( 'NONE', #40967, #2252 ) ;
#35295=ORIENTED_EDGE ( 'NONE', *, *, #26767, .T. ) ;
#35298=LINE ( 'NONE', #21623, #29599 ) ;
#35300=CIRCLE ( 'NONE', #38780, 59.00000000000001421 ) ;
#35301=ORIENTED_EDGE ( 'NONE', *, *, #874, .T. ) ;
#35304=VECTOR ( 'NONE', #24158, 1000.000000000000000 ) ;
#35305=CIRCLE ( 'NONE', #16527, 59.00000000000000711 ) ;
#35310=DIRECTION ( 'NONE',  ( 0.000000000000000000, 0.000000000000000000, 1.000000000000000000 ) ) ;
#35311=EDGE_CURVE ( 'NONE', #2440, #16214, #15167, .T. ) ;
#35315=ORIENTED_EDGE ( 'NONE', *, *, #18863, .F. ) ;
#35316=CARTESIAN_POINT ( 'NONE',  ( 17.99999999999999645, 103.1672962317651496, 44.09967643725903486 ) ) ;
#35317=LINE ( 'NONE', #1502, #40421 ) ;
#35318=AXIS2_PLACEMENT_3D ( 'NONE', #14866, #10488, #23827 ) ;
#35323=VERTEX_POINT ( 'NONE', #38268 ) ;
#35328=DIRECTION ( 'NONE',  ( -1.000000000000000000, -0.000000000000000000, -0.000000000000000000 ) ) ;
#35335=DIRECTION ( 'NONE',  ( 0.000000000000000000, 0.000000000000000000, 1.000000000000000000 ) ) ;
#35336=CARTESIAN_POINT ( 'NONE',  ( 17.99999999999999645, 90.81729652456265001, -72.16798910853526650 ) ) ;
#35340=CIRCLE ( 'NONE', #27012, 59.00000000000000000 ) ;
#35345=CARTESIAN_POINT ( 'NONE',  ( 17.99999999999999645, -45.89132998247981732, -102.3829004574634496 ) ) ;
#35349=EDGE_CURVE ( 'NONE', #9926, #714, #10260, .T. ) ;
#35351=EDGE_CURVE ( 'NONE', #41306, #41672, #37413, .T. ) ;
#35353=VERTEX_POINT ( 'NONE', #27836 ) ;
#35354=CARTESIAN_POINT ( 'NONE',  ( 0.000000000000000000, 0.000000000000000000, 0.000000000000000000 ) ) ;
#35358=ADVANCED_FACE ( 'NONE', ( #15190 ), #21313, .F. ) ;
#35360=CARTESIAN_POINT ( 'NONE',  ( 17.99999999999999645, 23.85344185397197947, 113.5209818126991621 ) ) ;
#35364=CYLINDRICAL_SURFACE ( 'NONE', #42649, 116.0000000000000000 ) ;
#35377=VERTEX_POINT ( 'NONE', #4896 ) ;
#35379=ORIENTED_EDGE ( 'NONE', *, *, #35010, .T. ) ;
#35382=AXIS2_PLACEMENT_3D ( 'NONE', #4758, #22245, #14819 ) ;
#35397=CARTESIAN_POINT ( 'NONE',  ( 17.99999999999999645, 71.21168426767221149, -86.70160608319253015 ) ) ;
#35398=LINE ( 'NONE', #28459, #36654 ) ;
#35399=DIRECTION ( 'NONE',  ( -1.000000000000000000, 0.000000000000000000, 0.000000000000000000 ) ) ;
#35401=ORIENTED_EDGE ( 'NONE', *, *, #14157, .F. ) ;
#35402=CARTESIAN_POINT ( 'NONE',  ( 0.000000000000000000, 0.000000000000000000, 0.000000000000000000 ) ) ;
#35404=VERTEX_POINT ( 'NONE', #31958 ) ;
#35405=LINE ( 'NONE', #37807, #10093 ) ;
#35408=VECTOR ( 'NONE', #33167, 1000.000000000000000 ) ;
#35409=ORIENTED_EDGE ( 'NONE', *, *, #39011, .T. ) ;
#35413=EDGE_LOOP ( 'NONE', ( #32822, #1889, #721, #1730 ) ) ;
#35414=CARTESIAN_POINT ( 'NONE',  ( 0.000000000000000000, 95.31344542257733110, 66.11616384574480776 ) ) ;
#35415=LINE ( 'NONE', #29106, #13034 ) ;
#35416=EDGE_CURVE ( 'NONE', #433, #19203, #42593, .T. ) ;
#35419=CYLINDRICAL_SURFACE ( 'NONE', #31356, 116.0000000000000000 ) ;
#35425=AXIS2_PLACEMENT_3D ( 'NONE', #3148, #1723, #16085 ) ;
#35426=CIRCLE ( 'NONE', #22244, 59.00000000000000000 ) ;
#35430=ORIENTED_EDGE ( 'NONE', *, *, #35792, .T. ) ;
#35431=VECTOR ( 'NONE', #35622, 1000.000000000000000 ) ;
#35433=VERTEX_POINT ( 'NONE', #8815 ) ;
#35435=ORIENTED_EDGE ( 'NONE', *, *, #35086, .T. ) ;
#35437=VERTEX_POINT ( 'NONE', #39311 ) ;
#35438=CARTESIAN_POINT ( 'NONE',  ( 0.000000000000000000, -68.61497464550522807, -99.05794392877676557 ) ) ;
#35439=EDGE_CURVE ( 'NONE', #36920, #4115, #31210, .T. ) ;
#35445=CARTESIAN_POINT ( 'NONE',  ( 0.000000000000000000, 111.2721026680460596, 44.61974821237342326 ) ) ;
#35448=VERTEX_POINT ( 'NONE', #16237 ) ;
#35449=FACE_OUTER_BOUND ( 'NONE', #3814, .T. ) ;
#35451=DIRECTION ( 'NONE',  ( -1.000000000000000000, -0.000000000000000000, -0.000000000000000000 ) ) ;
#35452=LINE ( 'NONE', #18495, #1101 ) ;
#35455=AXIS2_PLACEMENT_3D ( 'NONE', #33496, #4904, #18476 ) ;
#35457=DIRECTION ( 'NONE',  ( -1.000000000000000000, -0.000000000000000000, -0.000000000000000000 ) ) ;
#35460=DIRECTION ( 'NONE',  ( 0.000000000000000000, 0.000000000000000000, 1.000000000000000000 ) ) ;
#35461=VERTEX_POINT ( 'NONE', #12959 ) ;
#35462=CARTESIAN_POINT ( 'NONE',  ( 0.000000000000000000, -98.69720329640912837, -60.94966826380012037 ) ) ;
#35467=ORIENTED_EDGE ( 'NONE', *, *, #3043, .F. ) ;
#35468=DIRECTION ( 'NONE',  ( 1.000000000000000000, 0.000000000000000000, 0.000000000000000000 ) ) ;
#35475=FACE_OUTER_BOUND ( 'NONE', #4241, .T. ) ;
#35479=CIRCLE ( 'NONE', #3417, 116.0000000000000000 ) ;
#35480=CYLINDRICAL_SURFACE ( 'NONE', #41101, 116.0000000000000000 ) ;
#35482=EDGE_CURVE ( 'NONE', #1782, #40246, #39113, .T. ) ;
#35483=AXIS2_PLACEMENT_3D ( 'NONE', #42107, #12266, #25593 ) ;
#35487=DIRECTION ( 'NONE',  ( -1.000000000000000000, -0.000000000000000000, -0.000000000000000000 ) ) ;
#35490=DIRECTION ( 'NONE',  ( -1.000000000000000000, 0.000000000000000000, 0.000000000000000000 ) ) ;
#35491=ADVANCED_FACE ( 'NONE', ( #19522 ), #32582, .F. ) ;
#35492=FACE_OUTER_BOUND ( 'NONE', #31859, .T. ) ;
#35495=LINE ( 'NONE', #9744, #2805 ) ;
#35496=EDGE_CURVE ( 'NONE', #13162, #30365, #6112, .T. ) ;
#35497=ORIENTED_EDGE ( 'NONE', *, *, #33156, .T. ) ;
#35502=ORIENTED_EDGE ( 'NONE', *, *, #18565, .F. ) ;
#35504=ORIENTED_EDGE ( 'NONE', *, *, #13697, .F. ) ;
#35508=CIRCLE ( 'NONE', #16740, 59.00000000000000000 ) ;
#35509=CIRCLE ( 'NONE', #1377, 120.5010000000000474 ) ;
#35510=AXIS2_PLACEMENT_3D ( 'NONE', #15354, #2624, #12066 ) ;
#35511=CARTESIAN_POINT ( 'NONE',  ( 17.99999999999999645, -100.8494052988175298, 65.95368414178875582 ) ) ;
#35515=ORIENTED_EDGE ( 'NONE', *, *, #35439, .T. ) ;
#35516=EDGE_CURVE ( 'NONE', #8087, #38742, #18017, .T. ) ;
#35518=LINE ( 'NONE', #25320, #41692 ) ;
#35520=DIRECTION ( 'NONE',  ( 0.000000000000000000, -2.487417051993862264E-14, -1.000000000000000000 ) ) ;
#35522=DIRECTION ( 'NONE',  ( 0.000000000000000000, 0.000000000000000000, 1.000000000000000000 ) ) ;
#35529=ORIENTED_EDGE ( 'NONE', *, *, #7899, .F. ) ;
#35534=ORIENTED_EDGE ( 'NONE', *, *, #13364, .F. ) ;
#35535=DIRECTION ( 'NONE',  ( 1.000000000000000000, 0.000000000000000000, 0.000000000000000000 ) ) ;
#35538=VECTOR ( 'NONE', #34908, 1000.000000000000000 ) ;
#35546=ORIENTED_EDGE ( 'NONE', *, *, #17212, .F. ) ;
#35548=ORIENTED_EDGE ( 'NONE', *, *, #13697, .T. ) ;
#35550=FACE_OUTER_BOUND ( 'NONE', #41217, .T. ) ;
#35551=CARTESIAN_POINT ( 'NONE',  ( 0.000000000000000000, 110.8621702203453339, -34.14058016547420493 ) ) ;
#35553=ORIENTED_EDGE ( 'NONE', *, *, #758, .T. ) ;
#35554=DIRECTION ( 'NONE',  ( 0.000000000000000000, 0.7865515558026436871, -0.6175246149461904865 ) ) ;
#35555=CIRCLE ( 'NONE', #32755, 58.99999999999999289 ) ;
#35562=CARTESIAN_POINT ( 'NONE',  ( 0.000000000000000000, 0.000000000000000000, 0.000000000000000000 ) ) ;
#35564=AXIS2_PLACEMENT_3D ( 'NONE', #15035, #42027, #2526 ) ;
#35565=EDGE_CURVE ( 'NONE', #38794, #14329, #32158, .T. ) ;
#35567=CARTESIAN_POINT ( 'NONE',  ( 0.000000000000000000, -10.40101730206288622, -120.0512800434972149 ) ) ;
#35568=FACE_OUTER_BOUND ( 'NONE', #9859, .T. ) ;
#35569=ORIENTED_EDGE ( 'NONE', *, *, #25464, .T. ) ;
#35572=CARTESIAN_POINT ( 'NONE',  ( 17.99999999999999645, 0.000000000000000000, 0.000000000000000000 ) ) ;
#35578=ORIENTED_EDGE ( 'NONE', *, *, #24098, .T. ) ;
#35579=EDGE_CURVE ( 'NONE', #16529, #2667, #16687, .T. ) ;
#35581=LINE ( 'NONE', #2827, #26495 ) ;
#35583=ORIENTED_EDGE ( 'NONE', *, *, #41343, .F. ) ;
#35585=CIRCLE ( 'NONE', #6348, 120.5010000000000190 ) ;
#35587=ORIENTED_EDGE ( 'NONE', *, *, #12557, .F. ) ;
#35590=CARTESIAN_POINT ( 'NONE',  ( 17.99999999999999645, 0.000000000000000000, 0.000000000000000000 ) ) ;
#35591=AXIS2_PLACEMENT_3D ( 'NONE', #4246, #40021, #10595 ) ;
#35595=DIRECTION ( 'NONE',  ( 0.000000000000000000, 0.000000000000000000, 1.000000000000000000 ) ) ;
#35598=ADVANCED_FACE ( 'NONE', ( #30396 ), #6821, .F. ) ;
#35599=CARTESIAN_POINT ( 'NONE',  ( 0.000000000000000000, 71.21168426767107462, 86.70160608319346807 ) ) ;
#35605=ORIENTED_EDGE ( 'NONE', *, *, #22730, .F. ) ;
#35609=ORIENTED_EDGE ( 'NONE', *, *, #37600, .T. ) ;
#35611=EDGE_LOOP ( 'NONE', ( #35152, #29342, #33667, #14328 ) ) ;
#35613=DIRECTION ( 'NONE',  ( -1.000000000000000000, -0.000000000000000000, -0.000000000000000000 ) ) ;
#35617=DIRECTION ( 'NONE',  ( -1.000000000000000000, 0.000000000000000000, 0.000000000000000000 ) ) ;
#35618=CARTESIAN_POINT ( 'NONE',  ( 0.000000000000000000, 0.000000000000000000, 0.000000000000000000 ) ) ;
#35622=DIRECTION ( 'NONE',  ( -1.000000000000000000, 0.000000000000000000, 0.000000000000000000 ) ) ;
#35623=AXIS2_PLACEMENT_3D ( 'NONE', #32326, #25611, #29496 ) ;
#35624=DIRECTION ( 'NONE',  ( -1.000000000000000000, -0.000000000000000000, -0.000000000000000000 ) ) ;
#35626=AXIS2_PLACEMENT_3D ( 'NONE', #10274, #26650, #37685 ) ;
#35632=EDGE_LOOP ( 'NONE', ( #32340, #29267, #24323, #33123 ) ) ;
#35640=DIRECTION ( 'NONE',  ( 1.000000000000000000, 0.000000000000000000, 0.000000000000000000 ) ) ;
#35642=ADVANCED_FACE ( 'NONE', ( #20178 ), #13834, .F. ) ;
#35643=VERTEX_POINT ( 'NONE', #33437 ) ;
#35649=DIRECTION ( 'NONE',  ( -1.000000000000000000, -0.000000000000000000, 0.000000000000000000 ) ) ;
#35652=CARTESIAN_POINT ( 'NONE',  ( 0.000000000000000000, 107.2885202478273783, -54.86040852957203384 ) ) ;
#35653=CARTESIAN_POINT ( 'NONE',  ( 9.000000000000001776, 115.5737863835463628, -9.934782381632540904 ) ) ;
#35654=AXIS2_PLACEMENT_3D ( 'NONE', #30469, #14114, #20243 ) ;
#35656=CARTESIAN_POINT ( 'NONE',  ( 17.99999999999999645, 62.45178862086215332, 93.20969140437529177 ) ) ;
#35658=ORIENTED_EDGE ( 'NONE', *, *, #4541, .T. ) ;
#35660=CYLINDRICAL_SURFACE ( 'NONE', #33097, 116.0000000000000000 ) ;
#35663=DIRECTION ( 'NONE',  ( -1.000000000000000000, 0.000000000000000000, -0.000000000000000000 ) ) ;
#35668=EDGE_CURVE ( 'NONE', #25672, #14569, #22183, .T. ) ;
#35669=EDGE_CURVE ( 'NONE', #40129, #13510, #3979, .T. ) ;
#35670=LINE ( 'NONE', #9277, #18452 ) ;
#35671=EDGE_CURVE ( 'NONE', #13710, #9297, #4720, .T. ) ;
#35672=ORIENTED_EDGE ( 'NONE', *, *, #38570, .T. ) ;
#35673=CARTESIAN_POINT ( 'NONE',  ( 0.000000000000000000, 73.51007459736548810, -89.73443560133290475 ) ) ;
#35674=ORIENTED_EDGE ( 'NONE', *, *, #3883, .T. ) ;
#35675=DIRECTION ( 'NONE',  ( 0.000000000000000000, -3.528251137579946599E-15, -1.000000000000000000 ) ) ;
#35684=EDGE_LOOP ( 'NONE', ( #20490, #11808, #15368, #21184 ) ) ;
#35690=DIRECTION ( 'NONE',  ( 1.000000000000000000, 0.000000000000000000, 0.000000000000000000 ) ) ;
#35691=DIRECTION ( 'NONE',  ( -1.000000000000000000, 0.000000000000000000, 0.000000000000000000 ) ) ;
#35693=DIRECTION ( 'NONE',  ( 1.000000000000000000, 0.000000000000000000, 0.000000000000000000 ) ) ;
#35698=CARTESIAN_POINT ( 'NONE',  ( 17.99999999999999645, 0.000000000000000000, 0.000000000000000000 ) ) ;
#35699=ORIENTED_EDGE ( 'NONE', *, *, #18565, .T. ) ;
#35700=CARTESIAN_POINT ( 'NONE',  ( -10.00000000000000000, 0.000000000000000000, 0.000000000000000000 ) ) ;
#35701=LINE ( 'NONE', #15477, #12230 ) ;
#35703=EDGE_LOOP ( 'NONE', ( #6340, #3227, #12027, #6603 ) ) ;
#35704=ORIENTED_EDGE ( 'NONE', *, *, #31112, .T. ) ;
#35705=DIRECTION ( 'NONE',  ( -1.000000000000000000, 0.000000000000000000, 0.000000000000000000 ) ) ;
#35707=CARTESIAN_POINT ( 'NONE',  ( 0.000000000000000000, -74.56001736500559218, -88.86396238369110279 ) ) ;
#35708=ORIENTED_EDGE ( 'NONE', *, *, #30577, .T. ) ;
#35712=EDGE_CURVE ( 'NONE', #21873, #13037, #10296, .T. ) ;
#35718=DIRECTION ( 'NONE',  ( -1.000000000000000000, 0.000000000000000000, 0.000000000000000000 ) ) ;
#35719=CARTESIAN_POINT ( 'NONE',  ( 17.99999999999999645, -84.77518783075143460, 73.49448960231327987 ) ) ;
#35720=CARTESIAN_POINT ( 'NONE',  ( 17.99999999999999645, 41.33768078145642022, -104.3046912715537076 ) ) ;
#35721=VERTEX_POINT ( 'NONE', #13183 ) ;
#35722=LINE ( 'NONE', #26155, #39275 ) ;
#35728=ORIENTED_EDGE ( 'NONE', *, *, #22643, .F. ) ;
#35729=EDGE_CURVE ( 'NONE', #17094, #11164, #38218, .T. ) ;
#35732=AXIS2_PLACEMENT_3D ( 'NONE', #21124, #11489, #5133 ) ;
#35733=ORIENTED_EDGE ( 'NONE', *, *, #27111, .T. ) ;
#35735=ORIENTED_EDGE ( 'NONE', *, *, #12460, .T. ) ;
#35736=LINE ( 'NONE', #19438, #32099 ) ;
#35740=ORIENTED_EDGE ( 'NONE', *, *, #21375, .T. ) ;
#35741=DIRECTION ( 'NONE',  ( 1.000000000000000000, 0.000000000000000000, 0.000000000000000000 ) ) ;
#35744=DIRECTION ( 'NONE',  ( 1.000000000000000000, 0.000000000000000000, 0.000000000000000000 ) ) ;
#35745=ORIENTED_EDGE ( 'NONE', *, *, #6305, .F. ) ;
#35747=DIRECTION ( 'NONE',  ( 0.000000000000000000, 0.000000000000000000, 1.000000000000000000 ) ) ;
#35748=DIRECTION ( 'NONE',  ( 0.000000000000000000, -9.408669700213189617E-16, -1.000000000000000000 ) ) ;
#35751=CIRCLE ( 'NONE', #3697, 120.5010000000000190 ) ;
#35755=ADVANCED_FACE ( 'NONE', ( #14909 ), #24084, .F. ) ;
#35758=CIRCLE ( 'NONE', #40620, 116.0000000000000000 ) ;
#35761=CARTESIAN_POINT ( 'NONE',  ( 17.99999999999999645, 46.12538073176347808, 111.3235835452212825 ) ) ;
#35764=ORIENTED_EDGE ( 'NONE', *, *, #29198, .T. ) ;
#35766=DIRECTION ( 'NONE',  ( 0.000000000000000000, -0.8747630845319560589, -0.4845508703326597000 ) ) ;
#35775=VERTEX_POINT ( 'NONE', #18416 ) ;
#35779=DIRECTION ( 'NONE',  ( 1.000000000000000000, 0.000000000000000000, 0.000000000000000000 ) ) ;
#35783=CIRCLE ( 'NONE', #15628, 58.99999999999999289 ) ;
#35785=DIRECTION ( 'NONE',  ( 0.000000000000000000, -0.6382441836448261574, 0.7698339834299012807 ) ) ;
#35787=EDGE_CURVE ( 'NONE', #12205, #19014, #4755, .T. ) ;
#35788=CYLINDRICAL_SURFACE ( 'NONE', #25941, 120.5010000000000190 ) ;
#35789=DIRECTION ( 'NONE',  ( 1.000000000000000000, 0.000000000000000000, 0.000000000000000000 ) ) ;
#35790=ADVANCED_FACE ( 'NONE', ( #11196 ), #28001, .F. ) ;
#35791=CARTESIAN_POINT ( 'NONE',  ( 17.99999999999999645, 69.72480978690046527, 92.70626138606037614 ) ) ;
#35792=EDGE_CURVE ( 'NONE', #8378, #21461, #8251, .T. ) ;
#35793=CARTESIAN_POINT ( 'NONE',  ( 17.99999999999999645, -29.36437154452078246, 116.8684075565134890 ) ) ;
#35794=CARTESIAN_POINT ( 'NONE',  ( 17.99999999999999645, -41.62036691425604573, 113.0850832732712945 ) ) ;
#35796=DIRECTION ( 'NONE',  ( 1.000000000000000000, 0.000000000000000000, 0.000000000000000000 ) ) ;
#35801=CARTESIAN_POINT ( 'NONE',  ( 17.99999999999999645, -40.37724737310141165, 104.6802291180865865 ) ) ;
#35810=AXIS2_PLACEMENT_3D ( 'NONE', #24019, #31199, #41194 ) ;
#35813=DIRECTION ( 'NONE',  ( -1.000000000000000000, -0.000000000000000000, -0.000000000000000000 ) ) ;
#35815=VECTOR ( 'NONE', #14833, 1000.000000000000000 ) ;
#35816=CARTESIAN_POINT ( 'NONE',  ( 17.99999999999999645, 0.000000000000000000, 0.000000000000000000 ) ) ;
#35818=DIRECTION ( 'NONE',  ( 0.000000000000000000, 0.3641605752528168649, 0.9313361774523405412 ) ) ;
#35819=ADVANCED_FACE ( 'NONE', ( #21259 ), #34507, .F. ) ;
#35820=DIRECTION ( 'NONE',  ( 1.000000000000000000, 0.000000000000000000, 0.000000000000000000 ) ) ;
#35825=CARTESIAN_POINT ( 'NONE',  ( 17.99999999999999645, -69.90696807222551001, 98.15042952503490881 ) ) ;
#35828=DIRECTION ( 'NONE',  ( 1.000000000000000000, 0.000000000000000000, 0.000000000000000000 ) ) ;
#35830=EDGE_CURVE ( 'NONE', #20361, #4481, #36788, .T. ) ;
#35831=ORIENTED_EDGE ( 'NONE', *, *, #37501, .T. ) ;
#35833=ORIENTED_EDGE ( 'NONE', *, *, #4465, .F. ) ;
#35834=CARTESIAN_POINT ( 'NONE',  ( 17.99999999999999645, 111.9370513079675789, -44.61600100275060043 ) ) ;
#35835=AXIS2_PLACEMENT_3D ( 'NONE', #19342, #32613, #43060 ) ;
#35840=ORIENTED_EDGE ( 'NONE', *, *, #39664, .T. ) ;
#35845=CARTESIAN_POINT ( 'NONE',  ( 0.000000000000000000, 0.000000000000000000, 0.000000000000000000 ) ) ;
#35850=CARTESIAN_POINT ( 'NONE',  ( 17.99999999999999645, -8.827181066046698277, 120.1772519049559378 ) ) ;
#35851=DIRECTION ( 'NONE',  ( 0.000000000000000000, 0.7525707698561396874, -0.6585113790650372056 ) ) ;
#35853=CIRCLE ( 'NONE', #5902, 59.00000000000000711 ) ;
#35854=CYLINDRICAL_SURFACE ( 'NONE', #3160, 120.5010000000000190 ) ;
#35855=ORIENTED_EDGE ( 'NONE', *, *, #25362, .F. ) ;
#35856=CARTESIAN_POINT ( 'NONE',  ( 17.99999999999999645, 35.72777019205808813, -106.3569410558013715 ) ) ;
#35859=AXIS2_PLACEMENT_3D ( 'NONE', #7291, #37827, #4897 ) ;
#35860=DIRECTION ( 'NONE',  ( 0.000000000000000000, 0.000000000000000000, 1.000000000000000000 ) ) ;
#35861=LINE ( 'NONE', #35653, #12974 ) ;
#35863=FACE_OUTER_BOUND ( 'NONE', #28, .T. ) ;
#35864=CARTESIAN_POINT ( 'NONE',  ( 0.000000000000000000, -110.8621702203451065, 34.14058016547499363 ) ) ;
#35869=ORIENTED_EDGE ( 'NONE', *, *, #27266, .F. ) ;
#35874=DIRECTION ( 'NONE',  ( -1.000000000000000000, -0.000000000000000000, -0.000000000000000000 ) ) ;
#35875=CIRCLE ( 'NONE', #15039, 120.5010000000000190 ) ;
#35878=VERTEX_POINT ( 'NONE', #32528 ) ;
#35879=CARTESIAN_POINT ( 'NONE',  ( 17.99999999999999645, 115.9750404417044081, 2.406240749597859718 ) ) ;
#35881=DIRECTION ( 'NONE',  ( 0.000000000000000000, 0.000000000000000000, 1.000000000000000000 ) ) ;
#35888=DIRECTION ( 'NONE',  ( -1.000000000000000000, -0.000000000000000000, 0.000000000000000000 ) ) ;
#35890=CIRCLE ( 'NONE', #39375, 120.5010000000000190 ) ;
#35892=DIRECTION ( 'NONE',  ( 0.000000000000000000, 0.000000000000000000, 1.000000000000000000 ) ) ;
#35898=VERTEX_POINT ( 'NONE', #32110 ) ;
#35899=CYLINDRICAL_SURFACE ( 'NONE', #11536, 59.00000000000000000 ) ;
#35902=AXIS2_PLACEMENT_3D ( 'NONE', #12720, #16428, #15789 ) ;
#35903=DIRECTION ( 'NONE',  ( -1.000000000000000000, -0.000000000000000000, -0.000000000000000000 ) ) ;
#35904=EDGE_CURVE ( 'NONE', #37232, #11603, #6833, .T. ) ;
#35905=EDGE_CURVE ( 'NONE', #12448, #25238, #12486, .T. ) ;
#35912=DIRECTION ( 'NONE',  ( 0.000000000000000000, -0.8183027759081742403, 0.5747874102143992747 ) ) ;
#35914=ORIENTED_EDGE ( 'NONE', *, *, #21848, .F. ) ;
#35916=DIRECTION ( 'NONE',  ( -1.000000000000000000, -0.000000000000000000, -0.000000000000000000 ) ) ;
#35917=LINE ( 'NONE', #29618, #1764 ) ;
#35918=AXIS2_PLACEMENT_3D ( 'NONE', #35074, #31825, #5187 ) ;
#35920=DIRECTION ( 'NONE',  ( 1.000000000000000000, 0.000000000000000000, 0.000000000000000000 ) ) ;
#35924=DIRECTION ( 'NONE',  ( -1.000000000000000000, -0.000000000000000000, -0.000000000000000000 ) ) ;
#35935=CARTESIAN_POINT ( 'NONE',  ( 0.000000000000000000, -52.19040376560366923, -99.31985817764231683 ) ) ;
#35937=DIRECTION ( 'NONE',  ( 1.000000000000000000, 0.000000000000000000, 0.000000000000000000 ) ) ;
#35938=VERTEX_POINT ( 'NONE', #15979 ) ;
#35940=DIRECTION ( 'NONE',  ( 0.000000000000000000, -0.9574220383620081209, 0.2886919473396123981 ) ) ;
#35942=DIRECTION ( 'NONE',  ( -1.000000000000000000, 0.000000000000000000, 0.000000000000000000 ) ) ;
#35947=ORIENTED_EDGE ( 'NONE', *, *, #7623, .T. ) ;
#35948=CARTESIAN_POINT ( 'NONE',  ( 8.999999999999998224, -78.18175027177490222, 85.69488855492974722 ) ) ;
#35949=LINE ( 'NONE', #29650, #37779 ) ;
#35951=AXIS2_PLACEMENT_3D ( 'NONE', #17729, #10284, #14442 ) ;
#35952=ORIENTED_EDGE ( 'NONE', *, *, #25257, .F. ) ;
#35958=DIRECTION ( 'NONE',  ( -1.000000000000000000, 0.000000000000000000, 0.000000000000000000 ) ) ;
#35961=EDGE_CURVE ( 'NONE', #16718, #12969, #42112, .T. ) ;
#35967=ORIENTED_EDGE ( 'NONE', *, *, #12479, .T. ) ;
#35968=DIRECTION ( 'NONE',  ( -1.000000000000000000, -0.000000000000000000, -0.000000000000000000 ) ) ;
#35971=DIRECTION ( 'NONE',  ( 1.000000000000000000, -0.000000000000000000, -0.000000000000000000 ) ) ;
#35974=CIRCLE ( 'NONE', #21414, 116.0000000000000000 ) ;
#35975=AXIS2_PLACEMENT_3D ( 'NONE', #31993, #21986, #19355 ) ;
#35977=CARTESIAN_POINT ( 'NONE',  ( 17.99999999999999645, -110.0562500189201955, 49.07252625220073838 ) ) ;
#35981=EDGE_CURVE ( 'NONE', #29037, #189, #13846, .T. ) ;
#35982=ORIENTED_EDGE ( 'NONE', *, *, #21305, .F. ) ;
#35986=VECTOR ( 'NONE', #22607, 1000.000000000000000 ) ;
#35989=DIRECTION ( 'NONE',  ( -1.000000000000000000, 0.000000000000000000, 0.000000000000000000 ) ) ;
#35991=CARTESIAN_POINT ( 'NONE',  ( 17.99999999999999645, 0.000000000000000000, 0.000000000000000000 ) ) ;
#35992=ORIENTED_EDGE ( 'NONE', *, *, #22850, .T. ) ;
#35994=DIRECTION ( 'NONE',  ( 0.000000000000000000, 0.000000000000000000, 1.000000000000000000 ) ) ;
#35995=DIRECTION ( 'NONE',  ( 1.000000000000000000, -0.000000000000000000, 0.000000000000000000 ) ) ;
#35997=AXIS2_PLACEMENT_3D ( 'NONE', #36582, #20487, #4281 ) ;
#35998=CARTESIAN_POINT ( 'NONE',  ( 0.000000000000000000, -94.52951811191606168, 67.23221107124869889 ) ) ;
#36001=DIRECTION ( 'NONE',  ( 0.000000000000000000, 0.7164567402983164079, -0.6976315211349833900 ) ) ;
#36002=ORIENTED_EDGE ( 'NONE', *, *, #41841, .T. ) ;
#36004=CIRCLE ( 'NONE', #39489, 120.5010000000000332 ) ;
#36009=ORIENTED_EDGE ( 'NONE', *, *, #14964, .F. ) ;
#36010=CARTESIAN_POINT ( 'NONE',  ( 17.99999999999999645, 0.000000000000000000, 0.000000000000000000 ) ) ;
#36011=CIRCLE ( 'NONE', #26336, 59.00000000000000000 ) ;
#36013=EDGE_CURVE ( 'NONE', #29671, #33336, #25802, .T. ) ;
#36014=DIRECTION ( 'NONE',  ( 0.000000000000000000, -0.2631025642275089393, -0.9647678688145192583 ) ) ;
#36015=ORIENTED_EDGE ( 'NONE', *, *, #33439, .T. ) ;
#36016=DIRECTION ( 'NONE',  ( -1.000000000000000000, -0.000000000000000000, 0.000000000000000000 ) ) ;
#36020=DIRECTION ( 'NONE',  ( 0.000000000000000000, 0.000000000000000000, 1.000000000000000000 ) ) ;
#36022=DIRECTION ( 'NONE',  ( -1.000000000000000000, -0.000000000000000000, -0.000000000000000000 ) ) ;
#36023=EDGE_CURVE ( 'NONE', #34509, #21207, #34713, .T. ) ;
#36024=CARTESIAN_POINT ( 'NONE',  ( 0.000000000000000000, 0.000000000000000000, 0.000000000000000000 ) ) ;
#36025=VERTEX_POINT ( 'NONE', #29066 ) ;
#36026=EDGE_CURVE ( 'NONE', #33221, #25771, #40956, .T. ) ;
#36028=ORIENTED_EDGE ( 'NONE', *, *, #5886, .T. ) ;
#36030=ADVANCED_FACE ( 'NONE', ( #39059 ), #41706, .F. ) ;
#36038=AXIS2_PLACEMENT_3D ( 'NONE', #29724, #13153, #39506 ) ;
#36045=CIRCLE ( 'NONE', #39528, 116.0000000000000000 ) ;
#36046=CARTESIAN_POINT ( 'NONE',  ( 0.000000000000000000, 57.40245293794799153, -96.40140491896575270 ) ) ;
#36048=EDGE_CURVE ( 'NONE', #14037, #28151, #27766, .T. ) ;
#36049=DIRECTION ( 'NONE',  ( 1.000000000000000000, 0.000000000000000000, 0.000000000000000000 ) ) ;
#36051=CARTESIAN_POINT ( 'NONE',  ( 0.000000000000000000, 40.37724737310070111, 104.6802291180868565 ) ) ;
#36053=DIRECTION ( 'NONE',  ( 0.000000000000000000, 0.000000000000000000, 1.000000000000000000 ) ) ;
#36059=VERTEX_POINT ( 'NONE', #3677 ) ;
#36062=LINE ( 'NONE', #12966, #20492 ) ;
#36063=ORIENTED_EDGE ( 'NONE', *, *, #27625, .T. ) ;
#36064=CARTESIAN_POINT ( 'NONE',  ( 0.000000000000000000, -114.1529630473452386, 38.59523323561398200 ) ) ;
#36071=EDGE_CURVE ( 'NONE', #32693, #30365, #4040, .T. ) ;
#36072=VERTEX_POINT ( 'NONE', #33170 ) ;
#36076=AXIS2_PLACEMENT_3D ( 'NONE', #18021, #24550, #4206 ) ;
#36080=CARTESIAN_POINT ( 'NONE',  ( 17.99999999999999645, -84.62908780824929522, 85.78116633471262276 ) ) ;
#36081=DIRECTION ( 'NONE',  ( 0.000000000000000000, 0.000000000000000000, 1.000000000000000000 ) ) ;
#36083=CARTESIAN_POINT ( 'NONE',  ( 17.99999999999999645, -110.3490479609630910, -20.28201389785511211 ) ) ;
#36084=VERTEX_POINT ( 'NONE', #19681 ) ;
#36085=EDGE_CURVE ( 'NONE', #12374, #6899, #10262, .T. ) ;
#36086=DIRECTION ( 'NONE',  ( 1.000000000000000000, 0.000000000000000000, 0.000000000000000000 ) ) ;
#36089=DIRECTION ( 'NONE',  ( -1.000000000000000000, 0.000000000000000000, -0.000000000000000000 ) ) ;
#36091=CIRCLE ( 'NONE', #17244, 116.0000000000000000 ) ;
#36093=EDGE_CURVE ( 'NONE', #38913, #17808, #15234, .T. ) ;
#36094=FACE_OUTER_BOUND ( 'NONE', #16363, .T. ) ;
#36100=AXIS2_PLACEMENT_3D ( 'NONE', #15303, #2569, #21642 ) ;
#36103=CIRCLE ( 'NONE', #43044, 59.00000000000000000 ) ;
#36104=DIRECTION ( 'NONE',  ( 0.000000000000000000, 0.000000000000000000, 1.000000000000000000 ) ) ;
#36113=DIRECTION ( 'NONE',  ( 0.000000000000000000, -0.2113826236296314776, 0.9774033898178651203 ) ) ;
#36114=ORIENTED_EDGE ( 'NONE', *, *, #21622, .F. ) ;
#36118=DIRECTION ( 'NONE',  ( 0.000000000000000000, -0.7525707698561308057, -0.6585113790650474197 ) ) ;
#36119=EDGE_LOOP ( 'NONE', ( #32118, #39206, #29402, #40704 ) ) ;
#36121=LINE ( 'NONE', #32647, #11366 ) ;
#36123=ORIENTED_EDGE ( 'NONE', *, *, #6960, .F. ) ;
#36125=CARTESIAN_POINT ( 'NONE',  ( 0.000000000000000000, -87.74575819880118388, -75.87280091124561920 ) ) ;
#36130=VECTOR ( 'NONE', #6442, 1000.000000000000000 ) ;
#36131=DIRECTION ( 'NONE',  ( 0.000000000000000000, 0.000000000000000000, 1.000000000000000000 ) ) ;
#36134=AXIS2_PLACEMENT_3D ( 'NONE', #947, #14741, #40877 ) ;
#36135=DIRECTION ( 'NONE',  ( -1.000000000000000000, 0.000000000000000000, 0.000000000000000000 ) ) ;
#36136=ORIENTED_EDGE ( 'NONE', *, *, #41189, .F. ) ;
#36137=ADVANCED_FACE ( 'NONE', ( #2822 ), #27081, .F. ) ;
#36138=DIRECTION ( 'NONE',  ( -1.000000000000000000, -0.000000000000000000, -0.000000000000000000 ) ) ;
#36142=DIRECTION ( 'NONE',  ( 1.000000000000000000, 0.000000000000000000, 0.000000000000000000 ) ) ;
#36143=ORIENTED_EDGE ( 'NONE', *, *, #4244, .T. ) ;
#36146=CARTESIAN_POINT ( 'NONE',  ( 0.000000000000000000, 115.9387338813862129, -3.769613505534868736 ) ) ;
#36147=ORIENTED_EDGE ( 'NONE', *, *, #27805, .T. ) ;
#36150=CARTESIAN_POINT ( 'NONE',  ( 17.99999999999999645, 8.827181066047508295, -120.1772519049558667 ) ) ;
#36154=DIRECTION ( 'NONE',  ( -1.000000000000000000, -0.000000000000000000, -0.000000000000000000 ) ) ;
#36158=AXIS2_PLACEMENT_3D ( 'NONE', #32213, #28104, #11751 ) ;
#36163=ORIENTED_EDGE ( 'NONE', *, *, #11471, .F. ) ;
#36169=EDGE_LOOP ( 'NONE', ( #12662, #27349, #13840, #7128 ) ) ;
#36170=LINE ( 'NONE', #35948, #8785 ) ;
#36172=ORIENTED_EDGE ( 'NONE', *, *, #11676, .F. ) ;
#36173=ORIENTED_EDGE ( 'NONE', *, *, #4725, .T. ) ;
#36176=ORIENTED_EDGE ( 'NONE', *, *, #41189, .T. ) ;
#36177=CARTESIAN_POINT ( 'NONE',  ( 17.99999999999999645, 16.77566611177940104, -119.3275660838940553 ) ) ;
#36184=ADVANCED_FACE ( 'NONE', ( #30342 ), #40346, .F. ) ;
#36185=AXIS2_PLACEMENT_3D ( 'NONE', #13468, #96, #22885 ) ;
#36186=CARTESIAN_POINT ( 'NONE',  ( 0.000000000000000000, 23.10276247328100396, 118.2656051737070726 ) ) ;
#36188=AXIS2_PLACEMENT_3D ( 'NONE', #36709, #33, #16907 ) ;
#36189=VERTEX_POINT ( 'NONE', #23819 ) ;
#36191=EDGE_CURVE ( 'NONE', #33535, #39762, #42746, .T. ) ;
#36197=ORIENTED_EDGE ( 'NONE', *, *, #40881, .F. ) ;
#36200=DIRECTION ( 'NONE',  ( 0.000000000000000000, 0.6382441836448161654, 0.7698339834299094964 ) ) ;
#36201=CYLINDRICAL_SURFACE ( 'NONE', #1944, 59.00000000000000000 ) ;
#36204=CYLINDRICAL_SURFACE ( 'NONE', #10687, 116.0000000000000000 ) ;
#36205=CARTESIAN_POINT ( 'NONE',  ( 9.000000000000001776, -6.854627147197943415, -115.7972974066014018 ) ) ;
#36211=DIRECTION ( 'NONE',  ( 1.000000000000000000, 0.000000000000000000, 0.000000000000000000 ) ) ;
#36212=VERTEX_POINT ( 'NONE', #34040 ) ;
#36217=DIRECTION ( 'NONE',  ( 1.000000000000000000, 0.000000000000000000, 0.000000000000000000 ) ) ;
#36219=EDGE_LOOP ( 'NONE', ( #15472, #8502, #14352, #28324 ) ) ;
#36220=CARTESIAN_POINT ( 'NONE',  ( 17.99999999999999645, 111.1352304691229733, -15.40237066878481720 ) ) ;
#36223=ORIENTED_EDGE ( 'NONE', *, *, #28225, .F. ) ;
#36225=FACE_OUTER_BOUND ( 'NONE', #6130, .T. ) ;
#36226=DIRECTION ( 'NONE',  ( 1.000000000000000000, 0.000000000000000000, 0.000000000000000000 ) ) ;
#36227=VERTEX_POINT ( 'NONE', #38170 ) ;
#36230=AXIS2_PLACEMENT_3D ( 'NONE', #32504, #32083, #34919 ) ;
#36234=CARTESIAN_POINT ( 'NONE',  ( 17.99999999999999645, -25.18647942089817349, 113.2326863338526977 ) ) ;
#36235=ORIENTED_EDGE ( 'NONE', *, *, #17043, .F. ) ;
#36238=EDGE_LOOP ( 'NONE', ( #337, #41234, #28570, #30159 ) ) ;
#36239=DIRECTION ( 'NONE',  ( 0.000000000000000000, 0.9911528310040076395, -0.1327255272837190025 ) ) ;
#36243=AXIS2_PLACEMENT_3D ( 'NONE', #35991, #22962, #29057 ) ;
#36247=ORIENTED_EDGE ( 'NONE', *, *, #980, .T. ) ;
#36248=EDGE_LOOP ( 'NONE', ( #2779, #23784 ) ) ;
#36250=FACE_OUTER_BOUND ( 'NONE', #33555, .T. ) ;
#36253=CARTESIAN_POINT ( 'NONE',  ( 17.99999999999999645, 96.25468616236763353, -72.49500943364391503 ) ) ;
#36256=ORIENTED_EDGE ( 'NONE', *, *, #40266, .T. ) ;
#36258=ORIENTED_EDGE ( 'NONE', *, *, #8499, .F. ) ;
#36261=CARTESIAN_POINT ( 'NONE',  ( 0.000000000000000000, -29.36437154451922282, -116.8684075565139295 ) ) ;
#36262=CIRCLE ( 'NONE', #11834, 58.99999999999998579 ) ;
#36265=ORIENTED_EDGE ( 'NONE', *, *, #11920, .T. ) ;
#36267=ORIENTED_EDGE ( 'NONE', *, *, #18002, .T. ) ;
#36270=EDGE_CURVE ( 'NONE', #38197, #17094, #15292, .T. ) ;
#36273=CARTESIAN_POINT ( 'NONE',  ( 9.000000000000001776, -58.30069736313598128, -100.2847380560572930 ) ) ;
#36275=CIRCLE ( 'NONE', #8420, 58.99999999999999289 ) ;
#36276=EDGE_CURVE ( 'NONE', #18324, #21496, #26384, .T. ) ;
#36279=FACE_OUTER_BOUND ( 'NONE', #27671, .T. ) ;
#36292=DIRECTION ( 'NONE',  ( -1.000000000000000000, 0.000000000000000000, -0.000000000000000000 ) ) ;
#36293=ORIENTED_EDGE ( 'NONE', *, *, #31646, .T. ) ;
#36299=CARTESIAN_POINT ( 'NONE',  ( 17.99999999999999645, -47.58001226230612701, 110.7096808509482031 ) ) ;
#36301=ORIENTED_EDGE ( 'NONE', *, *, #38986, .F. ) ;
#36302=VECTOR ( 'NONE', #16262, 1000.000000000000000 ) ;
#36303=AXIS2_PLACEMENT_3D ( 'NONE', #40251, #23721, #36984 ) ;
#36305=ORIENTED_EDGE ( 'NONE', *, *, #35277, .T. ) ;
#36307=CARTESIAN_POINT ( 'NONE',  ( 17.99999999999999645, 2.418575551222434949, -120.4767259403368911 ) ) ;
#36312=VERTEX_POINT ( 'NONE', #37728 ) ;
#36313=CARTESIAN_POINT ( 'NONE',  ( 9.000000000000001776, -114.8812324315176312, 16.07179003769107339 ) ) ;
#36314=ORIENTED_EDGE ( 'NONE', *, *, #13535, .T. ) ;
#36315=AXIS2_PLACEMENT_3D ( 'NONE', #8028, #21397, #22191 ) ;
#36316=LINE ( 'NONE', #2711, #20069 ) ;
#36317=DIRECTION ( 'NONE',  ( 1.000000000000000000, 0.000000000000000000, 0.000000000000000000 ) ) ;
#36318=CARTESIAN_POINT ( 'NONE',  ( 0.000000000000000000, -0.6819280456820884240, -115.9979955608738607 ) ) ;
#36320=CARTESIAN_POINT ( 'NONE',  ( -10.00000000000000000, 0.000000000000000000, 0.000000000000000000 ) ) ;
#36325=ORIENTED_EDGE ( 'NONE', *, *, #5858, .T. ) ;
#36326=ADVANCED_FACE ( 'NONE', ( #21204 ), #28156, .F. ) ;
#36328=DIRECTION ( 'NONE',  ( 0.000000000000000000, 0.5963673585384969833, 0.8027116379309670036 ) ) ;
#36329=CARTESIAN_POINT ( 'NONE',  ( 0.000000000000000000, -115.0622509503833442, 14.72000021165104755 ) ) ;
#36330=ORIENTED_EDGE ( 'NONE', *, *, #10628, .F. ) ;
#36337=CIRCLE ( 'NONE', #34953, 58.99999999999999289 ) ;
#36341=ORIENTED_EDGE ( 'NONE', *, *, #11865, .F. ) ;
#36343=VERTEX_POINT ( 'NONE', #17940 ) ;
#36346=DIRECTION ( 'NONE',  ( 1.000000000000000000, 0.000000000000000000, 0.000000000000000000 ) ) ;
#36350=DIRECTION ( 'NONE',  ( -1.000000000000000000, -0.000000000000000000, -0.000000000000000000 ) ) ;
#36364=ORIENTED_EDGE ( 'NONE', *, *, #39763, .T. ) ;
#36368=CARTESIAN_POINT ( 'NONE',  ( 0.000000000000000000, -95.31344542257777164, 66.11616384574416827 ) ) ;
#36371=VERTEX_POINT ( 'NONE', #40775 ) ;
#36372=CARTESIAN_POINT ( 'NONE',  ( 0.000000000000000000, -100.8494052988166345, -65.95368414179012007 ) ) ;
#36373=ORIENTED_EDGE ( 'NONE', *, *, #19420, .F. ) ;
#36375=EDGE_CURVE ( 'NONE', #22361, #710, #10927, .T. ) ;
#36381=EDGE_CURVE ( 'NONE', #1564, #5006, #29595, .T. ) ;
#36383=ORIENTED_EDGE ( 'NONE', *, *, #35205, .T. ) ;
#36384=ORIENTED_EDGE ( 'NONE', *, *, #33042, .F. ) ;
#36386=ORIENTED_EDGE ( 'NONE', *, *, #42848, .F. ) ;
#36387=DIRECTION ( 'NONE',  ( 0.000000000000000000, -0.9968120070307509017, 0.07978610555307336094 ) ) ;
#36389=DIRECTION ( 'NONE',  ( 1.000000000000000000, 0.000000000000000000, 0.000000000000000000 ) ) ;
#36390=CARTESIAN_POINT ( 'NONE',  ( 9.000000000000001776, -5.492704054965900973, -115.8698847939556771 ) ) ;
#36392=CARTESIAN_POINT ( 'NONE',  ( 17.99999999999999645, 0.000000000000000000, 0.000000000000000000 ) ) ;
#36393=ORIENTED_EDGE ( 'NONE', *, *, #27625, .F. ) ;
#36395=LINE ( 'NONE', #8950, #23858 ) ;
#36396=EDGE_CURVE ( 'NONE', #18124, #35448, #39581, .T. ) ;
#36399=EDGE_LOOP ( 'NONE', ( #35704, #34822, #6874, #22143 ) ) ;
#36400=DIRECTION ( 'NONE',  ( -1.000000000000000000, 0.000000000000000000, -0.000000000000000000 ) ) ;
#36402=EDGE_CURVE ( 'NONE', #7888, #31916, #40297, .T. ) ;
#36411=DIRECTION ( 'NONE',  ( -1.000000000000000000, 0.000000000000000000, -0.000000000000000000 ) ) ;
#36412=FACE_OUTER_BOUND ( 'NONE', #3837, .T. ) ;
#36413=FACE_OUTER_BOUND ( 'NONE', #24988, .T. ) ;
#36415=CIRCLE ( 'NONE', #6467, 59.00000000000000000 ) ;
#36416=ORIENTED_EDGE ( 'NONE', *, *, #5542, .T. ) ;
#36418=FACE_OUTER_BOUND ( 'NONE', #22181, .T. ) ;
#36421=EDGE_CURVE ( 'NONE', #22420, #26402, #29882, .T. ) ;
#36426=ORIENTED_EDGE ( 'NONE', *, *, #19349, .T. ) ;
#36427=CIRCLE ( 'NONE', #21896, 58.99999999999998579 ) ;
#36428=ORIENTED_EDGE ( 'NONE', *, *, #32316, .F. ) ;
#36429=DIRECTION ( 'NONE',  ( 0.000000000000000000, 0.000000000000000000, 1.000000000000000000 ) ) ;
#36432=DIRECTION ( 'NONE',  ( 0.000000000000000000, -0.9714298932647074114, -0.2373266998711250908 ) ) ;
#36434=CARTESIAN_POINT ( 'NONE',  ( 0.000000000000000000, -114.1157422997281969, -20.82300072953048442 ) ) ;
#36436=CARTESIAN_POINT ( 'NONE',  ( 0.000000000000000000, -109.1131968883996848, -26.12628443612003437 ) ) ;
#36438=ADVANCED_FACE ( 'NONE', ( #39599 ), #8494, .F. ) ;
#36439=ADVANCED_FACE ( 'NONE', ( #21858 ), #34897, .F. ) ;
#36441=CARTESIAN_POINT ( 'NONE',  ( 17.99999999999999645, 34.03109950475885626, -115.5957406979046596 ) ) ;
#36444=VECTOR ( 'NONE', #34271, 1000.000000000000000 ) ;
#36445=CYLINDRICAL_SURFACE ( 'NONE', #31899, 59.00000000000000000 ) ;
#36446=ORIENTED_EDGE ( 'NONE', *, *, #28032, .F. ) ;
#36448=ADVANCED_FACE ( 'NONE', ( #6235 ), #22064, .F. ) ;
#36449=AXIS2_PLACEMENT_3D ( 'NONE', #40117, #23599, #40548 ) ;
#36451=ORIENTED_EDGE ( 'NONE', *, *, #31650, .F. ) ;
#36461=DIRECTION ( 'NONE',  ( 0.000000000000000000, 0.000000000000000000, 1.000000000000000000 ) ) ;
#36464=CIRCLE ( 'NONE', #227, 58.99999999999998579 ) ;
#36466=DIRECTION ( 'NONE',  ( 1.000000000000000000, 0.000000000000000000, 0.000000000000000000 ) ) ;
#36467=ORIENTED_EDGE ( 'NONE', *, *, #32961, .T. ) ;
#36469=ORIENTED_EDGE ( 'NONE', *, *, #25310, .F. ) ;
#36474=CIRCLE ( 'NONE', #28178, 59.00000000000000711 ) ;
#36475=CARTESIAN_POINT ( 'NONE',  ( 17.99999999999999645, 29.02167576844250618, -108.3790330702166926 ) ) ;
#36478=VERTEX_POINT ( 'NONE', #25130 ) ;
#36482=ORIENTED_EDGE ( 'NONE', *, *, #6960, .T. ) ;
#36483=FACE_OUTER_BOUND ( 'NONE', #6835, .T. ) ;
#36486=VERTEX_POINT ( 'NONE', #38583 ) ;
#36489=ORIENTED_EDGE ( 'NONE', *, *, #7961, .F. ) ;
#36490=FACE_OUTER_BOUND ( 'NONE', #14266, .T. ) ;
#36503=VECTOR ( 'NONE', #39663, 1000.000000000000000 ) ;
#36507=CYLINDRICAL_SURFACE ( 'NONE', #10004, 116.0000000000000000 ) ;
#36511=ADVANCED_FACE ( 'NONE', ( #30671 ), #20441, .F. ) ;
#36516=DIRECTION ( 'NONE',  ( 0.000000000000000000, -0.1062934856473523731, -0.9943348002101385363 ) ) ;
#36518=CYLINDRICAL_SURFACE ( 'NONE', #6543, 120.5010000000000190 ) ;
#36521=DIRECTION ( 'NONE',  ( 0.000000000000000000, 0.000000000000000000, 1.000000000000000000 ) ) ;
#36525=CARTESIAN_POINT ( 'NONE',  ( 8.999999999999998224, 112.5220807139884016, 28.19186676675879255 ) ) ;
#36528=VERTEX_POINT ( 'NONE', #4240 ) ;
#36529=LINE ( 'NONE', #43087, #13333 ) ;
#36535=VERTEX_POINT ( 'NONE', #36763 ) ;
#36538=CIRCLE ( 'NONE', #16398, 120.5010000000000190 ) ;
#36541=AXIS2_PLACEMENT_3D ( 'NONE', #25482, #39371, #36113 ) ;
#36542=ORIENTED_EDGE ( 'NONE', *, *, #14758, .F. ) ;
#36546=CYLINDRICAL_SURFACE ( 'NONE', #22321, 120.5010000000000190 ) ;
#36547=DIRECTION ( 'NONE',  ( 0.000000000000000000, -0.7525707698561308057, -0.6585113790650474197 ) ) ;
#36548=EDGE_CURVE ( 'NONE', #40777, #5141, #39806, .T. ) ;
#36553=VERTEX_POINT ( 'NONE', #17612 ) ;
#36555=FACE_OUTER_BOUND ( 'NONE', #6719, .T. ) ;
#36559=ADVANCED_FACE ( 'NONE', ( #17172 ), #14106, .F. ) ;
#36563=CARTESIAN_POINT ( 'NONE',  ( 17.99999999999999645, -69.72480978689985420, -92.70626138606085931 ) ) ;
#36566=CIRCLE ( 'NONE', #18517, 59.00000000000000711 ) ;
#36570=CARTESIAN_POINT ( 'NONE',  ( 17.99999999999999645, 0.000000000000000000, 0.000000000000000000 ) ) ;
#36573=CIRCLE ( 'NONE', #12940, 59.00000000000000000 ) ;
#36575=FACE_OUTER_BOUND ( 'NONE', #22488, .T. ) ;
#36580=DIRECTION ( 'NONE',  ( 0.000000000000000000, 0.000000000000000000, 1.000000000000000000 ) ) ;
#36582=CARTESIAN_POINT ( 'NONE',  ( 0.000000000000000000, 0.000000000000000000, 0.000000000000000000 ) ) ;
#36591=CIRCLE ( 'NONE', #42160, 120.5010000000000332 ) ;
#36596=AXIS2_PLACEMENT_3D ( 'NONE', #15419, #28294, #31760 ) ;
#36598=AXIS2_PLACEMENT_3D ( 'NONE', #40361, #13358, #13572 ) ;
#36601=DIRECTION ( 'NONE',  ( -1.000000000000000000, -0.000000000000000000, -0.000000000000000000 ) ) ;
#36604=CIRCLE ( 'NONE', #1762, 59.00000000000000711 ) ;
#36605=CYLINDRICAL_SURFACE ( 'NONE', #34174, 120.5010000000000190 ) ;
#36607=AXIS2_PLACEMENT_3D ( 'NONE', #28356, #41833, #41623 ) ;
#36608=DIRECTION ( 'NONE',  ( 1.000000000000000000, 0.000000000000000000, 0.000000000000000000 ) ) ;
#36617=VERTEX_POINT ( 'NONE', #6658 ) ;
#36619=CARTESIAN_POINT ( 'NONE',  ( 0.000000000000000000, 105.3681574666264282, 38.54638589714925700 ) ) ;
#36621=EDGE_CURVE ( 'NONE', #3514, #18580, #13181, .T. ) ;
#36622=DIRECTION ( 'NONE',  ( -1.000000000000000000, 0.000000000000000000, 0.000000000000000000 ) ) ;
#36626=EDGE_CURVE ( 'NONE', #5699, #23465, #21598, .T. ) ;
#36628=AXIS2_PLACEMENT_3D ( 'NONE', #33357, #3439, #23568 ) ;
#36631=VECTOR ( 'NONE', #21978, 1000.000000000000000 ) ;
#36632=DIRECTION ( 'NONE',  ( 0.000000000000000000, 0.000000000000000000, 1.000000000000000000 ) ) ;
#36633=AXIS2_PLACEMENT_3D ( 'NONE', #37538, #10709, #4145 ) ;
#36636=DIRECTION ( 'NONE',  ( 1.000000000000000000, -0.000000000000000000, -0.000000000000000000 ) ) ;
#36637=VERTEX_POINT ( 'NONE', #24583 ) ;
#36642=VERTEX_POINT ( 'NONE', #15201 ) ;
#36644=CARTESIAN_POINT ( 'NONE',  ( 17.99999999999999645, 51.98489025774302519, 108.7109110710163549 ) ) ;
#36648=EDGE_LOOP ( 'NONE', ( #23859, #42953, #34483, #35515 ) ) ;
#36653=DIRECTION ( 'NONE',  ( 0.000000000000000000, 0.000000000000000000, 1.000000000000000000 ) ) ;
#36654=VECTOR ( 'NONE', #8145, 1000.000000000000000 ) ;
#36655=DIRECTION ( 'NONE',  ( -1.000000000000000000, -0.000000000000000000, 0.000000000000000000 ) ) ;
#36657=VECTOR ( 'NONE', #22023, 1000.000000000000000 ) ;
#36658=CARTESIAN_POINT ( 'NONE',  ( 0.000000000000000000, 69.72480978690046527, 92.70626138606037614 ) ) ;
#36659=ORIENTED_EDGE ( 'NONE', *, *, #35496, .T. ) ;
#36660=AXIS2_PLACEMENT_3D ( 'NONE', #26948, #10574, #20001 ) ;
#36661=DIRECTION ( 'NONE',  ( 1.000000000000000000, 0.000000000000000000, 0.000000000000000000 ) ) ;
#36667=ORIENTED_EDGE ( 'NONE', *, *, #2413, .F. ) ;
#36673=ADVANCED_FACE ( 'NONE', ( #38480 ), #1618, .F. ) ;
#36675=ORIENTED_EDGE ( 'NONE', *, *, #39352, .T. ) ;
#36677=CARTESIAN_POINT ( 'NONE',  ( 0.000000000000000000, 0.000000000000000000, 0.000000000000000000 ) ) ;
#36681=VERTEX_POINT ( 'NONE', #5339 ) ;
#36683=CARTESIAN_POINT ( 'NONE',  ( 17.99999999999999645, -97.89532456239460601, -54.81585448086294576 ) ) ;
#36684=ADVANCED_FACE ( 'NONE', ( #34357 ), #4453, .F. ) ;
#36689=CARTESIAN_POINT ( 'NONE',  ( 0.000000000000000000, 16.77566611177774902, 119.3275660838943111 ) ) ;
#36696=ORIENTED_EDGE ( 'NONE', *, *, #12562, .T. ) ;
#36698=AXIS2_PLACEMENT_3D ( 'NONE', #17385, #36748, #37181 ) ;
#36702=CYLINDRICAL_SURFACE ( 'NONE', #345, 116.0000000000000000 ) ;
#36704=CARTESIAN_POINT ( 'NONE',  ( 17.99999999999999645, -42.87700105098536341, -107.7847984684009219 ) ) ;
#36706=DIRECTION ( 'NONE',  ( -1.000000000000000000, 0.000000000000000000, 0.000000000000000000 ) ) ;
#36709=CARTESIAN_POINT ( 'NONE',  ( 0.000000000000000000, 0.000000000000000000, 0.000000000000000000 ) ) ;
#36711=CIRCLE ( 'NONE', #38837, 120.5010000000000332 ) ;
#36721=AXIS2_PLACEMENT_3D ( 'NONE', #33923, #16944, #40234 ) ;
#36724=CARTESIAN_POINT ( 'NONE',  ( 0.000000000000000000, -34.03109950475653989, -115.5957406979053133 ) ) ;
#36725=ORIENTED_EDGE ( 'NONE', *, *, #22577, .F. ) ;
#36726=CYLINDRICAL_SURFACE ( 'NONE', #43049, 116.0000000000000000 ) ;
#36729=VECTOR ( 'NONE', #13656, 1000.000000000000000 ) ;
#36744=FACE_OUTER_BOUND ( 'NONE', #8327, .T. ) ;
#36745=VERTEX_POINT ( 'NONE', #41548 ) ;
#36746=CARTESIAN_POINT ( 'NONE',  ( 17.99999999999999645, -23.10276247328181398, 118.2656051737069021 ) ) ;
#36748=DIRECTION ( 'NONE',  ( -1.000000000000000000, -0.000000000000000000, -0.000000000000000000 ) ) ;
#36749=AXIS2_PLACEMENT_3D ( 'NONE', #2239, #15811, #28695 ) ;
#36750=DIRECTION ( 'NONE',  ( 0.000000000000000000, 0.000000000000000000, 1.000000000000000000 ) ) ;
#36752=EDGE_CURVE ( 'NONE', #4179, #5962, #43103, .T. ) ;
#36753=DIRECTION ( 'NONE',  ( -1.000000000000000000, -0.000000000000000000, -0.000000000000000000 ) ) ;
#36755=VERTEX_POINT ( 'NONE', #24371 ) ;
#36761=LINE ( 'NONE', #42869, #18796 ) ;
#36763=CARTESIAN_POINT ( 'NONE',  ( 17.99999999999999645, 51.98489025774302519, 108.7109110710163549 ) ) ;
#36764=ORIENTED_EDGE ( 'NONE', *, *, #15602, .F. ) ;
#36767=CIRCLE ( 'NONE', #39561, 116.0000000000000000 ) ;
#36770=ORIENTED_EDGE ( 'NONE', *, *, #38570, .F. ) ;
#36772=DIRECTION ( 'NONE',  ( 1.000000000000000000, 0.000000000000000000, 0.000000000000000000 ) ) ;
#36773=CARTESIAN_POINT ( 'NONE',  ( 17.99999999999999645, -118.8387007424469601, -19.94628303336605768 ) ) ;
#36777=VECTOR ( 'NONE', #17406, 1000.000000000000000 ) ;
#36778=EDGE_CURVE ( 'NONE', #19328, #39201, #2458, .T. ) ;
#36779=EDGE_CURVE ( 'NONE', #40725, #2052, #5531, .T. ) ;
#36781=DIRECTION ( 'NONE',  ( 1.000000000000000000, 0.000000000000000000, 0.000000000000000000 ) ) ;
#36782=ORIENTED_EDGE ( 'NONE', *, *, #13414, .T. ) ;
#36785=DIRECTION ( 'NONE',  ( 1.000000000000000000, 0.000000000000000000, 0.000000000000000000 ) ) ;
#36786=CARTESIAN_POINT ( 'NONE',  ( 0.000000000000000000, 64.69195966010022403, -96.28577441832183581 ) ) ;
#36788=CIRCLE ( 'NONE', #29159, 59.00000000000000711 ) ;
#36789=CARTESIAN_POINT ( 'NONE',  ( 0.000000000000000000, -73.51007459736489125, 89.73443560133338792 ) ) ;
#36790=ORIENTED_EDGE ( 'NONE', *, *, #36085, .F. ) ;
#36791=EDGE_CURVE ( 'NONE', #25336, #31117, #26464, .T. ) ;
#36792=AXIS2_PLACEMENT_3D ( 'NONE', #15064, #28142, #41642 ) ;
#36793=CIRCLE ( 'NONE', #18741, 116.0000000000000000 ) ;
#36795=EDGE_LOOP ( 'NONE', ( #34852, #23025, #39775, #17374 ) ) ;
#36797=VECTOR ( 'NONE', #14721, 1000.000000000000000 ) ;
#36799=ORIENTED_EDGE ( 'NONE', *, *, #28168, .F. ) ;
#36806=ORIENTED_EDGE ( 'NONE', *, *, #41424, .T. ) ;
#36808=CARTESIAN_POINT ( 'NONE',  ( 0.000000000000000000, 0.000000000000000000, 0.000000000000000000 ) ) ;
#36810=DIRECTION ( 'NONE',  ( -1.000000000000000000, -0.000000000000000000, -0.000000000000000000 ) ) ;
#36811=EDGE_LOOP ( 'NONE', ( #14517, #3432, #41551, #23362 ) ) ;
#36813=CARTESIAN_POINT ( 'NONE',  ( 0.000000000000000000, 19.12429268481714928, 114.4126803693779948 ) ) ;
#36814=VERTEX_POINT ( 'NONE', #5553 ) ;
#36822=AXIS2_PLACEMENT_3D ( 'NONE', #27233, #17878, #30721 ) ;
#36823=EDGE_CURVE ( 'NONE', #28231, #22633, #29543, .T. ) ;
#36824=ORIENTED_EDGE ( 'NONE', *, *, #10275, .T. ) ;
#36828=ORIENTED_EDGE ( 'NONE', *, *, #16565, .T. ) ;
#36829=CYLINDRICAL_SURFACE ( 'NONE', #28200, 120.5010000000000190 ) ;
#36830=ORIENTED_EDGE ( 'NONE', *, *, #39422, .F. ) ;
#36832=DIRECTION ( 'NONE',  ( 0.000000000000000000, 1.331914804436429787E-14, -1.000000000000000000 ) ) ;
#36835=DIRECTION ( 'NONE',  ( 1.000000000000000000, 0.000000000000000000, 0.000000000000000000 ) ) ;
#36836=LINE ( 'NONE', #36390, #27602 ) ;
#36838=DIRECTION ( 'NONE',  ( -1.000000000000000000, 0.000000000000000000, 0.000000000000000000 ) ) ;
#36839=DIRECTION ( 'NONE',  ( -1.000000000000000000, 0.000000000000000000, 0.000000000000000000 ) ) ;
#36840=ORIENTED_EDGE ( 'NONE', *, *, #20212, .T. ) ;
#36842=DIRECTION ( 'NONE',  ( -1.000000000000000000, 0.000000000000000000, 0.000000000000000000 ) ) ;
#36845=CARTESIAN_POINT ( 'NONE',  ( 0.000000000000000000, 0.000000000000000000, 0.000000000000000000 ) ) ;
#36849=DIRECTION ( 'NONE',  ( 1.000000000000000000, 0.000000000000000000, 0.000000000000000000 ) ) ;
#36853=VERTEX_POINT ( 'NONE', #19742 ) ;
#36854=AXIS2_PLACEMENT_3D ( 'NONE', #8876, #28960, #21595 ) ;
#36859=DIRECTION ( 'NONE',  ( -1.000000000000000000, 0.000000000000000000, -0.000000000000000000 ) ) ;
#36860=ORIENTED_EDGE ( 'NONE', *, *, #7384, .T. ) ;
#36862=CARTESIAN_POINT ( 'NONE',  ( 17.99999999999999645, 0.000000000000000000, 0.000000000000000000 ) ) ;
#36863=EDGE_CURVE ( 'NONE', #16214, #13292, #16714, .T. ) ;
#36867=CARTESIAN_POINT ( 'NONE',  ( 17.99999999999999645, 105.3681574666264282, 38.54638589714925700 ) ) ;
#36871=ORIENTED_EDGE ( 'NONE', *, *, #36950, .T. ) ;
#36874=ADVANCED_FACE ( 'NONE', ( #32798 ), #22813, .F. ) ;
#36875=ORIENTED_EDGE ( 'NONE', *, *, #40859, .F. ) ;
#36879=CARTESIAN_POINT ( 'NONE',  ( 17.99999999999999645, 96.25468616236763353, -72.49500943364391503 ) ) ;
#36880=CIRCLE ( 'NONE', #36188, 116.0000000000000000 ) ;
#36884=CARTESIAN_POINT ( 'NONE',  ( 17.99999999999999645, 0.000000000000000000, 0.000000000000000000 ) ) ;
#36886=VERTEX_POINT ( 'NONE', #36064 ) ;
#36891=DIRECTION ( 'NONE',  ( -1.000000000000000000, 0.000000000000000000, 0.000000000000000000 ) ) ;
#36895=EDGE_CURVE ( 'NONE', #2394, #41147, #40358, .T. ) ;
#36896=ORIENTED_EDGE ( 'NONE', *, *, #22139, .T. ) ;
#36897=DIRECTION ( 'NONE',  ( 1.000000000000000000, 0.000000000000000000, 0.000000000000000000 ) ) ;
#36898=ADVANCED_FACE ( 'NONE', ( #19530 ), #12971, .F. ) ;
#36899=CARTESIAN_POINT ( 'NONE',  ( 17.99999999999999645, 73.78980555658606022, 95.26571049922013401 ) ) ;
#36905=AXIS2_PLACEMENT_3D ( 'NONE', #25069, #15443, #37870 ) ;
#36906=ORIENTED_EDGE ( 'NONE', *, *, #4248, .F. ) ;
#36907=DIRECTION ( 'NONE',  ( -1.000000000000000000, -0.000000000000000000, -0.000000000000000000 ) ) ;
#36908=FACE_OUTER_BOUND ( 'NONE', #28720, .T. ) ;
#36909=CIRCLE ( 'NONE', #35510, 59.00000000000000000 ) ;
#36910=DIRECTION ( 'NONE',  ( -1.000000000000000000, -0.000000000000000000, -0.000000000000000000 ) ) ;
#36911=EDGE_CURVE ( 'NONE', #31565, #16155, #28908, .T. ) ;
#36914=ORIENTED_EDGE ( 'NONE', *, *, #28225, .T. ) ;
#36915=CARTESIAN_POINT ( 'NONE',  ( 0.000000000000000000, -59.47573314508800735, 99.59235496188593117 ) ) ;
#36919=CARTESIAN_POINT ( 'NONE',  ( 17.99999999999999645, -17.33727698085101565, -110.8498592715975519 ) ) ;
#36920=VERTEX_POINT ( 'NONE', #3092 ) ;
#36923=LINE ( 'NONE', #10534, #22611 ) ;
#36924=EDGE_CURVE ( 'NONE', #21205, #28718, #12524, .T. ) ;
#36925=VERTEX_POINT ( 'NONE', #13618 ) ;
#36927=VERTEX_POINT ( 'NONE', #26697 ) ;
#36929=EDGE_CURVE ( 'NONE', #38864, #22351, #36880, .T. ) ;
#36931=CARTESIAN_POINT ( 'NONE',  ( 17.99999999999999645, 119.7318547011703629, -13.59315897125608430 ) ) ;
#36932=ADVANCED_FACE ( 'NONE', ( #36483 ), #37140, .F. ) ;
#36933=VERTEX_POINT ( 'NONE', #40611 ) ;
#36935=ORIENTED_EDGE ( 'NONE', *, *, #40806, .F. ) ;
#36937=VECTOR ( 'NONE', #34360, 1000.000000000000000 ) ;
#36938=VECTOR ( 'NONE', #1516, 1000.000000000000000 ) ;
#36939=CARTESIAN_POINT ( 'NONE',  ( -10.00000000000000000, 0.000000000000000000, 0.000000000000000000 ) ) ;
#36940=CARTESIAN_POINT ( 'NONE',  ( 17.99999999999999645, 0.000000000000000000, 0.000000000000000000 ) ) ;
#36943=ORIENTED_EDGE ( 'NONE', *, *, #4004, .F. ) ;
#36944=CARTESIAN_POINT ( 'NONE',  ( 0.000000000000000000, 0.000000000000000000, 0.000000000000000000 ) ) ;
#36946=CARTESIAN_POINT ( 'NONE',  ( 17.99999999999999645, -48.55277268144259040, -105.3500273609084843 ) ) ;
#36950=EDGE_CURVE ( 'NONE', #21320, #22368, #1344, .T. ) ;
#36951=CARTESIAN_POINT ( 'NONE',  ( 17.99999999999999645, 62.45178862086345362, -93.20969140437443912 ) ) ;
#36952=VERTEX_POINT ( 'NONE', #3735 ) ;
#36954=EDGE_CURVE ( 'NONE', #2814, #40741, #35479, .T. ) ;
#36955=CARTESIAN_POINT ( 'NONE',  ( 17.99999999999999645, 97.19627249181095863, 71.22763238166520239 ) ) ;
#36959=DIRECTION ( 'NONE',  ( -1.000000000000000000, 0.000000000000000000, -0.000000000000000000 ) ) ;
#36960=DIRECTION ( 'NONE',  ( 0.000000000000000000, 0.000000000000000000, -1.000000000000000000 ) ) ;
#36961=CIRCLE ( 'NONE', #42526, 58.99999999999997868 ) ;
#36963=DIRECTION ( 'NONE',  ( 1.000000000000000000, 0.000000000000000000, 0.000000000000000000 ) ) ;
#36965=AXIS2_PLACEMENT_3D ( 'NONE', #24867, #18760, #8243 ) ;
#36968=CIRCLE ( 'NONE', #29338, 58.99999999999999289 ) ;
#36971=LINE ( 'NONE', #30451, #22682 ) ;
#36974=CARTESIAN_POINT ( 'NONE',  ( 17.99999999999999645, 116.4607004671428570, 30.94182036827244531 ) ) ;
#36975=DIRECTION ( 'NONE',  ( -1.000000000000000000, 0.000000000000000000, 0.000000000000000000 ) ) ;
#36981=EDGE_CURVE ( 'NONE', #25282, #17781, #31331, .T. ) ;
#36982=DIRECTION ( 'NONE',  ( -1.000000000000000000, -0.000000000000000000, -0.000000000000000000 ) ) ;
#36984=DIRECTION ( 'NONE',  ( 0.000000000000000000, 0.000000000000000000, 1.000000000000000000 ) ) ;
#36986=ORIENTED_EDGE ( 'NONE', *, *, #2752, .F. ) ;
#36987=LINE ( 'NONE', #20451, #33088 ) ;
#36990=LINE ( 'NONE', #98, #24218 ) ;
#36994=ORIENTED_EDGE ( 'NONE', *, *, #28593, .F. ) ;
#36995=FACE_OUTER_BOUND ( 'NONE', #23853, .T. ) ;
#36996=ORIENTED_EDGE ( 'NONE', *, *, #19701, .T. ) ;
#37009=DIRECTION ( 'NONE',  ( 1.000000000000000000, 0.000000000000000000, 0.000000000000000000 ) ) ;
#37018=EDGE_CURVE ( 'NONE', #3310, #252, #4137, .T. ) ;
#37019=CARTESIAN_POINT ( 'NONE',  ( 0.000000000000000000, 0.000000000000000000, 0.000000000000000000 ) ) ;
#37023=CARTESIAN_POINT ( 'NONE',  ( 17.99999999999999645, 0.000000000000000000, 0.000000000000000000 ) ) ;
#37027=CARTESIAN_POINT ( 'NONE',  ( 17.99999999999999645, -40.37724737310141165, 104.6802291180865865 ) ) ;
#37028=ORIENTED_EDGE ( 'NONE', *, *, #8648, .F. ) ;
#37031=FACE_OUTER_BOUND ( 'NONE', #16092, .T. ) ;
#37034=CIRCLE ( 'NONE', #3592, 120.5010000000000190 ) ;
#37037=DIRECTION ( 'NONE',  ( -1.000000000000000000, 0.000000000000000000, 0.000000000000000000 ) ) ;
#37038=AXIS2_PLACEMENT_3D ( 'NONE', #37727, #17497, #10926 ) ;
#37040=ADVANCED_FACE ( 'NONE', ( #20606, #10757 ), #24091, .F. ) ;
#37050=ORIENTED_EDGE ( 'NONE', *, *, #2254, .F. ) ;
#37055=CYLINDRICAL_SURFACE ( 'NONE', #3880, 120.5010000000000190 ) ;
#37057=CYLINDRICAL_SURFACE ( 'NONE', #7863, 120.5010000000000190 ) ;
#37058=ADVANCED_FACE ( 'NONE', ( #693 ), #7478, .F. ) ;
#37066=ORIENTED_EDGE ( 'NONE', *, *, #22377, .T. ) ;
#37072=CARTESIAN_POINT ( 'NONE',  ( 17.99999999999999645, -108.8880088604273766, -39.99251838046071583 ) ) ;
#37078=ORIENTED_EDGE ( 'NONE', *, *, #16474, .T. ) ;
#37081=DIRECTION ( 'NONE',  ( -1.000000000000000000, -0.000000000000000000, -0.000000000000000000 ) ) ;
#37082=ORIENTED_EDGE ( 'NONE', *, *, #25283, .T. ) ;
#37083=CARTESIAN_POINT ( 'NONE',  ( 17.99999999999999645, -101.8011932243944386, -55.61040422519432980 ) ) ;
#37084=DIRECTION ( 'NONE',  ( 0.000000000000000000, 0.2113826236296184047, 0.9774033898178678959 ) ) ;
#37087=ORIENTED_EDGE ( 'NONE', *, *, #37600, .F. ) ;
#37088=AXIS2_PLACEMENT_3D ( 'NONE', #1961, #24491, #8082 ) ;
#37089=FACE_OUTER_BOUND ( 'NONE', #32674, .T. ) ;
#37090=ORIENTED_EDGE ( 'NONE', *, *, #20397, .F. ) ;
#37091=DIRECTION ( 'NONE',  ( -1.000000000000000000, -0.000000000000000000, 0.000000000000000000 ) ) ;
#37095=AXIS2_PLACEMENT_3D ( 'NONE', #15458, #22011, #41603 ) ;
#37097=DIRECTION ( 'NONE',  ( -1.000000000000000000, -0.000000000000000000, 0.000000000000000000 ) ) ;
#37099=DIRECTION ( 'NONE',  ( 0.000000000000000000, -0.7865515558026355825, -0.6175246149462008116 ) ) ;
#37100=CIRCLE ( 'NONE', #12043, 59.00000000000000711 ) ;
#37102=CARTESIAN_POINT ( 'NONE',  ( 17.99999999999999645, 0.000000000000000000, 0.000000000000000000 ) ) ;
#37103=CARTESIAN_POINT ( 'NONE',  ( 0.000000000000000000, 120.4984140710909202, 0.7894348306988416830 ) ) ;
#37106=ADVANCED_FACE ( 'NONE', ( #31481 ), #1569, .F. ) ;
#37107=ORIENTED_EDGE ( 'NONE', *, *, #20866, .T. ) ;
#37114=EDGE_LOOP ( 'NONE', ( #36725, #14956, #5916, #8030 ) ) ;
#37115=FACE_OUTER_BOUND ( 'NONE', #22205, .T. ) ;
#37120=ORIENTED_EDGE ( 'NONE', *, *, #11073, .T. ) ;
#37121=FACE_OUTER_BOUND ( 'NONE', #36219, .T. ) ;
#37122=ADVANCED_FACE ( 'NONE', ( #40837 ), #7687, .F. ) ;
#37123=DIRECTION ( 'NONE',  ( -1.000000000000000000, -0.000000000000000000, 0.000000000000000000 ) ) ;
#37125=VERTEX_POINT ( 'NONE', #24750 ) ;
#37128=DIRECTION ( 'NONE',  ( -1.000000000000000000, -0.000000000000000000, -0.000000000000000000 ) ) ;
#37129=DIRECTION ( 'NONE',  ( -1.000000000000000000, -0.000000000000000000, -0.000000000000000000 ) ) ;
#37132=CARTESIAN_POINT ( 'NONE',  ( 17.99999999999999645, -99.97660604680010010, 67.26937820704857529 ) ) ;
#37133=VERTEX_POINT ( 'NONE', #8549 ) ;
#37134=CARTESIAN_POINT ( 'NONE',  ( 0.000000000000000000, 0.000000000000000000, 0.000000000000000000 ) ) ;
#37136=CARTESIAN_POINT ( 'NONE',  ( 0.000000000000000000, 112.8457601792519256, -26.86697618949260402 ) ) ;
#37140=CYLINDRICAL_SURFACE ( 'NONE', #30649, 59.00000000000000000 ) ;
#37141=ORIENTED_EDGE ( 'NONE', *, *, #5491, .T. ) ;
#37145=DIRECTION ( 'NONE',  ( 0.000000000000000000, 0.9826841245925201918, 0.1852887240871181063 ) ) ;
#37149=AXIS2_PLACEMENT_3D ( 'NONE', #28519, #41569, #8410 ) ;
#37152=DIRECTION ( 'NONE',  ( 0.000000000000000000, -0.9826841245925190815, -0.1852887240871243235 ) ) ;
#37153=CARTESIAN_POINT ( 'NONE',  ( -10.00000000000000000, 0.000000000000000000, 0.000000000000000000 ) ) ;
#37154=ORIENTED_EDGE ( 'NONE', *, *, #37278, .F. ) ;
#37159=LINE ( 'NONE', #14073, #40771 ) ;
#37160=CIRCLE ( 'NONE', #22567, 120.5010000000000474 ) ;
#37165=AXIS2_PLACEMENT_3D ( 'NONE', #21000, #30779, #34252 ) ;
#37166=CARTESIAN_POINT ( 'NONE',  ( 17.99999999999999645, -93.26762629039475883, 76.29967815892324268 ) ) ;
#37168=ORIENTED_EDGE ( 'NONE', *, *, #25467, .F. ) ;
#37170=EDGE_CURVE ( 'NONE', #22504, #28053, #16047, .T. ) ;
#37171=DIRECTION ( 'NONE',  ( -1.000000000000000000, -0.000000000000000000, -0.000000000000000000 ) ) ;
#37172=CARTESIAN_POINT ( 'NONE',  ( 17.99999999999999645, 57.69704296431184787, 105.7900857083231472 ) ) ;
#37174=EDGE_CURVE ( 'NONE', #32990, #21041, #42477, .T. ) ;
#37176=DIRECTION ( 'NONE',  ( 0.000000000000000000, 0.000000000000000000, 1.000000000000000000 ) ) ;
#37178=ORIENTED_EDGE ( 'NONE', *, *, #18891, .F. ) ;
#37181=DIRECTION ( 'NONE',  ( 0.000000000000000000, 0.000000000000000000, 1.000000000000000000 ) ) ;
#37182=CARTESIAN_POINT ( 'NONE',  ( -10.00000000000000000, 0.000000000000000000, 0.000000000000000000 ) ) ;
#37183=DIRECTION ( 'NONE',  ( 0.000000000000000000, 0.9407002666710341243, -0.3392388661180279485 ) ) ;
#37186=CARTESIAN_POINT ( 'NONE',  ( 0.000000000000000000, -47.58001226230464908, -110.7096808509488284 ) ) ;
#37193=EDGE_CURVE ( 'NONE', #25554, #6179, #8764, .T. ) ;
#37194=CYLINDRICAL_SURFACE ( 'NONE', #8393, 59.00000000000000000 ) ;
#37195=EDGE_CURVE ( 'NONE', #11794, #8918, #36909, .T. ) ;
#37199=ORIENTED_EDGE ( 'NONE', *, *, #34966, .T. ) ;
#37203=DIRECTION ( 'NONE',  ( -1.000000000000000000, 0.000000000000000000, -0.000000000000000000 ) ) ;
#37208=EDGE_CURVE ( 'NONE', #41141, #1487, #8364, .T. ) ;
#37209=VERTEX_POINT ( 'NONE', #32319 ) ;
#37212=DIRECTION ( 'NONE',  ( -1.000000000000000000, 0.000000000000000000, -0.000000000000000000 ) ) ;
#37214=DIRECTION ( 'NONE',  ( 0.000000000000000000, 0.7525707698561399095, -0.6585113790650372056 ) ) ;
#37217=DIRECTION ( 'NONE',  ( 0.000000000000000000, 0.9213119778704139673, -0.3888241754733182676 ) ) ;
#37221=ORIENTED_EDGE ( 'NONE', *, *, #38068, .F. ) ;
#37224=DIRECTION ( 'NONE',  ( -1.000000000000000000, 0.000000000000000000, 0.000000000000000000 ) ) ;
#37232=VERTEX_POINT ( 'NONE', #32536 ) ;
#37233=FILL_AREA_STYLE ('',( #10634 ) ) ;
#37234=CIRCLE ( 'NONE', #7997, 116.0000000000000000 ) ;
#37238=ORIENTED_EDGE ( 'NONE', *, *, #12080, .F. ) ;
#37242=CIRCLE ( 'NONE', #5880, 120.5010000000000474 ) ;
#37247=CARTESIAN_POINT ( 'NONE',  ( 17.99999999999999645, 108.8684555192050425, -27.12806418649509865 ) ) ;
#37248=EDGE_CURVE ( 'NONE', #11164, #20981, #29274, .T. ) ;
#37251=EDGE_CURVE ( 'NONE', #20139, #10415, #35581, .T. ) ;
#37252=ORIENTED_EDGE ( 'NONE', *, *, #42296, .F. ) ;
#37254=VERTEX_POINT ( 'NONE', #39065 ) ;
#37255=DIRECTION ( 'NONE',  ( -1.000000000000000000, -0.000000000000000000, -0.000000000000000000 ) ) ;
#37257=DIRECTION ( 'NONE',  ( -1.000000000000000000, -0.000000000000000000, 0.000000000000000000 ) ) ;
#37259=CARTESIAN_POINT ( 'NONE',  ( 17.99999999999999645, 48.55277268144325120, 105.3500273609081432 ) ) ;
#37261=FACE_OUTER_BOUND ( 'NONE', #34084, .T. ) ;
#37265=CIRCLE ( 'NONE', #35176, 116.0000000000000000 ) ;
#37267=AXIS2_PLACEMENT_3D ( 'NONE', #24673, #37931, #8048 ) ;
#37270=ORIENTED_EDGE ( 'NONE', *, *, #12855, .T. ) ;
#37271=LINE ( 'NONE', #7387, #14155 ) ;
#37273=DIRECTION ( 'NONE',  ( 0.000000000000000000, 0.000000000000000000, 1.000000000000000000 ) ) ;
#37278=EDGE_CURVE ( 'NONE', #29277, #31219, #14656, .T. ) ;
#37284=AXIS2_PLACEMENT_3D ( 'NONE', #30583, #37313, #7428 ) ;
#37285=DIRECTION ( 'NONE',  ( 1.000000000000000000, 0.000000000000000000, 0.000000000000000000 ) ) ;
#37287=AXIS2_PLACEMENT_3D ( 'NONE', #38836, #32509, #42522 ) ;
#37290=DIRECTION ( 'NONE',  ( 0.000000000000000000, 0.2113826236296247885, -0.9774033898178665636 ) ) ;
#37294=CARTESIAN_POINT ( 'NONE',  ( 0.000000000000000000, -107.1354928292866759, -44.47455650398174498 ) ) ;
#37296=AXIS2_PLACEMENT_3D ( 'NONE', #27815, #713, #13638 ) ;
#37297=EDGE_LOOP ( 'NONE', ( #31205, #38611, #10163, #23963 ) ) ;
#37299=DIRECTION ( 'NONE',  ( 1.000000000000000000, 0.000000000000000000, 0.000000000000000000 ) ) ;
#37303=ADVANCED_FACE ( 'NONE', ( #12913 ), #22543, .F. ) ;
#37304=ORIENTED_EDGE ( 'NONE', *, *, #30000, .F. ) ;
#37308=CARTESIAN_POINT ( 'NONE',  ( 17.99999999999999645, 35.72777019205667415, 106.3569410558018404 ) ) ;
#37310=CARTESIAN_POINT ( 'NONE',  ( 0.000000000000000000, 59.07817985939141181, -105.0250430397503294 ) ) ;
#37312=ORIENTED_EDGE ( 'NONE', *, *, #36191, .F. ) ;
#37313=DIRECTION ( 'NONE',  ( -1.000000000000000000, -0.000000000000000000, -0.000000000000000000 ) ) ;
#37315=ORIENTED_EDGE ( 'NONE', *, *, #11635, .T. ) ;
#37316=CARTESIAN_POINT ( 'NONE',  ( 0.000000000000000000, 116.4607004671428570, 30.94182036827243465 ) ) ;
#37318=EDGE_CURVE ( 'NONE', #25294, #27015, #32737, .T. ) ;
#37319=CIRCLE ( 'NONE', #30359, 116.0000000000000000 ) ;
#37320=LINE ( 'NONE', #19921, #41267 ) ;
#37321=CARTESIAN_POINT ( 'NONE',  ( 9.000000000000001776, -35.78484819117709748, 110.3423972910431701 ) ) ;
#37322=AXIS2_PLACEMENT_3D ( 'NONE', #1027, #27913, #10446 ) ;
#37323=ORIENTED_EDGE ( 'NONE', *, *, #14553, .F. ) ;
#37324=VECTOR ( 'NONE', #14134, 1000.000000000000000 ) ;
#37326=CARTESIAN_POINT ( 'NONE',  ( 17.99999999999999645, -109.3506818544107659, -38.70953859161124910 ) ) ;
#37328=EDGE_LOOP ( 'NONE', ( #34770, #32433, #4707, #3328 ) ) ;
#37330=DIRECTION ( 'NONE',  ( -1.000000000000000000, -0.000000000000000000, -0.000000000000000000 ) ) ;
#37331=ORIENTED_EDGE ( 'NONE', *, *, #20791, .T. ) ;
#37332=VECTOR ( 'NONE', #5532, 1000.000000000000000 ) ;
#37333=AXIS2_PLACEMENT_3D ( 'NONE', #16867, #3695, #17074 ) ;
#37334=CARTESIAN_POINT ( 'NONE',  ( 17.99999999999999645, 51.27532863109503580, -99.79535634195073612 ) ) ;
#37337=CIRCLE ( 'NONE', #18592, 59.00000000000000000 ) ;
#37339=CARTESIAN_POINT ( 'NONE',  ( 17.99999999999999645, 5.456439917444967591, 112.0647122740742105 ) ) ;
#37344=VERTEX_POINT ( 'NONE', #5910 ) ;
#37347=ORIENTED_EDGE ( 'NONE', *, *, #28168, .T. ) ;
#37348=AXIS2_PLACEMENT_3D ( 'NONE', #30105, #15569, #29900 ) ;
#37352=ORIENTED_EDGE ( 'NONE', *, *, #30376, .T. ) ;
#37353=CARTESIAN_POINT ( 'NONE',  ( 17.99999999999999645, 29.36437154451999021, 116.8684075565137164 ) ) ;
#37355=EDGE_LOOP ( 'NONE', ( #25816, #32597, #26424, #11506 ) ) ;
#37356=VECTOR ( 'NONE', #18544, 1000.000000000000000 ) ;
#37357=LINE ( 'NONE', #40186, #30239 ) ;
#37359=ORIENTED_EDGE ( 'NONE', *, *, #20978, .T. ) ;
#37360=AXIS2_PLACEMENT_3D ( 'NONE', #4663, #16223, #19943 ) ;
#37361=DIRECTION ( 'NONE',  ( 0.000000000000000000, 0.000000000000000000, -1.000000000000000000 ) ) ;
#37364=AXIS2_PLACEMENT_3D ( 'NONE', #38875, #42565, #22767 ) ;
#37365=VERTEX_POINT ( 'NONE', #1994 ) ;
#37368=EDGE_CURVE ( 'NONE', #13787, #26181, #15376, .T. ) ;
#37375=DIRECTION ( 'NONE',  ( 1.000000000000000000, 0.000000000000000000, 0.000000000000000000 ) ) ;
#37378=CYLINDRICAL_SURFACE ( 'NONE', #394, 116.0000000000000000 ) ;
#37380=VERTEX_POINT ( 'NONE', #3909 ) ;
#37382=CARTESIAN_POINT ( 'NONE',  ( 0.000000000000000000, 110.1579703617969130, -21.29539948940136540 ) ) ;
#37385=VECTOR ( 'NONE', #22425, 1000.000000000000000 ) ;
#37386=ORIENTED_EDGE ( 'NONE', *, *, #28317, .T. ) ;
#37390=VERTEX_POINT ( 'NONE', #3034 ) ;
#37392=DIRECTION ( 'NONE',  ( 1.000000000000000000, 0.000000000000000000, 0.000000000000000000 ) ) ;
#37393=DIRECTION ( 'NONE',  ( -1.000000000000000000, -0.000000000000000000, 0.000000000000000000 ) ) ;
#37394=AXIS2_PLACEMENT_3D ( 'NONE', #18303, #5152, #14794 ) ;
#37398=ORIENTED_EDGE ( 'NONE', *, *, #16627, .T. ) ;
#37400=AXIS2_PLACEMENT_3D ( 'NONE', #8201, #11712, #31332 ) ;
#37401=DIRECTION ( 'NONE',  ( 0.000000000000000000, -0.6783118362696075598, -0.7347741508630750706 ) ) ;
#37402=CARTESIAN_POINT ( 'NONE',  ( 17.99999999999999645, 111.2721026680460596, 44.61974821237341615 ) ) ;
#37404=EDGE_LOOP ( 'NONE', ( #36172, #41957, #30568, #8061 ) ) ;
#37405=DIRECTION ( 'NONE',  ( 0.000000000000000000, 0.000000000000000000, 1.000000000000000000 ) ) ;
#37408=ORIENTED_EDGE ( 'NONE', *, *, #38823, .T. ) ;
#37410=ORIENTED_EDGE ( 'NONE', *, *, #33010, .T. ) ;
#37413=CIRCLE ( 'NONE', #29095, 116.0000000000000000 ) ;
#37416=AXIS2_PLACEMENT_3D ( 'NONE', #20386, #14254, #23872 ) ;
#37417=CARTESIAN_POINT ( 'NONE',  ( 0.000000000000000000, 75.72520367775085504, 82.78868281116005789 ) ) ;
#37419=ORIENTED_EDGE ( 'NONE', *, *, #16007, .T. ) ;
#37420=CYLINDRICAL_SURFACE ( 'NONE', #30790, 116.0000000000000000 ) ;
#37422=AXIS2_PLACEMENT_3D ( 'NONE', #41140, #3832, #24621 ) ;
#37425=CYLINDRICAL_SURFACE ( 'NONE', #6819, 120.5010000000000190 ) ;
#37428=VERTEX_POINT ( 'NONE', #26645 ) ;
#37430=ORIENTED_EDGE ( 'NONE', *, *, #26348, .T. ) ;
#37435=DIRECTION ( 'NONE',  ( 0.000000000000000000, -0.1590634960190596137, -0.9872683547213465527 ) ) ;
#37438=CARTESIAN_POINT ( 'NONE',  ( 17.99999999999999645, 119.8996782608629985, 12.02323392193397211 ) ) ;
#37444=EDGE_CURVE ( 'NONE', #10305, #41147, #32954, .T. ) ;
#37445=CARTESIAN_POINT ( 'NONE',  ( 0.000000000000000000, -114.1157422997284669, 20.82300072952894610 ) ) ;
#37449=DIRECTION ( 'NONE',  ( 0.000000000000000000, -0.9574220383620022368, -0.2886919473396314384 ) ) ;
#37452=ORIENTED_EDGE ( 'NONE', *, *, #24164, .F. ) ;
#37453=CARTESIAN_POINT ( 'NONE',  ( 0.000000000000000000, 97.19627249181095863, 71.22763238166520239 ) ) ;
#37454=AXIS2_PLACEMENT_3D ( 'NONE', #16000, #22345, #19072 ) ;
#37457=SURFACE_SIDE_STYLE ('',( #24189 ) ) ;
#37458=DIRECTION ( 'NONE',  ( 0.000000000000000000, 0.9996456111234526265, -0.02662052143777148688 ) ) ;
#37459=VECTOR ( 'NONE', #33866, 1000.000000000000000 ) ;
#37460=CARTESIAN_POINT ( 'NONE',  ( 17.99999999999999645, 71.21168426767221149, -86.70160608319253015 ) ) ;
#37462=LINE ( 'NONE', #14798, #19845 ) ;
#37463=ORIENTED_EDGE ( 'NONE', *, *, #28948, .F. ) ;
#37464=DIRECTION ( 'NONE',  ( -1.000000000000000000, -0.000000000000000000, 0.000000000000000000 ) ) ;
#37469=VERTEX_POINT ( 'NONE', #26859 ) ;
#37470=DIRECTION ( 'NONE',  ( 0.000000000000000000, -0.6783118362696074488, -0.7347741508630751817 ) ) ;
#37486=DIRECTION ( 'NONE',  ( 0.000000000000000000, 0.000000000000000000, 1.000000000000000000 ) ) ;
#37487=DIRECTION ( 'NONE',  ( -1.000000000000000000, -0.000000000000000000, -0.000000000000000000 ) ) ;
#37488=AXIS2_PLACEMENT_3D ( 'NONE', #1870, #15232, #35033 ) ;
#37490=AXIS2_PLACEMENT_3D ( 'NONE', #31498, #1583, #7707 ) ;
#37491=AXIS2_PLACEMENT_3D ( 'NONE', #10323, #10090, #23231 ) ;
#37494=EDGE_LOOP ( 'NONE', ( #20043, #2244, #26114, #334 ) ) ;
#37495=DIRECTION ( 'NONE',  ( 0.000000000000000000, 0.000000000000000000, 1.000000000000000000 ) ) ;
#37496=CIRCLE ( 'NONE', #27056, 59.00000000000000000 ) ;
#37498=DIRECTION ( 'NONE',  ( 0.000000000000000000, 0.000000000000000000, 1.000000000000000000 ) ) ;
#37501=EDGE_CURVE ( 'NONE', #12205, #33352, #9756, .T. ) ;
#37505=EDGE_CURVE ( 'NONE', #13412, #37603, #17296, .T. ) ;
#37510=AXIS2_PLACEMENT_3D ( 'NONE', #16292, #26113, #42650 ) ;
#37513=EDGE_LOOP ( 'NONE', ( #37078, #24640, #33202, #21177 ) ) ;
#37514=DIRECTION ( 'NONE',  ( 0.000000000000000000, 0.9911528310040066403, 0.1327255272837255529 ) ) ;
#37515=DIRECTION ( 'NONE',  ( 1.000000000000000000, 0.000000000000000000, 0.000000000000000000 ) ) ;
#37516=CIRCLE ( 'NONE', #15299, 59.00000000000000000 ) ;
#37519=DIRECTION ( 'NONE',  ( 1.000000000000000000, 0.000000000000000000, 0.000000000000000000 ) ) ;
#37522=ORIENTED_EDGE ( 'NONE', *, *, #4961, .T. ) ;
#37524=DIRECTION ( 'NONE',  ( -1.000000000000000000, 0.000000000000000000, 0.000000000000000000 ) ) ;
#37525=VERTEX_POINT ( 'NONE', #27087 ) ;
#37526=CARTESIAN_POINT ( 'NONE',  ( 0.000000000000000000, -69.90696807222415998, -98.15042952503588936 ) ) ;
#37527=ORIENTED_EDGE ( 'NONE', *, *, #41312, .F. ) ;
#37528=ADVANCED_FACE ( 'NONE', ( #7195 ), #6776, .F. ) ;
#37533=ORIENTED_EDGE ( 'NONE', *, *, #129, .F. ) ;
#37538=CARTESIAN_POINT ( 'NONE',  ( 0.000000000000000000, 62.45178862086215332, 93.20969140437529177 ) ) ;
#37540=CARTESIAN_POINT ( 'NONE',  ( 0.000000000000000000, 119.7318547011701497, 13.59315897125768124 ) ) ;
#37546=ORIENTED_EDGE ( 'NONE', *, *, #4433, .T. ) ;
#37548=DIRECTION ( 'NONE',  ( 0.000000000000000000, 0.000000000000000000, 1.000000000000000000 ) ) ;
#37551=ORIENTED_EDGE ( 'NONE', *, *, #26933, .F. ) ;
#37552=ADVANCED_FACE ( 'NONE', ( #17947 ), #37951, .F. ) ;
#37557=ADVANCED_FACE ( 'NONE', ( #14429 ), #4805, .F. ) ;
#37558=DIRECTION ( 'NONE',  ( -1.000000000000000000, 0.000000000000000000, 0.000000000000000000 ) ) ;
#37559=CYLINDRICAL_SURFACE ( 'NONE', #9588, 58.99999999999999289 ) ;
#37560=EDGE_CURVE ( 'NONE', #16913, #1690, #29993, .T. ) ;
#37561=DIRECTION ( 'NONE',  ( -1.000000000000000000, -0.000000000000000000, -0.000000000000000000 ) ) ;
#37562=LINE ( 'NONE', #7019, #1525 ) ;
#37563=ORIENTED_EDGE ( 'NONE', *, *, #25485, .T. ) ;
#37566=CARTESIAN_POINT ( 'NONE',  ( 17.99999999999999645, 0.000000000000000000, 0.000000000000000000 ) ) ;
#37567=CARTESIAN_POINT ( 'NONE',  ( 0.000000000000000000, 0.000000000000000000, 0.000000000000000000 ) ) ;
#37570=VECTOR ( 'NONE', #5752, 1000.000000000000000 ) ;
#37572=DIRECTION ( 'NONE',  ( 0.000000000000000000, 0.000000000000000000, 1.000000000000000000 ) ) ;
#37575=DIRECTION ( 'NONE',  ( 0.000000000000000000, 0.000000000000000000, 1.000000000000000000 ) ) ;
#37577=ORIENTED_EDGE ( 'NONE', *, *, #36621, .F. ) ;
#37578=DIRECTION ( 'NONE',  ( -1.000000000000000000, -0.000000000000000000, -0.000000000000000000 ) ) ;
#37579=VERTEX_POINT ( 'NONE', #11583 ) ;
#37581=ORIENTED_EDGE ( 'NONE', *, *, #4411, .F. ) ;
#37585=CARTESIAN_POINT ( 'NONE',  ( -10.00000000000000000, 0.000000000000000000, 0.000000000000000000 ) ) ;
#37586=EDGE_LOOP ( 'NONE', ( #30202, #41758, #28687, #8123 ) ) ;
#37588=DIRECTION ( 'NONE',  ( -1.000000000000000000, -0.000000000000000000, 0.000000000000000000 ) ) ;
#37589=CYLINDRICAL_SURFACE ( 'NONE', #33954, 59.00000000000000000 ) ;
#37594=AXIS2_PLACEMENT_3D ( 'NONE', #38465, #31725, #22796 ) ;
#37595=CARTESIAN_POINT ( 'NONE',  ( 8.999999999999998224, 115.5737863835462349, 9.934782381634081005 ) ) ;
#37597=AXIS2_PLACEMENT_3D ( 'NONE', #1135, #18212, #1354 ) ;
#37600=EDGE_CURVE ( 'NONE', #8918, #33767, #24694, .T. ) ;
#37602=ORIENTED_EDGE ( 'NONE', *, *, #38261, .F. ) ;
#37603=VERTEX_POINT ( 'NONE', #40783 ) ;
#37607=CARTESIAN_POINT ( 'NONE',  ( 0.000000000000000000, -112.1702510623870666, 2.471285140322257323 ) ) ;
#37614=DIRECTION ( 'NONE',  ( 0.000000000000000000, 0.8993121301712202476, -0.4373073204588531770 ) ) ;
#37615=DIRECTION ( 'NONE',  ( 0.000000000000000000, 0.000000000000000000, 1.000000000000000000 ) ) ;
#37617=EDGE_LOOP ( 'NONE', ( #20893, #18875, #25405, #41205 ) ) ;
#37618=DIRECTION ( 'NONE',  ( -1.000000000000000000, -0.000000000000000000, -0.000000000000000000 ) ) ;
#37621=AXIS2_PLACEMENT_3D ( 'NONE', #6376, #1058, #9665 ) ;
#37622=EDGE_LOOP ( 'NONE', ( #24130, #37452, #2682, #17400 ) ) ;
#37624=ORIENTED_EDGE ( 'NONE', *, *, #42325, .T. ) ;
#37630=DIRECTION ( 'NONE',  ( 1.000000000000000000, 0.000000000000000000, 0.000000000000000000 ) ) ;
#37632=EDGE_LOOP ( 'NONE', ( #8985, #36314, #18978, #11030 ) ) ;
#37634=DIRECTION ( 'NONE',  ( 1.000000000000000000, -0.000000000000000000, 0.000000000000000000 ) ) ;
#37639=( NAMED_UNIT ( * ) PLANE_ANGLE_UNIT ( ) SI_UNIT ( $, .RADIAN. ) );
#37646=EDGE_CURVE ( 'NONE', #6459, #33918, #27217, .T. ) ;
#37648=EDGE_CURVE ( 'NONE', #2879, #9347, #14865, .T. ) ;
#37650=ORIENTED_EDGE ( 'NONE', *, *, #33189, .F. ) ;
#37653=ORIENTED_EDGE ( 'NONE', *, *, #17864, .T. ) ;
#37661=ADVANCED_FACE ( 'NONE', ( #31636 ), #27512, .F. ) ;
#37662=ORIENTED_EDGE ( 'NONE', *, *, #40195, .F. ) ;
#37666=EDGE_CURVE ( 'NONE', #19378, #6489, #40565, .T. ) ;
#37671=VERTEX_POINT ( 'NONE', #37310 ) ;
#37672=CARTESIAN_POINT ( 'NONE',  ( 8.999999999999998224, 73.51007459736548810, -89.73443560133290475 ) ) ;
#37679=AXIS2_PLACEMENT_3D ( 'NONE', #33720, #30477, #40471 ) ;
#37681=DIRECTION ( 'NONE',  ( -1.000000000000000000, -0.000000000000000000, 0.000000000000000000 ) ) ;
#37684=ORIENTED_EDGE ( 'NONE', *, *, #26503, .F. ) ;
#37685=DIRECTION ( 'NONE',  ( 0.000000000000000000, 0.000000000000000000, 1.000000000000000000 ) ) ;
#37687=DIRECTION ( 'NONE',  ( -1.000000000000000000, 0.000000000000000000, 0.000000000000000000 ) ) ;
#37688=EDGE_CURVE ( 'NONE', #2641, #35377, #29303, .T. ) ;
#37692=VERTEX_POINT ( 'NONE', #24271 ) ;
#37693=LINE ( 'NONE', #7812, #12678 ) ;
#37701=CYLINDRICAL_SURFACE ( 'NONE', #22, 120.5010000000000190 ) ;
#37706=ORIENTED_EDGE ( 'NONE', *, *, #3804, .T. ) ;
#37714=ADVANCED_FACE ( 'NONE', ( #15942 ), #39018, .F. ) ;
#37715=CARTESIAN_POINT ( 'NONE',  ( 0.000000000000000000, 80.02407177073062883, -78.64108602299866391 ) ) ;
#37718=EDGE_CURVE ( 'NONE', #22420, #27172, #5587, .T. ) ;
#37720=CARTESIAN_POINT ( 'NONE',  ( 9.000000000000001776, 112.5220807139887853, -28.19186676675729331 ) ) ;
#37721=VERTEX_POINT ( 'NONE', #12450 ) ;
#37723=DIRECTION ( 'NONE',  ( -1.000000000000000000, 0.000000000000000000, -0.000000000000000000 ) ) ;
#37726=ORIENTED_EDGE ( 'NONE', *, *, #14546, .F. ) ;
#37727=CARTESIAN_POINT ( 'NONE',  ( 17.99999999999999645, 0.000000000000000000, 0.000000000000000000 ) ) ;
#37728=CARTESIAN_POINT ( 'NONE',  ( 17.99999999999999645, -0.6819280456836842585, 115.9979955608738607 ) ) ;
#37730=DIRECTION ( 'NONE',  ( 1.000000000000000000, 0.000000000000000000, 0.000000000000000000 ) ) ;
#37731=ORIENTED_EDGE ( 'NONE', *, *, #39655, .F. ) ;
#37732=DIRECTION ( 'NONE',  ( -1.000000000000000000, 0.000000000000000000, 0.000000000000000000 ) ) ;
#37733=ORIENTED_EDGE ( 'NONE', *, *, #32301, .T. ) ;
#37734=DIRECTION ( 'NONE',  ( -1.000000000000000000, -0.000000000000000000, -0.000000000000000000 ) ) ;
#37735=FACE_OUTER_BOUND ( 'NONE', #30192, .T. ) ;
#37737=EDGE_CURVE ( 'NONE', #21959, #6529, #18195, .T. ) ;
#37739=EDGE_CURVE ( 'NONE', #35216, #18335, #15411, .T. ) ;
#37741=FACE_OUTER_BOUND ( 'NONE', #12929, .T. ) ;
#37742=EDGE_LOOP ( 'NONE', ( #25682, #25665, #5777, #32910 ) ) ;
#37743=FACE_OUTER_BOUND ( 'NONE', #20672, .T. ) ;
#37744=CIRCLE ( 'NONE', #7096, 58.99999999999999289 ) ;
#37745=AXIS2_PLACEMENT_3D ( 'NONE', #6034, #13039, #18969 ) ;
#37746=CARTESIAN_POINT ( 'NONE',  ( 17.99999999999999645, -5.456439917444183330, -112.0647122740742390 ) ) ;
#37748=AXIS2_PLACEMENT_3D ( 'NONE', #33596, #3676, #10693 ) ;
#37749=FACE_OUTER_BOUND ( 'NONE', #1074, .T. ) ;
#37753=ADVANCED_FACE ( 'NONE', ( #12653 ), #15722, .F. ) ;
#37757=DIRECTION ( 'NONE',  ( 0.000000000000000000, 0.000000000000000000, 1.000000000000000000 ) ) ;
#37758=CARTESIAN_POINT ( 'NONE',  ( 0.000000000000000000, 89.07460286905958924, -81.15544420874873310 ) ) ;
#37760=ORIENTED_EDGE ( 'NONE', *, *, #19099, .T. ) ;
#37761=DIRECTION ( 'NONE',  ( 1.000000000000000000, 0.000000000000000000, 0.000000000000000000 ) ) ;
#37768=CARTESIAN_POINT ( 'NONE',  ( 17.99999999999999645, -24.22031524825905890, -109.5520369638039710 ) ) ;
#37770=VECTOR ( 'NONE', #13526, 1000.000000000000000 ) ;
#37771=ORIENTED_EDGE ( 'NONE', *, *, #7404, .T. ) ;
#37773=ORIENTED_EDGE ( 'NONE', *, *, #42785, .F. ) ;
#37779=VECTOR ( 'NONE', #5648, 1000.000000000000000 ) ;
#37783=VERTEX_POINT ( 'NONE', #22496 ) ;
#37784=AXIS2_PLACEMENT_3D ( 'NONE', #1528, #5241, #11374 ) ;
#37785=ORIENTED_EDGE ( 'NONE', *, *, #21848, .T. ) ;
#37786=DIRECTION ( 'NONE',  ( -1.000000000000000000, 0.000000000000000000, -0.000000000000000000 ) ) ;
#37787=EDGE_CURVE ( 'NONE', #20272, #31337, #21681, .T. ) ;
#37789=ORIENTED_EDGE ( 'NONE', *, *, #3139, .F. ) ;
#37790=DIRECTION ( 'NONE',  ( -1.000000000000000000, -0.000000000000000000, 0.000000000000000000 ) ) ;
#37794=DIRECTION ( 'NONE',  ( 1.000000000000000000, 0.000000000000000000, 0.000000000000000000 ) ) ;
#37797=EDGE_LOOP ( 'NONE', ( #41621, #26803, #3257, #1512 ) ) ;
#37802=CYLINDRICAL_SURFACE ( 'NONE', #34006, 59.00000000000000000 ) ;
#37805=CARTESIAN_POINT ( 'NONE',  ( 17.99999999999999645, 118.8387007424470738, 19.94628303336527608 ) ) ;
#37807=CARTESIAN_POINT ( 'NONE',  ( 17.99999999999999645, 64.58410930313523579, 101.7319213743684685 ) ) ;
#37809=FACE_OUTER_BOUND ( 'NONE', #42619, .T. ) ;
#37810=VERTEX_POINT ( 'NONE', #9351 ) ;
#37813=VECTOR ( 'NONE', #38604, 1000.000000000000000 ) ;
#37814=ORIENTED_EDGE ( 'NONE', *, *, #22788, .F. ) ;
#37815=ORIENTED_EDGE ( 'NONE', *, *, #1573, .F. ) ;
#37816=DIRECTION ( 'NONE',  ( -1.000000000000000000, -0.000000000000000000, 0.000000000000000000 ) ) ;
#37817=CARTESIAN_POINT ( 'NONE',  ( 17.99999999999999645, 111.7974656912330005, 9.465682155095883843 ) ) ;
#37821=ORIENTED_EDGE ( 'NONE', *, *, #10567, .F. ) ;
#37824=DIRECTION ( 'NONE',  ( 0.000000000000000000, -0.7865515558026354714, -0.6175246149462008116 ) ) ;
#37827=DIRECTION ( 'NONE',  ( -1.000000000000000000, -0.000000000000000000, 0.000000000000000000 ) ) ;
#37837=EDGE_CURVE ( 'NONE', #10944, #33553, #35736, .T. ) ;
#37841=ADVANCED_FACE ( 'NONE', ( #8942 ), #18596, .F. ) ;
#37843=DIRECTION ( 'NONE',  ( -1.000000000000000000, -0.000000000000000000, -0.000000000000000000 ) ) ;
#37846=CARTESIAN_POINT ( 'NONE',  ( 0.000000000000000000, 111.2559044912524939, 32.83479428644713494 ) ) ;
#37850=ORIENTED_EDGE ( 'NONE', *, *, #20968, .F. ) ;
#37860=CIRCLE ( 'NONE', #14921, 59.00000000000000711 ) ;
#37862=VERTEX_POINT ( 'NONE', #5454 ) ;
#37863=AXIS2_PLACEMENT_3D ( 'NONE', #33804, #16841, #27492 ) ;
#37867=CARTESIAN_POINT ( 'NONE',  ( 0.000000000000000000, 68.63002662989875091, -93.51962064069435598 ) ) ;
#37870=DIRECTION ( 'NONE',  ( 0.000000000000000000, -0.9968120070307509017, 0.07978610555307336094 ) ) ;
#37872=ORIENTED_EDGE ( 'NONE', *, *, #32087, .T. ) ;
#37879=EDGE_LOOP ( 'NONE', ( #1943, #42339, #34916, #37653 ) ) ;
#37886=ORIENTED_EDGE ( 'NONE', *, *, #17389, .T. ) ;
#37888=DIRECTION ( 'NONE',  ( -1.000000000000000000, -0.000000000000000000, -0.000000000000000000 ) ) ;
#37889=AXIS2_PLACEMENT_3D ( 'NONE', #13111, #23153, #19028 ) ;
#37890=ADVANCED_FACE ( 'NONE', ( #23343 ), #36605, .F. ) ;
#37892=CARTESIAN_POINT ( 'NONE',  ( 0.000000000000000000, 0.000000000000000000, 0.000000000000000000 ) ) ;
#37894=CIRCLE ( 'NONE', #25393, 120.5010000000000332 ) ;
#37900=CARTESIAN_POINT ( 'NONE',  ( 17.99999999999999645, -97.89532456239533076, 54.81585448086167389 ) ) ;
#37908=ORIENTED_EDGE ( 'NONE', *, *, #37837, .F. ) ;
#37910=DIRECTION ( 'NONE',  ( -1.000000000000000000, 0.000000000000000000, 0.000000000000000000 ) ) ;
#37914=EDGE_LOOP ( 'NONE', ( #9433, #14105, #19262, #10879 ) ) ;
#37917=AXIS2_PLACEMENT_3D ( 'NONE', #26390, #19435, #23137 ) ;
#37921=ORIENTED_EDGE ( 'NONE', *, *, #23973, .F. ) ;
#37923=AXIS2_PLACEMENT_3D ( 'NONE', #31399, #34659, #28572 ) ;
#37928=CARTESIAN_POINT ( 'NONE',  ( 17.99999999999999645, 0.000000000000000000, 0.000000000000000000 ) ) ;
#37929=DIRECTION ( 'NONE',  ( -1.000000000000000000, -0.000000000000000000, -0.000000000000000000 ) ) ;
#37931=DIRECTION ( 'NONE',  ( 1.000000000000000000, 0.000000000000000000, 0.000000000000000000 ) ) ;
#37934=CARTESIAN_POINT ( 'NONE',  ( 17.99999999999999645, -0.5156212287272186057, -112.1962860721878172 ) ) ;
#37939=DIRECTION ( 'NONE',  ( -1.000000000000000000, -0.000000000000000000, -0.000000000000000000 ) ) ;
#37943=CLOSED_SHELL ( 'NONE', ( #40412, #5755, #14698, #36448, #10983, #25967, #14292, #24439, #21783, #37040, #11539, #36137, #17794, #4391, #21656, #10493, #13662, #34085, #5638, #9720, #14753, #1945, #11669, #17254, #17844, #42906, #16191, #3414, #42907, #9812, #39585, #42502, #16978, #41768, #34599, #16370, #4112, #25718, #38548, #5778, #40163, #14985, #38309, #25239, #5857, #9687, #8012, #40333, #8828, #41668, #38785, #24739, #35133, #38464, #439, #42554, #22062, #19417, #27003, #26927, #42179, #34843, #504, #27535, #18074, #29451, #40648, #4508, #33273, #37303, #30322, #27300, #11100, #23273, #13977, #29432, #27684, #24548, #11208, #8447, #932, #20257, #6993, #25261, #39871, #43030, #26247, #8710, #36439, #14949, #2605, #18728, #29059, #16259, #41251, #32293, #7603, #4314, #7460, #14325, #7755, #34468, #38497, #19174, #17974, #25576, #8097, #14779, #34038, #32620, #14087, #9861, #31533, #19917, #14720, #6888, #5698, #37058, #40316, #42472, #34772, #40300, #5417, #20496, #12569, #7511, #11364, #19957, #40116, #38390, #19549, #37106, #24114, #13854, #23395, #4809, #35034, #33752, #13569, #25158, #12895, #13295, #22082, #11839, #20760, #35790, #23453, #38472, #22934, #15571, #14508, #306, #443, #25330, #17700, #24473, #6021, #41915, #9846, #34344, #32428, #21112, #9507, #34163, #19755, #25391, #39225, #30295, #10161, #13767, #31242, #27593, #30627, #16159, #16174, #30153, #18942, #41123, #22088, #17233, #1161, #36684, #35067, #38533, #36898, #31083, #12517, #21610, #33836, #21139, #3140, #4139, #1051, #10376, #13409, #40439, #12276, #31140, #23075, #29323, #38565, #19899, #14140, #21976, #22515, #42853, #43107, #18206, #25743, #22246, #38369, #3861, #3511, #36438, #12409, #36326, #22206, #4996, #20719, #19327, #13540, #5652, #1248, #8022, #35819, #42974, #5719, #12371, #7513, #25800, #41102, #34020, #25786, #3937, #14560, #6864, #33780, #26575, #30347, #36932, #33077, #38235, #2538, #30725, #5543, #35115, #33216, #2476, #38167, #27177, #21635, #18001, #12511, #36511, #7178, #4657, #1455, #9531, #5935, #30762, #4698, #32724, #23765, #31937, #24354, #2792, #2361, #24131, #1075, #41458, #40993, #20475, #36030, #12211, #28765, #31462, #42042, #1964, #32061, #26743, #11677, #10775, #19629, #6976, #1207, #8610, #25683, #7048, #12539, #29848, #40402, #31547, #23578, #11952, #6384, #28533, #12210, #36673, #32719, #5805, #19826, #27989, #4028, #19599, #38267, #34395, #8991, #29251, #2514, #25285, #23751, #20390, #19223, #4548, #32114, #20831, #1433, #18943, #32641, #28764, #42863, #2503, #19381, #8215, #26945, #18084, #18499, #15269, #37552, #42909, #5787, #25626, #36184, #8626, #20615, #20120, #38237, #34056, #14066, #10715, #11818, #30485, #31483, #41883, #20726, #34327, #42531, #1541, #13962, #22648, #17850, #41679, #26036, #36559, #9389, #13735, #31529, #33857, #30442, #39606, #3557, #29244, #10511, #22878, #32456, #33471, #30266, #2679, #12570, #2606, #42284, #29704, #8990, #5239, #16416, #25105, #2355, #4948, #13595, #37557, #23291, #37890, #10389, #6078, #16315, #3350, #22309, #40132, #176, #15725, #13624, #14825, #21208, #10795, #37661, #4978, #2997, #438, #39457, #22189, #38828, #35491, #12717, #26553, #2139, #22874, #31277, #38747, #18348, #33193, #20036, #39026, #42020, #35358, #1875, #4109, #13298, #1138, #1486, #417, #39469, #4603, #32550, #41720, #37122, #9374, #3535, #37753, #1992, #8322, #20155, #18447, #18459, #35755, #40227, #32938, #38974, #7266, #16366, #5242, #31109, #15712, #18826, #40733, #12024, #16502, #37528, #36874, #38927, #27678, #38822, #23700, #35598, #40060, #6581, #1040, #37841, #7289, #28193, #7455, #18349, #9585, #19955, #41683, #31411, #21661, #5440, #30843, #25031, #35642, #37714, #8983, #12123, #2026, #14183, #5027, #40987, #14528, #26580, #39839, #180 ) ) ;
#37944=VERTEX_POINT ( 'NONE', #22939 ) ;
#37948=DIRECTION ( 'NONE',  ( -1.000000000000000000, 0.000000000000000000, -0.000000000000000000 ) ) ;
#37949=ORIENTED_EDGE ( 'NONE', *, *, #18518, .F. ) ;
#37951=CYLINDRICAL_SURFACE ( 'NONE', #1406, 59.00000000000000711 ) ;
#37954=AXIS2_PLACEMENT_3D ( 'NONE', #114, #3402, #16770 ) ;
#37955=FACE_OUTER_BOUND ( 'NONE', #21750, .T. ) ;
#37956=CARTESIAN_POINT ( 'NONE',  ( 0.000000000000000000, 0.000000000000000000, 0.000000000000000000 ) ) ;
#37959=EDGE_CURVE ( 'NONE', #12545, #32231, #21713, .T. ) ;
#37962=VERTEX_POINT ( 'NONE', #17015 ) ;
#37964=DIRECTION ( 'NONE',  ( 1.000000000000000000, 0.000000000000000000, 0.000000000000000000 ) ) ;
#37967=CIRCLE ( 'NONE', #2407, 59.00000000000000000 ) ;
#37968=DIRECTION ( 'NONE',  ( 1.000000000000000000, -0.000000000000000000, -0.000000000000000000 ) ) ;
#37970=ORIENTED_EDGE ( 'NONE', *, *, #11865, .T. ) ;
#37973=DIRECTION ( 'NONE',  ( 0.000000000000000000, 0.000000000000000000, 1.000000000000000000 ) ) ;
#37974=ORIENTED_EDGE ( 'NONE', *, *, #11991, .F. ) ;
#37981=CARTESIAN_POINT ( 'NONE',  ( -10.00000000000000000, 0.000000000000000000, 0.000000000000000000 ) ) ;
#37984=AXIS2_PLACEMENT_3D ( 'NONE', #1601, #21938, #25216 ) ;
#37990=ORIENTED_EDGE ( 'NONE', *, *, #32529, .T. ) ;
#37992=DIRECTION ( 'NONE',  ( 1.000000000000000000, 0.000000000000000000, 0.000000000000000000 ) ) ;
#37993=ORIENTED_EDGE ( 'NONE', *, *, #35496, .F. ) ;
#38001=DIRECTION ( 'NONE',  ( 0.000000000000000000, 0.000000000000000000, 1.000000000000000000 ) ) ;
#38003=ORIENTED_EDGE ( 'NONE', *, *, #41186, .T. ) ;
#38008=VERTEX_POINT ( 'NONE', #36177 ) ;
#38019=CIRCLE ( 'NONE', #19248, 116.0000000000000000 ) ;
#38022=ORIENTED_EDGE ( 'NONE', *, *, #19237, .F. ) ;
#38025=DIRECTION ( 'NONE',  ( 1.000000000000000000, 0.000000000000000000, 0.000000000000000000 ) ) ;
#38026=ORIENTED_EDGE ( 'NONE', *, *, #39654, .F. ) ;
#38027=DIRECTION ( 'NONE',  ( 1.000000000000000000, 0.000000000000000000, -0.000000000000000000 ) ) ;
#38029=DIRECTION ( 'NONE',  ( 0.000000000000000000, -0.5528000653612000770, 0.8333139190825105125 ) ) ;
#38030=ORIENTED_EDGE ( 'NONE', *, *, #23205, .F. ) ;
#38033=EDGE_CURVE ( 'NONE', #30765, #16529, #24474, .T. ) ;
#38040=EDGE_CURVE ( 'NONE', #15479, #2864, #14715, .T. ) ;
#38042=DIRECTION ( 'NONE',  ( 1.000000000000000000, 0.000000000000000000, 0.000000000000000000 ) ) ;
#38046=ORIENTED_EDGE ( 'NONE', *, *, #16442, .F. ) ;
#38048=ORIENTED_EDGE ( 'NONE', *, *, #9532, .T. ) ;
#38051=VECTOR ( 'NONE', #15175, 1000.000000000000000 ) ;
#38052=AXIS2_PLACEMENT_3D ( 'NONE', #13493, #32680, #2760 ) ;
#38055=CYLINDRICAL_SURFACE ( 'NONE', #35859, 120.5010000000000190 ) ;
#38056=EDGE_LOOP ( 'NONE', ( #10183, #33298, #13368, #25716 ) ) ;
#38057=EDGE_LOOP ( 'NONE', ( #34427, #26023, #42023, #42403 ) ) ;
#38058=DIRECTION ( 'NONE',  ( 0.000000000000000000, 0.000000000000000000, 1.000000000000000000 ) ) ;
#38061=ORIENTED_EDGE ( 'NONE', *, *, #19414, .F. ) ;
#38063=ORIENTED_EDGE ( 'NONE', *, *, #496, .F. ) ;
#38067=DIRECTION ( 'NONE',  ( -1.000000000000000000, 0.000000000000000000, 0.000000000000000000 ) ) ;
#38068=EDGE_CURVE ( 'NONE', #12547, #36920, #24431, .T. ) ;
#38069=ORIENTED_EDGE ( 'NONE', *, *, #20498, .T. ) ;
#38072=FACE_OUTER_BOUND ( 'NONE', #7171, .T. ) ;
#38075=ORIENTED_EDGE ( 'NONE', *, *, #42461, .F. ) ;
#38076=CARTESIAN_POINT ( 'NONE',  ( 0.000000000000000000, 0.000000000000000000, 0.000000000000000000 ) ) ;
#38077=VECTOR ( 'NONE', #23906, 1000.000000000000000 ) ;
#38079=SURFACE_SIDE_STYLE ('',( #31339 ) ) ;
#38082=CARTESIAN_POINT ( 'NONE',  ( 0.000000000000000000, 34.03109950475727175, 115.5957406979051285 ) ) ;
#38084=CARTESIAN_POINT ( 'NONE',  ( 17.99999999999999645, 0.000000000000000000, 0.000000000000000000 ) ) ;
#38085=VECTOR ( 'NONE', #15864, 1000.000000000000000 ) ;
#38087=CARTESIAN_POINT ( 'NONE',  ( 17.99999999999999645, 0.000000000000000000, 0.000000000000000000 ) ) ;
#38090=ORIENTED_EDGE ( 'NONE', *, *, #9611, .T. ) ;
#38100=CARTESIAN_POINT ( 'NONE',  ( 17.99999999999999645, -5.456439917445724319, 112.0647122740741963 ) ) ;
#38109=CYLINDRICAL_SURFACE ( 'NONE', #39761, 116.0000000000000000 ) ;
#38113=CIRCLE ( 'NONE', #20034, 59.00000000000000000 ) ;
#38114=CIRCLE ( 'NONE', #8162, 120.5010000000000332 ) ;
#38115=ORIENTED_EDGE ( 'NONE', *, *, #27805, .F. ) ;
#38117=CARTESIAN_POINT ( 'NONE',  ( 8.999999999999998224, -101.1403355683142422, -56.80345518653591341 ) ) ;
#38118=DIRECTION ( 'NONE',  ( -1.000000000000000000, 0.000000000000000000, -0.000000000000000000 ) ) ;
#38119=AXIS2_PLACEMENT_3D ( 'NONE', #10062, #16654, #36020 ) ;
#38122=ORIENTED_EDGE ( 'NONE', *, *, #21949, .F. ) ;
#38125=CARTESIAN_POINT ( 'NONE',  ( 0.000000000000000000, -72.00556975657760006, 86.04342158279364128 ) ) ;
#38128=CIRCLE ( 'NONE', #14456, 120.5010000000000190 ) ;
#38130=LINE ( 'NONE', #5178, #37356 ) ;
#38131=VERTEX_POINT ( 'NONE', #28117 ) ;
#38133=CARTESIAN_POINT ( 'NONE',  ( 17.99999999999999645, 0.000000000000000000, 116.0000000000000000 ) ) ;
#38134=CARTESIAN_POINT ( 'NONE',  ( 17.99999999999999645, -111.2721026680459602, 44.61974821237267719 ) ) ;
#38135=ORIENTED_EDGE ( 'NONE', *, *, #8199, .F. ) ;
#38139=AXIS2_PLACEMENT_3D ( 'NONE', #19785, #16733, #16515 ) ;
#38146=CIRCLE ( 'NONE', #19375, 58.99999999999998579 ) ;
#38148=ORIENTED_EDGE ( 'NONE', *, *, #15377, .T. ) ;
#38154=CARTESIAN_POINT ( 'NONE',  ( 0.000000000000000000, 0.000000000000000000, 0.000000000000000000 ) ) ;
#38157=DIRECTION ( 'NONE',  ( -1.000000000000000000, 0.000000000000000000, -0.000000000000000000 ) ) ;
#38158=DIRECTION ( 'NONE',  ( 0.000000000000000000, 0.9714298932647090767, 0.2373266998711185127 ) ) ;
#38165=DIRECTION ( 'NONE',  ( -1.000000000000000000, -0.000000000000000000, -0.000000000000000000 ) ) ;
#38166=ORIENTED_EDGE ( 'NONE', *, *, #19821, .T. ) ;
#38167=ADVANCED_FACE ( 'NONE', ( #20950 ), #7594, .F. ) ;
#38170=CARTESIAN_POINT ( 'NONE',  ( 17.99999999999999645, -115.0622509503831452, -14.72000021165260897 ) ) ;
#38174=AXIS2_PLACEMENT_3D ( 'NONE', #24245, #34022, #4111 ) ;
#38179=DIRECTION ( 'NONE',  ( 1.000000000000000000, 0.000000000000000000, 0.000000000000000000 ) ) ;
#38180=CIRCLE ( 'NONE', #6125, 120.5010000000000190 ) ;
#38181=CARTESIAN_POINT ( 'NONE',  ( -10.00000000000000000, 0.000000000000000000, 0.000000000000000000 ) ) ;
#38182=CARTESIAN_POINT ( 'NONE',  ( 0.000000000000000000, -52.88069566989388903, -103.2454939717374032 ) ) ;
#38183=EDGE_LOOP ( 'NONE', ( #3041, #39287, #7860, #25372 ) ) ;
#38186=DIRECTION ( 'NONE',  ( -1.000000000000000000, -0.000000000000000000, 0.000000000000000000 ) ) ;
#38189=AXIS2_PLACEMENT_3D ( 'NONE', #10107, #4202, #17571 ) ;
#38195=CARTESIAN_POINT ( 'NONE',  ( 0.000000000000000000, 0.000000000000000000, 0.000000000000000000 ) ) ;
#38197=VERTEX_POINT ( 'NONE', #34639 ) ;
#38201=CIRCLE ( 'NONE', #19433, 116.0000000000000000 ) ;
#38205=VECTOR ( 'NONE', #13398, 1000.000000000000000 ) ;
#38206=LINE ( 'NONE', #8106, #3955 ) ;
#38207=DIRECTION ( 'NONE',  ( 0.000000000000000000, 0.000000000000000000, 1.000000000000000000 ) ) ;
#38211=ORIENTED_EDGE ( 'NONE', *, *, #28317, .F. ) ;
#38213=ORIENTED_EDGE ( 'NONE', *, *, #11172, .F. ) ;
#38216=ORIENTED_EDGE ( 'NONE', *, *, #32676, .T. ) ;
#38218=LINE ( 'NONE', #27787, #38842 ) ;
#38220=EDGE_CURVE ( 'NONE', #27792, #3514, #598, .T. ) ;
#38221=ORIENTED_EDGE ( 'NONE', *, *, #14801, .T. ) ;
#38227=VERTEX_POINT ( 'NONE', #38760 ) ;
#38228=CARTESIAN_POINT ( 'NONE',  ( 0.000000000000000000, 8.827181066045881153, 120.1772519049559662 ) ) ;
#38233=VERTEX_POINT ( 'NONE', #12181 ) ;
#38235=ADVANCED_FACE ( 'NONE', ( #41824 ), #8892, .F. ) ;
#38237=ADVANCED_FACE ( 'NONE', ( #25721 ), #22020, .F. ) ;
#38238=CARTESIAN_POINT ( 'NONE',  ( 0.000000000000000000, 91.65951123222482977, 71.09524597798119316 ) ) ;
#38239=DIRECTION ( 'NONE',  ( -1.000000000000000000, -0.000000000000000000, -0.000000000000000000 ) ) ;
#38240=CYLINDRICAL_SURFACE ( 'NONE', #1789, 59.00000000000000000 ) ;
#38243=CARTESIAN_POINT ( 'NONE',  ( 17.99999999999999645, 0.000000000000000000, 0.000000000000000000 ) ) ;
#38244=VERTEX_POINT ( 'NONE', #2103 ) ;
#38245=CARTESIAN_POINT ( 'NONE',  ( 17.99999999999999645, 105.7179949885867956, -37.57629584241721687 ) ) ;
#38246=EDGE_CURVE ( 'NONE', #40508, #69, #25500, .T. ) ;
#38248=CARTESIAN_POINT ( 'NONE',  ( 17.99999999999999645, -111.7974656912329436, -9.465682155096647676 ) ) ;
#38249=ORIENTED_EDGE ( 'NONE', *, *, #9105, .F. ) ;
#38252=EDGE_LOOP ( 'NONE', ( #25125, #1412, #33698, #4592 ) ) ;
#38253=ORIENTED_EDGE ( 'NONE', *, *, #38220, .T. ) ;
#38254=DIRECTION ( 'NONE',  ( 0.000000000000000000, 0.000000000000000000, 1.000000000000000000 ) ) ;
#38260=VECTOR ( 'NONE', #16449, 1000.000000000000000 ) ;
#38261=EDGE_CURVE ( 'NONE', #19203, #2829, #27950, .T. ) ;
#38262=ORIENTED_EDGE ( 'NONE', *, *, #2105, .F. ) ;
#38263=CARTESIAN_POINT ( 'NONE',  ( 17.99999999999999645, -23.10276247328019039, -118.2656051737072431 ) ) ;
#38264=ORIENTED_EDGE ( 'NONE', *, *, #751, .F. ) ;
#38267=ADVANCED_FACE ( 'NONE', ( #42460 ), #1683, .F. ) ;
#38268=CARTESIAN_POINT ( 'NONE',  ( 17.99999999999999645, 42.87700105098753056, -107.7847984684000551 ) ) ;
#38273=DIRECTION ( 'NONE',  ( -1.000000000000000000, 0.000000000000000000, 0.000000000000000000 ) ) ;
#38279=CARTESIAN_POINT ( 'NONE',  ( 0.000000000000000000, 0.000000000000000000, 0.000000000000000000 ) ) ;
#38280=CYLINDRICAL_SURFACE ( 'NONE', #31, 120.5010000000000190 ) ;
#38285=VECTOR ( 'NONE', #37687, 1000.000000000000000 ) ;
#38286=EDGE_CURVE ( 'NONE', #16376, #28961, #36968, .T. ) ;
#38288=EDGE_CURVE ( 'NONE', #3729, #10037, #32709, .T. ) ;
#38289=CARTESIAN_POINT ( 'NONE',  ( 17.99999999999999645, -24.22031524826050841, 109.5520369638036584 ) ) ;
#38291=EDGE_CURVE ( 'NONE', #36886, #7958, #39669, .T. ) ;
#38295=CYLINDRICAL_SURFACE ( 'NONE', #22411, 59.00000000000000000 ) ;
#38296=ORIENTED_EDGE ( 'NONE', *, *, #4427, .F. ) ;
#38297=FACE_OUTER_BOUND ( 'NONE', #7637, .T. ) ;
#38298=CARTESIAN_POINT ( 'NONE',  ( 17.99999999999999645, -10.40101730206288444, -120.0512800434972149 ) ) ;
#38300=DIRECTION ( 'NONE',  ( 1.000000000000000000, 0.000000000000000000, 0.000000000000000000 ) ) ;
#38301=ORIENTED_EDGE ( 'NONE', *, *, #27419, .T. ) ;
#38302=DIRECTION ( 'NONE',  ( -1.000000000000000000, 0.000000000000000000, 0.000000000000000000 ) ) ;
#38308=DIRECTION ( 'NONE',  ( 0.000000000000000000, 0.9911528310040067513, 0.1327255272837256084 ) ) ;
#38309=ADVANCED_FACE ( 'NONE', ( #38541 ), #22447, .F. ) ;
#38310=VERTEX_POINT ( 'NONE', #18540 ) ;
#38311=FACE_OUTER_BOUND ( 'NONE', #10292, .T. ) ;
#38315=CIRCLE ( 'NONE', #669, 120.5010000000000190 ) ;
#38318=DIRECTION ( 'NONE',  ( -1.000000000000000000, -0.000000000000000000, 0.000000000000000000 ) ) ;
#38320=DIRECTION ( 'NONE',  ( -1.000000000000000000, -0.000000000000000000, -0.000000000000000000 ) ) ;
#38327=DIRECTION ( 'NONE',  ( -1.000000000000000000, -0.000000000000000000, 0.000000000000000000 ) ) ;
#38335=EDGE_CURVE ( 'NONE', #20914, #30242, #29957, .T. ) ;
#38336=CIRCLE ( 'NONE', #16098, 116.0000000000000000 ) ;
#38338=CYLINDRICAL_SURFACE ( 'NONE', #8920, 116.0000000000000000 ) ;
#38339=EDGE_CURVE ( 'NONE', #5363, #19975, #8359, .T. ) ;
#38341=DIRECTION ( 'NONE',  ( 1.000000000000000000, 0.000000000000000000, 0.000000000000000000 ) ) ;
#38342=VERTEX_POINT ( 'NONE', #9740 ) ;
#38347=DIRECTION ( 'NONE',  ( 0.000000000000000000, 0.000000000000000000, 1.000000000000000000 ) ) ;
#38348=CARTESIAN_POINT ( 'NONE',  ( 8.999999999999998224, -87.74575819880118388, -75.87280091124561920 ) ) ;
#38352=DIRECTION ( 'NONE',  ( 0.000000000000000000, 0.000000000000000000, 1.000000000000000000 ) ) ;
#38353=AXIS2_PLACEMENT_3D ( 'NONE', #4118, #13981, #10251 ) ;
#38356=CARTESIAN_POINT ( 'NONE',  ( -10.00000000000000000, 0.000000000000000000, 0.000000000000000000 ) ) ;
#38358=VERTEX_POINT ( 'NONE', #26757 ) ;
#38364=DIRECTION ( 'NONE',  ( 1.000000000000000000, 0.000000000000000000, 0.000000000000000000 ) ) ;
#38366=CARTESIAN_POINT ( 'NONE',  ( 9.000000000000001776, -110.8621702203446659, -34.14058016547651420 ) ) ;
#38367=AXIS2_PLACEMENT_3D ( 'NONE', #6458, #32869, #26352 ) ;
#38368=CARTESIAN_POINT ( 'NONE',  ( 17.99999999999999645, -64.69195966009955612, 96.28577441832231898 ) ) ;
#38369=ADVANCED_FACE ( 'NONE', ( #16754 ), #36546, .F. ) ;
#38373=AXIS2_PLACEMENT_3D ( 'NONE', #37417, #37630, #13894 ) ;
#38376=VECTOR ( 'NONE', #35490, 1000.000000000000000 ) ;
#38379=AXIS2_PLACEMENT_3D ( 'NONE', #20075, #43140, #30078 ) ;
#38381=ORIENTED_EDGE ( 'NONE', *, *, #4733, .F. ) ;
#38384=ORIENTED_EDGE ( 'NONE', *, *, #12191, .F. ) ;
#38388=DIRECTION ( 'NONE',  ( 0.000000000000000000, 0.000000000000000000, 1.000000000000000000 ) ) ;
#38390=ADVANCED_FACE ( 'NONE', ( #29608 ), #42665, .F. ) ;
#38391=CARTESIAN_POINT ( 'NONE',  ( 0.000000000000000000, -68.63002662989681824, -93.51962064069581970 ) ) ;
#38392=EDGE_LOOP ( 'NONE', ( #25914, #40321, #3000, #27242 ) ) ;
#38397=CARTESIAN_POINT ( 'NONE',  ( 17.99999999999999645, 89.07460286905958924, -81.15544420874873310 ) ) ;
#38398=AXIS2_PLACEMENT_3D ( 'NONE', #38076, #34371, #31118 ) ;
#38399=DIRECTION ( 'NONE',  ( -1.000000000000000000, -0.000000000000000000, 0.000000000000000000 ) ) ;
#38405=CARTESIAN_POINT ( 'NONE',  ( 0.000000000000000000, 0.000000000000000000, 0.000000000000000000 ) ) ;
#38412=DIRECTION ( 'NONE',  ( -1.000000000000000000, 0.000000000000000000, -0.000000000000000000 ) ) ;
#38413=CARTESIAN_POINT ( 'NONE',  ( 17.99999999999999645, -83.49789599728842404, 86.88263557826738293 ) ) ;
#38414=CARTESIAN_POINT ( 'NONE',  ( 17.99999999999999645, -114.1157422997281969, -20.82300072953048442 ) ) ;
#38418=EDGE_LOOP ( 'NONE', ( #35024, #21336, #28637, #19502 ) ) ;
#38424=ORIENTED_EDGE ( 'NONE', *, *, #28926, .F. ) ;
#38425=CARTESIAN_POINT ( 'NONE',  ( 17.99999999999999645, -114.6488492393077081, -37.09625815500128709 ) ) ;
#38429=CARTESIAN_POINT ( 'NONE',  ( 17.99999999999999645, 6.486220790509957368, -112.0098273076986715 ) ) ;
#38434=EDGE_CURVE ( 'NONE', #29115, #35353, #32863, .T. ) ;
#38439=AXIS2_PLACEMENT_3D ( 'NONE', #36939, #33664, #11217 ) ;
#38444=DIRECTION ( 'NONE',  ( 0.000000000000000000, -0.2113826236296315053, 0.9774033898178651203 ) ) ;
#38446=EDGE_CURVE ( 'NONE', #38310, #29868, #18846, .T. ) ;
#38447=DIRECTION ( 'NONE',  ( -1.000000000000000000, -0.000000000000000000, -0.000000000000000000 ) ) ;
#38448=ORIENTED_EDGE ( 'NONE', *, *, #6842, .F. ) ;
#38449=CARTESIAN_POINT ( 'NONE',  ( 17.99999999999999645, 0.000000000000000000, 0.000000000000000000 ) ) ;
#38452=CYLINDRICAL_SURFACE ( 'NONE', #12814, 59.00000000000000000 ) ;
#38462=AXIS2_PLACEMENT_3D ( 'NONE', #31426, #25546, #21644 ) ;
#38464=ADVANCED_FACE ( 'NONE', ( #13042 ), #26343, .F. ) ;
#38465=CARTESIAN_POINT ( 'NONE',  ( 0.000000000000000000, 0.000000000000000000, 0.000000000000000000 ) ) ;
#38466=ORIENTED_EDGE ( 'NONE', *, *, #15006, .T. ) ;
#38469=CARTESIAN_POINT ( 'NONE',  ( 17.99999999999999645, 0.000000000000000000, 0.000000000000000000 ) ) ;
#38472=ADVANCED_FACE ( 'NONE', ( #6037 ), #19388, .F. ) ;
#38473=DIRECTION ( 'NONE',  ( 0.000000000000000000, -0.7865515558026479059, 0.6175246149461850464 ) ) ;
#38474=FACE_OUTER_BOUND ( 'NONE', #41008, .T. ) ;
#38476=VERTEX_POINT ( 'NONE', #19304 ) ;
#38477=LINE ( 'NONE', #21544, #13790 ) ;
#38480=FACE_OUTER_BOUND ( 'NONE', #32305, .T. ) ;
#38484=DIRECTION ( 'NONE',  ( -1.000000000000000000, -0.000000000000000000, -0.000000000000000000 ) ) ;
#38492=VECTOR ( 'NONE', #5166, 1000.000000000000000 ) ;
#38493=DIRECTION ( 'NONE',  ( 1.000000000000000000, 0.000000000000000000, 0.000000000000000000 ) ) ;
#38494=ORIENTED_EDGE ( 'NONE', *, *, #40934, .F. ) ;
#38495=DIRECTION ( 'NONE',  ( 0.000000000000000000, 0.000000000000000000, 1.000000000000000000 ) ) ;
#38496=VERTEX_POINT ( 'NONE', #11890 ) ;
#38497=ADVANCED_FACE ( 'NONE', ( #42383 ), #35419, .F. ) ;
#38499=CIRCLE ( 'NONE', #41985, 59.00000000000001421 ) ;
#38505=ORIENTED_EDGE ( 'NONE', *, *, #40981, .T. ) ;
#38509=DIRECTION ( 'NONE',  ( 0.000000000000000000, 0.000000000000000000, 1.000000000000000000 ) ) ;
#38513=DIRECTION ( 'NONE',  ( 0.000000000000000000, 0.8477344278896721264, -0.5304209081197405196 ) ) ;
#38515=ORIENTED_EDGE ( 'NONE', *, *, #18062, .F. ) ;
#38516=DIRECTION ( 'NONE',  ( -1.000000000000000000, -0.000000000000000000, -0.000000000000000000 ) ) ;
#38520=EDGE_CURVE ( 'NONE', #19286, #32742, #18164, .T. ) ;
#38524=DIRECTION ( 'NONE',  ( 0.000000000000000000, 0.000000000000000000, 1.000000000000000000 ) ) ;
#38525=ORIENTED_EDGE ( 'NONE', *, *, #27133, .F. ) ;
#38529=VECTOR ( 'NONE', #27208, 1000.000000000000000 ) ;
#38532=CARTESIAN_POINT ( 'NONE',  ( 0.000000000000000000, -104.6166166098448826, 50.11350645393640235 ) ) ;
#38533=ADVANCED_FACE ( 'NONE', ( #12101 ), #8806, .F. ) ;
#38537=DIRECTION ( 'NONE',  ( -1.000000000000000000, -0.000000000000000000, -0.000000000000000000 ) ) ;
#38538=EDGE_LOOP ( 'NONE', ( #7848, #34011, #6117, #2548 ) ) ;
#38539=DIRECTION ( 'NONE',  ( 0.000000000000000000, -0.7164567402983067490, -0.6976315211349933820 ) ) ;
#38541=FACE_OUTER_BOUND ( 'NONE', #33482, .T. ) ;
#38544=FACE_OUTER_BOUND ( 'NONE', #26818, .T. ) ;
#38545=ORIENTED_EDGE ( 'NONE', *, *, #34213, .F. ) ;
#38548=ADVANCED_FACE ( 'NONE', ( #18460 ), #12735, .F. ) ;
#38550=CARTESIAN_POINT ( 'NONE',  ( 0.000000000000000000, 109.4038418350903470, 50.51029986767587587 ) ) ;
#38554=EDGE_LOOP ( 'NONE', ( #9829, #23731, #29987, #15617 ) ) ;
#38555=CARTESIAN_POINT ( 'NONE',  ( 17.99999999999999645, 27.83061035786954918, 117.2431154827798281 ) ) ;
#38556=CARTESIAN_POINT ( 'NONE',  ( 0.000000000000000000, 54.09091620264722877, 102.6166301549519488 ) ) ;
#38558=CIRCLE ( 'NONE', #2293, 120.5010000000000474 ) ;
#38559=EDGE_LOOP ( 'NONE', ( #8898, #24389, #37814, #3482 ) ) ;
#38562=AXIS2_PLACEMENT_3D ( 'NONE', #20603, #33876, #20838 ) ;
#38565=ADVANCED_FACE ( 'NONE', ( #41956 ), #32357, .F. ) ;
#38569=EDGE_CURVE ( 'NONE', #10316, #37810, #2750, .T. ) ;
#38570=EDGE_CURVE ( 'NONE', #26693, #5822, #10451, .T. ) ;
#38571=EDGE_CURVE ( 'NONE', #38997, #40885, #32733, .T. ) ;
#38572=CIRCLE ( 'NONE', #941, 116.0000000000000000 ) ;
#38573=FACE_OUTER_BOUND ( 'NONE', #6432, .T. ) ;
#38576=DIRECTION ( 'NONE',  ( -1.000000000000000000, 0.000000000000000000, -0.000000000000000000 ) ) ;
#38577=VECTOR ( 'NONE', #28586, 1000.000000000000000 ) ;
#38581=VERTEX_POINT ( 'NONE', #29112 ) ;
#38583=CARTESIAN_POINT ( 'NONE',  ( 17.99999999999999645, 23.85344185397347161, -113.5209818126988779 ) ) ;
#38584=DIRECTION ( 'NONE',  ( -1.000000000000000000, -0.000000000000000000, 0.000000000000000000 ) ) ;
#38587=ORIENTED_EDGE ( 'NONE', *, *, #9227, .F. ) ;
#38588=CARTESIAN_POINT ( 'NONE',  ( 17.99999999999999645, -29.86146781000025285, 112.0905559814577970 ) ) ;
#38589=AXIS2_PLACEMENT_3D ( 'NONE', #29152, #38300, #42419 ) ;
#38592=DIRECTION ( 'NONE',  ( 0.000000000000000000, 0.000000000000000000, -1.000000000000000000 ) ) ;
#38595=DIRECTION ( 'NONE',  ( -1.000000000000000000, -0.000000000000000000, -0.000000000000000000 ) ) ;
#38596=CIRCLE ( 'NONE', #263, 120.5010000000000190 ) ;
#38598=CARTESIAN_POINT ( 'NONE',  ( 0.000000000000000000, 46.12538073176347808, 111.3235835452212825 ) ) ;
#38600=ORIENTED_EDGE ( 'NONE', *, *, #39579, .F. ) ;
#38601=AXIS2_PLACEMENT_3D ( 'NONE', #5786, #18945, #32201 ) ;
#38602=CARTESIAN_POINT ( 'NONE',  ( 17.99999999999999645, 0.000000000000000000, 0.000000000000000000 ) ) ;
#38604=DIRECTION ( 'NONE',  ( -1.000000000000000000, 0.000000000000000000, -0.000000000000000000 ) ) ;
#38607=DIRECTION ( 'NONE',  ( 0.000000000000000000, -0.9911528310040057521, -0.1327255272837324362 ) ) ;
#38611=ORIENTED_EDGE ( 'NONE', *, *, #26679, .T. ) ;
#38613=ORIENTED_EDGE ( 'NONE', *, *, #6607, .F. ) ;
#38619=LINE ( 'NONE', #38413, #27011 ) ;
#38620=EDGE_CURVE ( 'NONE', #35353, #5127, #35508, .T. ) ;
#38621=EDGE_CURVE ( 'NONE', #36853, #19393, #41069, .T. ) ;
#38622=DIRECTION ( 'NONE',  ( 0.000000000000000000, -0.1062934856473523731, -0.9943348002101385363 ) ) ;
#38627=ORIENTED_EDGE ( 'NONE', *, *, #31388, .T. ) ;
#38632=CIRCLE ( 'NONE', #25478, 59.00000000000000000 ) ;
#38636=VECTOR ( 'NONE', #14999, 1000.000000000000000 ) ;
#38637=ORIENTED_EDGE ( 'NONE', *, *, #23110, .T. ) ;
#38638=LINE ( 'NONE', #8761, #6773 ) ;
#38639=ORIENTED_EDGE ( 'NONE', *, *, #23914, .T. ) ;
#38640=VECTOR ( 'NONE', #40883, 1000.000000000000000 ) ;
#38641=ORIENTED_EDGE ( 'NONE', *, *, #5906, .F. ) ;
#38646=DIRECTION ( 'NONE',  ( 0.000000000000000000, 0.4132121857683790922, -0.9106347728549127885 ) ) ;
#38648=ORIENTED_EDGE ( 'NONE', *, *, #1113, .T. ) ;
#38649=CARTESIAN_POINT ( 'NONE',  ( 17.99999999999999645, 11.65176648921190150, -115.4133282497341355 ) ) ;
#38650=CIRCLE ( 'NONE', #19180, 59.00000000000000000 ) ;
#38658=CYLINDRICAL_SURFACE ( 'NONE', #22187, 116.0000000000000000 ) ;
#38663=VECTOR ( 'NONE', #38157, 1000.000000000000000 ) ;
#38664=DIRECTION ( 'NONE',  ( 0.000000000000000000, 0.000000000000000000, 1.000000000000000000 ) ) ;
#38667=DIRECTION ( 'NONE',  ( 0.000000000000000000, 0.000000000000000000, -1.000000000000000000 ) ) ;
#38676=FACE_OUTER_BOUND ( 'NONE', #4104, .T. ) ;
#38677=EDGE_CURVE ( 'NONE', #14692, #2034, #839, .T. ) ;
#38678=FACE_OUTER_BOUND ( 'NONE', #16231, .T. ) ;
#38681=DIRECTION ( 'NONE',  ( -1.000000000000000000, -0.000000000000000000, 0.000000000000000000 ) ) ;
#38682=ORIENTED_EDGE ( 'NONE', *, *, #9326, .F. ) ;
#38684=AXIS2_PLACEMENT_3D ( 'NONE', #877, #39933, #17525 ) ;
#38689=DIRECTION ( 'NONE',  ( -1.000000000000000000, -0.000000000000000000, -0.000000000000000000 ) ) ;
#38693=LINE ( 'NONE', #22176, #6097 ) ;
#38694=EDGE_CURVE ( 'NONE', #36535, #844, #18874, .T. ) ;
#38700=EDGE_CURVE ( 'NONE', #22923, #6899, #14677, .T. ) ;
#38704=CARTESIAN_POINT ( 'NONE',  ( 0.000000000000000000, 57.69704296431325474, -105.7900857083224082 ) ) ;
#38705=DIRECTION ( 'NONE',  ( 0.000000000000000000, 1.505387152034110654E-14, -1.000000000000000000 ) ) ;
#38706=AXIS2_PLACEMENT_3D ( 'NONE', #32694, #25175, #2771 ) ;
#38712=CARTESIAN_POINT ( 'NONE',  ( 0.000000000000000000, -57.69704296431255131, 105.7900857083227635 ) ) ;
#38713=VERTEX_POINT ( 'NONE', #13174 ) ;
#38714=( LENGTH_UNIT ( ) NAMED_UNIT ( * ) SI_UNIT ( .MILLI., .METRE. ) );
#38715=EDGE_CURVE ( 'NONE', #35323, #14426, #42501, .T. ) ;
#38716=CARTESIAN_POINT ( 'NONE',  ( 17.99999999999999645, 0.000000000000000000, 0.000000000000000000 ) ) ;
#38720=CARTESIAN_POINT ( 'NONE',  ( 0.000000000000000000, -106.6051926090968180, -45.73109345704927620 ) ) ;
#38722=ORIENTED_EDGE ( 'NONE', *, *, #27475, .F. ) ;
#38723=AXIS2_PLACEMENT_3D ( 'NONE', #6730, #12868, #26177 ) ;
#38724=CIRCLE ( 'NONE', #25540, 120.5010000000000190 ) ;
#38726=CIRCLE ( 'NONE', #19968, 59.00000000000001421 ) ;
#38727=ORIENTED_EDGE ( 'NONE', *, *, #21360, .T. ) ;
#38729=CARTESIAN_POINT ( 'NONE',  ( 9.000000000000001776, -47.31079789947556691, 105.9135893174949530 ) ) ;
#38731=CIRCLE ( 'NONE', #24172, 116.0000000000000000 ) ;
#38736=AXIS2_PLACEMENT_3D ( 'NONE', #5057, #41481, #19635 ) ;
#38738=CARTESIAN_POINT ( 'NONE',  ( 0.000000000000000000, -104.0201923570379137, 51.34003878071028026 ) ) ;
#38742=VERTEX_POINT ( 'NONE', #32989 ) ;
#38747=ADVANCED_FACE ( 'NONE', ( #7619 ), #16230, .F. ) ;
#38753=CIRCLE ( 'NONE', #3195, 58.99999999999999289 ) ;
#38754=CYLINDRICAL_SURFACE ( 'NONE', #9101, 120.5010000000000190 ) ;
#38755=DIRECTION ( 'NONE',  ( 0.000000000000000000, 0.9574220383620042352, 0.2886919473396248326 ) ) ;
#38756=ORIENTED_EDGE ( 'NONE', *, *, #37648, .F. ) ;
#38760=CARTESIAN_POINT ( 'NONE',  ( 17.99999999999999645, -89.07460286905904923, 81.15544420874930154 ) ) ;
#38761=CIRCLE ( 'NONE', #20003, 58.99999999999999289 ) ;
#38763=DIRECTION ( 'NONE',  ( -1.000000000000000000, 0.000000000000000000, -0.000000000000000000 ) ) ;
#38765=CARTESIAN_POINT ( 'NONE',  ( 17.99999999999999645, -100.6739960869714139, -49.52796165323368172 ) ) ;
#38766=VECTOR ( 'NONE', #31222, 1000.000000000000000 ) ;
#38768=EDGE_CURVE ( 'NONE', #1680, #24177, #16773, .T. ) ;
#38774=CARTESIAN_POINT ( 'NONE',  ( 17.99999999999999645, -51.98489025774233596, -108.7109110710166391 ) ) ;
#38775=ORIENTED_EDGE ( 'NONE', *, *, #18162, .F. ) ;
#38780=AXIS2_PLACEMENT_3D ( 'NONE', #15449, #15866, #19151 ) ;
#38785=ADVANCED_FACE ( 'NONE', ( #39736 ), #32782, .F. ) ;
#38786=ORIENTED_EDGE ( 'NONE', *, *, #33882, .T. ) ;
#38788=DIRECTION ( 'NONE',  ( -1.000000000000000000, -0.000000000000000000, -0.000000000000000000 ) ) ;
#38791=CYLINDRICAL_SURFACE ( 'NONE', #24804, 59.00000000000001421 ) ;
#38793=DIRECTION ( 'NONE',  ( 0.000000000000000000, 0.9407002666710341243, -0.3392388661180278930 ) ) ;
#38794=VERTEX_POINT ( 'NONE', #14410 ) ;
#38798=EDGE_CURVE ( 'NONE', #17354, #38008, #17464, .T. ) ;
#38799=ORIENTED_EDGE ( 'NONE', *, *, #24685, .T. ) ;
#38801=DIRECTION ( 'NONE',  ( 1.000000000000000000, 0.000000000000000000, 0.000000000000000000 ) ) ;
#38803=ORIENTED_EDGE ( 'NONE', *, *, #12133, .F. ) ;
#38804=EDGE_CURVE ( 'NONE', #596, #39282, #27918, .T. ) ;
#38805=CARTESIAN_POINT ( 'NONE',  ( 17.99999999999999645, -51.98489025774375705, 108.7109110710159854 ) ) ;
#38807=EDGE_CURVE ( 'NONE', #2567, #39845, #2863, .T. ) ;
#38809=CARTESIAN_POINT ( 'NONE',  ( 9.000000000000001776, 63.55543939553764687, 97.03971415477347762 ) ) ;
#38812=DIRECTION ( 'NONE',  ( -1.000000000000000000, 0.000000000000000000, 0.000000000000000000 ) ) ;
#38813=AXIS2_PLACEMENT_3D ( 'NONE', #17601, #25024, #7945 ) ;
#38814=CARTESIAN_POINT ( 'NONE',  ( 17.99999999999999645, 99.97660604680052643, -67.26937820704789317 ) ) ;
#38816=ORIENTED_EDGE ( 'NONE', *, *, #22439, .F. ) ;
#38818=AXIS2_PLACEMENT_3D ( 'NONE', #21048, #34302, #3963 ) ;
#38820=AXIS2_PLACEMENT_3D ( 'NONE', #10632, #27223, #34611 ) ;
#38821=FACE_OUTER_BOUND ( 'NONE', #3476, .T. ) ;
#38822=ADVANCED_FACE ( 'NONE', ( #34884 ), #21193, .F. ) ;
#38823=EDGE_CURVE ( 'NONE', #36920, #17401, #19569, .T. ) ;
#38824=ORIENTED_EDGE ( 'NONE', *, *, #41064, .F. ) ;
#38825=DIRECTION ( 'NONE',  ( 0.000000000000000000, 0.9574220383620042352, 0.2886919473396248881 ) ) ;
#38827=EDGE_CURVE ( 'NONE', #3472, #10645, #2778, .T. ) ;
#38828=ADVANCED_FACE ( 'NONE', ( #8280 ), #5207, .F. ) ;
#38829=EDGE_CURVE ( 'NONE', #16730, #30917, #25159, .T. ) ;
#38830=AXIS2_PLACEMENT_3D ( 'NONE', #17743, #17972, #37973 ) ;
#38836=CARTESIAN_POINT ( 'NONE',  ( 17.99999999999999645, 30.01658535635262481, 108.1077105353199102 ) ) ;
#38837=AXIS2_PLACEMENT_3D ( 'NONE', #20623, #23246, #37152 ) ;
#38840=DIRECTION ( 'NONE',  ( 0.000000000000000000, 0.000000000000000000, 1.000000000000000000 ) ) ;
#38841=CARTESIAN_POINT ( 'NONE',  ( 0.000000000000000000, -91.51415974874635140, 64.91094698989267897 ) ) ;
#38842=VECTOR ( 'NONE', #30824, 1000.000000000000000 ) ;
#38846=CIRCLE ( 'NONE', #24267, 59.00000000000000711 ) ;
#38847=EDGE_CURVE ( 'NONE', #8080, #4507, #31616, .T. ) ;
#38848=VERTEX_POINT ( 'NONE', #4549 ) ;
#38850=ORIENTED_EDGE ( 'NONE', *, *, #11149, .F. ) ;
#38851=DIRECTION ( 'NONE',  ( 0.000000000000000000, -0.9826841245925228563, 0.1852887240871046171 ) ) ;
#38854=ORIENTED_EDGE ( 'NONE', *, *, #11342, .F. ) ;
#38858=CARTESIAN_POINT ( 'NONE',  ( 17.99999999999999645, 0.000000000000000000, 0.000000000000000000 ) ) ;
#38859=ORIENTED_EDGE ( 'NONE', *, *, #35712, .T. ) ;
#38860=ORIENTED_EDGE ( 'NONE', *, *, #29609, .F. ) ;
#38864=VERTEX_POINT ( 'NONE', #41644 ) ;
#38867=ORIENTED_EDGE ( 'NONE', *, *, #35277, .F. ) ;
#38868=FACE_OUTER_BOUND ( 'NONE', #5661, .T. ) ;
#38872=AXIS2_PLACEMENT_3D ( 'NONE', #17762, #24971, #1346 ) ;
#38874=DIRECTION ( 'NONE',  ( 1.000000000000000000, 0.000000000000000000, -0.000000000000000000 ) ) ;
#38875=CARTESIAN_POINT ( 'NONE',  ( 17.99999999999999645, 105.7179949885863266, 37.57629584241859533 ) ) ;
#38877=EDGE_CURVE ( 'NONE', #9730, #25913, #4902, .T. ) ;
#38878=DIRECTION ( 'NONE',  ( 1.000000000000000000, 0.000000000000000000, 0.000000000000000000 ) ) ;
#38879=LINE ( 'NONE', #2417, #1948 ) ;
#38880=VECTOR ( 'NONE', #9974, 1000.000000000000000 ) ;
#38882=AXIS2_PLACEMENT_3D ( 'NONE', #25466, #28938, #22414 ) ;
#38889=CYLINDRICAL_SURFACE ( 'NONE', #7749, 59.00000000000001421 ) ;
#38894=EDGE_LOOP ( 'NONE', ( #14842, #22370, #14814, #37624 ) ) ;
#38895=ORIENTED_EDGE ( 'NONE', *, *, #14879, .F. ) ;
#38896=DIRECTION ( 'NONE',  ( 0.000000000000000000, -6.538873467836204094E-15, 1.000000000000000000 ) ) ;
#38900=DIRECTION ( 'NONE',  ( 0.000000000000000000, 0.000000000000000000, 1.000000000000000000 ) ) ;
#38904=DIRECTION ( 'NONE',  ( 1.000000000000000000, 0.000000000000000000, 0.000000000000000000 ) ) ;
#38906=AXIS2_PLACEMENT_3D ( 'NONE', #41000, #31427, #7847 ) ;
#38909=LINE ( 'NONE', #42165, #35223 ) ;
#38913=VERTEX_POINT ( 'NONE', #35095 ) ;
#38917=CARTESIAN_POINT ( 'NONE',  ( 17.99999999999999645, 111.8797445107944810, -8.437727291343108504 ) ) ;
#38918=ORIENTED_EDGE ( 'NONE', *, *, #6318, .T. ) ;
#38920=EDGE_LOOP ( 'NONE', ( #28904, #11809, #37908, #26295 ) ) ;
#38923=ORIENTED_EDGE ( 'NONE', *, *, #14326, .T. ) ;
#38926=CARTESIAN_POINT ( 'NONE',  ( 0.000000000000000000, 110.3490479609632615, -20.28201389785435182 ) ) ;
#38927=ADVANCED_FACE ( 'NONE', ( #38573 ), #31845, .F. ) ;
#38928=CARTESIAN_POINT ( 'NONE',  ( 0.000000000000000000, 111.2721026680458749, 14.38025178762809908 ) ) ;
#38931=ORIENTED_EDGE ( 'NONE', *, *, #27683, .T. ) ;
#38932=CARTESIAN_POINT ( 'NONE',  ( 0.000000000000000000, 15.21076497709711184, 119.5371223922155792 ) ) ;
#38935=CARTESIAN_POINT ( 'NONE',  ( 0.000000000000000000, -67.32409792376445523, -89.75376489259431878 ) ) ;
#38939=AXIS2_PLACEMENT_3D ( 'NONE', #2186, #9179, #5487 ) ;
#38940=EDGE_CURVE ( 'NONE', #12095, #10939, #16073, .T. ) ;
#38943=ORIENTED_EDGE ( 'NONE', *, *, #31830, .T. ) ;
#38948=DIRECTION ( 'NONE',  ( 0.000000000000000000, 0.000000000000000000, 1.000000000000000000 ) ) ;
#38949=ORIENTED_EDGE ( 'NONE', *, *, #15660, .F. ) ;
#38950=DIRECTION ( 'NONE',  ( -1.000000000000000000, -0.000000000000000000, -0.000000000000000000 ) ) ;
#38952=CARTESIAN_POINT ( 'NONE',  ( 17.99999999999999645, 0.000000000000000000, 0.000000000000000000 ) ) ;
#38956=ORIENTED_EDGE ( 'NONE', *, *, #2717, .F. ) ;
#38958=DIRECTION ( 'NONE',  ( 0.000000000000000000, 0.9574220383620062336, -0.2886919473396183933 ) ) ;
#38960=ORIENTED_EDGE ( 'NONE', *, *, #10616, .T. ) ;
#38965=AXIS2_PLACEMENT_3D ( 'NONE', #13774, #16180, #10030 ) ;
#38972=DIRECTION ( 'NONE',  ( 0.000000000000000000, 2.140472356798500845E-14, -1.000000000000000000 ) ) ;
#38974=ADVANCED_FACE ( 'NONE', ( #7835 ), #31201, .F. ) ;
#38976=ORIENTED_EDGE ( 'NONE', *, *, #23365, .T. ) ;
#38979=EDGE_LOOP ( 'NONE', ( #1779, #41046, #18723, #3313 ) ) ;
#38980=DIRECTION ( 'NONE',  ( 0.000000000000000000, 0.4610925014493266194, -0.8873520750565710991 ) ) ;
#38981=CARTESIAN_POINT ( 'NONE',  ( 17.99999999999999645, -110.1579703617967567, 21.29539948940213634 ) ) ;
#38983=ORIENTED_EDGE ( 'NONE', *, *, #12708, .F. ) ;
#38986=EDGE_CURVE ( 'NONE', #21881, #33572, #703, .T. ) ;
#38987=DIRECTION ( 'NONE',  ( -1.000000000000000000, -0.000000000000000000, -0.000000000000000000 ) ) ;
#38989=AXIS2_PLACEMENT_3D ( 'NONE', #25297, #11972, #29190 ) ;
#38990=AXIS2_PLACEMENT_3D ( 'NONE', #20271, #20479, #37449 ) ;
#38993=ORIENTED_EDGE ( 'NONE', *, *, #14398, .F. ) ;
#38997=VERTEX_POINT ( 'NONE', #21600 ) ;
#38999=FACE_OUTER_BOUND ( 'NONE', #12221, .T. ) ;
#39000=DIRECTION ( 'NONE',  ( 0.000000000000000000, 0.000000000000000000, 1.000000000000000000 ) ) ;
#39003=VERTEX_POINT ( 'NONE', #25493 ) ;
#39004=DIRECTION ( 'NONE',  ( -1.000000000000000000, 0.000000000000000000, 0.000000000000000000 ) ) ;
#39010=ORIENTED_EDGE ( 'NONE', *, *, #21583, .F. ) ;
#39011=EDGE_CURVE ( 'NONE', #28805, #26249, #9755, .T. ) ;
#39014=ORIENTED_EDGE ( 'NONE', *, *, #41286, .T. ) ;
#39018=CYLINDRICAL_SURFACE ( 'NONE', #9072, 59.00000000000000000 ) ;
#39022=CARTESIAN_POINT ( 'NONE',  ( 17.99999999999999645, 92.10690493017145286, -64.06707842432085442 ) ) ;
#39025=CARTESIAN_POINT ( 'NONE',  ( 17.99999999999999645, 0.000000000000000000, 0.000000000000000000 ) ) ;
#39026=ADVANCED_FACE ( 'NONE', ( #8885 ), #38754, .F. ) ;
#39028=ORIENTED_EDGE ( 'NONE', *, *, #21298, .F. ) ;
#39034=CARTESIAN_POINT ( 'NONE',  ( 0.000000000000000000, 99.97660604680052643, -67.26937820704789317 ) ) ;
#39036=ORIENTED_EDGE ( 'NONE', *, *, #34361, .F. ) ;
#39040=VERTEX_POINT ( 'NONE', #41156 ) ;
#39043=AXIS2_PLACEMENT_3D ( 'NONE', #35698, #36135, #12607 ) ;
#39046=CARTESIAN_POINT ( 'NONE',  ( 17.99999999999999645, 0.000000000000000000, 0.000000000000000000 ) ) ;
#39048=AXIS2_PLACEMENT_3D ( 'NONE', #11764, #34857, #39180 ) ;
#39052=ORIENTED_EDGE ( 'NONE', *, *, #9409, .T. ) ;
#39054=CARTESIAN_POINT ( 'NONE',  ( 17.99999999999999645, 0.000000000000000000, 0.000000000000000000 ) ) ;
#39057=EDGE_CURVE ( 'NONE', #16946, #1540, #19598, .T. ) ;
#39059=FACE_OUTER_BOUND ( 'NONE', #25379, .T. ) ;
#39063=ORIENTED_EDGE ( 'NONE', *, *, #21530, .T. ) ;
#39064=ORIENTED_EDGE ( 'NONE', *, *, #24701, .T. ) ;
#39065=CARTESIAN_POINT ( 'NONE',  ( 0.000000000000000000, 68.63002662989747193, 93.51962064069530811 ) ) ;
#39069=AXIS2_PLACEMENT_3D ( 'NONE', #35856, #5982, #19337 ) ;
#39071=ORIENTED_EDGE ( 'NONE', *, *, #34653, .T. ) ;
#39073=EDGE_CURVE ( 'NONE', #27001, #25725, #5615, .T. ) ;
#39074=EDGE_CURVE ( 'NONE', #3831, #41306, #4962, .T. ) ;
#39075=DIRECTION ( 'NONE',  ( 1.000000000000000000, 0.000000000000000000, 0.000000000000000000 ) ) ;
#39079=LINE ( 'NONE', #29721, #12711 ) ;
#39081=AXIS2_PLACEMENT_3D ( 'NONE', #1448, #4503, #25079 ) ;
#39084=ORIENTED_EDGE ( 'NONE', *, *, #20319, .T. ) ;
#39088=AXIS2_PLACEMENT_3D ( 'NONE', #11112, #4763, #37486 ) ;
#39091=EDGE_CURVE ( 'NONE', #3822, #7775, #25857, .T. ) ;
#39092=CYLINDRICAL_SURFACE ( 'NONE', #11258, 116.0000000000000000 ) ;
#39093=ORIENTED_EDGE ( 'NONE', *, *, #23993, .T. ) ;
#39096=VERTEX_POINT ( 'NONE', #24638 ) ;
#39102=DIRECTION ( 'NONE',  ( -1.000000000000000000, -0.000000000000000000, -0.000000000000000000 ) ) ;
#39103=CARTESIAN_POINT ( 'NONE',  ( 17.99999999999999645, 0.000000000000000000, 0.000000000000000000 ) ) ;
#39104=ORIENTED_EDGE ( 'NONE', *, *, #33029, .T. ) ;
#39106=ORIENTED_EDGE ( 'NONE', *, *, #10281, .T. ) ;
#39109=CYLINDRICAL_SURFACE ( 'NONE', #29108, 116.0000000000000000 ) ;
#39111=EDGE_CURVE ( 'NONE', #34589, #32501, #20292, .T. ) ;
#39113=LINE ( 'NONE', #9237, #34681 ) ;
#39115=EDGE_CURVE ( 'NONE', #32554, #18274, #11757, .T. ) ;
#39120=ORIENTED_EDGE ( 'NONE', *, *, #37018, .F. ) ;
#39121=DIRECTION ( 'NONE',  ( -1.000000000000000000, 0.000000000000000000, 0.000000000000000000 ) ) ;
#39122=CIRCLE ( 'NONE', #30094, 59.00000000000001421 ) ;
#39123=ORIENTED_EDGE ( 'NONE', *, *, #42990, .T. ) ;
#39124=DIRECTION ( 'NONE',  ( 0.000000000000000000, 0.8477344278896721264, -0.5304209081197406306 ) ) ;
#39129=DIRECTION ( 'NONE',  ( 0.000000000000000000, 0.000000000000000000, 1.000000000000000000 ) ) ;
#39131=ORIENTED_EDGE ( 'NONE', *, *, #9519, .F. ) ;
#39133=CARTESIAN_POINT ( 'NONE',  ( 17.99999999999999645, -87.92975456462950490, 69.68953103478128241 ) ) ;
#39134=LINE ( 'NONE', #26497, #26957 ) ;
#39135=CARTESIAN_POINT ( 'NONE',  ( 17.99999999999999645, 88.56657216608614647, 68.87840567545953263 ) ) ;
#39139=DIRECTION ( 'NONE',  ( 1.000000000000000000, 0.000000000000000000, 0.000000000000000000 ) ) ;
#39145=ORIENTED_EDGE ( 'NONE', *, *, #11635, .F. ) ;
#39146=CIRCLE ( 'NONE', #10603, 59.00000000000000000 ) ;
#39147=AXIS2_PLACEMENT_3D ( 'NONE', #5512, #28660, #8143 ) ;
#39150=CARTESIAN_POINT ( 'NONE',  ( 17.99999999999999645, 79.94368240339547071, -90.16373242487824768 ) ) ;
#39153=CARTESIAN_POINT ( 'NONE',  ( 17.99999999999999645, 88.56657216608705596, -68.87840567545838155 ) ) ;
#39155=DIRECTION ( 'NONE',  ( 0.000000000000000000, 0.000000000000000000, 1.000000000000000000 ) ) ;
#39157=CARTESIAN_POINT ( 'NONE',  ( 17.99999999999999645, -6.854627147197943415, -115.7972974066014018 ) ) ;
#39158=CARTESIAN_POINT ( 'NONE',  ( 17.99999999999999645, 12.43843445475317822, 111.5058645182329968 ) ) ;
#39163=DIRECTION ( 'NONE',  ( 0.000000000000000000, 0.000000000000000000, 1.000000000000000000 ) ) ;
#39169=ORIENTED_EDGE ( 'NONE', *, *, #36396, .T. ) ;
#39173=DIRECTION ( 'NONE',  ( 1.000000000000000000, 0.000000000000000000, 0.000000000000000000 ) ) ;
#39178=AXIS2_PLACEMENT_3D ( 'NONE', #34265, #4361, #31002 ) ;
#39180=DIRECTION ( 'NONE',  ( 0.000000000000000000, -0.6783118362696075598, -0.7347741508630750706 ) ) ;
#39181=EDGE_CURVE ( 'NONE', #35178, #18183, #19382, .T. ) ;
#39182=FACE_OUTER_BOUND ( 'NONE', #27606, .T. ) ;
#39184=EDGE_LOOP ( 'NONE', ( #12651, #576, #17596, #31478 ) ) ;
#39185=CARTESIAN_POINT ( 'NONE',  ( 17.99999999999999645, -107.2703412112697094, 32.88383143828427535 ) ) ;
#39187=DIRECTION ( 'NONE',  ( 0.000000000000000000, 0.000000000000000000, 1.000000000000000000 ) ) ;
#39188=DIRECTION ( 'NONE',  ( 0.000000000000000000, 0.000000000000000000, 1.000000000000000000 ) ) ;
#39190=CARTESIAN_POINT ( 'NONE',  ( 17.99999999999999645, 76.48293397876260258, 82.08917884620340999 ) ) ;
#39191=VERTEX_POINT ( 'NONE', #42658 ) ;
#39195=CARTESIAN_POINT ( 'NONE',  ( 17.99999999999999645, 114.1529630473449686, 38.59523323561477781 ) ) ;
#39200=DIRECTION ( 'NONE',  ( 1.000000000000000000, 0.000000000000000000, 0.000000000000000000 ) ) ;
#39201=VERTEX_POINT ( 'NONE', #3152 ) ;
#39203=CARTESIAN_POINT ( 'NONE',  ( 0.000000000000000000, 108.8684555192046872, 27.12806418649654105 ) ) ;
#39204=DIRECTION ( 'NONE',  ( 1.000000000000000000, 0.000000000000000000, 0.000000000000000000 ) ) ;
#39205=DIRECTION ( 'NONE',  ( 0.000000000000000000, -0.6382441836448109473, -0.7698339834299138262 ) ) ;
#39206=ORIENTED_EDGE ( 'NONE', *, *, #42840, .T. ) ;
#39208=CARTESIAN_POINT ( 'NONE',  ( 0.000000000000000000, 100.6739960869717834, 49.52796165323294986 ) ) ;
#39212=DIRECTION ( 'NONE',  ( -1.000000000000000000, -0.000000000000000000, -0.000000000000000000 ) ) ;
#39213=EDGE_LOOP ( 'NONE', ( #31363, #40526, #15807, #4921 ) ) ;
#39215=LINE ( 'NONE', #39862, #23216 ) ;
#39219=CIRCLE ( 'NONE', #41316, 59.00000000000000000 ) ;
#39220=ORIENTED_EDGE ( 'NONE', *, *, #7553, .T. ) ;
#39222=EDGE_LOOP ( 'NONE', ( #13657, #23079, #30558, #33243 ) ) ;
#39223=DIRECTION ( 'NONE',  ( -1.000000000000000000, -0.000000000000000000, -0.000000000000000000 ) ) ;
#39224=DIRECTION ( 'NONE',  ( 0.000000000000000000, 2.211037379550099895E-14, -1.000000000000000000 ) ) ;
#39225=ADVANCED_FACE ( 'NONE', ( #2935 ), #23083, .F. ) ;
#39226=DIRECTION ( 'NONE',  ( 0.000000000000000000, 0.7164567402983162969, -0.6976315211349835010 ) ) ;
#39227=CARTESIAN_POINT ( 'NONE',  ( 0.000000000000000000, -80.02407177072905142, -78.64108602300026973 ) ) ;
#39230=LINE ( 'NONE', #9149, #24515 ) ;
#39232=CARTESIAN_POINT ( 'NONE',  ( 17.99999999999999645, 0.000000000000000000, 0.000000000000000000 ) ) ;
#39233=ORIENTED_EDGE ( 'NONE', *, *, #22498, .T. ) ;
#39234=CARTESIAN_POINT ( 'NONE',  ( 0.000000000000000000, -112.1702510623870239, -2.471285140323770335 ) ) ;
#39237=CARTESIAN_POINT ( 'NONE',  ( 17.99999999999999645, 68.63002662989747193, 93.51962064069530811 ) ) ;
#39240=FACE_OUTER_BOUND ( 'NONE', #11948, .T. ) ;
#39250=EDGE_CURVE ( 'NONE', #27794, #22079, #16803, .T. ) ;
#39251=ORIENTED_EDGE ( 'NONE', *, *, #27935, .F. ) ;
#39254=CIRCLE ( 'NONE', #2324, 58.99999999999999289 ) ;
#39260=CARTESIAN_POINT ( 'NONE',  ( 0.000000000000000000, 107.2703412112694963, 32.88383143828500721 ) ) ;
#39265=DIRECTION ( 'NONE',  ( -1.000000000000000000, -0.000000000000000000, -0.000000000000000000 ) ) ;
#39267=VERTEX_POINT ( 'NONE', #36329 ) ;
#39268=DIRECTION ( 'NONE',  ( 0.000000000000000000, 0.000000000000000000, 1.000000000000000000 ) ) ;
#39269=AXIS2_PLACEMENT_3D ( 'NONE', #29906, #19661, #3006 ) ;
#39271=EDGE_CURVE ( 'NONE', #26760, #39508, #6446, .T. ) ;
#39274=CARTESIAN_POINT ( 'NONE',  ( 0.000000000000000000, 97.97378550988226209, 62.10585602713792497 ) ) ;
#39275=VECTOR ( 'NONE', #12432, 1000.000000000000000 ) ;
#39276=DIRECTION ( 'NONE',  ( -1.000000000000000000, 0.000000000000000000, -0.000000000000000000 ) ) ;
#39282=VERTEX_POINT ( 'NONE', #12392 ) ;
#39287=ORIENTED_EDGE ( 'NONE', *, *, #29198, .F. ) ;
#39288=DIRECTION ( 'NONE',  ( -1.000000000000000000, -0.000000000000000000, -0.000000000000000000 ) ) ;
#39289=EDGE_CURVE ( 'NONE', #26508, #27767, #30731, .T. ) ;
#39290=CARTESIAN_POINT ( 'NONE',  ( 0.000000000000000000, 0.000000000000000000, 0.000000000000000000 ) ) ;
#39300=CARTESIAN_POINT ( 'NONE',  ( 0.000000000000000000, -66.49630760163661591, 90.36876423295966276 ) ) ;
#39302=VECTOR ( 'NONE', #2322, 1000.000000000000000 ) ;
#39304=CARTESIAN_POINT ( 'NONE',  ( 17.99999999999999645, 89.07460286905850921, 81.15544420874991260 ) ) ;
#39305=DIRECTION ( 'NONE',  ( -1.000000000000000000, 0.000000000000000000, 0.000000000000000000 ) ) ;
#39308=ORIENTED_EDGE ( 'NONE', *, *, #28676, .F. ) ;
#39309=DIRECTION ( 'NONE',  ( 1.000000000000000000, 0.000000000000000000, 0.000000000000000000 ) ) ;
#39311=CARTESIAN_POINT ( 'NONE',  ( 0.000000000000000000, 63.24564713401792204, 102.5693868539697178 ) ) ;
#39314=DIRECTION ( 'NONE',  ( 0.000000000000000000, 0.000000000000000000, 1.000000000000000000 ) ) ;
#39315=VERTEX_POINT ( 'NONE', #20670 ) ;
#39319=EDGE_CURVE ( 'NONE', #32698, #36927, #17177, .T. ) ;
#39321=DIRECTION ( 'NONE',  ( -1.000000000000000000, -0.000000000000000000, -0.000000000000000000 ) ) ;
#39322=VERTEX_POINT ( 'NONE', #27401 ) ;
#39324=EDGE_CURVE ( 'NONE', #10364, #13484, #23773, .T. ) ;
#39326=CARTESIAN_POINT ( 'NONE',  ( 17.99999999999999645, 61.59243992711585491, -93.77976230225978327 ) ) ;
#39328=EDGE_LOOP ( 'NONE', ( #39989, #3524, #4882, #12577 ) ) ;
#39329=CARTESIAN_POINT ( 'NONE',  ( 0.000000000000000000, 0.000000000000000000, 0.000000000000000000 ) ) ;
#39330=CIRCLE ( 'NONE', #29624, 120.5010000000000474 ) ;
#39334=CARTESIAN_POINT ( 'NONE',  ( 17.99999999999999645, -75.72520367775142347, 82.78868281115956052 ) ) ;
#39335=DIRECTION ( 'NONE',  ( 1.000000000000000000, 0.000000000000000000, 0.000000000000000000 ) ) ;
#39337=FACE_OUTER_BOUND ( 'NONE', #20417, .T. ) ;
#39340=VERTEX_POINT ( 'NONE', #6882 ) ;
#39343=FACE_OUTER_BOUND ( 'NONE', #13081, .T. ) ;
#39348=FACE_OUTER_BOUND ( 'NONE', #39700, .T. ) ;
#39352=EDGE_CURVE ( 'NONE', #41913, #42713, #11215, .T. ) ;
#39353=VERTEX_POINT ( 'NONE', #7305 ) ;
#39360=DIRECTION ( 'NONE',  ( -1.000000000000000000, 0.000000000000000000, 0.000000000000000000 ) ) ;
#39362=CIRCLE ( 'NONE', #12252, 59.00000000000000000 ) ;
#39365=CARTESIAN_POINT ( 'NONE',  ( 17.99999999999999645, -119.8996782608630838, 12.02323392193314966 ) ) ;
#39367=LINE ( 'NONE', #12791, #38085 ) ;
#39368=CIRCLE ( 'NONE', #22031, 59.00000000000000711 ) ;
#39370=CARTESIAN_POINT ( 'NONE',  ( 8.999999999999998224, 101.1403355683146117, 56.80345518653519576 ) ) ;
#39371=DIRECTION ( 'NONE',  ( 1.000000000000000000, 0.000000000000000000, 0.000000000000000000 ) ) ;
#39375=AXIS2_PLACEMENT_3D ( 'NONE', #20599, #33870, #7901 ) ;
#39376=EDGE_CURVE ( 'NONE', #28381, #26365, #34169, .T. ) ;
#39381=EDGE_CURVE ( 'NONE', #17417, #553, #26521, .T. ) ;
#39382=CARTESIAN_POINT ( 'NONE',  ( 0.000000000000000000, 116.0452958106484971, -32.46506308663343532 ) ) ;
#39385=ORIENTED_EDGE ( 'NONE', *, *, #11472, .T. ) ;
#39392=FACE_OUTER_BOUND ( 'NONE', #25020, .T. ) ;
#39393=CIRCLE ( 'NONE', #18575, 120.5010000000000190 ) ;
#39394=CARTESIAN_POINT ( 'NONE',  ( 17.99999999999999645, 91.65951123222482977, 71.09524597798119316 ) ) ;
#39395=VECTOR ( 'NONE', #37097, 1000.000000000000000 ) ;
#39399=ORIENTED_EDGE ( 'NONE', *, *, #15188, .F. ) ;
#39400=CIRCLE ( 'NONE', #42890, 59.00000000000000000 ) ;
#39401=CARTESIAN_POINT ( 'NONE',  ( 17.99999999999999645, -71.21168426767047777, -86.70160608319397966 ) ) ;
#39407=EDGE_CURVE ( 'NONE', #40263, #34617, #5645, .T. ) ;
#39411=CARTESIAN_POINT ( 'NONE',  ( 17.99999999999999645, 0.000000000000000000, 0.000000000000000000 ) ) ;
#39414=CARTESIAN_POINT ( 'NONE',  ( 0.000000000000000000, 75.03166794516924654, -94.29071961951432002 ) ) ;
#39415=ORIENTED_EDGE ( 'NONE', *, *, #32149, .F. ) ;
#39420=VERTEX_POINT ( 'NONE', #30241 ) ;
#39422=EDGE_CURVE ( 'NONE', #36553, #9338, #18935, .T. ) ;
#39423=CARTESIAN_POINT ( 'NONE',  ( 0.000000000000000000, -104.0201923570372173, -51.34003878071168003 ) ) ;
#39425=VECTOR ( 'NONE', #25749, 1000.000000000000000 ) ;
#39428=AXIS2_PLACEMENT_3D ( 'NONE', #8257, #5181, #11113 ) ;
#39435=AXIS2_PLACEMENT_3D ( 'NONE', #14463, #36907, #23423 ) ;
#39436=ORIENTED_EDGE ( 'NONE', *, *, #27901, .T. ) ;
#39438=DIRECTION ( 'NONE',  ( -1.000000000000000000, 0.000000000000000000, 0.000000000000000000 ) ) ;
#39441=EDGE_CURVE ( 'NONE', #8823, #39420, #33500, .T. ) ;
#39447=CIRCLE ( 'NONE', #14423, 58.99999999999998579 ) ;
#39448=LINE ( 'NONE', #32914, #34462 ) ;
#39449=DIRECTION ( 'NONE',  ( 1.000000000000000000, -0.000000000000000000, -0.000000000000000000 ) ) ;
#39451=CARTESIAN_POINT ( 'NONE',  ( 0.000000000000000000, 42.87700105098753056, -107.7847984684000551 ) ) ;
#39453=CARTESIAN_POINT ( 'NONE',  ( 17.99999999999999645, 0.000000000000000000, 0.000000000000000000 ) ) ;
#39454=VECTOR ( 'NONE', #14148, 1000.000000000000000 ) ;
#39456=DIRECTION ( 'NONE',  ( 0.000000000000000000, 0.000000000000000000, -1.000000000000000000 ) ) ;
#39457=ADVANCED_FACE ( 'NONE', ( #13673 ), #26973, .F. ) ;
#39458=CARTESIAN_POINT ( 'NONE',  ( 17.99999999999999645, 19.12429268481864142, -114.4126803693777248 ) ) ;
#39459=AXIS2_PLACEMENT_3D ( 'NONE', #21612, #34859, #4974 ) ;
#39460=AXIS2_PLACEMENT_3D ( 'NONE', #16016, #35813, #42583 ) ;
#39462=LINE ( 'NONE', #16613, #21912 ) ;
#39464=DIRECTION ( 'NONE',  ( 0.000000000000000000, 0.5963673585384969833, 0.8027116379309670036 ) ) ;
#39465=ORIENTED_EDGE ( 'NONE', *, *, #16442, .T. ) ;
#39466=AXIS2_PLACEMENT_3D ( 'NONE', #40707, #27885, #23541 ) ;
#39469=ADVANCED_FACE ( 'NONE', ( #7092 ), #38280, .F. ) ;
#39471=CIRCLE ( 'NONE', #20733, 116.0000000000000000 ) ;
#39474=CARTESIAN_POINT ( 'NONE',  ( 9.000000000000001776, -58.30069736313733131, 100.2847380560565256 ) ) ;
#39475=CARTESIAN_POINT ( 'NONE',  ( 17.99999999999999645, 94.83915810436401728, 59.94836581341619564 ) ) ;
#39477=EDGE_LOOP ( 'NONE', ( #31454, #5653, #19853, #37352 ) ) ;
#39481=ORIENTED_EDGE ( 'NONE', *, *, #9795, .F. ) ;
#39483=DIRECTION ( 'NONE',  ( -1.000000000000000000, -0.000000000000000000, -0.000000000000000000 ) ) ;
#39484=CARTESIAN_POINT ( 'NONE',  ( 0.000000000000000000, -84.77518783075143460, 73.49448960231327987 ) ) ;
#39489=AXIS2_PLACEMENT_3D ( 'NONE', #39697, #32950, #10038 ) ;
#39495=ORIENTED_EDGE ( 'NONE', *, *, #38621, .F. ) ;
#39497=CIRCLE ( 'NONE', #40901, 120.5010000000000332 ) ;
#39499=DIRECTION ( 'NONE',  ( 0.000000000000000000, 0.000000000000000000, 1.000000000000000000 ) ) ;
#39503=LINE ( 'NONE', #26014, #8781 ) ;
#39506=DIRECTION ( 'NONE',  ( 0.000000000000000000, 0.000000000000000000, 1.000000000000000000 ) ) ;
#39508=VERTEX_POINT ( 'NONE', #18272 ) ;
#39513=CARTESIAN_POINT ( 'NONE',  ( 17.99999999999999645, 46.12538073176499154, -111.3235835452206857 ) ) ;
#39514=AXIS2_PLACEMENT_3D ( 'NONE', #3725, #23867, #684 ) ;
#39520=EDGE_CURVE ( 'NONE', #19587, #6806, #41160, .T. ) ;
#39521=CIRCLE ( 'NONE', #15905, 116.0000000000000000 ) ;
#39524=VERTEX_POINT ( 'NONE', #35222 ) ;
#39525=DIRECTION ( 'NONE',  ( -1.000000000000000000, -0.000000000000000000, -0.000000000000000000 ) ) ;
#39526=EDGE_CURVE ( 'NONE', #7422, #8430, #21742, .T. ) ;
#39527=DIRECTION ( 'NONE',  ( -1.000000000000000000, 0.000000000000000000, -0.000000000000000000 ) ) ;
#39528=AXIS2_PLACEMENT_3D ( 'NONE', #10743, #37129, #6818 ) ;
#39530=DIRECTION ( 'NONE',  ( 0.000000000000000000, 0.000000000000000000, 1.000000000000000000 ) ) ;
#39531=CARTESIAN_POINT ( 'NONE',  ( 9.000000000000001776, -104.6166166098448826, 50.11350645393640235 ) ) ;
#39533=ORIENTED_EDGE ( 'NONE', *, *, #16561, .T. ) ;
#39540=DIRECTION ( 'NONE',  ( 1.000000000000000000, 0.000000000000000000, 0.000000000000000000 ) ) ;
#39542=LINE ( 'NONE', #13186, #38205 ) ;
#39546=VERTEX_POINT ( 'NONE', #41553 ) ;
#39550=ORIENTED_EDGE ( 'NONE', *, *, #18658, .F. ) ;
#39551=EDGE_CURVE ( 'NONE', #10089, #1932, #31753, .T. ) ;
#39553=AXIS2_PLACEMENT_3D ( 'NONE', #39484, #32739, #37084 ) ;
#39556=CIRCLE ( 'NONE', #37488, 59.00000000000000000 ) ;
#39561=AXIS2_PLACEMENT_3D ( 'NONE', #25594, #8975, #22322 ) ;
#39563=CARTESIAN_POINT ( 'NONE',  ( 0.000000000000000000, -35.54274411427983438, -115.1399337407609949 ) ) ;
#39564=DIRECTION ( 'NONE',  ( 1.000000000000000000, 0.000000000000000000, -0.000000000000000000 ) ) ;
#39565=ORIENTED_EDGE ( 'NONE', *, *, #30862, .T. ) ;
#39566=DIRECTION ( 'NONE',  ( 0.000000000000000000, 0.000000000000000000, 1.000000000000000000 ) ) ;
#39568=ORIENTED_EDGE ( 'NONE', *, *, #6677, .F. ) ;
#39572=DIRECTION ( 'NONE',  ( -1.000000000000000000, -0.000000000000000000, -0.000000000000000000 ) ) ;
#39573=DIRECTION ( 'NONE',  ( 1.000000000000000000, 0.000000000000000000, 0.000000000000000000 ) ) ;
#39579=EDGE_CURVE ( 'NONE', #14947, #7950, #41888, .T. ) ;
#39580=CARTESIAN_POINT ( 'NONE',  ( 17.99999999999999645, 40.13512380274120517, -113.6206972269517905 ) ) ;
#39581=CIRCLE ( 'NONE', #37510, 120.5010000000000190 ) ;
#39585=ADVANCED_FACE ( 'NONE', ( #24811 ), #41975, .F. ) ;
#39586=CARTESIAN_POINT ( 'NONE',  ( 17.99999999999999645, 48.55277268144470781, -105.3500273609075180 ) ) ;
#39587=CIRCLE ( 'NONE', #23601, 59.00000000000001421 ) ;
#39590=CARTESIAN_POINT ( 'NONE',  ( -10.00000000000000000, 0.000000000000000000, 0.000000000000000000 ) ) ;
#39592=DIRECTION ( 'NONE',  ( -1.000000000000000000, -0.000000000000000000, -0.000000000000000000 ) ) ;
#39593=LINE ( 'NONE', #39370, #22790 ) ;
#39594=LINE ( 'NONE', #23708, #17102 ) ;
#39599=FACE_OUTER_BOUND ( 'NONE', #31084, .T. ) ;
#39600=ORIENTED_EDGE ( 'NONE', *, *, #18035, .T. ) ;
#39606=ADVANCED_FACE ( 'NONE', ( #5974 ), #12981, .F. ) ;
#39609=EDGE_LOOP ( 'NONE', ( #36373, #17567, #23754, #14771 ) ) ;
#39614=CIRCLE ( 'NONE', #8305, 58.99999999999999289 ) ;
#39615=DIRECTION ( 'NONE',  ( 1.000000000000000000, 0.000000000000000000, 0.000000000000000000 ) ) ;
#39617=ORIENTED_EDGE ( 'NONE', *, *, #5473, .T. ) ;
#39618=VECTOR ( 'NONE', #5100, 1000.000000000000000 ) ;
#39619=FACE_OUTER_BOUND ( 'NONE', #7026, .T. ) ;
#39630=DIRECTION ( 'NONE',  ( 0.000000000000000000, -0.5528000653611835347, -0.8333139190825215037 ) ) ;
#39635=ORIENTED_EDGE ( 'NONE', *, *, #28549, .T. ) ;
#39636=DIRECTION ( 'NONE',  ( 0.000000000000000000, 0.000000000000000000, 1.000000000000000000 ) ) ;
#39637=DIRECTION ( 'NONE',  ( 0.000000000000000000, 0.000000000000000000, 1.000000000000000000 ) ) ;
#39638=DIRECTION ( 'NONE',  ( -1.000000000000000000, 0.000000000000000000, -0.000000000000000000 ) ) ;
#39640=CIRCLE ( 'NONE', #34808, 59.00000000000000000 ) ;
#39641=DIRECTION ( 'NONE',  ( 1.000000000000000000, -0.000000000000000000, -0.000000000000000000 ) ) ;
#39650=EDGE_CURVE ( 'NONE', #25132, #1568, #29343, .T. ) ;
#39654=EDGE_CURVE ( 'NONE', #36637, #18411, #3527, .T. ) ;
#39655=EDGE_CURVE ( 'NONE', #19094, #41276, #29364, .T. ) ;
#39658=ORIENTED_EDGE ( 'NONE', *, *, #6347, .F. ) ;
#39661=DIRECTION ( 'NONE',  ( 1.000000000000000000, 0.000000000000000000, 0.000000000000000000 ) ) ;
#39663=DIRECTION ( 'NONE',  ( -1.000000000000000000, 0.000000000000000000, 0.000000000000000000 ) ) ;
#39664=EDGE_CURVE ( 'NONE', #32792, #22071, #19632, .T. ) ;
#39667=CYLINDRICAL_SURFACE ( 'NONE', #14029, 59.00000000000000000 ) ;
#39669=CIRCLE ( 'NONE', #40382, 59.00000000000000000 ) ;
#39670=FACE_OUTER_BOUND ( 'NONE', #19936, .T. ) ;
#39675=DIRECTION ( 'NONE',  ( 0.000000000000000000, -0.2631025642275088838, -0.9647678688145193693 ) ) ;
#39681=CARTESIAN_POINT ( 'NONE',  ( 17.99999999999999645, 0.000000000000000000, 0.000000000000000000 ) ) ;
#39682=DIRECTION ( 'NONE',  ( -1.000000000000000000, 0.000000000000000000, 0.000000000000000000 ) ) ;
#39683=DIRECTION ( 'NONE',  ( -1.000000000000000000, -0.000000000000000000, -0.000000000000000000 ) ) ;
#39684=ORIENTED_EDGE ( 'NONE', *, *, #14881, .F. ) ;
#39686=CARTESIAN_POINT ( 'NONE',  ( 9.000000000000001776, -115.6826031496111398, -8.575274253898639287 ) ) ;
#39689=ORIENTED_EDGE ( 'NONE', *, *, #42791, .T. ) ;
#39691=CARTESIAN_POINT ( 'NONE',  ( 0.000000000000000000, -46.83041522348565167, 101.9567785075599744 ) ) ;
#39695=VECTOR ( 'NONE', #36636, 1000.000000000000000 ) ;
#39696=ORIENTED_EDGE ( 'NONE', *, *, #28772, .F. ) ;
#39697=CARTESIAN_POINT ( 'NONE',  ( 17.99999999999999645, 0.000000000000000000, 0.000000000000000000 ) ) ;
#39698=ORIENTED_EDGE ( 'NONE', *, *, #24716, .F. ) ;
#39700=EDGE_LOOP ( 'NONE', ( #42512, #8050, #6422, #18647 ) ) ;
#39703=VERTEX_POINT ( 'NONE', #39764 ) ;
#39706=CARTESIAN_POINT ( 'NONE',  ( 17.99999999999999645, -94.83915810436360516, -59.94836581341685644 ) ) ;
#39707=ORIENTED_EDGE ( 'NONE', *, *, #24388, .T. ) ;
#39712=CIRCLE ( 'NONE', #28620, 58.99999999999998579 ) ;
#39715=CIRCLE ( 'NONE', #27944, 116.0000000000000000 ) ;
#39720=AXIS2_PLACEMENT_3D ( 'NONE', #6242, #12594, #33296 ) ;
#39721=VERTEX_POINT ( 'NONE', #40411 ) ;
#39722=DIRECTION ( 'NONE',  ( -1.000000000000000000, -0.000000000000000000, -0.000000000000000000 ) ) ;
#39723=AXIS2_PLACEMENT_3D ( 'NONE', #23720, #36982, #40461 ) ;
#39725=CARTESIAN_POINT ( 'NONE',  ( 0.000000000000000000, 111.8797445107944810, -8.437727291343108504 ) ) ;
#39727=AXIS2_PLACEMENT_3D ( 'NONE', #625, #10686, #30123 ) ;
#39732=VERTEX_POINT ( 'NONE', #6611 ) ;
#39735=DIRECTION ( 'NONE',  ( 1.000000000000000000, 0.000000000000000000, 0.000000000000000000 ) ) ;
#39736=FACE_OUTER_BOUND ( 'NONE', #36795, .T. ) ;
#39742=VECTOR ( 'NONE', #20966, 1000.000000000000000 ) ;
#39743=ORIENTED_EDGE ( 'NONE', *, *, #17284, .T. ) ;
#39746=CARTESIAN_POINT ( 'NONE',  ( 0.000000000000000000, -64.58410930313591791, 101.7319213743680422 ) ) ;
#39749=EDGE_LOOP ( 'NONE', ( #1755, #31797, #5781, #24921 ) ) ;
#39754=CARTESIAN_POINT ( 'NONE',  ( 0.000000000000000000, 0.000000000000000000, 0.000000000000000000 ) ) ;
#39758=ORIENTED_EDGE ( 'NONE', *, *, #12258, .T. ) ;
#39759=LINE ( 'NONE', #26487, #9810 ) ;
#39761=AXIS2_PLACEMENT_3D ( 'NONE', #8646, #28327, #41594 ) ;
#39762=VERTEX_POINT ( 'NONE', #20400 ) ;
#39763=EDGE_CURVE ( 'NONE', #35448, #28827, #31479, .T. ) ;
#39764=CARTESIAN_POINT ( 'NONE',  ( 17.99999999999999645, 75.03166794516801019, 94.29071961951534320 ) ) ;
#39770=CARTESIAN_POINT ( 'NONE',  ( 17.99999999999999645, 68.61497464550593861, 99.05794392877625398 ) ) ;
#39772=DIRECTION ( 'NONE',  ( -1.000000000000000000, -0.000000000000000000, 0.000000000000000000 ) ) ;
#39774=CARTESIAN_POINT ( 'NONE',  ( 0.000000000000000000, 0.000000000000000000, 0.000000000000000000 ) ) ;
#39775=ORIENTED_EDGE ( 'NONE', *, *, #21333, .F. ) ;
#39779=DIRECTION ( 'NONE',  ( -1.000000000000000000, -0.000000000000000000, 0.000000000000000000 ) ) ;
#39784=CIRCLE ( 'NONE', #9161, 116.0000000000000000 ) ;
#39786=ORIENTED_EDGE ( 'NONE', *, *, #28964, .F. ) ;
#39787=DIRECTION ( 'NONE',  ( 0.000000000000000000, -0.8183027759081743513, 0.5747874102143992747 ) ) ;
#39789=CARTESIAN_POINT ( 'NONE',  ( 0.000000000000000000, 91.65951123222582453, -71.09524597797991419 ) ) ;
#39791=CIRCLE ( 'NONE', #21062, 120.5010000000000332 ) ;
#39792=CARTESIAN_POINT ( 'NONE',  ( 17.99999999999999645, 0.000000000000000000, 0.000000000000000000 ) ) ;
#39794=ORIENTED_EDGE ( 'NONE', *, *, #43104, .T. ) ;
#39796=ORIENTED_EDGE ( 'NONE', *, *, #35311, .F. ) ;
#39799=CARTESIAN_POINT ( 'NONE',  ( 17.99999999999999645, 46.12538073176499154, -111.3235835452206857 ) ) ;
#39800=CARTESIAN_POINT ( 'NONE',  ( 17.99999999999999645, 0.000000000000000000, 0.000000000000000000 ) ) ;
#39802=DIRECTION ( 'NONE',  ( -1.000000000000000000, -0.000000000000000000, -0.000000000000000000 ) ) ;
#39806=LINE ( 'NONE', #34142, #17404 ) ;
#39809=FACE_OUTER_BOUND ( 'NONE', #32361, .T. ) ;
#39810=EDGE_CURVE ( 'NONE', #21330, #31605, #42591, .T. ) ;
#39820=LINE ( 'NONE', #2528, #14516 ) ;
#39821=AXIS2_PLACEMENT_3D ( 'NONE', #30774, #37299, #3900 ) ;
#39824=VERTEX_POINT ( 'NONE', #27573 ) ;
#39825=LINE ( 'NONE', #7315, #27239 ) ;
#39828=DIRECTION ( 'NONE',  ( 0.000000000000000000, 0.9407002666710320149, 0.3392388661180340548 ) ) ;
#39832=ORIENTED_EDGE ( 'NONE', *, *, #29118, .T. ) ;
#39839=ADVANCED_FACE ( 'NONE', ( #36490 ), #29988, .F. ) ;
#39840=DIRECTION ( 'NONE',  ( 1.000000000000000000, 0.000000000000000000, 0.000000000000000000 ) ) ;
#39841=ORIENTED_EDGE ( 'NONE', *, *, #28423, .F. ) ;
#39845=VERTEX_POINT ( 'NONE', #10102 ) ;
#39846=ORIENTED_EDGE ( 'NONE', *, *, #14553, .T. ) ;
#39849=DIRECTION ( 'NONE',  ( -1.000000000000000000, -0.000000000000000000, -0.000000000000000000 ) ) ;
#39853=CARTESIAN_POINT ( 'NONE',  ( 17.99999999999999645, 119.0898412705474385, 18.38751498043773935 ) ) ;
#39861=LINE ( 'NONE', #10207, #30416 ) ;
#39862=CARTESIAN_POINT ( 'NONE',  ( 8.999999999999998224, 74.56001736500617483, 88.86396238369059120 ) ) ;
#39866=CARTESIAN_POINT ( 'NONE',  ( 17.99999999999999645, -18.35539002514308038, -110.6858262410711831 ) ) ;
#39867=ORIENTED_EDGE ( 'NONE', *, *, #13119, .T. ) ;
#39870=CARTESIAN_POINT ( 'NONE',  ( 17.99999999999999645, 0.000000000000000000, 0.000000000000000000 ) ) ;
#39871=ADVANCED_FACE ( 'NONE', ( #21500 ), #41723, .F. ) ;
#39872=DIRECTION ( 'NONE',  ( 0.000000000000000000, 0.8477344278896721264, -0.5304209081197405196 ) ) ;
#39877=AXIS2_PLACEMENT_3D ( 'NONE', #41175, #1476, #11115 ) ;
#39878=DIRECTION ( 'NONE',  ( 0.000000000000000000, 1.234887898152981424E-13, -1.000000000000000000 ) ) ;
#39879=DIRECTION ( 'NONE',  ( -1.000000000000000000, -0.000000000000000000, -0.000000000000000000 ) ) ;
#39881=DIRECTION ( 'NONE',  ( -1.000000000000000000, -0.000000000000000000, 0.000000000000000000 ) ) ;
#39892=EDGE_CURVE ( 'NONE', #14569, #36642, #14494, .T. ) ;
#39897=EDGE_LOOP ( 'NONE', ( #11704, #33884, #41635, #19317 ) ) ;
#39898=DIRECTION ( 'NONE',  ( 1.000000000000000000, 0.000000000000000000, 0.000000000000000000 ) ) ;
#39899=CARTESIAN_POINT ( 'NONE',  ( 9.000000000000001776, -0.6819280456820884240, -115.9979955608738607 ) ) ;
#39900=CIRCLE ( 'NONE', #12786, 120.5010000000000332 ) ;
#39903=CARTESIAN_POINT ( 'NONE',  ( -10.00000000000000000, 0.000000000000000000, 0.000000000000000000 ) ) ;
#39917=DIRECTION ( 'NONE',  ( -1.000000000000000000, 0.000000000000000000, 0.000000000000000000 ) ) ;
#39918=EDGE_CURVE ( 'NONE', #10403, #10198, #8478, .T. ) ;
#39920=CARTESIAN_POINT ( 'NONE',  ( 0.000000000000000000, 0.000000000000000000, 0.000000000000000000 ) ) ;
#39921=ORIENTED_EDGE ( 'NONE', *, *, #30036, .T. ) ;
#39922=DIRECTION ( 'NONE',  ( 1.000000000000000000, 0.000000000000000000, 0.000000000000000000 ) ) ;
#39925=DIRECTION ( 'NONE',  ( 1.000000000000000000, 0.000000000000000000, 0.000000000000000000 ) ) ;
#39928=ORIENTED_EDGE ( 'NONE', *, *, #38677, .T. ) ;
#39933=DIRECTION ( 'NONE',  ( -1.000000000000000000, -0.000000000000000000, 0.000000000000000000 ) ) ;
#39935=VERTEX_POINT ( 'NONE', #34313 ) ;
#39946=CARTESIAN_POINT ( 'NONE',  ( 0.000000000000000000, -88.56657216608662964, 68.87840567545892156 ) ) ;
#39947=CYLINDRICAL_SURFACE ( 'NONE', #31508, 130.0000000000000000 ) ;
#39952=FACE_OUTER_BOUND ( 'NONE', #26292, .T. ) ;
#39955=ORIENTED_EDGE ( 'NONE', *, *, #38434, .F. ) ;
#39958=FACE_OUTER_BOUND ( 'NONE', #1380, .T. ) ;
#39959=ORIENTED_EDGE ( 'NONE', *, *, #25501, .T. ) ;
#39964=ORIENTED_EDGE ( 'NONE', *, *, #24254, .F. ) ;
#39965=DIRECTION ( 'NONE',  ( -1.000000000000000000, -0.000000000000000000, -0.000000000000000000 ) ) ;
#39966=ORIENTED_EDGE ( 'NONE', *, *, #16912, .T. ) ;
#39969=CARTESIAN_POINT ( 'NONE',  ( 17.99999999999999645, 0.000000000000000000, 0.000000000000000000 ) ) ;
#39972=DIRECTION ( 'NONE',  ( 0.000000000000000000, 0.000000000000000000, 1.000000000000000000 ) ) ;
#39973=AXIS2_PLACEMENT_3D ( 'NONE', #33416, #36897, #16878 ) ;
#39974=VERTEX_POINT ( 'NONE', #8348 ) ;
#39977=CARTESIAN_POINT ( 'NONE',  ( 17.99999999999999645, 107.1354928292869744, 44.47455650398100602 ) ) ;
#39981=AXIS2_PLACEMENT_3D ( 'NONE', #2988, #12650, #9784 ) ;
#39985=DIRECTION ( 'NONE',  ( 0.000000000000000000, 0.000000000000000000, 1.000000000000000000 ) ) ;
#39989=ORIENTED_EDGE ( 'NONE', *, *, #34228, .T. ) ;
#39990=AXIS2_PLACEMENT_3D ( 'NONE', #39411, #38987, #9112 ) ;
#39991=EDGE_CURVE ( 'NONE', #40772, #40246, #798, .T. ) ;
#39993=VECTOR ( 'NONE', #23548, 1000.000000000000000 ) ;
#39995=CARTESIAN_POINT ( 'NONE',  ( 0.000000000000000000, 86.84764344322962870, 76.89919913989776035 ) ) ;
#40000=EDGE_CURVE ( 'NONE', #7485, #3574, #39784, .T. ) ;
#40001=CIRCLE ( 'NONE', #17807, 59.00000000000000711 ) ;
#40003=DIRECTION ( 'NONE',  ( 1.000000000000000000, 0.000000000000000000, 0.000000000000000000 ) ) ;
#40004=VERTEX_POINT ( 'NONE', #1143 ) ;
#40007=DIRECTION ( 'NONE',  ( 1.000000000000000000, 0.000000000000000000, 0.000000000000000000 ) ) ;
#40011=DIRECTION ( 'NONE',  ( -1.000000000000000000, -0.000000000000000000, -0.000000000000000000 ) ) ;
#40014=FACE_OUTER_BOUND ( 'NONE', #41264, .T. ) ;
#40015=CIRCLE ( 'NONE', #298, 59.00000000000000000 ) ;
#40016=DIRECTION ( 'NONE',  ( 1.000000000000000000, 0.000000000000000000, 0.000000000000000000 ) ) ;
#40019=DIRECTION ( 'NONE',  ( -1.000000000000000000, -0.000000000000000000, 0.000000000000000000 ) ) ;
#40020=VECTOR ( 'NONE', #6420, 1000.000000000000000 ) ;
#40021=DIRECTION ( 'NONE',  ( -1.000000000000000000, -0.000000000000000000, -0.000000000000000000 ) ) ;
#40022=ORIENTED_EDGE ( 'NONE', *, *, #31071, .T. ) ;
#40024=ORIENTED_EDGE ( 'NONE', *, *, #10352, .T. ) ;
#40025=FACE_OUTER_BOUND ( 'NONE', #4868, .T. ) ;
#40032=VERTEX_POINT ( 'NONE', #38649 ) ;
#40033=DIRECTION ( 'NONE',  ( -1.000000000000000000, -0.000000000000000000, -0.000000000000000000 ) ) ;
#40035=DIRECTION ( 'NONE',  ( -1.000000000000000000, -0.000000000000000000, -0.000000000000000000 ) ) ;
#40036=CYLINDRICAL_SURFACE ( 'NONE', #8746, 59.00000000000000000 ) ;
#40039=ORIENTED_EDGE ( 'NONE', *, *, #35482, .F. ) ;
#40042=DIRECTION ( 'NONE',  ( 0.000000000000000000, -0.4132121857683668797, -0.9106347728549183396 ) ) ;
#40046=ORIENTED_EDGE ( 'NONE', *, *, #5217, .F. ) ;
#40058=CYLINDRICAL_SURFACE ( 'NONE', #20709, 116.0000000000000000 ) ;
#40059=EDGE_LOOP ( 'NONE', ( #27898, #13522, #11253, #30800 ) ) ;
#40060=ADVANCED_FACE ( 'NONE', ( #3042 ), #26011, .F. ) ;
#40061=CARTESIAN_POINT ( 'NONE',  ( 17.99999999999999645, 40.37724737310206535, -104.6802291180863023 ) ) ;
#40063=LINE ( 'NONE', #6711, #1437 ) ;
#40068=ORIENTED_EDGE ( 'NONE', *, *, #14612, .F. ) ;
#40072=ORIENTED_EDGE ( 'NONE', *, *, #7526, .F. ) ;
#40073=AXIS2_PLACEMENT_3D ( 'NONE', #41219, #14658, #863 ) ;
#40074=AXIS2_PLACEMENT_3D ( 'NONE', #28199, #21473, #38622 ) ;
#40081=CARTESIAN_POINT ( 'NONE',  ( 17.99999999999999645, 0.000000000000000000, 0.000000000000000000 ) ) ;
#40082=AXIS2_PLACEMENT_3D ( 'NONE', #27205, #27413, #40686 ) ;
#40086=VECTOR ( 'NONE', #10054, 1000.000000000000000 ) ;
#40088=ORIENTED_EDGE ( 'NONE', *, *, #25283, .F. ) ;
#40089=CARTESIAN_POINT ( 'NONE',  ( 0.000000000000000000, 82.63181128086733906, 81.41243003647002752 ) ) ;
#40090=DIRECTION ( 'NONE',  ( 0.000000000000000000, -0.9714298932647122964, 0.2373266998711055509 ) ) ;
#40091=CIRCLE ( 'NONE', #38706, 116.0000000000000000 ) ;
#40092=VERTEX_POINT ( 'NONE', #25817 ) ;
#40093=DIRECTION ( 'NONE',  ( 0.000000000000000000, 0.9574220383620062336, -0.2886919473396183933 ) ) ;
#40096=DIRECTION ( 'NONE',  ( 0.000000000000000000, 0.5076658003388351270, 0.8615540813938089570 ) ) ;
#40097=DIRECTION ( 'NONE',  ( -1.000000000000000000, -0.000000000000000000, -0.000000000000000000 ) ) ;
#40099=EDGE_CURVE ( 'NONE', #22186, #38131, #7760, .T. ) ;
#40110=AXIS2_PLACEMENT_3D ( 'NONE', #2266, #28077, #8842 ) ;
#40116=ADVANCED_FACE ( 'NONE', ( #38868 ), #9199, .F. ) ;
#40117=CARTESIAN_POINT ( 'NONE',  ( 17.99999999999999645, 97.89532456239568603, -54.81585448086097045 ) ) ;
#40119=CIRCLE ( 'NONE', #28353, 59.00000000000000000 ) ;
#40120=VERTEX_POINT ( 'NONE', #39274 ) ;
#40122=CYLINDRICAL_SURFACE ( 'NONE', #13848, 120.5010000000000190 ) ;
#40125=DIRECTION ( 'NONE',  ( 0.000000000000000000, 0.000000000000000000, 1.000000000000000000 ) ) ;
#40126=CARTESIAN_POINT ( 'NONE',  ( 17.99999999999999645, 106.5605152861902951, 56.26142179985861702 ) ) ;
#40129=VERTEX_POINT ( 'NONE', #9405 ) ;
#40132=ADVANCED_FACE ( 'NONE', ( #6142 ), #35788, .F. ) ;
#40134=ORIENTED_EDGE ( 'NONE', *, *, #1542, .F. ) ;
#40135=CARTESIAN_POINT ( 'NONE',  ( 0.000000000000000000, 0.000000000000000000, 0.000000000000000000 ) ) ;
#40137=AXIS2_PLACEMENT_3D ( 'NONE', #26375, #22479, #32257 ) ;
#40140=DIRECTION ( 'NONE',  ( 0.000000000000000000, 0.000000000000000000, 1.000000000000000000 ) ) ;
#40144=ORIENTED_EDGE ( 'NONE', *, *, #2072, .T. ) ;
#40145=AXIS2_PLACEMENT_3D ( 'NONE', #37817, #37392, #7509 ) ;
#40150=CIRCLE ( 'NONE', #42954, 120.5010000000000048 ) ;
#40151=DIRECTION ( 'NONE',  ( -1.000000000000000000, 0.000000000000000000, 0.000000000000000000 ) ) ;
#40152=ORIENTED_EDGE ( 'NONE', *, *, #17446, .F. ) ;
#40153=VECTOR ( 'NONE', #25138, 1000.000000000000000 ) ;
#40158=CARTESIAN_POINT ( 'NONE',  ( 17.99999999999999645, -29.02167576844032482, -108.3790330702172611 ) ) ;
#40159=ORIENTED_EDGE ( 'NONE', *, *, #34960, .F. ) ;
#40163=ADVANCED_FACE ( 'NONE', ( #19916 ), #10280, .F. ) ;
#40164=ORIENTED_EDGE ( 'NONE', *, *, #23368, .T. ) ;
#40165=DIRECTION ( 'NONE',  ( -1.000000000000000000, 0.000000000000000000, -0.000000000000000000 ) ) ;
#40166=DIRECTION ( 'NONE',  ( 1.000000000000000000, 0.000000000000000000, 0.000000000000000000 ) ) ;
#40169=CARTESIAN_POINT ( 'NONE',  ( 17.99999999999999645, 57.69704296431325474, -105.7900857083224224 ) ) ;
#40173=ORIENTED_EDGE ( 'NONE', *, *, #36402, .F. ) ;
#40176=AXIS2_PLACEMENT_3D ( 'NONE', #31251, #41465, #28421 ) ;
#40179=CIRCLE ( 'NONE', #29796, 116.0000000000000000 ) ;
#40182=VERTEX_POINT ( 'NONE', #203 ) ;
#40183=FACE_OUTER_BOUND ( 'NONE', #19315, .T. ) ;
#40186=CARTESIAN_POINT ( 'NONE',  ( 17.99999999999999645, 21.55123232222474172, 118.5581519187672654 ) ) ;
#40187=AXIS2_PLACEMENT_3D ( 'NONE', #24074, #22988, #23194 ) ;
#40188=ORIENTED_EDGE ( 'NONE', *, *, #9409, .F. ) ;
#40190=VERTEX_POINT ( 'NONE', #14005 ) ;
#40193=VERTEX_POINT ( 'NONE', #16652 ) ;
#40194=CYLINDRICAL_SURFACE ( 'NONE', #2144, 59.00000000000000000 ) ;
#40195=EDGE_CURVE ( 'NONE', #35175, #21953, #37744, .T. ) ;
#40197=EDGE_CURVE ( 'NONE', #32209, #41913, #34981, .T. ) ;
#40206=DIRECTION ( 'NONE',  ( 1.000000000000000000, 0.000000000000000000, 0.000000000000000000 ) ) ;
#40208=ORIENTED_EDGE ( 'NONE', *, *, #30862, .F. ) ;
#40211=ORIENTED_EDGE ( 'NONE', *, *, #13301, .F. ) ;
#40214=AXIS2_PLACEMENT_3D ( 'NONE', #42216, #35254, #5149 ) ;
#40221=VERTEX_POINT ( 'NONE', #30357 ) ;
#40222=DIRECTION ( 'NONE',  ( 0.000000000000000000, 0.1590634960190655256, 0.9872683547213456645 ) ) ;
#40227=ADVANCED_FACE ( 'NONE', ( #6556 ), #23399, .F. ) ;
#40228=EDGE_CURVE ( 'NONE', #15115, #42828, #28035, .T. ) ;
#40229=ORIENTED_EDGE ( 'NONE', *, *, #10027, .T. ) ;
#40234=DIRECTION ( 'NONE',  ( 0.000000000000000000, 0.000000000000000000, 1.000000000000000000 ) ) ;
#40236=ORIENTED_EDGE ( 'NONE', *, *, #24361, .F. ) ;
#40237=EDGE_LOOP ( 'NONE', ( #32144, #32007, #34457, #13581 ) ) ;
#40238=DIRECTION ( 'NONE',  ( 0.000000000000000000, -0.9911528310040085277, 0.1327255272837126188 ) ) ;
#40241=AXIS2_PLACEMENT_3D ( 'NONE', #20549, #37730, #27736 ) ;
#40243=AXIS2_PLACEMENT_3D ( 'NONE', #28868, #35173, #5300 ) ;
#40246=VERTEX_POINT ( 'NONE', #13361 ) ;
#40248=CARTESIAN_POINT ( 'NONE',  ( 17.99999999999999645, -103.4151313792866489, -61.85306461934516875 ) ) ;
#40251=CARTESIAN_POINT ( 'NONE',  ( 17.99999999999999645, 61.59243992711585491, -93.77976230225978327 ) ) ;
#40254=ORIENTED_EDGE ( 'NONE', *, *, #33726, .F. ) ;
#40260=ORIENTED_EDGE ( 'NONE', *, *, #41983, .F. ) ;
#40262=EDGE_CURVE ( 'NONE', #848, #1445, #7793, .T. ) ;
#40263=VERTEX_POINT ( 'NONE', #37316 ) ;
#40264=CARTESIAN_POINT ( 'NONE',  ( 17.99999999999999645, 0.000000000000000000, 0.000000000000000000 ) ) ;
#40265=CARTESIAN_POINT ( 'NONE',  ( 0.000000000000000000, -101.1403355683142422, -56.80345518653591341 ) ) ;
#40266=EDGE_CURVE ( 'NONE', #41379, #30344, #30151, .T. ) ;
#40269=DIRECTION ( 'NONE',  ( 0.000000000000000000, 0.000000000000000000, 1.000000000000000000 ) ) ;
#40278=CARTESIAN_POINT ( 'NONE',  ( 0.000000000000000000, 0.000000000000000000, 0.000000000000000000 ) ) ;
#40282=DIRECTION ( 'NONE',  ( -1.000000000000000000, 0.000000000000000000, 0.000000000000000000 ) ) ;
#40283=EDGE_LOOP ( 'NONE', ( #14599, #8492, #15109, #29833 ) ) ;
#40290=DIRECTION ( 'NONE',  ( 0.000000000000000000, 0.000000000000000000, 1.000000000000000000 ) ) ;
#40294=CARTESIAN_POINT ( 'NONE',  ( 17.99999999999999645, -52.19040376560500505, 99.31985817764160629 ) ) ;
#40297=CIRCLE ( 'NONE', #43071, 116.0000000000000000 ) ;
#40300=ADVANCED_FACE ( 'NONE', ( #20795 ), #34052, .F. ) ;
#40301=VERTEX_POINT ( 'NONE', #26441 ) ;
#40306=CARTESIAN_POINT ( 'NONE',  ( 0.000000000000000000, 18.35539002514383711, 110.6858262410710410 ) ) ;
#40307=ORIENTED_EDGE ( 'NONE', *, *, #24164, .T. ) ;
#40312=DIRECTION ( 'NONE',  ( 1.000000000000000000, 0.000000000000000000, 0.000000000000000000 ) ) ;
#40313=VERTEX_POINT ( 'NONE', #24490 ) ;
#40315=DIRECTION ( 'NONE',  ( 0.000000000000000000, 0.2631025642275217069, -0.9647678688145158166 ) ) ;
#40316=ADVANCED_FACE ( 'NONE', ( #1739 ), #8509, .F. ) ;
#40317=ORIENTED_EDGE ( 'NONE', *, *, #14801, .F. ) ;
#40321=ORIENTED_EDGE ( 'NONE', *, *, #14758, .T. ) ;
#40325=CARTESIAN_POINT ( 'NONE',  ( 17.99999999999999645, -72.00556975657644898, -86.04342158279462183 ) ) ;
#40328=ORIENTED_EDGE ( 'NONE', *, *, #34593, .F. ) ;
#40332=AXIS2_PLACEMENT_3D ( 'NONE', #39054, #22320, #5691 ) ;
#40333=ADVANCED_FACE ( 'NONE', ( #37743 ), #4812, .F. ) ;
#40334=CARTESIAN_POINT ( 'NONE',  ( 0.000000000000000000, -73.51007459736368332, -89.73443560133438268 ) ) ;
#40337=ORIENTED_EDGE ( 'NONE', *, *, #28452, .F. ) ;
#40338=DIRECTION ( 'NONE',  ( 0.000000000000000000, -0.7164567402983210709, 0.6976315211349786161 ) ) ;
#40339=DIRECTION ( 'NONE',  ( 0.000000000000000000, 0.000000000000000000, 1.000000000000000000 ) ) ;
#40340=VERTEX_POINT ( 'NONE', #24700 ) ;
#40346=CYLINDRICAL_SURFACE ( 'NONE', #21571, 59.00000000000000000 ) ;
#40351=DIRECTION ( 'NONE',  ( -1.000000000000000000, -0.000000000000000000, 0.000000000000000000 ) ) ;
#40352=AXIS2_PLACEMENT_3D ( 'NONE', #18971, #35063, #32228 ) ;
#40353=ORIENTED_EDGE ( 'NONE', *, *, #1113, .F. ) ;
#40357=DIRECTION ( 'NONE',  ( -1.000000000000000000, -0.000000000000000000, -0.000000000000000000 ) ) ;
#40358=CIRCLE ( 'NONE', #22296, 116.0000000000000000 ) ;
#40359=CIRCLE ( 'NONE', #20901, 116.0000000000000000 ) ;
#40361=CARTESIAN_POINT ( 'NONE',  ( 17.99999999999999645, 111.7974656912330005, 9.465682155095883843 ) ) ;
#40364=DIRECTION ( 'NONE',  ( -1.000000000000000000, -0.000000000000000000, -0.000000000000000000 ) ) ;
#40370=DIRECTION ( 'NONE',  ( -1.000000000000000000, 0.000000000000000000, 0.000000000000000000 ) ) ;
#40382=AXIS2_PLACEMENT_3D ( 'NONE', #32438, #25094, #38972 ) ;
#40384=LINE ( 'NONE', #10520, #22835 ) ;
#40392=ORIENTED_EDGE ( 'NONE', *, *, #26401, .F. ) ;
#40395=ORIENTED_EDGE ( 'NONE', *, *, #32026, .T. ) ;
#40398=EDGE_LOOP ( 'NONE', ( #9309, #13664, #18092, #17204 ) ) ;
#40402=ADVANCED_FACE ( 'NONE', ( #34260 ), #8301, .F. ) ;
#40405=DIRECTION ( 'NONE',  ( 1.000000000000000000, 0.000000000000000000, 0.000000000000000000 ) ) ;
#40406=ORIENTED_EDGE ( 'NONE', *, *, #4703, .T. ) ;
#40410=ORIENTED_EDGE ( 'NONE', *, *, #38798, .F. ) ;
#40411=CARTESIAN_POINT ( 'NONE',  ( 17.99999999999999645, 25.18647942089895153, -113.2326863338525271 ) ) ;
#40412=ADVANCED_FACE ( 'NONE', ( #40790 ), #34913, .F. ) ;
#40413=ORIENTED_EDGE ( 'NONE', *, *, #11040, .T. ) ;
#40415=AXIS2_PLACEMENT_3D ( 'NONE', #17698, #20767, #34026 ) ;
#40418=AXIS2_PLACEMENT_3D ( 'NONE', #2578, #2351, #41874 ) ;
#40419=LINE ( 'NONE', #24336, #32842 ) ;
#40420=DIRECTION ( 'NONE',  ( 1.000000000000000000, 0.000000000000000000, 0.000000000000000000 ) ) ;
#40421=VECTOR ( 'NONE', #24909, 1000.000000000000000 ) ;
#40422=DIRECTION ( 'NONE',  ( 1.000000000000000000, 0.000000000000000000, -0.000000000000000000 ) ) ;
#40423=ORIENTED_EDGE ( 'NONE', *, *, #6733, .T. ) ;
#40424=DIRECTION ( 'NONE',  ( -1.000000000000000000, -0.000000000000000000, -0.000000000000000000 ) ) ;
#40426=DIRECTION ( 'NONE',  ( 0.000000000000000000, 0.4610925014493206242, 0.8873520750565743187 ) ) ;
#40427=LINE ( 'NONE', #37595, #34449 ) ;
#40431=DIRECTION ( 'NONE',  ( 1.000000000000000000, 0.000000000000000000, 0.000000000000000000 ) ) ;
#40434=ORIENTED_EDGE ( 'NONE', *, *, #27130, .T. ) ;
#40435=DIRECTION ( 'NONE',  ( -1.000000000000000000, 0.000000000000000000, 0.000000000000000000 ) ) ;
#40437=EDGE_CURVE ( 'NONE', #36312, #40855, #23181, .T. ) ;
#40439=ADVANCED_FACE ( 'NONE', ( #32078 ), #32707, .F. ) ;
#40440=CARTESIAN_POINT ( 'NONE',  ( 17.99999999999999645, -105.7179949885865256, -37.57629584241794163 ) ) ;
#40444=ORIENTED_EDGE ( 'NONE', *, *, #31388, .F. ) ;
#40450=CIRCLE ( 'NONE', #2810, 59.00000000000000000 ) ;
#40452=ORIENTED_EDGE ( 'NONE', *, *, #9139, .T. ) ;
#40454=CYLINDRICAL_SURFACE ( 'NONE', #10545, 116.0000000000000000 ) ;
#40455=CARTESIAN_POINT ( 'NONE',  ( 17.99999999999999645, 107.2703412112694963, 32.88383143828500721 ) ) ;
#40461=DIRECTION ( 'NONE',  ( 0.000000000000000000, 0.000000000000000000, 1.000000000000000000 ) ) ;
#40462=CARTESIAN_POINT ( 'NONE',  ( 17.99999999999999645, -111.2721026680461733, 14.38025178762581469 ) ) ;
#40463=EDGE_LOOP ( 'NONE', ( #18673, #163, #33004, #12796 ) ) ;
#40469=CARTESIAN_POINT ( 'NONE',  ( 0.000000000000000000, -46.12538073176274622, -111.3235835452215952 ) ) ;
#40470=ORIENTED_EDGE ( 'NONE', *, *, #829, .F. ) ;
#40471=DIRECTION ( 'NONE',  ( 0.000000000000000000, 0.000000000000000000, 1.000000000000000000 ) ) ;
#40472=ORIENTED_EDGE ( 'NONE', *, *, #21375, .F. ) ;
#40473=AXIS2_PLACEMENT_3D ( 'NONE', #41771, #28062, #14977 ) ;
#40475=CYLINDRICAL_SURFACE ( 'NONE', #42860, 120.5010000000000190 ) ;
#40478=LINE ( 'NONE', #10172, #38529 ) ;
#40479=ORIENTED_EDGE ( 'NONE', *, *, #40934, .T. ) ;
#40480=CIRCLE ( 'NONE', #24511, 120.5010000000000190 ) ;
#40482=VERTEX_POINT ( 'NONE', #6094 ) ;
#40485=ORIENTED_EDGE ( 'NONE', *, *, #13653, .F. ) ;
#40486=CARTESIAN_POINT ( 'NONE',  ( 9.000000000000001776, -29.86146781000025285, 112.0905559814577970 ) ) ;
#40487=LINE ( 'NONE', #780, #37324 ) ;
#40490=EDGE_CURVE ( 'NONE', #6927, #24346, #45, .T. ) ;
#40493=EDGE_CURVE ( 'NONE', #9120, #17669, #39230, .T. ) ;
#40494=VERTEX_POINT ( 'NONE', #28609 ) ;
#40495=CARTESIAN_POINT ( 'NONE',  ( 0.000000000000000000, 46.83041522348496954, 101.9567785075603155 ) ) ;
#40508=VERTEX_POINT ( 'NONE', #12234 ) ;
#40511=DIRECTION ( 'NONE',  ( 0.000000000000000000, 0.000000000000000000, 1.000000000000000000 ) ) ;
#40512=AXIS2_PLACEMENT_3D ( 'NONE', #14534, #37618, #14305 ) ;
#40518=VECTOR ( 'NONE', #38874, 1000.000000000000000 ) ;
#40521=CARTESIAN_POINT ( 'NONE',  ( 0.000000000000000000, -27.83061035786878890, -117.2431154827800270 ) ) ;
#40523=EDGE_LOOP ( 'NONE', ( #28954, #15450, #18072, #33867 ) ) ;
#40526=ORIENTED_EDGE ( 'NONE', *, *, #29956, .F. ) ;
#40527=CARTESIAN_POINT ( 'NONE',  ( 17.99999999999999645, 64.58410930313523579, 101.7319213743684685 ) ) ;
#40532=DIRECTION ( 'NONE',  ( -1.000000000000000000, 0.000000000000000000, 0.000000000000000000 ) ) ;
#40533=VECTOR ( 'NONE', #25971, 1000.000000000000000 ) ;
#40535=AXIS2_PLACEMENT_3D ( 'NONE', #30998, #41221, #27519 ) ;
#40537=ORIENTED_EDGE ( 'NONE', *, *, #11125, .F. ) ;
#40542=CIRCLE ( 'NONE', #9202, 59.00000000000000000 ) ;
#40543=CARTESIAN_POINT ( 'NONE',  ( 0.000000000000000000, -94.52951811191513798, -67.23221107124996365 ) ) ;
#40544=DIRECTION ( 'NONE',  ( -1.000000000000000000, -0.000000000000000000, -0.000000000000000000 ) ) ;
#40545=CARTESIAN_POINT ( 'NONE',  ( 17.99999999999999645, 0.000000000000000000, 0.000000000000000000 ) ) ;
#40546=EDGE_CURVE ( 'NONE', #32806, #39315, #23815, .T. ) ;
#40547=ORIENTED_EDGE ( 'NONE', *, *, #23162, .F. ) ;
#40548=DIRECTION ( 'NONE',  ( 0.000000000000000000, -0.8477344278896650209, -0.5304209081197521769 ) ) ;
#40553=DIRECTION ( 'NONE',  ( 0.000000000000000000, 0.000000000000000000, 1.000000000000000000 ) ) ;
#40554=DIRECTION ( 'NONE',  ( 0.000000000000000000, 0.000000000000000000, 1.000000000000000000 ) ) ;
#40555=EDGE_LOOP ( 'NONE', ( #18322, #33522, #38976, #39635 ) ) ;
#40560=CARTESIAN_POINT ( 'NONE',  ( 0.000000000000000000, 59.07817985939001915, 105.0250430397510968 ) ) ;
#40562=AXIS2_PLACEMENT_3D ( 'NONE', #27919, #37910, #38347 ) ;
#40564=VERTEX_POINT ( 'NONE', #38598 ) ;
#40565=LINE ( 'NONE', #10702, #7700 ) ;
#40566=VECTOR ( 'NONE', #19617, 1000.000000000000000 ) ;
#40568=ORIENTED_EDGE ( 'NONE', *, *, #28964, .T. ) ;
#40573=CARTESIAN_POINT ( 'NONE',  ( 0.000000000000000000, 0.000000000000000000, 0.000000000000000000 ) ) ;
#40579=ORIENTED_EDGE ( 'NONE', *, *, #3636, .F. ) ;
#40583=ORIENTED_EDGE ( 'NONE', *, *, #16536, .T. ) ;
#40587=CYLINDRICAL_SURFACE ( 'NONE', #30366, 59.00000000000000000 ) ;
#40591=VERTEX_POINT ( 'NONE', #39451 ) ;
#40593=CARTESIAN_POINT ( 'NONE',  ( 17.99999999999999645, 74.56001736500736854, -88.86396238368961065 ) ) ;
#40597=ORIENTED_EDGE ( 'NONE', *, *, #29656, .T. ) ;
#40599=ORIENTED_EDGE ( 'NONE', *, *, #13535, .F. ) ;
#40600=CARTESIAN_POINT ( 'NONE',  ( 0.000000000000000000, 117.9424311864589185, 24.69967462999075991 ) ) ;
#40601=CIRCLE ( 'NONE', #29487, 58.99999999999999289 ) ;
#40604=DIRECTION ( 'NONE',  ( 1.000000000000000000, 0.000000000000000000, 0.000000000000000000 ) ) ;
#40608=ORIENTED_EDGE ( 'NONE', *, *, #13791, .F. ) ;
#40609=CARTESIAN_POINT ( 'NONE',  ( 17.99999999999999645, 6.486220790508443912, 112.0098273076987567 ) ) ;
#40611=CARTESIAN_POINT ( 'NONE',  ( 0.000000000000000000, -19.12429268481792732, 114.4126803693778669 ) ) ;
#40614=ORIENTED_EDGE ( 'NONE', *, *, #5351, .F. ) ;
#40620=AXIS2_PLACEMENT_3D ( 'NONE', #42961, #12477, #42533 ) ;
#40624=FACE_OUTER_BOUND ( 'NONE', #30880, .T. ) ;
#40631=CARTESIAN_POINT ( 'NONE',  ( 0.000000000000000000, -63.55543939553828636, 97.03971415477303708 ) ) ;
#40638=EDGE_CURVE ( 'NONE', #252, #40190, #13341, .T. ) ;
#40640=EDGE_LOOP ( 'NONE', ( #11461, #22912, #30484, #35295 ) ) ;
#40643=CIRCLE ( 'NONE', #1639, 116.0000000000000000 ) ;
#40646=DIRECTION ( 'NONE',  ( 0.000000000000000000, 0.000000000000000000, 1.000000000000000000 ) ) ;
#40648=ADVANCED_FACE ( 'NONE', ( #26606 ), #7156, .F. ) ;
#40651=VERTEX_POINT ( 'NONE', #40089 ) ;
#40653=EDGE_CURVE ( 'NONE', #28377, #23473, #10658, .T. ) ;
#40658=CARTESIAN_POINT ( 'NONE',  ( 17.99999999999999645, 0.000000000000000000, 0.000000000000000000 ) ) ;
#40660=CARTESIAN_POINT ( 'NONE',  ( 17.99999999999999645, -110.8621702203446659, -34.14058016547651420 ) ) ;
#40662=AXIS2_PLACEMENT_3D ( 'NONE', #2066, #15844, #25460 ) ;
#40663=ORIENTED_EDGE ( 'NONE', *, *, #41789, .T. ) ;
#40668=VECTOR ( 'NONE', #8294, 1000.000000000000000 ) ;
#40679=AXIS2_PLACEMENT_3D ( 'NONE', #4778, #27927, #31603 ) ;
#40684=CIRCLE ( 'NONE', #6557, 59.00000000000000711 ) ;
#40686=DIRECTION ( 'NONE',  ( 0.000000000000000000, 0.5076658003388352380, 0.8615540813938089570 ) ) ;
#40691=DIRECTION ( 'NONE',  ( 1.000000000000000000, 0.000000000000000000, 0.000000000000000000 ) ) ;
#40694=CIRCLE ( 'NONE', #5184, 116.0000000000000000 ) ;
#40695=EDGE_LOOP ( 'NONE', ( #23664, #9880, #29874, #11900 ) ) ;
#40697=DIRECTION ( 'NONE',  ( 0.000000000000000000, 0.9826841245925200807, 0.1852887240871181618 ) ) ;
#40703=EDGE_CURVE ( 'NONE', #40190, #37810, #6506, .T. ) ;
#40704=ORIENTED_EDGE ( 'NONE', *, *, #24960, .T. ) ;
#40705=LINE ( 'NONE', #11505, #23511 ) ;
#40707=CARTESIAN_POINT ( 'NONE',  ( 17.99999999999999645, 0.000000000000000000, 0.000000000000000000 ) ) ;
#40709=DIRECTION ( 'NONE',  ( -1.000000000000000000, 0.000000000000000000, -0.000000000000000000 ) ) ;
#40714=DIRECTION ( 'NONE',  ( 1.000000000000000000, 0.000000000000000000, 0.000000000000000000 ) ) ;
#40715=ORIENTED_EDGE ( 'NONE', *, *, #8471, .F. ) ;
#40717=AXIS2_PLACEMENT_3D ( 'NONE', #41146, #40714, #14586 ) ;
#40721=CYLINDRICAL_SURFACE ( 'NONE', #26238, 59.00000000000000000 ) ;
#40724=AXIS2_PLACEMENT_3D ( 'NONE', #7712, #21076, #39985 ) ;
#40725=VERTEX_POINT ( 'NONE', #16360 ) ;
#40727=EDGE_LOOP ( 'NONE', ( #26582, #2874, #30007, #38301 ) ) ;
#40731=DIRECTION ( 'NONE',  ( 1.000000000000000000, 0.000000000000000000, 0.000000000000000000 ) ) ;
#40732=EDGE_CURVE ( 'NONE', #5010, #14947, #13099, .T. ) ;
#40733=ADVANCED_FACE ( 'NONE', ( #20303 ), #39667, .F. ) ;
#40739=FACE_OUTER_BOUND ( 'NONE', #24341, .T. ) ;
#40741=VERTEX_POINT ( 'NONE', #30307 ) ;
#40742=VECTOR ( 'NONE', #33538, 1000.000000000000000 ) ;
#40745=VERTEX_POINT ( 'NONE', #27046 ) ;
#40747=AXIS2_PLACEMENT_3D ( 'NONE', #18248, #28041, #21087 ) ;
#40748=CARTESIAN_POINT ( 'NONE',  ( 17.99999999999999645, 0.000000000000000000, 0.000000000000000000 ) ) ;
#40754=ORIENTED_EDGE ( 'NONE', *, *, #8559, .T. ) ;
#40758=CARTESIAN_POINT ( 'NONE',  ( 0.000000000000000000, 53.40478689619876462, -108.0204598100360016 ) ) ;
#40759=DIRECTION ( 'NONE',  ( 1.000000000000000000, -0.000000000000000000, 0.000000000000000000 ) ) ;
#40762=VERTEX_POINT ( 'NONE', #34645 ) ;
#40769=CYLINDRICAL_SURFACE ( 'NONE', #27800, 59.00000000000000000 ) ;
#40770=DIRECTION ( 'NONE',  ( 0.000000000000000000, 0.000000000000000000, 1.000000000000000000 ) ) ;
#40771=VECTOR ( 'NONE', #7057, 1000.000000000000000 ) ;
#40772=VERTEX_POINT ( 'NONE', #35445 ) ;
#40773=AXIS2_PLACEMENT_3D ( 'NONE', #13051, #9748, #25928 ) ;
#40774=CARTESIAN_POINT ( 'NONE',  ( 17.99999999999999645, 87.74575819880270444, -75.87280091124384285 ) ) ;
#40775=CARTESIAN_POINT ( 'NONE',  ( 0.000000000000000000, -52.88069566989523906, 103.2454939717367211 ) ) ;
#40777=VERTEX_POINT ( 'NONE', #21170 ) ;
#40779=ORIENTED_EDGE ( 'NONE', *, *, #38877, .T. ) ;
#40780=AXIS2_PLACEMENT_3D ( 'NONE', #30397, #10088, #23436 ) ;
#40783=CARTESIAN_POINT ( 'NONE',  ( 0.000000000000000000, -16.77566611177699940, -119.3275660838943963 ) ) ;
#40787=EDGE_CURVE ( 'NONE', #41769, #15814, #11949, .T. ) ;
#40788=DIRECTION ( 'NONE',  ( 0.000000000000000000, -0.9996456111234522934, -0.02662052143778456323 ) ) ;
#40789=ORIENTED_EDGE ( 'NONE', *, *, #14634, .T. ) ;
#40790=FACE_OUTER_BOUND ( 'NONE', #532, .T. ) ;
#40792=VECTOR ( 'NONE', #39564, 1000.000000000000000 ) ;
#40795=DIRECTION ( 'NONE',  ( -1.000000000000000000, -0.000000000000000000, 0.000000000000000000 ) ) ;
#40796=ORIENTED_EDGE ( 'NONE', *, *, #13301, .T. ) ;
#40797=EDGE_CURVE ( 'NONE', #36072, #7950, #1472, .T. ) ;
#40798=AXIS2_PLACEMENT_3D ( 'NONE', #20699, #39840, #40697 ) ;
#40800=LINE ( 'NONE', #10956, #42029 ) ;
#40803=AXIS2_PLACEMENT_3D ( 'NONE', #9003, #8149, #41288 ) ;
#40804=CYLINDRICAL_SURFACE ( 'NONE', #222, 116.0000000000000000 ) ;
#40806=EDGE_CURVE ( 'NONE', #29283, #21974, #10891, .T. ) ;
#40817=CARTESIAN_POINT ( 'NONE',  ( 0.000000000000000000, 92.25992191227497585, -77.51514567967302582 ) ) ;
#40822=ORIENTED_EDGE ( 'NONE', *, *, #17821, .T. ) ;
#40826=CIRCLE ( 'NONE', #3190, 116.0000000000000000 ) ;
#40829=ORIENTED_EDGE ( 'NONE', *, *, #28934, .T. ) ;
#40831=CIRCLE ( 'NONE', #10907, 59.00000000000000000 ) ;
#40834=AXIS2_PLACEMENT_3D ( 'NONE', #30014, #278, #42843 ) ;
#40837=FACE_OUTER_BOUND ( 'NONE', #33729, .T. ) ;
#40848=ORIENTED_EDGE ( 'NONE', *, *, #30631, .T. ) ;
#40850=DIRECTION ( 'NONE',  ( 0.000000000000000000, 0.9213119778704113028, 0.3888241754733245403 ) ) ;
#40852=AXIS2_PLACEMENT_3D ( 'NONE', #22841, #6208, #19554 ) ;
#40853=FACE_OUTER_BOUND ( 'NONE', #20550, .T. ) ;
#40854=LINE ( 'NONE', #34110, #21514 ) ;
#40855=VERTEX_POINT ( 'NONE', #38133 ) ;
#40859=EDGE_CURVE ( 'NONE', #32785, #9347, #27990, .T. ) ;
#40866=AXIS2_PLACEMENT_3D ( 'NONE', #35562, #5682, #15969 ) ;
#40867=ORIENTED_EDGE ( 'NONE', *, *, #22672, .T. ) ;
#40874=ORIENTED_EDGE ( 'NONE', *, *, #6268, .T. ) ;
#40875=CYLINDRICAL_SURFACE ( 'NONE', #1233, 116.0000000000000000 ) ;
#40877=DIRECTION ( 'NONE',  ( 0.000000000000000000, -0.5076658003388293539, -0.8615540813938123987 ) ) ;
#40879=CARTESIAN_POINT ( 'NONE',  ( 17.99999999999999645, -2.418575551220017328, -120.4767259403369053 ) ) ;
#40881=EDGE_CURVE ( 'NONE', #27385, #36371, #14754, .T. ) ;
#40883=DIRECTION ( 'NONE',  ( -1.000000000000000000, 0.000000000000000000, 0.000000000000000000 ) ) ;
#40884=EDGE_LOOP ( 'NONE', ( #15681, #25769, #38786, #23130 ) ) ;
#40885=VERTEX_POINT ( 'NONE', #1264 ) ;
#40887=CARTESIAN_POINT ( 'NONE',  ( 17.99999999999999645, -120.2856157092987388, 7.201503623196430226 ) ) ;
#40890=DIRECTION ( 'NONE',  ( 0.000000000000000000, 0.000000000000000000, -1.000000000000000000 ) ) ;
#40894=AXIS2_PLACEMENT_3D ( 'NONE', #3777, #13232, #30449 ) ;
#40895=CIRCLE ( 'NONE', #29098, 116.0000000000000000 ) ;
#40901=AXIS2_PLACEMENT_3D ( 'NONE', #16514, #25700, #9506 ) ;
#40902=CARTESIAN_POINT ( 'NONE',  ( 0.000000000000000000, -107.1354928292872728, 44.47455650398029547 ) ) ;
#40905=ORIENTED_EDGE ( 'NONE', *, *, #27683, .F. ) ;
#40906=DIRECTION ( 'NONE',  ( 0.000000000000000000, 0.000000000000000000, 1.000000000000000000 ) ) ;
#40907=EDGE_LOOP ( 'NONE', ( #33650, #3908, #21966, #6107 ) ) ;
#40908=EDGE_CURVE ( 'NONE', #26205, #40508, #20333, .T. ) ;
#40916=DIRECTION ( 'NONE',  ( -1.000000000000000000, -0.000000000000000000, -0.000000000000000000 ) ) ;
#40919=ORIENTED_EDGE ( 'NONE', *, *, #28914, .T. ) ;
#40921=ORIENTED_EDGE ( 'NONE', *, *, #17362, .F. ) ;
#40927=DIRECTION ( 'NONE',  ( 0.000000000000000000, 0.000000000000000000, 1.000000000000000000 ) ) ;
#40930=VECTOR ( 'NONE', #654, 1000.000000000000000 ) ;
#40934=EDGE_CURVE ( 'NONE', #16359, #848, #34244, .T. ) ;
#40935=DIRECTION ( 'NONE',  ( 0.000000000000000000, 0.000000000000000000, 1.000000000000000000 ) ) ;
#40937=CIRCLE ( 'NONE', #33295, 59.00000000000000000 ) ;
#40938=EDGE_CURVE ( 'NONE', #4481, #6529, #17678, .T. ) ;
#40939=EDGE_CURVE ( 'NONE', #28172, #11528, #23139, .T. ) ;
#40941=ORIENTED_EDGE ( 'NONE', *, *, #36548, .T. ) ;
#40942=DIRECTION ( 'NONE',  ( 0.000000000000000000, -0.9826841245925190815, -0.1852887240871243235 ) ) ;
#40943=ORIENTED_EDGE ( 'NONE', *, *, #5517, .F. ) ;
#40944=LINE ( 'NONE', #37672, #20996 ) ;
#40949=DIRECTION ( 'NONE',  ( -1.000000000000000000, 0.000000000000000000, -0.000000000000000000 ) ) ;
#40950=DIRECTION ( 'NONE',  ( 1.000000000000000000, 0.000000000000000000, 0.000000000000000000 ) ) ;
#40952=CARTESIAN_POINT ( 'NONE',  ( 17.99999999999999645, 78.75547124681493472, -91.20343606296920314 ) ) ;
#40953=EDGE_LOOP ( 'NONE', ( #186, #10166, #29784, #4026 ) ) ;
#40956=CIRCLE ( 'NONE', #3325, 58.99999999999998579 ) ;
#40960=CIRCLE ( 'NONE', #5447, 116.0000000000000000 ) ;
#40961=CARTESIAN_POINT ( 'NONE',  ( 0.000000000000000000, -75.03166794516862126, 94.29071961951481740 ) ) ;
#40962=CARTESIAN_POINT ( 'NONE',  ( 0.000000000000000000, 115.9387338813861419, 3.769613505536437259 ) ) ;
#40963=AXIS2_PLACEMENT_3D ( 'NONE', #8855, #35663, #15438 ) ;
#40965=EDGE_CURVE ( 'NONE', #9979, #34324, #4269, .T. ) ;
#40966=CIRCLE ( 'NONE', #23605, 120.5010000000000332 ) ;
#40967=CARTESIAN_POINT ( 'NONE',  ( 8.999999999999998224, 83.58328028049768932, -80.43528614701241963 ) ) ;
#40970=VERTEX_POINT ( 'NONE', #40961 ) ;
#40971=CYLINDRICAL_SURFACE ( 'NONE', #23224, 59.00000000000000000 ) ;
#40972=AXIS2_PLACEMENT_3D ( 'NONE', #7415, #37081, #40554 ) ;
#40973=CARTESIAN_POINT ( 'NONE',  ( 0.000000000000000000, 107.5680526044919674, -31.89649718262133149 ) ) ;
#40975=CARTESIAN_POINT ( 'NONE',  ( 0.000000000000000000, 105.7179949885867956, -37.57629584241721687 ) ) ;
#40980=CARTESIAN_POINT ( 'NONE',  ( 0.000000000000000000, 0.000000000000000000, 0.000000000000000000 ) ) ;
#40981=EDGE_CURVE ( 'NONE', #32785, #29037, #37693, .T. ) ;
#40984=AXIS2_PLACEMENT_3D ( 'NONE', #32644, #28595, #11805 ) ;
#40987=ADVANCED_FACE ( 'NONE', ( #3105 ), #6197, .F. ) ;
#40988=DIRECTION ( 'NONE',  ( 0.000000000000000000, -0.9911528310040057521, -0.1327255272837325473 ) ) ;
#40992=CIRCLE ( 'NONE', #28525, 58.99999999999999289 ) ;
#40993=ADVANCED_FACE ( 'NONE', ( #19543 ), #32811, .F. ) ;
#40994=VERTEX_POINT ( 'NONE', #2889 ) ;
#40996=FACE_OUTER_BOUND ( 'NONE', #41653, .T. ) ;
#41000=CARTESIAN_POINT ( 'NONE',  ( 17.99999999999999645, 0.000000000000000000, 0.000000000000000000 ) ) ;
#41001=ORIENTED_EDGE ( 'NONE', *, *, #33267, .T. ) ;
#41003=ORIENTED_EDGE ( 'NONE', *, *, #19953, .F. ) ;
#41006=DIRECTION ( 'NONE',  ( -1.000000000000000000, 0.000000000000000000, -0.000000000000000000 ) ) ;
#41008=EDGE_LOOP ( 'NONE', ( #562, #34626, #42984, #20023 ) ) ;
#41009=CARTESIAN_POINT ( 'NONE',  ( 17.99999999999999645, 91.51415974874679193, -64.91094698989203948 ) ) ;
#41012=DIRECTION ( 'NONE',  ( -1.000000000000000000, 0.000000000000000000, 0.000000000000000000 ) ) ;
#41014=AXIS2_PLACEMENT_3D ( 'NONE', #11907, #31969, #40890 ) ;
#41016=CARTESIAN_POINT ( 'NONE',  ( 17.99999999999999645, 34.74871106919766106, -106.6808302961368327 ) ) ;
#41022=ORIENTED_EDGE ( 'NONE', *, *, #34517, .F. ) ;
#41024=DIRECTION ( 'NONE',  ( 1.000000000000000000, 0.000000000000000000, 0.000000000000000000 ) ) ;
#41026=ORIENTED_EDGE ( 'NONE', *, *, #22735, .T. ) ;
#41030=DIRECTION ( 'NONE',  ( -1.000000000000000000, -0.000000000000000000, -0.000000000000000000 ) ) ;
#41031=DIRECTION ( 'NONE',  ( 1.000000000000000000, 0.000000000000000000, 0.000000000000000000 ) ) ;
#41036=EDGE_CURVE ( 'NONE', #40221, #13380, #42824, .T. ) ;
#41037=EDGE_LOOP ( 'NONE', ( #1196, #28585, #5164, #2938 ) ) ;
#41040=CARTESIAN_POINT ( 'NONE',  ( 17.99999999999999645, 0.000000000000000000, 0.000000000000000000 ) ) ;
#41043=AXIS2_PLACEMENT_3D ( 'NONE', #20664, #16951, #34140 ) ;
#41046=ORIENTED_EDGE ( 'NONE', *, *, #18863, .T. ) ;
#41057=ORIENTED_EDGE ( 'NONE', *, *, #24547, .T. ) ;
#41058=CARTESIAN_POINT ( 'NONE',  ( 17.99999999999999645, -103.1672962317654338, 44.09967643725834563 ) ) ;
#41059=ORIENTED_EDGE ( 'NONE', *, *, #29415, .F. ) ;
#41062=CYLINDRICAL_SURFACE ( 'NONE', #10247, 120.5010000000000190 ) ;
#41064=EDGE_CURVE ( 'NONE', #31468, #38864, #14783, .T. ) ;
#41069=CIRCLE ( 'NONE', #26493, 59.00000000000000000 ) ;
#41070=VERTEX_POINT ( 'NONE', #35850 ) ;
#41080=CARTESIAN_POINT ( 'NONE',  ( 0.000000000000000000, 69.72480978690171582, -92.70626138605946664 ) ) ;
#41081=FACE_OUTER_BOUND ( 'NONE', #753, .T. ) ;
#41084=ORIENTED_EDGE ( 'NONE', *, *, #2444, .T. ) ;
#41087=DIRECTION ( 'NONE',  ( 1.000000000000000000, 0.000000000000000000, 0.000000000000000000 ) ) ;
#41090=CARTESIAN_POINT ( 'NONE',  ( 17.99999999999999645, 0.000000000000000000, 0.000000000000000000 ) ) ;
#41091=FACE_OUTER_BOUND ( 'NONE', #26775, .T. ) ;
#41092=ORIENTED_EDGE ( 'NONE', *, *, #14612, .T. ) ;
#41093=ORIENTED_EDGE ( 'NONE', *, *, #7104, .T. ) ;
#41097=AXIS2_PLACEMENT_3D ( 'NONE', #27941, #11793, #28376 ) ;
#41100=VERTEX_POINT ( 'NONE', #9046 ) ;
#41101=AXIS2_PLACEMENT_3D ( 'NONE', #18963, #22649, #32429 ) ;
#41102=ADVANCED_FACE ( 'NONE', ( #5763 ), #19120, .F. ) ;
#41108=VERTEX_POINT ( 'NONE', #25873 ) ;
#41113=ORIENTED_EDGE ( 'NONE', *, *, #35416, .T. ) ;
#41114=LINE ( 'NONE', #34587, #16833 ) ;
#41115=EDGE_CURVE ( 'NONE', #33767, #7030, #39122, .T. ) ;
#41117=( NAMED_UNIT ( * ) SI_UNIT ( $, .STERADIAN. ) SOLID_ANGLE_UNIT ( ) );
#41118=EDGE_CURVE ( 'NONE', #3101, #10939, #3570, .T. ) ;
#41119=DIRECTION ( 'NONE',  ( 1.000000000000000000, 0.000000000000000000, 0.000000000000000000 ) ) ;
#41120=DIRECTION ( 'NONE',  ( -1.000000000000000000, -0.000000000000000000, -0.000000000000000000 ) ) ;
#41123=ADVANCED_FACE ( 'NONE', ( #17570 ), #24105, .F. ) ;
#41126=CIRCLE ( 'NONE', #12605, 58.99999999999999289 ) ;
#41132=DIRECTION ( 'NONE',  ( -1.000000000000000000, 0.000000000000000000, 0.000000000000000000 ) ) ;
#41136=VECTOR ( 'NONE', #35942, 1000.000000000000000 ) ;
#41140=CARTESIAN_POINT ( 'NONE',  ( 17.99999999999999645, -61.59243992711522964, 93.77976230226020959 ) ) ;
#41141=VERTEX_POINT ( 'NONE', #23888 ) ;
#41146=CARTESIAN_POINT ( 'NONE',  ( 0.000000000000000000, 0.000000000000000000, 0.000000000000000000 ) ) ;
#41147=VERTEX_POINT ( 'NONE', #7701 ) ;
#41152=ORIENTED_EDGE ( 'NONE', *, *, #23317, .F. ) ;
#41156=CARTESIAN_POINT ( 'NONE',  ( 17.99999999999999645, -52.88069566989523906, 103.2454939717367211 ) ) ;
#41158=ORIENTED_EDGE ( 'NONE', *, *, #2691, .T. ) ;
#41160=CIRCLE ( 'NONE', #2143, 59.00000000000000000 ) ;
#41161=ORIENTED_EDGE ( 'NONE', *, *, #16310, .F. ) ;
#41164=CARTESIAN_POINT ( 'NONE',  ( 17.99999999999999645, -27.83061035787034498, 117.2431154827796576 ) ) ;
#41165=AXIS2_PLACEMENT_3D ( 'NONE', #1787, #37790, #34310 ) ;
#41168=DIRECTION ( 'NONE',  ( -1.000000000000000000, 0.000000000000000000, 0.000000000000000000 ) ) ;
#41170=DIRECTION ( 'NONE',  ( 0.000000000000000000, 0.000000000000000000, 1.000000000000000000 ) ) ;
#41172=ORIENTED_EDGE ( 'NONE', *, *, #854, .F. ) ;
#41175=CARTESIAN_POINT ( 'NONE',  ( 17.99999999999999645, -80.74349901498459303, 77.90224541347254217 ) ) ;
#41178=EDGE_CURVE ( 'NONE', #28718, #36227, #10580, .T. ) ;
#41181=CARTESIAN_POINT ( 'NONE',  ( 0.000000000000000000, 59.47573314508733944, 99.59235496188628645 ) ) ;
#41186=EDGE_CURVE ( 'NONE', #31219, #21374, #40419, .T. ) ;
#41189=EDGE_CURVE ( 'NONE', #37133, #18706, #27285, .T. ) ;
#41194=DIRECTION ( 'NONE',  ( 0.000000000000000000, 0.5076658003388410112, -0.8615540813938056264 ) ) ;
#41195=AXIS2_PLACEMENT_3D ( 'NONE', #1836, #10807, #38058 ) ;
#41196=DIRECTION ( 'NONE',  ( 0.000000000000000000, 0.000000000000000000, 1.000000000000000000 ) ) ;
#41197=ORIENTED_EDGE ( 'NONE', *, *, #27127, .T. ) ;
#41201=EDGE_LOOP ( 'NONE', ( #16081, #27786, #3833, #3213 ) ) ;
#41203=CYLINDRICAL_SURFACE ( 'NONE', #34715, 59.00000000000000000 ) ;
#41205=ORIENTED_EDGE ( 'NONE', *, *, #39115, .T. ) ;
#41206=EDGE_CURVE ( 'NONE', #1540, #42489, #30844, .T. ) ;
#41212=CARTESIAN_POINT ( 'NONE',  ( 17.99999999999999645, 0.000000000000000000, 0.000000000000000000 ) ) ;
#41217=EDGE_LOOP ( 'NONE', ( #1850, #27747, #18985, #8896 ) ) ;
#41218=DIRECTION ( 'NONE',  ( 0.000000000000000000, 0.000000000000000000, 1.000000000000000000 ) ) ;
#41219=CARTESIAN_POINT ( 'NONE',  ( 17.99999999999999645, 94.83915810436481308, -59.94836581341496640 ) ) ;
#41221=DIRECTION ( 'NONE',  ( -1.000000000000000000, 0.000000000000000000, 0.000000000000000000 ) ) ;
#41224=CIRCLE ( 'NONE', #27305, 59.00000000000000000 ) ;
#41228=ORIENTED_EDGE ( 'NONE', *, *, #5649, .T. ) ;
#41229=DIRECTION ( 'NONE',  ( -1.000000000000000000, -0.000000000000000000, -0.000000000000000000 ) ) ;
#41234=ORIENTED_EDGE ( 'NONE', *, *, #11413, .T. ) ;
#41238=AXIS2_PLACEMENT_3D ( 'NONE', #1580, #8352, #34758 ) ;
#41240=DIRECTION ( 'NONE',  ( 1.000000000000000000, 0.000000000000000000, 0.000000000000000000 ) ) ;
#41241=CARTESIAN_POINT ( 'NONE',  ( 17.99999999999999645, 10.40101730206366959, 120.0512800434971581 ) ) ;
#41242=CYLINDRICAL_SURFACE ( 'NONE', #10559, 59.00000000000000000 ) ;
#41250=DIRECTION ( 'NONE',  ( -1.000000000000000000, 0.000000000000000000, 0.000000000000000000 ) ) ;
#41251=ADVANCED_FACE ( 'NONE', ( #40624 ), #917, .F. ) ;
#41252=AXIS2_PLACEMENT_3D ( 'NONE', #26403, #29034, #23148 ) ;
#41253=VERTEX_POINT ( 'NONE', #24762 ) ;
#41257=CARTESIAN_POINT ( 'NONE',  ( 17.99999999999999645, 100.6739960869717834, 49.52796165323294986 ) ) ;
#41263=DIRECTION ( 'NONE',  ( 0.000000000000000000, -0.2113826236296113270, -0.9774033898178695612 ) ) ;
#41264=EDGE_LOOP ( 'NONE', ( #6623, #40423, #36256, #20576 ) ) ;
#41265=DIRECTION ( 'NONE',  ( 1.000000000000000000, 0.000000000000000000, 0.000000000000000000 ) ) ;
#41266=ORIENTED_EDGE ( 'NONE', *, *, #980, .F. ) ;
#41267=VECTOR ( 'NONE', #3277, 1000.000000000000000 ) ;
#41268=ORIENTED_EDGE ( 'NONE', *, *, #39551, .T. ) ;
#41272=DIRECTION ( 'NONE',  ( 1.000000000000000000, -0.000000000000000000, -0.000000000000000000 ) ) ;
#41274=ORIENTED_EDGE ( 'NONE', *, *, #37688, .T. ) ;
#41276=VERTEX_POINT ( 'NONE', #38238 ) ;
#41280=FACE_OUTER_BOUND ( 'NONE', #10701, .T. ) ;
#41281=EDGE_CURVE ( 'NONE', #10089, #10944, #40542, .T. ) ;
#41286=EDGE_CURVE ( 'NONE', #26752, #14373, #1534, .T. ) ;
#41287=AXIS2_PLACEMENT_3D ( 'NONE', #2949, #2742, #16106 ) ;
#41288=DIRECTION ( 'NONE',  ( 0.000000000000000000, 0.000000000000000000, 1.000000000000000000 ) ) ;
#41290=FACE_OUTER_BOUND ( 'NONE', #29449, .T. ) ;
#41294=CIRCLE ( 'NONE', #14868, 59.00000000000000000 ) ;
#41296=AXIS2_PLACEMENT_3D ( 'NONE', #19872, #20309, #13320 ) ;
#41300=DIRECTION ( 'NONE',  ( -1.000000000000000000, -0.000000000000000000, -0.000000000000000000 ) ) ;
#41301=DIRECTION ( 'NONE',  ( 1.000000000000000000, 0.000000000000000000, 0.000000000000000000 ) ) ;
#41306=VERTEX_POINT ( 'NONE', #14716 ) ;
#41310=DIRECTION ( 'NONE',  ( 0.000000000000000000, 0.1590634960190723812, -0.9872683547213445543 ) ) ;
#41312=EDGE_CURVE ( 'NONE', #18784, #18043, #29436, .T. ) ;
#41314=CARTESIAN_POINT ( 'NONE',  ( 0.000000000000000000, -23.85344185397275041, 113.5209818126990200 ) ) ;
#41315=DIRECTION ( 'NONE',  ( -1.000000000000000000, -0.000000000000000000, 0.000000000000000000 ) ) ;
#41316=AXIS2_PLACEMENT_3D ( 'NONE', #27204, #40035, #10169 ) ;
#41319=ORIENTED_EDGE ( 'NONE', *, *, #36621, .T. ) ;
#41321=CARTESIAN_POINT ( 'NONE',  ( 9.000000000000001776, -98.69720329640912837, -60.94966826380012037 ) ) ;
#41324=CARTESIAN_POINT ( 'NONE',  ( 17.99999999999999645, 117.9424311864589185, 24.69967462999075281 ) ) ;
#41326=FACE_OUTER_BOUND ( 'NONE', #30726, .T. ) ;
#41327=AXIS2_PLACEMENT_3D ( 'NONE', #26560, #10402, #37214 ) ;
#41333=FACE_OUTER_BOUND ( 'NONE', #12752, .T. ) ;
#41334=AXIS2_PLACEMENT_3D ( 'NONE', #20553, #37732, #33822 ) ;
#41337=FACE_OUTER_BOUND ( 'NONE', #23042, .T. ) ;
#41340=CARTESIAN_POINT ( 'NONE',  ( 0.000000000000000000, -111.2559044912522950, -32.83479428644788811 ) ) ;
#41342=CIRCLE ( 'NONE', #3700, 116.0000000000000000 ) ;
#41343=EDGE_CURVE ( 'NONE', #35191, #39524, #10608, .T. ) ;
#41345=AXIS2_PLACEMENT_3D ( 'NONE', #41697, #1980, #8750 ) ;
#41348=CARTESIAN_POINT ( 'NONE',  ( 17.99999999999999645, 0.000000000000000000, 0.000000000000000000 ) ) ;
#41355=EDGE_LOOP ( 'NONE', ( #23752, #25431, #38799, #11266 ) ) ;
#41356=FACE_OUTER_BOUND ( 'NONE', #4729, .T. ) ;
#41361=EDGE_LOOP ( 'NONE', ( #4267, #41092, #36247, #35708 ) ) ;
#41363=ORIENTED_EDGE ( 'NONE', *, *, #36071, .F. ) ;
#41364=CARTESIAN_POINT ( 'NONE',  ( 17.99999999999999645, -23.10276247328019039, -118.2656051737072431 ) ) ;
#41367=CARTESIAN_POINT ( 'NONE',  ( 17.99999999999999645, -112.5120133921110295, 43.14554256760978745 ) ) ;
#41369=AXIS2_PLACEMENT_3D ( 'NONE', #39792, #24783, #34554 ) ;
#41372=CARTESIAN_POINT ( 'NONE',  ( 0.000000000000000000, 5.456439917446431309, -112.0647122740741253 ) ) ;
#41377=VERTEX_POINT ( 'NONE', #41726 ) ;
#41379=VERTEX_POINT ( 'NONE', #11868 ) ;
#41384=CARTESIAN_POINT ( 'NONE',  ( 17.99999999999999645, 78.75547124681493472, -91.20343606296920314 ) ) ;
#41385=ORIENTED_EDGE ( 'NONE', *, *, #36929, .T. ) ;
#41393=FACE_OUTER_BOUND ( 'NONE', #10531, .T. ) ;
#41397=DIRECTION ( 'NONE',  ( 0.000000000000000000, -0.8477344278896651319, -0.5304209081197519549 ) ) ;
#41400=CARTESIAN_POINT ( 'NONE',  ( 17.99999999999999645, 118.8387007424470738, 19.94628303336527608 ) ) ;
#41402=AXIS2_PLACEMENT_3D ( 'NONE', #35816, #15588, #5735 ) ;
#41403=EDGE_CURVE ( 'NONE', #28259, #9950, #31059, .T. ) ;
#41404=VERTEX_POINT ( 'NONE', #27810 ) ;
#41409=CIRCLE ( 'NONE', #11488, 116.0000000000000000 ) ;
#41416=DIRECTION ( 'NONE',  ( 0.000000000000000000, -0.8747630845319658288, 0.4845508703326422140 ) ) ;
#41421=CARTESIAN_POINT ( 'NONE',  ( 17.99999999999999645, 0.000000000000000000, 0.000000000000000000 ) ) ;
#41422=EDGE_CURVE ( 'NONE', #21320, #39191, #34995, .T. ) ;
#41424=EDGE_CURVE ( 'NONE', #33606, #33175, #25614, .T. ) ;
#41425=DIRECTION ( 'NONE',  ( -1.000000000000000000, -0.000000000000000000, -0.000000000000000000 ) ) ;
#41427=ORIENTED_EDGE ( 'NONE', *, *, #19704, .F. ) ;
#41433=CIRCLE ( 'NONE', #41464, 116.0000000000000000 ) ;
#41434=DIRECTION ( 'NONE',  ( 0.000000000000000000, 0.000000000000000000, 1.000000000000000000 ) ) ;
#41435=DIRECTION ( 'NONE',  ( 1.000000000000000000, 0.000000000000000000, 0.000000000000000000 ) ) ;
#41436=VERTEX_POINT ( 'NONE', #22766 ) ;
#41444=DIRECTION ( 'NONE',  ( -1.000000000000000000, -0.000000000000000000, -0.000000000000000000 ) ) ;
#41447=CARTESIAN_POINT ( 'NONE',  ( 17.99999999999999645, 0.000000000000000000, 0.000000000000000000 ) ) ;
#41449=EDGE_CURVE ( 'NONE', #37862, #26858, #6354, .T. ) ;
#41458=ADVANCED_FACE ( 'NONE', ( #19492 ), #23195, .F. ) ;
#41459=DIRECTION ( 'NONE',  ( 1.000000000000000000, 0.000000000000000000, 0.000000000000000000 ) ) ;
#41461=AXIS2_PLACEMENT_3D ( 'NONE', #26122, #35690, #19167 ) ;
#41464=AXIS2_PLACEMENT_3D ( 'NONE', #13076, #39849, #20068 ) ;
#41465=DIRECTION ( 'NONE',  ( 1.000000000000000000, 0.000000000000000000, 0.000000000000000000 ) ) ;
#41466=CIRCLE ( 'NONE', #17096, 59.00000000000000711 ) ;
#41467=CARTESIAN_POINT ( 'NONE',  ( 0.000000000000000000, 0.000000000000000000, 0.000000000000000000 ) ) ;
#41471=ORIENTED_EDGE ( 'NONE', *, *, #6837, .T. ) ;
#41476=ORIENTED_EDGE ( 'NONE', *, *, #1490, .F. ) ;
#41477=EDGE_CURVE ( 'NONE', #28172, #20222, #2841, .T. ) ;
#41481=DIRECTION ( 'NONE',  ( -1.000000000000000000, -0.000000000000000000, -0.000000000000000000 ) ) ;
#41482=ORIENTED_EDGE ( 'NONE', *, *, #27229, .T. ) ;
#41485=VERTEX_POINT ( 'NONE', #15998 ) ;
#41489=FACE_OUTER_BOUND ( 'NONE', #32059, .T. ) ;
#41490=AXIS2_PLACEMENT_3D ( 'NONE', #11006, #14069, #7490 ) ;
#41499=VECTOR ( 'NONE', #21618, 1000.000000000000000 ) ;
#41501=DIRECTION ( 'NONE',  ( -1.000000000000000000, 0.000000000000000000, -0.000000000000000000 ) ) ;
#41506=ORIENTED_EDGE ( 'NONE', *, *, #28452, .T. ) ;
#41510=CARTESIAN_POINT ( 'NONE',  ( 17.99999999999999645, 64.69195966009891663, 96.28577441832274530 ) ) ;
#41511=ORIENTED_EDGE ( 'NONE', *, *, #39057, .F. ) ;
#41517=ORIENTED_EDGE ( 'NONE', *, *, #17271, .F. ) ;
#41518=ORIENTED_EDGE ( 'NONE', *, *, #24612, .T. ) ;
#41519=CYLINDRICAL_SURFACE ( 'NONE', #9529, 59.00000000000000000 ) ;
#41520=DIRECTION ( 'NONE',  ( -1.000000000000000000, -0.000000000000000000, -0.000000000000000000 ) ) ;
#41523=DIRECTION ( 'NONE',  ( 0.000000000000000000, 0.000000000000000000, 1.000000000000000000 ) ) ;
#41525=AXIS2_PLACEMENT_3D ( 'NONE', #34209, #27251, #30944 ) ;
#41526=CIRCLE ( 'NONE', #12284, 59.00000000000001421 ) ;
#41527=VERTEX_POINT ( 'NONE', #35793 ) ;
#41528=CARTESIAN_POINT ( 'NONE',  ( 0.000000000000000000, 0.000000000000000000, 0.000000000000000000 ) ) ;
#41529=ORIENTED_EDGE ( 'NONE', *, *, #8749, .F. ) ;
#41530=CARTESIAN_POINT ( 'NONE',  ( 17.99999999999999645, 93.26762629039428987, 76.29967815892386795 ) ) ;
#41531=CARTESIAN_POINT ( 'NONE',  ( 17.99999999999999645, -40.13512380273891011, -113.6206972269525863 ) ) ;
#41532=AXIS2_PLACEMENT_3D ( 'NONE', #4871, #18236, #5518 ) ;
#41534=EDGE_CURVE ( 'NONE', #29429, #17680, #39079, .T. ) ;
#41536=DIRECTION ( 'NONE',  ( 1.000000000000000000, 0.000000000000000000, 0.000000000000000000 ) ) ;
#41538=EDGE_CURVE ( 'NONE', #21041, #21374, #21785, .T. ) ;
#41543=DIRECTION ( 'NONE',  ( 0.000000000000000000, 0.6783118362696123338, 0.7347741508630706297 ) ) ;
#41547=ORIENTED_EDGE ( 'NONE', *, *, #28685, .T. ) ;
#41548=CARTESIAN_POINT ( 'NONE',  ( 0.000000000000000000, -42.87700105098536341, -107.7847984684009219 ) ) ;
#41549=EDGE_LOOP ( 'NONE', ( #35855, #41172, #2866, #40229 ) ) ;
#41551=ORIENTED_EDGE ( 'NONE', *, *, #19819, .T. ) ;
#41552=FACE_OUTER_BOUND ( 'NONE', #15677, .T. ) ;
#41553=CARTESIAN_POINT ( 'NONE',  ( 17.99999999999999645, -114.6488492393077081, -37.09625815500128709 ) ) ;
#41559=CARTESIAN_POINT ( 'NONE',  ( 0.000000000000000000, 0.000000000000000000, 0.000000000000000000 ) ) ;
#41560=AXIS2_PLACEMENT_3D ( 'NONE', #18393, #17970, #25153 ) ;
#41561=DIRECTION ( 'NONE',  ( 0.000000000000000000, -2.128711519673234442E-14, -1.000000000000000000 ) ) ;
#41562=AXIS2_PLACEMENT_3D ( 'NONE', #31591, #11535, #24881 ) ;
#41563=ORIENTED_EDGE ( 'NONE', *, *, #2238, .T. ) ;
#41564=CARTESIAN_POINT ( 'NONE',  ( 0.000000000000000000, 0.000000000000000000, 0.000000000000000000 ) ) ;
#41565=VECTOR ( 'NONE', #9271, 1000.000000000000000 ) ;
#41568=AXIS2_PLACEMENT_3D ( 'NONE', #9434, #39525, #9660 ) ;
#41569=DIRECTION ( 'NONE',  ( 1.000000000000000000, 0.000000000000000000, 0.000000000000000000 ) ) ;
#41570=CARTESIAN_POINT ( 'NONE',  ( 8.999999999999998224, 82.63181128086846172, -81.41243003646886223 ) ) ;
#41574=ORIENTED_EDGE ( 'NONE', *, *, #17496, .F. ) ;
#41575=AXIS2_PLACEMENT_3D ( 'NONE', #33825, #21866, #15314 ) ;
#41576=VECTOR ( 'NONE', #12556, 1000.000000000000000 ) ;
#41577=ORIENTED_EDGE ( 'NONE', *, *, #39376, .F. ) ;
#41578=DIRECTION ( 'NONE',  ( 0.000000000000000000, 0.3140767120219429276, 0.9493976084683832806 ) ) ;
#41582=LINE ( 'NONE', #24406, #33424 ) ;
#41586=CARTESIAN_POINT ( 'NONE',  ( 17.99999999999999645, 111.2559044912529345, -32.83479428644565701 ) ) ;
#41591=EDGE_CURVE ( 'NONE', #23465, #38913, #30360, .T. ) ;
#41592=CARTESIAN_POINT ( 'NONE',  ( 17.99999999999999645, -109.4038418350907023, 50.51029986767514401 ) ) ;
#41593=ORIENTED_EDGE ( 'NONE', *, *, #14298, .F. ) ;
#41594=DIRECTION ( 'NONE',  ( 0.000000000000000000, 0.000000000000000000, 1.000000000000000000 ) ) ;
#41603=DIRECTION ( 'NONE',  ( 0.000000000000000000, 0.000000000000000000, 1.000000000000000000 ) ) ;
#41612=CARTESIAN_POINT ( 'NONE',  ( 17.99999999999999645, 30.01658535635412406, -108.1077105353194838 ) ) ;
#41616=EDGE_CURVE ( 'NONE', #26508, #28297, #8522, .T. ) ;
#41620=CARTESIAN_POINT ( 'NONE',  ( 17.99999999999999645, -110.8621702203451065, 34.14058016547499363 ) ) ;
#41621=ORIENTED_EDGE ( 'NONE', *, *, #28638, .T. ) ;
#41623=DIRECTION ( 'NONE',  ( 0.000000000000000000, 0.4610925014493207352, 0.8873520750565742077 ) ) ;
#41628=VECTOR ( 'NONE', #8107, 1000.000000000000000 ) ;
#41629=CIRCLE ( 'NONE', #13100, 120.5010000000000474 ) ;
#41630=CARTESIAN_POINT ( 'NONE',  ( 17.99999999999999645, 78.18175027177548486, -85.69488855492920720 ) ) ;
#41634=AXIS2_PLACEMENT_3D ( 'NONE', #5336, #18473, #15403 ) ;
#41635=ORIENTED_EDGE ( 'NONE', *, *, #41424, .F. ) ;
#41639=ORIENTED_EDGE ( 'NONE', *, *, #24045, .T. ) ;
#41642=DIRECTION ( 'NONE',  ( 0.000000000000000000, 0.2113826236296247885, -0.9774033898178665636 ) ) ;
#41644=CARTESIAN_POINT ( 'NONE',  ( 0.000000000000000000, -5.492704054965900973, -115.8698847939556771 ) ) ;
#41645=ORIENTED_EDGE ( 'NONE', *, *, #38335, .T. ) ;
#41648=CYLINDRICAL_SURFACE ( 'NONE', #31397, 116.0000000000000000 ) ;
#41649=EDGE_CURVE ( 'NONE', #30521, #17817, #2910, .T. ) ;
#41653=EDGE_LOOP ( 'NONE', ( #23, #27550, #20928, #42173 ) ) ;
#41661=VERTEX_POINT ( 'NONE', #14010 ) ;
#41662=CIRCLE ( 'NONE', #37490, 116.0000000000000000 ) ;
#41664=EDGE_LOOP ( 'NONE', ( #626, #37581, #9400, #4929 ) ) ;
#41668=ADVANCED_FACE ( 'NONE', ( #33615 ), #3698, .F. ) ;
#41669=CIRCLE ( 'NONE', #543, 120.5010000000000190 ) ;
#41672=VERTEX_POINT ( 'NONE', #23631 ) ;
#41675=ORIENTED_EDGE ( 'NONE', *, *, #16912, .F. ) ;
#41676=DIRECTION ( 'NONE',  ( 0.000000000000000000, 1.243708525996931132E-14, -1.000000000000000000 ) ) ;
#41678=CARTESIAN_POINT ( 'NONE',  ( 17.99999999999999645, 0.000000000000000000, 0.000000000000000000 ) ) ;
#41679=ADVANCED_FACE ( 'NONE', ( #23838 ), #20149, .F. ) ;
#41681=CARTESIAN_POINT ( 'NONE',  ( 0.000000000000000000, 93.26762629039427566, 76.29967815892388217 ) ) ;
#41683=ADVANCED_FACE ( 'NONE', ( #6559 ), #33832, .F. ) ;
#41685=CARTESIAN_POINT ( 'NONE',  ( 17.99999999999999645, 0.000000000000000000, 0.000000000000000000 ) ) ;
#41690=AXIS2_PLACEMENT_3D ( 'NONE', #25328, #12220, #18804 ) ;
#41692=VECTOR ( 'NONE', #35718, 1000.000000000000000 ) ;
#41695=CARTESIAN_POINT ( 'NONE',  ( 0.000000000000000000, -119.0898412705473390, -18.38751498043854227 ) ) ;
#41697=CARTESIAN_POINT ( 'NONE',  ( 17.99999999999999645, 0.000000000000000000, 0.000000000000000000 ) ) ;
#41702=ORIENTED_EDGE ( 'NONE', *, *, #41944, .T. ) ;
#41704=DIRECTION ( 'NONE',  ( -1.000000000000000000, 0.000000000000000000, 0.000000000000000000 ) ) ;
#41705=ORIENTED_EDGE ( 'NONE', *, *, #36895, .T. ) ;
#41706=CYLINDRICAL_SURFACE ( 'NONE', #8932, 58.99999999999999289 ) ;
#41710=ORIENTED_EDGE ( 'NONE', *, *, #5983, .T. ) ;
#41711=EDGE_CURVE ( 'NONE', #34938, #10000, #37320, .T. ) ;
#41713=DIRECTION ( 'NONE',  ( -1.000000000000000000, 0.000000000000000000, 0.000000000000000000 ) ) ;
#41717=CARTESIAN_POINT ( 'NONE',  ( 17.99999999999999645, -35.78484819117565507, -110.3423972910436390 ) ) ;
#41719=AXIS2_PLACEMENT_3D ( 'NONE', #32850, #9931, #6233 ) ;
#41720=ADVANCED_FACE ( 'NONE', ( #11594 ), #15100, .F. ) ;
#41721=DIRECTION ( 'NONE',  ( -1.000000000000000000, -0.000000000000000000, -0.000000000000000000 ) ) ;
#41723=CYLINDRICAL_SURFACE ( 'NONE', #34950, 116.0000000000000000 ) ;
#41726=CARTESIAN_POINT ( 'NONE',  ( 0.000000000000000000, 83.49789599728782719, 86.88263557826796557 ) ) ;
#41730=ORIENTED_EDGE ( 'NONE', *, *, #14303, .F. ) ;
#41731=DIRECTION ( 'NONE',  ( 0.000000000000000000, 0.000000000000000000, 1.000000000000000000 ) ) ;
#41736=CARTESIAN_POINT ( 'NONE',  ( 17.99999999999999645, 0.000000000000000000, 0.000000000000000000 ) ) ;
#41737=ORIENTED_EDGE ( 'NONE', *, *, #19902, .T. ) ;
#41740=ORIENTED_EDGE ( 'NONE', *, *, #36791, .T. ) ;
#41741=CARTESIAN_POINT ( 'NONE',  ( 17.99999999999999645, 108.8684555192046872, 27.12806418649654105 ) ) ;
#41743=AXIS2_PLACEMENT_3D ( 'NONE', #31100, #21756, #1186 ) ;
#41747=AXIS2_PLACEMENT_3D ( 'NONE', #37566, #8114, #7677 ) ;
#41750=EDGE_LOOP ( 'NONE', ( #20600, #17629, #32740, #7679 ) ) ;
#41751=DIRECTION ( 'NONE',  ( -1.000000000000000000, -0.000000000000000000, 0.000000000000000000 ) ) ;
#41754=DIRECTION ( 'NONE',  ( 0.000000000000000000, 0.000000000000000000, 1.000000000000000000 ) ) ;
#41757=DIRECTION ( 'NONE',  ( 0.000000000000000000, 0.000000000000000000, 1.000000000000000000 ) ) ;
#41758=ORIENTED_EDGE ( 'NONE', *, *, #16094, .F. ) ;
#41760=DIRECTION ( 'NONE',  ( -1.000000000000000000, -0.000000000000000000, -0.000000000000000000 ) ) ;
#41763=VECTOR ( 'NONE', #27262, 1000.000000000000000 ) ;
#41764=EDGE_LOOP ( 'NONE', ( #40337, #12152, #4679, #5905 ) ) ;
#41766=ORIENTED_EDGE ( 'NONE', *, *, #23226, .T. ) ;
#41768=ADVANCED_FACE ( 'NONE', ( #14443 ), #17730, .F. ) ;
#41769=VERTEX_POINT ( 'NONE', #37540 ) ;
#41770=LINE ( 'NONE', #17615, #11216 ) ;
#41771=CARTESIAN_POINT ( 'NONE',  ( 17.99999999999999645, 51.27532863109366446, 99.79535634195144667 ) ) ;
#41777=CYLINDRICAL_SURFACE ( 'NONE', #13052, 59.00000000000000000 ) ;
#41779=ORIENTED_EDGE ( 'NONE', *, *, #34346, .T. ) ;
#41780=CARTESIAN_POINT ( 'NONE',  ( 0.000000000000000000, 103.4151313792879421, -61.85306461934304423 ) ) ;
#41781=VERTEX_POINT ( 'NONE', #8306 ) ;
#41782=CARTESIAN_POINT ( 'NONE',  ( 0.000000000000000000, -99.97660604680010010, 67.26937820704856108 ) ) ;
#41783=CARTESIAN_POINT ( 'NONE',  ( 17.99999999999999645, -116.0452958106482981, 32.46506308663420270 ) ) ;
#41787=DIRECTION ( 'NONE',  ( 0.000000000000000000, 0.000000000000000000, 1.000000000000000000 ) ) ;
#41789=EDGE_CURVE ( 'NONE', #18411, #37133, #25145, .T. ) ;
#41792=VERTEX_POINT ( 'NONE', #31232 ) ;
#41793=CARTESIAN_POINT ( 'NONE',  ( 8.999999999999998224, -79.18387647320821543, 84.76976882518735579 ) ) ;
#41799=DIRECTION ( 'NONE',  ( -1.000000000000000000, -0.000000000000000000, 0.000000000000000000 ) ) ;
#41800=VERTEX_POINT ( 'NONE', #4818 ) ;
#41802=CARTESIAN_POINT ( 'NONE',  ( 0.000000000000000000, 0.000000000000000000, 0.000000000000000000 ) ) ;
#41803=AXIS2_PLACEMENT_3D ( 'NONE', #21791, #5146, #18510 ) ;
#41809=ORIENTED_EDGE ( 'NONE', *, *, #17043, .T. ) ;
#41814=CARTESIAN_POINT ( 'NONE',  ( 0.000000000000000000, 0.000000000000000000, 0.000000000000000000 ) ) ;
#41816=FACE_OUTER_BOUND ( 'NONE', #10890, .T. ) ;
#41820=CARTESIAN_POINT ( 'NONE',  ( 17.99999999999999645, -23.10276247328181398, 118.2656051737069021 ) ) ;
#41822=CYLINDRICAL_SURFACE ( 'NONE', #32864, 130.0000000000000000 ) ;
#41824=FACE_OUTER_BOUND ( 'NONE', #6867, .T. ) ;
#41826=FACE_OUTER_BOUND ( 'NONE', #5559, .T. ) ;
#41830=EDGE_LOOP ( 'NONE', ( #20543, #38648, #17771, #5585 ) ) ;
#41833=DIRECTION ( 'NONE',  ( 1.000000000000000000, 0.000000000000000000, 0.000000000000000000 ) ) ;
#41838=EDGE_CURVE ( 'NONE', #22001, #22222, #21455, .T. ) ;
#41839=EDGE_CURVE ( 'NONE', #10857, #29797, #835, .T. ) ;
#41840=CIRCLE ( 'NONE', #1408, 116.0000000000000000 ) ;
#41841=EDGE_CURVE ( 'NONE', #37209, #3729, #28177, .T. ) ;
#41842=DIRECTION ( 'NONE',  ( 1.000000000000000000, 0.000000000000000000, 0.000000000000000000 ) ) ;
#41844=EDGE_LOOP ( 'NONE', ( #40848, #8247, #7890, #38637 ) ) ;
#41846=AXIS2_PLACEMENT_3D ( 'NONE', #40158, #23641, #26454 ) ;
#41850=EDGE_CURVE ( 'NONE', #36637, #30242, #19030, .T. ) ;
#41851=CIRCLE ( 'NONE', #6313, 59.00000000000000711 ) ;
#41857=VECTOR ( 'NONE', #12989, 1000.000000000000000 ) ;
#41859=VERTEX_POINT ( 'NONE', #7865 ) ;
#41864=VERTEX_POINT ( 'NONE', #21223 ) ;
#41866=CARTESIAN_POINT ( 'NONE',  ( 17.99999999999999645, 110.3490479609632615, -20.28201389785435182 ) ) ;
#41867=CIRCLE ( 'NONE', #28663, 116.0000000000000000 ) ;
#41868=DIRECTION ( 'NONE',  ( 1.000000000000000000, 0.000000000000000000, 0.000000000000000000 ) ) ;
#41870=EDGE_CURVE ( 'NONE', #14903, #27389, #9235, .T. ) ;
#41874=DIRECTION ( 'NONE',  ( 0.000000000000000000, 0.3140767120219427611, 0.9493976084683832806 ) ) ;
#41875=CARTESIAN_POINT ( 'NONE',  ( 9.000000000000001776, -106.6051926090968180, -45.73109345704926909 ) ) ;
#41881=ORIENTED_EDGE ( 'NONE', *, *, #8368, .F. ) ;
#41883=ADVANCED_FACE ( 'NONE', ( #17959 ), #1319, .F. ) ;
#41888=CIRCLE ( 'NONE', #20320, 59.00000000000000711 ) ;
#41889=EDGE_LOOP ( 'NONE', ( #12999, #4083, #19524, #25600 ) ) ;
#41890=FACE_OUTER_BOUND ( 'NONE', #10345, .T. ) ;
#41892=ORIENTED_EDGE ( 'NONE', *, *, #32769, .F. ) ;
#41893=EDGE_CURVE ( 'NONE', #42630, #4481, #33613, .T. ) ;
#41897=EDGE_CURVE ( 'NONE', #20272, #5216, #37100, .T. ) ;
#41908=DIRECTION ( 'NONE',  ( 0.000000000000000000, 0.05322217484217878214, -0.9985826956767620555 ) ) ;
#41910=DIRECTION ( 'NONE',  ( 0.000000000000000000, 0.9714298932647107421, -0.2373266998711119347 ) ) ;
#41913=VERTEX_POINT ( 'NONE', #32082 ) ;
#41915=ADVANCED_FACE ( 'NONE', ( #32502 ), #22299, .F. ) ;
#41916=ORIENTED_EDGE ( 'NONE', *, *, #42431, .F. ) ;
#41918=CIRCLE ( 'NONE', #37745, 58.99999999999999289 ) ;
#41922=CIRCLE ( 'NONE', #39821, 58.99999999999999289 ) ;
#41930=DIRECTION ( 'NONE',  ( 0.000000000000000000, 0.000000000000000000, 1.000000000000000000 ) ) ;
#41934=EDGE_LOOP ( 'NONE', ( #30282, #33659, #28248, #10988 ) ) ;
#41937=ORIENTED_EDGE ( 'NONE', *, *, #1246, .F. ) ;
#41938=CARTESIAN_POINT ( 'NONE',  ( 17.99999999999999645, 56.51398178981952469, -96.92493144647394843 ) ) ;
#41944=EDGE_CURVE ( 'NONE', #35377, #9926, #19232, .T. ) ;
#41947=VERTEX_POINT ( 'NONE', #12240 ) ;
#41948=CIRCLE ( 'NONE', #21116, 116.0000000000000000 ) ;
#41950=FACE_OUTER_BOUND ( 'NONE', #33992, .T. ) ;
#41952=CARTESIAN_POINT ( 'NONE',  ( 17.99999999999999645, 0.000000000000000000, 0.000000000000000000 ) ) ;
#41953=VECTOR ( 'NONE', #18586, 1000.000000000000000 ) ;
#41954=EDGE_CURVE ( 'NONE', #6044, #21659, #9911, .T. ) ;
#41955=CARTESIAN_POINT ( 'NONE',  ( 17.99999999999999645, 5.456439917446431309, -112.0647122740741253 ) ) ;
#41956=FACE_OUTER_BOUND ( 'NONE', #39328, .T. ) ;
#41957=ORIENTED_EDGE ( 'NONE', *, *, #22262, .F. ) ;
#41959=ORIENTED_EDGE ( 'NONE', *, *, #22850, .F. ) ;
#41967=EDGE_CURVE ( 'NONE', #29185, #26760, #15531, .T. ) ;
#41968=VERTEX_POINT ( 'NONE', #2166 ) ;
#41969=DIRECTION ( 'NONE',  ( 1.000000000000000000, 0.000000000000000000, 0.000000000000000000 ) ) ;
#41970=ORIENTED_EDGE ( 'NONE', *, *, #43009, .T. ) ;
#41973=EDGE_CURVE ( 'NONE', #32693, #566, #6100, .T. ) ;
#41975=CYLINDRICAL_SURFACE ( 'NONE', #42561, 116.0000000000000000 ) ;
#41976=ORIENTED_EDGE ( 'NONE', *, *, #17408, .T. ) ;
#41982=DIRECTION ( 'NONE',  ( 1.000000000000000000, 0.000000000000000000, 0.000000000000000000 ) ) ;
#41983=EDGE_CURVE ( 'NONE', #42855, #38496, #26656, .T. ) ;
#41984=ORIENTED_EDGE ( 'NONE', *, *, #29915, .T. ) ;
#41985=AXIS2_PLACEMENT_3D ( 'NONE', #13966, #27260, #40096 ) ;
#41987=DIRECTION ( 'NONE',  ( 1.000000000000000000, 0.000000000000000000, 0.000000000000000000 ) ) ;
#41994=DIRECTION ( 'NONE',  ( 1.000000000000000000, 0.000000000000000000, 0.000000000000000000 ) ) ;
#41999=DIRECTION ( 'NONE',  ( -1.000000000000000000, -0.000000000000000000, 0.000000000000000000 ) ) ;
#42001=CIRCLE ( 'NONE', #35039, 116.0000000000000000 ) ;
#42002=VERTEX_POINT ( 'NONE', #32924 ) ;
#42003=DIRECTION ( 'NONE',  ( 0.000000000000000000, 0.000000000000000000, 1.000000000000000000 ) ) ;
#42006=DIRECTION ( 'NONE',  ( -1.000000000000000000, 0.000000000000000000, 0.000000000000000000 ) ) ;
#42007=VERTEX_POINT ( 'NONE', #42087 ) ;
#42008=CARTESIAN_POINT ( 'NONE',  ( 17.99999999999999645, -41.60679253225688967, -108.2814610871950265 ) ) ;
#42013=AXIS2_PLACEMENT_3D ( 'NONE', #16768, #36350, #40269 ) ;
#42015=EDGE_CURVE ( 'NONE', #23269, #37692, #16368, .T. ) ;
#42016=CARTESIAN_POINT ( 'NONE',  ( 0.000000000000000000, 84.77518783075197462, -73.49448960231268302 ) ) ;
#42017=EDGE_CURVE ( 'NONE', #5275, #40032, #40601, .T. ) ;
#42020=ADVANCED_FACE ( 'NONE', ( #30315 ), #7164, .F. ) ;
#42021=DIRECTION ( 'NONE',  ( 0.000000000000000000, -0.4610925014493144625, -0.8873520750565775383 ) ) ;
#42023=ORIENTED_EDGE ( 'NONE', *, *, #35482, .T. ) ;
#42027=DIRECTION ( 'NONE',  ( -1.000000000000000000, -0.000000000000000000, 0.000000000000000000 ) ) ;
#42028=CARTESIAN_POINT ( 'NONE',  ( 17.99999999999999645, 53.40478689619730090, 108.0204598100367548 ) ) ;
#42029=VECTOR ( 'NONE', #37968, 1000.000000000000000 ) ;
#42032=DIRECTION ( 'NONE',  ( 0.000000000000000000, 0.000000000000000000, 1.000000000000000000 ) ) ;
#42034=DIRECTION ( 'NONE',  ( -1.000000000000000000, -0.000000000000000000, 0.000000000000000000 ) ) ;
#42042=ADVANCED_FACE ( 'NONE', ( #30542 ), #37057, .F. ) ;
#42045=ORIENTED_EDGE ( 'NONE', *, *, #19883, .F. ) ;
#42048=ORIENTED_EDGE ( 'NONE', *, *, #5201, .F. ) ;
#42051=CARTESIAN_POINT ( 'NONE',  ( -10.00000000000000000, 0.000000000000000000, 0.000000000000000000 ) ) ;
#42052=LINE ( 'NONE', #5635, #38663 ) ;
#42055=VERTEX_POINT ( 'NONE', #3873 ) ;
#42056=CARTESIAN_POINT ( 'NONE',  ( 17.99999999999999645, 115.6826031496113529, -8.575274253896266075 ) ) ;
#42063=EDGE_CURVE ( 'NONE', #6563, #20905, #8575, .T. ) ;
#42067=ORIENTED_EDGE ( 'NONE', *, *, #33387, .T. ) ;
#42069=EDGE_CURVE ( 'NONE', #41404, #6009, #7169, .T. ) ;
#42075=CARTESIAN_POINT ( 'NONE',  ( 17.99999999999999645, -112.1702510623870239, -2.471285140323770335 ) ) ;
#42080=DIRECTION ( 'NONE',  ( 0.000000000000000000, 0.000000000000000000, -1.000000000000000000 ) ) ;
#42082=ORIENTED_EDGE ( 'NONE', *, *, #21333, .T. ) ;
#42084=CYLINDRICAL_SURFACE ( 'NONE', #10598, 116.0000000000000000 ) ;
#42085=EDGE_CURVE ( 'NONE', #20139, #25483, #38499, .T. ) ;
#42087=CARTESIAN_POINT ( 'NONE',  ( 17.99999999999999645, -104.6166166098442147, -50.11350645393781633 ) ) ;
#42088=AXIS2_PLACEMENT_3D ( 'NONE', #10842, #37009, #37217 ) ;
#42089=LINE ( 'NONE', #31877, #8381 ) ;
#42093=VERTEX_POINT ( 'NONE', #10009 ) ;
#42095=EDGE_CURVE ( 'NONE', #1613, #16471, #37271, .T. ) ;
#42099=DIRECTION ( 'NONE',  ( -1.000000000000000000, 0.000000000000000000, 0.000000000000000000 ) ) ;
#42101=CARTESIAN_POINT ( 'NONE',  ( 0.000000000000000000, 0.000000000000000000, 0.000000000000000000 ) ) ;
#42102=CIRCLE ( 'NONE', #10072, 116.0000000000000000 ) ;
#42103=DIRECTION ( 'NONE',  ( -1.000000000000000000, -0.000000000000000000, -0.000000000000000000 ) ) ;
#42104=ORIENTED_EDGE ( 'NONE', *, *, #38827, .F. ) ;
#42107=CARTESIAN_POINT ( 'NONE',  ( 17.99999999999999645, 46.83041522348496954, 101.9567785075603155 ) ) ;
#42108=DIRECTION ( 'NONE',  ( 0.000000000000000000, 0.000000000000000000, 1.000000000000000000 ) ) ;
#42111=EDGE_CURVE ( 'NONE', #36025, #3831, #18383, .T. ) ;
#42112=LINE ( 'NONE', #9391, #2635 ) ;
#42113=CIRCLE ( 'NONE', #305, 59.00000000000000000 ) ;
#42114=EDGE_CURVE ( 'NONE', #14037, #43080, #13107, .T. ) ;
#42116=DIRECTION ( 'NONE',  ( 0.000000000000000000, 0.000000000000000000, -1.000000000000000000 ) ) ;
#42118=VERTEX_POINT ( 'NONE', #6512 ) ;
#42121=ORIENTED_EDGE ( 'NONE', *, *, #7615, .F. ) ;
#42124=ORIENTED_EDGE ( 'NONE', *, *, #38620, .T. ) ;
#42125=EDGE_CURVE ( 'NONE', #26365, #38244, #16609, .T. ) ;
#42133=AXIS2_PLACEMENT_3D ( 'NONE', #26863, #36655, #40140 ) ;
#42134=CARTESIAN_POINT ( 'NONE',  ( 17.99999999999999645, 0.000000000000000000, 0.000000000000000000 ) ) ;
#42136=AXIS2_PLACEMENT_3D ( 'NONE', #10155, #34522, #11210 ) ;
#42137=VERTEX_POINT ( 'NONE', #10232 ) ;
#42141=CIRCLE ( 'NONE', #37267, 58.99999999999999289 ) ;
#42142=CARTESIAN_POINT ( 'NONE',  ( 17.99999999999999645, -101.8011932243951634, 55.61040422519296555 ) ) ;
#42144=EDGE_LOOP ( 'NONE', ( #36806, #555, #1187, #21099 ) ) ;
#42149=ORIENTED_EDGE ( 'NONE', *, *, #27985, .F. ) ;
#42153=DIRECTION ( 'NONE',  ( 1.000000000000000000, 0.000000000000000000, 0.000000000000000000 ) ) ;
#42154=DIRECTION ( 'NONE',  ( -1.000000000000000000, -0.000000000000000000, -0.000000000000000000 ) ) ;
#42155=DIRECTION ( 'NONE',  ( 0.000000000000000000, 0.000000000000000000, 1.000000000000000000 ) ) ;
#42156=ORIENTED_EDGE ( 'NONE', *, *, #10562, .F. ) ;
#42158=ORIENTED_EDGE ( 'NONE', *, *, #29769, .F. ) ;
#42159=DIRECTION ( 'NONE',  ( 1.000000000000000000, 0.000000000000000000, 0.000000000000000000 ) ) ;
#42160=AXIS2_PLACEMENT_3D ( 'NONE', #19933, #13373, #10509 ) ;
#42162=CIRCLE ( 'NONE', #36596, 58.99999999999999289 ) ;
#42164=EDGE_CURVE ( 'NONE', #1568, #34051, #9943, .T. ) ;
#42165=CARTESIAN_POINT ( 'NONE',  ( 9.000000000000001776, -115.0622509503831452, -14.72000021165260897 ) ) ;
#42166=ORIENTED_EDGE ( 'NONE', *, *, #30582, .T. ) ;
#42168=CIRCLE ( 'NONE', #6641, 59.00000000000000711 ) ;
#42170=CARTESIAN_POINT ( 'NONE',  ( 17.99999999999999645, 107.2885202478273783, -54.86040852957203384 ) ) ;
#42172=CARTESIAN_POINT ( 'NONE',  ( 8.999999999999998224, -87.74575819880217864, 75.87280091124445391 ) ) ;
#42173=ORIENTED_EDGE ( 'NONE', *, *, #21737, .T. ) ;
#42176=ORIENTED_EDGE ( 'NONE', *, *, #36270, .T. ) ;
#42179=ADVANCED_FACE ( 'NONE', ( #11327 ), #24658, .F. ) ;
#42182=ORIENTED_EDGE ( 'NONE', *, *, #17921, .F. ) ;
#42184=EDGE_CURVE ( 'NONE', #6476, #19975, #14873, .T. ) ;
#42186=DIRECTION ( 'NONE',  ( -1.000000000000000000, -0.000000000000000000, -0.000000000000000000 ) ) ;
#42189=ORIENTED_EDGE ( 'NONE', *, *, #25942, .T. ) ;
#42192=CARTESIAN_POINT ( 'NONE',  ( -10.00000000000000000, 0.000000000000000000, 0.000000000000000000 ) ) ;
#42196=CARTESIAN_POINT ( 'NONE',  ( 0.000000000000000000, 0.000000000000000000, 0.000000000000000000 ) ) ;
#42201=CIRCLE ( 'NONE', #23442, 59.00000000000000711 ) ;
#42203=EDGE_CURVE ( 'NONE', #29542, #3729, #1596, .T. ) ;
#42204=AXIS2_PLACEMENT_3D ( 'NONE', #38243, #38447, #41731 ) ;
#42205=VERTEX_POINT ( 'NONE', #34870 ) ;
#42206=FACE_OUTER_BOUND ( 'NONE', #35632, .T. ) ;
#42216=CARTESIAN_POINT ( 'NONE',  ( 17.99999999999999645, 111.2721026680460596, -14.38025178762657852 ) ) ;
#42218=DIRECTION ( 'NONE',  ( 0.000000000000000000, 0.000000000000000000, 1.000000000000000000 ) ) ;
#42220=ORIENTED_EDGE ( 'NONE', *, *, #20049, .T. ) ;
#42221=CYLINDRICAL_SURFACE ( 'NONE', #33036, 120.5010000000000190 ) ;
#42226=CARTESIAN_POINT ( 'NONE',  ( 17.99999999999999645, -59.47573314508669284, -99.59235496188668435 ) ) ;
#42231=AXIS2_PLACEMENT_3D ( 'NONE', #22763, #32753, #23999 ) ;
#42232=CIRCLE ( 'NONE', #12314, 59.00000000000000000 ) ;
#42233=AXIS2_PLACEMENT_3D ( 'NONE', #32624, #12367, #22211 ) ;
#42236=ORIENTED_EDGE ( 'NONE', *, *, #31172, .T. ) ;
#42238=ORIENTED_EDGE ( 'NONE', *, *, #17496, .T. ) ;
#42240=DIRECTION ( 'NONE',  ( 1.000000000000000000, 0.000000000000000000, 0.000000000000000000 ) ) ;
#42243=DIRECTION ( 'NONE',  ( 0.000000000000000000, 0.000000000000000000, 1.000000000000000000 ) ) ;
#42247=CARTESIAN_POINT ( 'NONE',  ( 17.99999999999999645, -35.54274411428134073, 115.1399337407605259 ) ) ;
#42255=EDGE_LOOP ( 'NONE', ( #6157, #36305, #36173, #35099 ) ) ;
#42256=LINE ( 'NONE', #38774, #35081 ) ;
#42259=CYLINDRICAL_SURFACE ( 'NONE', #14984, 120.5010000000000190 ) ;
#42264=ORIENTED_EDGE ( 'NONE', *, *, #37174, .F. ) ;
#42266=EDGE_CURVE ( 'NONE', #25997, #28092, #19731, .T. ) ;
#42268=AXIS2_PLACEMENT_3D ( 'NONE', #10793, #24123, #19088 ) ;
#42271=LINE ( 'NONE', #34668, #33159 ) ;
#42273=CARTESIAN_POINT ( 'NONE',  ( 17.99999999999999645, 0.000000000000000000, 0.000000000000000000 ) ) ;
#42275=VECTOR ( 'NONE', #17599, 1000.000000000000000 ) ;
#42277=ORIENTED_EDGE ( 'NONE', *, *, #37666, .F. ) ;
#42279=CIRCLE ( 'NONE', #6782, 59.00000000000000000 ) ;
#42282=ORIENTED_EDGE ( 'NONE', *, *, #40638, .F. ) ;
#42284=ADVANCED_FACE ( 'NONE', ( #24890 ), #40971, .F. ) ;
#42286=AXIS2_PLACEMENT_3D ( 'NONE', #27360, #10553, #26926 ) ;
#42292=DIRECTION ( 'NONE',  ( 0.000000000000000000, 0.7164567402983164079, -0.6976315211349833900 ) ) ;
#42293=ORIENTED_EDGE ( 'NONE', *, *, #26825, .F. ) ;
#42294=CARTESIAN_POINT ( 'NONE',  ( 17.99999999999999645, 0.000000000000000000, 0.000000000000000000 ) ) ;
#42296=EDGE_CURVE ( 'NONE', #28773, #596, #34332, .T. ) ;
#42297=AXIS2_PLACEMENT_3D ( 'NONE', #23274, #40007, #528 ) ;
#42298=CARTESIAN_POINT ( 'NONE',  ( 17.99999999999999645, -107.1354928292866759, -44.47455650398174498 ) ) ;
#42301=CIRCLE ( 'NONE', #20747, 58.99999999999999289 ) ;
#42303=ORIENTED_EDGE ( 'NONE', *, *, #16505, .F. ) ;
#42306=ORIENTED_EDGE ( 'NONE', *, *, #21666, .T. ) ;
#42307=CARTESIAN_POINT ( 'NONE',  ( 8.999999999999998224, -68.63002662989681824, -93.51962064069581970 ) ) ;
#42308=AXIS2_PLACEMENT_3D ( 'NONE', #2663, #35624, #42802 ) ;
#42312=VERTEX_POINT ( 'NONE', #17685 ) ;
#42314=AXIS2_PLACEMENT_3D ( 'NONE', #32229, #8458, #21820 ) ;
#42319=EDGE_CURVE ( 'NONE', #4351, #31916, #36427, .T. ) ;
#42321=DIRECTION ( 'NONE',  ( 0.000000000000000000, 0.5076658003388410112, -0.8615540813938056264 ) ) ;
#42325=EDGE_CURVE ( 'NONE', #7533, #41913, #15682, .T. ) ;
#42326=CARTESIAN_POINT ( 'NONE',  ( 0.000000000000000000, -97.89532456239533076, 54.81585448086167389 ) ) ;
#42328=AXIS2_PLACEMENT_3D ( 'NONE', #21190, #4545, #13766 ) ;
#42329=VECTOR ( 'NONE', #30703, 1000.000000000000000 ) ;
#42332=AXIS2_PLACEMENT_3D ( 'NONE', #21457, #17312, #31003 ) ;
#42335=AXIS2_PLACEMENT_3D ( 'NONE', #9020, #38681, #32360 ) ;
#42338=DIRECTION ( 'NONE',  ( 0.000000000000000000, 0.1062934856473589651, 0.9943348002101377592 ) ) ;
#42339=ORIENTED_EDGE ( 'NONE', *, *, #4703, .F. ) ;
#42341=ORIENTED_EDGE ( 'NONE', *, *, #39441, .T. ) ;
#42344=AXIS2_PLACEMENT_3D ( 'NONE', #20902, #17184, #34151 ) ;
#42346=ORIENTED_EDGE ( 'NONE', *, *, #21887, .F. ) ;
#42347=CARTESIAN_POINT ( 'NONE',  ( 0.000000000000000000, 111.8797445107943531, 8.437727291344614855 ) ) ;
#42355=CIRCLE ( 'NONE', #25115, 116.0000000000000000 ) ;
#42358=CARTESIAN_POINT ( 'NONE',  ( 17.99999999999999645, 0.000000000000000000, 0.000000000000000000 ) ) ;
#42359=CARTESIAN_POINT ( 'NONE',  ( 17.99999999999999645, -106.5605152861899256, -56.26142179985931335 ) ) ;
#42360=AXIS2_PLACEMENT_3D ( 'NONE', #3415, #25944, #19200 ) ;
#42369=CARTESIAN_POINT ( 'NONE',  ( 0.000000000000000000, -18.35539002514308038, -110.6858262410711831 ) ) ;
#42370=AXIS2_PLACEMENT_3D ( 'NONE', #2508, #15872, #16289 ) ;
#42373=EDGE_CURVE ( 'NONE', #8238, #28805, #9546, .T. ) ;
#42377=ORIENTED_EDGE ( 'NONE', *, *, #12743, .F. ) ;
#42379=CYLINDRICAL_SURFACE ( 'NONE', #28399, 116.0000000000000000 ) ;
#42382=EDGE_CURVE ( 'NONE', #21931, #34938, #20484, .T. ) ;
#42383=FACE_OUTER_BOUND ( 'NONE', #22954, .T. ) ;
#42384=ORIENTED_EDGE ( 'NONE', *, *, #33949, .T. ) ;
#42386=ORIENTED_EDGE ( 'NONE', *, *, #41449, .F. ) ;
#42387=CYLINDRICAL_SURFACE ( 'NONE', #34062, 120.5010000000000190 ) ;
#42389=EDGE_CURVE ( 'NONE', #6539, #10288, #38558, .T. ) ;
#42391=AXIS2_PLACEMENT_3D ( 'NONE', #34401, #4741, #7580 ) ;
#42396=VERTEX_POINT ( 'NONE', #15902 ) ;
#42397=AXIS2_PLACEMENT_3D ( 'NONE', #28490, #18254, #1607 ) ;
#42403=ORIENTED_EDGE ( 'NONE', *, *, #39991, .F. ) ;
#42405=EDGE_CURVE ( 'NONE', #40129, #28564, #42256, .T. ) ;
#42407=ORIENTED_EDGE ( 'NONE', *, *, #30326, .T. ) ;
#42409=DIRECTION ( 'NONE',  ( 0.000000000000000000, 0.000000000000000000, 1.000000000000000000 ) ) ;
#42410=CARTESIAN_POINT ( 'NONE',  ( 17.99999999999999645, 113.8630351447208824, -22.16324045874292636 ) ) ;
#42411=CARTESIAN_POINT ( 'NONE',  ( 0.000000000000000000, 35.78484819117785776, -110.3423972910429143 ) ) ;
#42413=FACE_OUTER_BOUND ( 'NONE', #2627, .T. ) ;
#42414=ORIENTED_EDGE ( 'NONE', *, *, #20698, .F. ) ;
#42415=DIRECTION ( 'NONE',  ( 0.000000000000000000, 0.000000000000000000, 1.000000000000000000 ) ) ;
#42416=LINE ( 'NONE', #16055, #24056 ) ;
#42419=DIRECTION ( 'NONE',  ( 0.000000000000000000, -0.9714298932647122964, 0.2373266998711055509 ) ) ;
#42420=DIRECTION ( 'NONE',  ( -1.000000000000000000, -0.000000000000000000, -0.000000000000000000 ) ) ;
#42421=AXIS2_PLACEMENT_3D ( 'NONE', #2509, #6018, #42444 ) ;
#42424=CIRCLE ( 'NONE', #4820, 58.99999999999999289 ) ;
#42425=CARTESIAN_POINT ( 'NONE',  ( 17.99999999999999645, 110.3490479609629489, 20.28201389785587949 ) ) ;
#42426=ORIENTED_EDGE ( 'NONE', *, *, #22924, .T. ) ;
#42428=DIRECTION ( 'NONE',  ( -1.000000000000000000, -0.000000000000000000, -0.000000000000000000 ) ) ;
#42431=EDGE_CURVE ( 'NONE', #12907, #14877, #28818, .T. ) ;
#42435=DIRECTION ( 'NONE',  ( 0.000000000000000000, 0.000000000000000000, 1.000000000000000000 ) ) ;
#42436=VERTEX_POINT ( 'NONE', #13263 ) ;
#42438=EDGE_CURVE ( 'NONE', #22974, #36853, #4388, .T. ) ;
#42444=DIRECTION ( 'NONE',  ( 0.000000000000000000, 0.000000000000000000, 1.000000000000000000 ) ) ;
#42445=AXIS2_PLACEMENT_3D ( 'NONE', #9091, #35281, #12600 ) ;
#42448=AXIS2_PLACEMENT_3D ( 'NONE', #14053, #7037, #23235 ) ;
#42450=CIRCLE ( 'NONE', #41043, 120.5010000000000190 ) ;
#42455=VERTEX_POINT ( 'NONE', #42895 ) ;
#42457=EDGE_CURVE ( 'NONE', #20175, #33403, #40478, .T. ) ;
#42458=DIRECTION ( 'NONE',  ( 0.000000000000000000, 0.8747630845319623871, -0.4845508703326481537 ) ) ;
#42460=FACE_OUTER_BOUND ( 'NONE', #31213, .T. ) ;
#42461=EDGE_CURVE ( 'NONE', #6563, #14428, #32983, .T. ) ;
#42463=DIRECTION ( 'NONE',  ( -1.000000000000000000, -0.000000000000000000, -0.000000000000000000 ) ) ;
#42465=CARTESIAN_POINT ( 'NONE',  ( 0.000000000000000000, 109.1131968883998695, -26.12628443611929896 ) ) ;
#42467=DIRECTION ( 'NONE',  ( 0.000000000000000000, 0.8183027759081662467, 0.5747874102144109321 ) ) ;
#42468=CARTESIAN_POINT ( 'NONE',  ( 17.99999999999999645, -6.486220790509180212, 112.0098273076987283 ) ) ;
#42472=ADVANCED_FACE ( 'NONE', ( #6463 ), #10614, .F. ) ;
#42476=AXIS2_PLACEMENT_3D ( 'NONE', #37019, #13489, #33967 ) ;
#42477=CIRCLE ( 'NONE', #6950, 120.5010000000000474 ) ;
#42479=ORIENTED_EDGE ( 'NONE', *, *, #19419, .T. ) ;
#42486=DIRECTION ( 'NONE',  ( 0.000000000000000000, 0.6783118362696173298, -0.7347741508630660778 ) ) ;
#42487=CARTESIAN_POINT ( 'NONE',  ( 0.000000000000000000, -73.78980555658542073, -95.26571049922065981 ) ) ;
#42489=VERTEX_POINT ( 'NONE', #36789 ) ;
#42495=ORIENTED_EDGE ( 'NONE', *, *, #32431, .F. ) ;
#42496=FACE_OUTER_BOUND ( 'NONE', #41934, .T. ) ;
#42499=VERTEX_POINT ( 'NONE', #3813 ) ;
#42500=FACE_OUTER_BOUND ( 'NONE', #29317, .T. ) ;
#42501=CIRCLE ( 'NONE', #37621, 116.0000000000000000 ) ;
#42502=ADVANCED_FACE ( 'NONE', ( #17199 ), #33084, .F. ) ;
#42503=ORIENTED_EDGE ( 'NONE', *, *, #4434, .F. ) ;
#42504=DIRECTION ( 'NONE',  ( -1.000000000000000000, 0.000000000000000000, -0.000000000000000000 ) ) ;
#42508=EDGE_CURVE ( 'NONE', #16661, #34831, #37160, .T. ) ;
#42511=DIRECTION ( 'NONE',  ( -1.000000000000000000, 0.000000000000000000, 0.000000000000000000 ) ) ;
#42512=ORIENTED_EDGE ( 'NONE', *, *, #24190, .T. ) ;
#42516=ORIENTED_EDGE ( 'NONE', *, *, #32480, .F. ) ;
#42518=CARTESIAN_POINT ( 'NONE',  ( 17.99999999999999645, 34.74871106919766106, -106.6808302961368327 ) ) ;
#42519=EDGE_CURVE ( 'NONE', #24013, #33535, #32280, .T. ) ;
#42522=DIRECTION ( 'NONE',  ( 0.000000000000000000, 0.7164567402983164079, -0.6976315211349833900 ) ) ;
#42526=AXIS2_PLACEMENT_3D ( 'NONE', #13258, #20459, #17189 ) ;
#42528=VECTOR ( 'NONE', #34362, 1000.000000000000000 ) ;
#42529=CARTESIAN_POINT ( 'NONE',  ( 17.99999999999999645, -100.8494052988175298, 65.95368414178875582 ) ) ;
#42530=DIRECTION ( 'NONE',  ( 1.000000000000000000, 0.000000000000000000, 0.000000000000000000 ) ) ;
#42531=ADVANCED_FACE ( 'NONE', ( #20466 ), #9751, .F. ) ;
#42533=DIRECTION ( 'NONE',  ( 0.000000000000000000, 0.000000000000000000, 1.000000000000000000 ) ) ;
#42534=LINE ( 'NONE', #19040, #25165 ) ;
#42537=DIRECTION ( 'NONE',  ( 1.000000000000000000, -0.000000000000000000, -0.000000000000000000 ) ) ;
#42540=CARTESIAN_POINT ( 'NONE',  ( 17.99999999999999645, 114.1529630473454944, -38.59523323561318620 ) ) ;
#42554=ADVANCED_FACE ( 'NONE', ( #110 ), #24605, .F. ) ;
#42555=CARTESIAN_POINT ( 'NONE',  ( 17.99999999999999645, -52.88069566989388903, -103.2454939717374032 ) ) ;
#42556=CIRCLE ( 'NONE', #34198, 58.99999999999999289 ) ;
#42558=ORIENTED_EDGE ( 'NONE', *, *, #10282, .T. ) ;
#42560=DIRECTION ( 'NONE',  ( 1.000000000000000000, 0.000000000000000000, 0.000000000000000000 ) ) ;
#42561=AXIS2_PLACEMENT_3D ( 'NONE', #12124, #21327, #11259 ) ;
#42563=CARTESIAN_POINT ( 'NONE',  ( 17.99999999999999645, 93.26762629039527042, -76.29967815892260319 ) ) ;
#42564=DIRECTION ( 'NONE',  ( 0.000000000000000000, 0.000000000000000000, 1.000000000000000000 ) ) ;
#42565=DIRECTION ( 'NONE',  ( -1.000000000000000000, 0.000000000000000000, -0.000000000000000000 ) ) ;
#42566=VECTOR ( 'NONE', #32848, 1000.000000000000000 ) ;
#42573=DIRECTION ( 'NONE',  ( -1.000000000000000000, 0.000000000000000000, 0.000000000000000000 ) ) ;
#42580=ORIENTED_EDGE ( 'NONE', *, *, #21126, .T. ) ;
#42582=CARTESIAN_POINT ( 'NONE',  ( 17.99999999999999645, 64.58410930313661424, -101.7319213743675732 ) ) ;
#42583=DIRECTION ( 'NONE',  ( 0.000000000000000000, 0.000000000000000000, -1.000000000000000000 ) ) ;
#42584=CARTESIAN_POINT ( 'NONE',  ( 17.99999999999999645, 0.000000000000000000, 0.000000000000000000 ) ) ;
#42585=DIRECTION ( 'NONE',  ( 1.000000000000000000, 0.000000000000000000, 0.000000000000000000 ) ) ;
#42587=ORIENTED_EDGE ( 'NONE', *, *, #30133, .F. ) ;
#42591=CIRCLE ( 'NONE', #20349, 59.00000000000000711 ) ;
#42592=CARTESIAN_POINT ( 'NONE',  ( -10.00000000000000000, 0.000000000000000000, 0.000000000000000000 ) ) ;
#42593=LINE ( 'NONE', #19100, #25662 ) ;
#42601=CARTESIAN_POINT ( 'NONE',  ( 17.99999999999999645, 0.000000000000000000, 0.000000000000000000 ) ) ;
#42606=EDGE_CURVE ( 'NONE', #14728, #33431, #26714, .T. ) ;
#42612=ORIENTED_EDGE ( 'NONE', *, *, #36375, .F. ) ;
#42615=CARTESIAN_POINT ( 'NONE',  ( 17.99999999999999645, 0.000000000000000000, 0.000000000000000000 ) ) ;
#42618=CARTESIAN_POINT ( 'NONE',  ( 0.000000000000000000, 29.86146781000101669, -112.0905559814575696 ) ) ;
#42619=EDGE_LOOP ( 'NONE', ( #22292, #26644, #26917, #11859 ) ) ;
#42621=AXIS2_PLACEMENT_3D ( 'NONE', #23625, #40364, #649 ) ;
#42625=EDGE_CURVE ( 'NONE', #35323, #35191, #5802, .T. ) ;
#42629=ORIENTED_EDGE ( 'NONE', *, *, #13223, .F. ) ;
#42630=VERTEX_POINT ( 'NONE', #24396 ) ;
#42636=EDGE_CURVE ( 'NONE', #2648, #5275, #8638, .T. ) ;
#42641=CARTESIAN_POINT ( 'NONE',  ( 0.000000000000000000, 0.000000000000000000, 0.000000000000000000 ) ) ;
#42642=CYLINDRICAL_SURFACE ( 'NONE', #26287, 59.00000000000000000 ) ;
#42643=FACE_OUTER_BOUND ( 'NONE', #38894, .T. ) ;
#42647=CIRCLE ( 'NONE', #7160, 59.00000000000000000 ) ;
#42649=AXIS2_PLACEMENT_3D ( 'NONE', #2181, #42103, #14685 ) ;
#42650=DIRECTION ( 'NONE',  ( 0.000000000000000000, -0.6382441836448108363, -0.7698339834299139373 ) ) ;
#42651=ORIENTED_EDGE ( 'NONE', *, *, #8199, .T. ) ;
#42655=CIRCLE ( 'NONE', #2258, 59.00000000000000000 ) ;
#42657=EDGE_CURVE ( 'NONE', #32645, #2567, #24002, .T. ) ;
#42658=CARTESIAN_POINT ( 'NONE',  ( 17.99999999999999645, -104.0201923570379137, 51.34003878071028026 ) ) ;
#42662=DIRECTION ( 'NONE',  ( 0.000000000000000000, 0.000000000000000000, 1.000000000000000000 ) ) ;
#42665=CYLINDRICAL_SURFACE ( 'NONE', #20232, 120.5010000000000190 ) ;
#42667=DIRECTION ( 'NONE',  ( 1.000000000000000000, -0.000000000000000000, -0.000000000000000000 ) ) ;
#42669=LINE ( 'NONE', #12819, #20288 ) ;
#42671=VERTEX_POINT ( 'NONE', #25057 ) ;
#42673=CARTESIAN_POINT ( 'NONE',  ( 17.99999999999999645, -91.51415974874635140, 64.91094698989267897 ) ) ;
#42678=LINE ( 'NONE', #15906, #39302 ) ;
#42681=CARTESIAN_POINT ( 'NONE',  ( 17.99999999999999645, -17.77780072541773748, 114.6296200873375284 ) ) ;
#42682=ORIENTED_EDGE ( 'NONE', *, *, #28951, .T. ) ;
#42691=FACE_OUTER_BOUND ( 'NONE', #28820, .T. ) ;
#42693=DIRECTION ( 'NONE',  ( 1.000000000000000000, -0.000000000000000000, -0.000000000000000000 ) ) ;
#42695=CYLINDRICAL_SURFACE ( 'NONE', #19136, 59.00000000000000000 ) ;
#42698=DIRECTION ( 'NONE',  ( 0.000000000000000000, 0.000000000000000000, 1.000000000000000000 ) ) ;
#42699=VERTEX_POINT ( 'NONE', #30898 ) ;
#42703=EDGE_LOOP ( 'NONE', ( #9130, #30902, #24828, #4239 ) ) ;
#42705=AXIS2_PLACEMENT_3D ( 'NONE', #13689, #20463, #23301 ) ;
#42706=ORIENTED_EDGE ( 'NONE', *, *, #10628, .T. ) ;
#42707=DIRECTION ( 'NONE',  ( -1.000000000000000000, -0.000000000000000000, 0.000000000000000000 ) ) ;
#42708=ORIENTED_EDGE ( 'NONE', *, *, #38446, .T. ) ;
#42712=CARTESIAN_POINT ( 'NONE',  ( 0.000000000000000000, -63.24564713401724703, -102.5693868539701299 ) ) ;
#42713=VERTEX_POINT ( 'NONE', #34376 ) ;
#42715=EDGE_CURVE ( 'NONE', #30836, #21873, #17847, .T. ) ;
#42716=VERTEX_POINT ( 'NONE', #41340 ) ;
#42718=LINE ( 'NONE', #12661, #40533 ) ;
#42720=ORIENTED_EDGE ( 'NONE', *, *, #39551, .F. ) ;
#42727=DIRECTION ( 'NONE',  ( 1.000000000000000000, 0.000000000000000000, 0.000000000000000000 ) ) ;
#42731=CIRCLE ( 'NONE', #28833, 116.0000000000000000 ) ;
#42733=CARTESIAN_POINT ( 'NONE',  ( 17.99999999999999645, 41.60679253225906393, -108.2814610871942165 ) ) ;
#42735=EDGE_CURVE ( 'NONE', #34842, #16033, #28843, .T. ) ;
#42736=LINE ( 'NONE', #12681, #4409 ) ;
#42737=DIRECTION ( 'NONE',  ( 0.000000000000000000, 0.000000000000000000, 1.000000000000000000 ) ) ;
#42738=PRODUCT_DEFINITION_FORMATION_WITH_SPECIFIED_SOURCE ( 'ANY', '', #5687, .NOT_KNOWN. ) ;
#42741=DIRECTION ( 'NONE',  ( -1.000000000000000000, -0.000000000000000000, -0.000000000000000000 ) ) ;
#42742=VECTOR ( 'NONE', #36089, 1000.000000000000000 ) ;
#42743=CARTESIAN_POINT ( 'NONE',  ( 0.000000000000000000, 106.6051926090971023, 45.73109345704855855 ) ) ;
#42746=LINE ( 'NONE', #23176, #4074 ) ;
#42749=ORIENTED_EDGE ( 'NONE', *, *, #34577, .T. ) ;
#42750=AXIS2_PLACEMENT_3D ( 'NONE', #25134, #18594, #1949 ) ;
#42751=EDGE_LOOP ( 'NONE', ( #19468, #37546, #8947, #37120 ) ) ;
#42752=CIRCLE ( 'NONE', #12168, 59.00000000000000711 ) ;
#42753=DIRECTION ( 'NONE',  ( 0.000000000000000000, -0.9407002666710364558, 0.3392388661180213427 ) ) ;
#42756=CARTESIAN_POINT ( 'NONE',  ( 17.99999999999999645, -111.8797445107944100, -8.437727291343872338 ) ) ;
#42757=VECTOR ( 'NONE', #27264, 1000.000000000000000 ) ;
#42758=CARTESIAN_POINT ( 'NONE',  ( 0.000000000000000000, 34.74871106919766106, -106.6808302961368327 ) ) ;
#42759=DIRECTION ( 'NONE',  ( -1.000000000000000000, 0.000000000000000000, -0.000000000000000000 ) ) ;
#42764=DIRECTION ( 'NONE',  ( 0.000000000000000000, 0.000000000000000000, 1.000000000000000000 ) ) ;
#42765=EDGE_CURVE ( 'NONE', #4296, #6476, #26745, .T. ) ;
#42768=CARTESIAN_POINT ( 'NONE',  ( 17.99999999999999645, -111.2721026680459602, -14.38025178762732104 ) ) ;
#42770=ORIENTED_EDGE ( 'NONE', *, *, #42928, .T. ) ;
#42774=CIRCLE ( 'NONE', #32339, 120.5010000000000190 ) ;
#42775=ORIENTED_EDGE ( 'NONE', *, *, #10143, .T. ) ;
#42777=FACE_OUTER_BOUND ( 'NONE', #27892, .T. ) ;
#42778=ORIENTED_EDGE ( 'NONE', *, *, #8666, .T. ) ;
#42779=CARTESIAN_POINT ( 'NONE',  ( 0.000000000000000000, 0.000000000000000000, 0.000000000000000000 ) ) ;
#42781=CIRCLE ( 'NONE', #21964, 120.5010000000000332 ) ;
#42783=VECTOR ( 'NONE', #15724, 1000.000000000000000 ) ;
#42785=EDGE_CURVE ( 'NONE', #39524, #17179, #18497, .T. ) ;
#42789=CARTESIAN_POINT ( 'NONE',  ( -10.00000000000000000, 0.000000000000000000, 0.000000000000000000 ) ) ;
#42791=EDGE_CURVE ( 'NONE', #1326, #40885, #924, .T. ) ;
#42794=DIRECTION ( 'NONE',  ( -1.000000000000000000, 0.000000000000000000, 0.000000000000000000 ) ) ;
#42797=CIRCLE ( 'NONE', #275, 116.0000000000000000 ) ;
#42801=CARTESIAN_POINT ( 'NONE',  ( 17.99999999999999645, -119.8996782608629275, -12.02323392193477325 ) ) ;
#42802=DIRECTION ( 'NONE',  ( 0.000000000000000000, 0.000000000000000000, 1.000000000000000000 ) ) ;
#42804=DIRECTION ( 'NONE',  ( 0.000000000000000000, 0.6783118362696124448, 0.7347741508630706297 ) ) ;
#42806=DIRECTION ( 'NONE',  ( -1.000000000000000000, -0.000000000000000000, -0.000000000000000000 ) ) ;
#42807=ORIENTED_EDGE ( 'NONE', *, *, #20014, .F. ) ;
#42808=LINE ( 'NONE', #39686, #4757 ) ;
#42809=CARTESIAN_POINT ( 'NONE',  ( 0.000000000000000000, 59.47573314508867526, -99.59235496188547643 ) ) ;
#42811=VERTEX_POINT ( 'NONE', #5572 ) ;
#42816=CARTESIAN_POINT ( 'NONE',  ( 0.000000000000000000, 78.75547124681369837, 91.20343606297029737 ) ) ;
#42820=AXIS2_PLACEMENT_3D ( 'NONE', #24219, #33773, #20952 ) ;
#42824=LINE ( 'NONE', #9473, #21068 ) ;
#42826=CIRCLE ( 'NONE', #31715, 120.5010000000000190 ) ;
#42828=VERTEX_POINT ( 'NONE', #21780 ) ;
#42829=CARTESIAN_POINT ( 'NONE',  ( 9.000000000000001776, 17.77780072541695944, 114.6296200873376563 ) ) ;
#42832=AXIS2_PLACEMENT_3D ( 'NONE', #12161, #8870, #37183 ) ;
#42833=DIRECTION ( 'NONE',  ( 0.000000000000000000, 0.000000000000000000, 1.000000000000000000 ) ) ;
#42838=ORIENTED_EDGE ( 'NONE', *, *, #32913, .F. ) ;
#42840=EDGE_CURVE ( 'NONE', #42205, #8016, #39254, .T. ) ;
#42843=DIRECTION ( 'NONE',  ( 0.000000000000000000, 0.4132121857683728194, 0.9106347728549155640 ) ) ;
#42845=AXIS2_PLACEMENT_3D ( 'NONE', #1854, #12128, #18071 ) ;
#42848=EDGE_CURVE ( 'NONE', #821, #36952, #30234, .T. ) ;
#42850=DIRECTION ( 'NONE',  ( 0.000000000000000000, 0.8993121301712172500, 0.4373073204588593388 ) ) ;
#42851=CIRCLE ( 'NONE', #24097, 120.5010000000000474 ) ;
#42852=CIRCLE ( 'NONE', #12930, 58.99999999999999289 ) ;
#42853=ADVANCED_FACE ( 'NONE', ( #35863 ), #32615, .F. ) ;
#42854=DIRECTION ( 'NONE',  ( -1.000000000000000000, -0.000000000000000000, -0.000000000000000000 ) ) ;
#42855=VERTEX_POINT ( 'NONE', #21980 ) ;
#42857=ORIENTED_EDGE ( 'NONE', *, *, #34446, .F. ) ;
#42860=AXIS2_PLACEMENT_3D ( 'NONE', #769, #20464, #20911 ) ;
#42863=ADVANCED_FACE ( 'NONE', ( #15227 ), #8621, .F. ) ;
#42865=ORIENTED_EDGE ( 'NONE', *, *, #10059, .F. ) ;
#42868=AXIS2_PLACEMENT_3D ( 'NONE', #22172, #32365, #15813 ) ;
#42869=CARTESIAN_POINT ( 'NONE',  ( 8.999999999999998224, 74.56001736500738275, -88.86396238368959644 ) ) ;
#42875=ORIENTED_EDGE ( 'NONE', *, *, #10832, .F. ) ;
#42877=CARTESIAN_POINT ( 'NONE',  ( 0.000000000000000000, 104.6166166098452379, -50.11350645393572023 ) ) ;
#42878=CYLINDRICAL_SURFACE ( 'NONE', #18286, 116.0000000000000000 ) ;
#42883=AXIS2_PLACEMENT_3D ( 'NONE', #1457, #17886, #1675 ) ;
#42884=CARTESIAN_POINT ( 'NONE',  ( 17.99999999999999645, -104.2166695095708491, -60.49278301857915352 ) ) ;
#42886=ORIENTED_EDGE ( 'NONE', *, *, #12665, .F. ) ;
#42890=AXIS2_PLACEMENT_3D ( 'NONE', #18873, #28026, #28466 ) ;
#42895=CARTESIAN_POINT ( 'NONE',  ( 0.000000000000000000, -83.49789599728840983, 86.88263557826738293 ) ) ;
#42897=ORIENTED_EDGE ( 'NONE', *, *, #12030, .F. ) ;
#42898=CIRCLE ( 'NONE', #24135, 59.00000000000000000 ) ;
#42899=CARTESIAN_POINT ( 'NONE',  ( 17.99999999999999645, 0.000000000000000000, 0.000000000000000000 ) ) ;
#42903=VERTEX_POINT ( 'NONE', #26082 ) ;
#42906=ADVANCED_FACE ( 'NONE', ( #9484 ), #36507, .F. ) ;
#42907=ADVANCED_FACE ( 'NONE', ( #30005 ), #40804, .F. ) ;
#42909=ADVANCED_FACE ( 'NONE', ( #39348 ), #26506, .F. ) ;
#42910=EDGE_LOOP ( 'NONE', ( #15737, #37970, #5398, #38860 ) ) ;
#42912=CARTESIAN_POINT ( 'NONE',  ( 17.99999999999999645, -82.63181128086679905, -81.41243003647058174 ) ) ;
#42913=DIRECTION ( 'NONE',  ( 0.000000000000000000, -6.586068790149233915E-15, 1.000000000000000000 ) ) ;
#42914=AXIS2_PLACEMENT_3D ( 'NONE', #13105, #38878, #162 ) ;
#42917=CIRCLE ( 'NONE', #13002, 120.5010000000000332 ) ;
#42918=FACE_OUTER_BOUND ( 'NONE', #12236, .T. ) ;
#42919=VECTOR ( 'NONE', #42667, 1000.000000000000000 ) ;
#42920=ORIENTED_EDGE ( 'NONE', *, *, #11109, .F. ) ;
#42923=CIRCLE ( 'NONE', #21415, 116.0000000000000000 ) ;
#42926=AXIS2_PLACEMENT_3D ( 'NONE', #18887, #34986, #38896 ) ;
#42927=ORIENTED_EDGE ( 'NONE', *, *, #12507, .T. ) ;
#42928=EDGE_CURVE ( 'NONE', #2980, #37365, #3713, .T. ) ;
#42930=CARTESIAN_POINT ( 'NONE',  ( 17.99999999999999645, 18.35539002514383711, 110.6858262410710410 ) ) ;
#42935=CYLINDRICAL_SURFACE ( 'NONE', #9325, 120.5010000000000190 ) ;
#42938=DIRECTION ( 'NONE',  ( -1.000000000000000000, -0.000000000000000000, -0.000000000000000000 ) ) ;
#42939=CIRCLE ( 'NONE', #21435, 120.5010000000000190 ) ;
#42942=EDGE_LOOP ( 'NONE', ( #27332, #15202, #21386, #25886 ) ) ;
#42943=DIRECTION ( 'NONE',  ( -1.000000000000000000, -0.000000000000000000, -0.000000000000000000 ) ) ;
#42944=ORIENTED_EDGE ( 'NONE', *, *, #1489, .T. ) ;
#42945=CARTESIAN_POINT ( 'NONE',  ( 17.99999999999999645, 0.000000000000000000, 0.000000000000000000 ) ) ;
#42950=CIRCLE ( 'NONE', #7432, 58.99999999999999289 ) ;
#42951=DIRECTION ( 'NONE',  ( -1.000000000000000000, -0.000000000000000000, -0.000000000000000000 ) ) ;
#42953=ORIENTED_EDGE ( 'NONE', *, *, #14157, .T. ) ;
#42954=AXIS2_PLACEMENT_3D ( 'NONE', #22859, #29172, #2502 ) ;
#42960=DIRECTION ( 'NONE',  ( 0.000000000000000000, 0.6382441836448211614, -0.7698339834299053885 ) ) ;
#42961=CARTESIAN_POINT ( 'NONE',  ( 17.99999999999999645, 0.000000000000000000, 0.000000000000000000 ) ) ;
#42962=DIRECTION ( 'NONE',  ( -1.000000000000000000, -0.000000000000000000, -0.000000000000000000 ) ) ;
#42967=DIRECTION ( 'NONE',  ( 0.000000000000000000, 0.000000000000000000, 1.000000000000000000 ) ) ;
#42971=AXIS2_PLACEMENT_3D ( 'NONE', #41090, #18467, #1178 ) ;
#42972=DIRECTION ( 'NONE',  ( 0.000000000000000000, 0.000000000000000000, 1.000000000000000000 ) ) ;
#42973=DIRECTION ( 'NONE',  ( 0.000000000000000000, 0.000000000000000000, 1.000000000000000000 ) ) ;
#42974=ADVANCED_FACE ( 'NONE', ( #1099 ), #32820, .F. ) ;
#42977=EDGE_LOOP ( 'NONE', ( #38918, #11148, #10450, #24806 ) ) ;
#42978=VECTOR ( 'NONE', #28196, 1000.000000000000000 ) ;
#42981=AXIS2_PLACEMENT_3D ( 'NONE', #25696, #38516, #42003 ) ;
#42984=ORIENTED_EDGE ( 'NONE', *, *, #22643, .T. ) ;
#42985=CYLINDRICAL_SURFACE ( 'NONE', #26590, 120.5010000000000190 ) ;
#42990=EDGE_CURVE ( 'NONE', #37365, #3752, #17740, .T. ) ;
#42991=DIRECTION ( 'NONE',  ( 0.000000000000000000, 0.000000000000000000, 1.000000000000000000 ) ) ;
#42993=CARTESIAN_POINT ( 'NONE',  ( -10.00000000000000000, 0.000000000000000000, 0.000000000000000000 ) ) ;
#42997=CARTESIAN_POINT ( 'NONE',  ( 17.99999999999999645, 0.000000000000000000, 0.000000000000000000 ) ) ;
#43001=VERTEX_POINT ( 'NONE', #36299 ) ;
#43002=CARTESIAN_POINT ( 'NONE',  ( 17.99999999999999645, -112.8457601792517124, 26.86697618949339272 ) ) ;
#43009=EDGE_CURVE ( 'NONE', #25806, #40745, #26774, .T. ) ;
#43016=FACE_OUTER_BOUND ( 'NONE', #22436, .T. ) ;
#43020=DIRECTION ( 'NONE',  ( -1.000000000000000000, 0.000000000000000000, 0.000000000000000000 ) ) ;
#43022=DIRECTION ( 'NONE',  ( 1.000000000000000000, 0.000000000000000000, 0.000000000000000000 ) ) ;
#43025=ORIENTED_EDGE ( 'NONE', *, *, #33213, .T. ) ;
#43030=ADVANCED_FACE ( 'NONE', ( #21233 ), #31658, .F. ) ;
#43032=DIRECTION ( 'NONE',  ( 0.000000000000000000, 0.000000000000000000, 1.000000000000000000 ) ) ;
#43035=CARTESIAN_POINT ( 'NONE',  ( 0.000000000000000000, -104.6166166098442147, -50.11350645393781633 ) ) ;
#43037=CARTESIAN_POINT ( 'NONE',  ( 0.000000000000000000, 0.000000000000000000, 0.000000000000000000 ) ) ;
#43038=ORIENTED_EDGE ( 'NONE', *, *, #38940, .F. ) ;
#43040=ORIENTED_EDGE ( 'NONE', *, *, #36023, .T. ) ;
#43044=AXIS2_PLACEMENT_3D ( 'NONE', #29637, #19415, #26576 ) ;
#43049=AXIS2_PLACEMENT_3D ( 'NONE', #23043, #16921, #6848 ) ;
#43053=DIRECTION ( 'NONE',  ( -1.000000000000000000, 0.000000000000000000, -0.000000000000000000 ) ) ;
#43055=EDGE_CURVE ( 'NONE', #2738, #40340, #3746, .T. ) ;
#43056=CARTESIAN_POINT ( 'NONE',  ( 9.000000000000001776, -114.1157422997281969, -20.82300072953048442 ) ) ;
#43060=DIRECTION ( 'NONE',  ( 0.000000000000000000, 0.000000000000000000, 1.000000000000000000 ) ) ;
#43062=CARTESIAN_POINT ( 'NONE',  ( -10.00000000000000000, 0.000000000000000000, 0.000000000000000000 ) ) ;
#43064=EDGE_CURVE ( 'NONE', #41100, #16577, #40694, .T. ) ;
#43067=DIRECTION ( 'NONE',  ( -1.000000000000000000, 0.000000000000000000, 0.000000000000000000 ) ) ;
#43068=ORIENTED_EDGE ( 'NONE', *, *, #33562, .F. ) ;
#43071=AXIS2_PLACEMENT_3D ( 'NONE', #15082, #2720, #23078 ) ;
#43075=CIRCLE ( 'NONE', #14567, 58.99999999999999289 ) ;
#43080=VERTEX_POINT ( 'NONE', #34925 ) ;
#43082=CARTESIAN_POINT ( 'NONE',  ( 17.99999999999999645, 117.9424311864589185, 24.69967462999075281 ) ) ;
#43086=ORIENTED_EDGE ( 'NONE', *, *, #32188, .T. ) ;
#43087=CARTESIAN_POINT ( 'NONE',  ( 8.999999999999998224, 115.0622509503832589, 14.72000021165183803 ) ) ;
#43088=DIRECTION ( 'NONE',  ( -1.000000000000000000, -0.000000000000000000, -0.000000000000000000 ) ) ;
#43089=CARTESIAN_POINT ( 'NONE',  ( 0.000000000000000000, 30.01658535635412406, -108.1077105353194838 ) ) ;
#43094=EDGE_CURVE ( 'NONE', #22222, #3675, #33047, .T. ) ;
#43097=ORIENTED_EDGE ( 'NONE', *, *, #30677, .F. ) ;
#43099=CARTESIAN_POINT ( 'NONE',  ( 9.000000000000001776, -111.2559044912522950, -32.83479428644788811 ) ) ;
#43103=CIRCLE ( 'NONE', #41014, 59.00000000000000000 ) ;
#43104=EDGE_CURVE ( 'NONE', #6927, #35878, #42774, .T. ) ;
#43107=ADVANCED_FACE ( 'NONE', ( #24714 ), #24506, .F. ) ;
#43108=EDGE_CURVE ( 'NONE', #20315, #553, #25435, .T. ) ;
#43114=CARTESIAN_POINT ( 'NONE',  ( 0.000000000000000000, -111.7974656912330715, 9.465682155095141326 ) ) ;
#43117=CARTESIAN_POINT ( 'NONE',  ( 17.99999999999999645, -66.49630760163542220, -90.36876423296052963 ) ) ;
#43118=ORIENTED_EDGE ( 'NONE', *, *, #32483, .T. ) ;
#43120=ORIENTED_EDGE ( 'NONE', *, *, #7254, .T. ) ;
#43128=EDGE_LOOP ( 'NONE', ( #9553, #15702, #15001, #15903 ) ) ;
#43130=CARTESIAN_POINT ( 'NONE',  ( 17.99999999999999645, -99.97660604679919061, -67.26937820704989690 ) ) ;
#43136=CARTESIAN_POINT ( 'NONE',  ( 17.99999999999999645, -97.19627249181141337, 71.22763238166453448 ) ) ;
#43137=ORIENTED_EDGE ( 'NONE', *, *, #42015, .F. ) ;
#43138=FACE_OUTER_BOUND ( 'NONE', #13334, .T. ) ;
#43140=DIRECTION ( 'NONE',  ( -1.000000000000000000, -0.000000000000000000, -0.000000000000000000 ) ) ;
#43141=CIRCLE ( 'NONE', #24386, 120.5010000000000332 ) ;
#43143=CARTESIAN_POINT ( 'NONE',  ( -10.00000000000000000, 0.000000000000000000, 0.000000000000000000 ) ) ;
#43144=ORIENTED_EDGE ( 'NONE', *, *, #15539, .T. ) ;
#43145=CARTESIAN_POINT ( 'NONE',  ( 17.99999999999999645, -35.72777019205738469, 106.3569410558016273 ) ) ;
#43150=VERTEX_POINT ( 'NONE', #10649 ) ;
#43158=ORIENTED_EDGE ( 'NONE', *, *, #13536, .F. ) ;
#43160=EDGE_CURVE ( 'NONE', #18913, #37390, #9349, .T. ) ;
#43165=ORIENTED_EDGE ( 'NONE', *, *, #2425, .F. ) ;
#43169=DIRECTION ( 'NONE',  ( -1.000000000000000000, 0.000000000000000000, 0.000000000000000000 ) ) ;
ENDSEC;
END-ISO-10303-21;
